ISO-10303-21;
HEADER;
/* Generated by software containing ST-Developer
 * from STEP Tools, Inc. (www.steptools.com) 
 */

FILE_DESCRIPTION(
/* description */ ('Spring compression tester'),
/* implementation_level */ '2;1');

FILE_NAME(
/* name */ 'Supported TR12x3 screw.step',
/* time_stamp */ '2026-10-28T03:24:11-07:00',
/* author */ (''),
/* organization */ (''),
/* preprocessor_version */ 'ST-DEVELOPER v20.2',
/* originating_system */ 'Autodesk Translation Framework v15.17.0.0',
/* authorisation */ '');

FILE_SCHEMA (('AUTOMOTIVE_DESIGN { 1 0 10303 214 3 1 1 }'));
ENDSEC;

DATA;
#10=MECHANICAL_DESIGN_GEOMETRIC_PRESENTATION_REPRESENTATION('',(#1169),#43521);
#13=B_SPLINE_SURFACE_WITH_KNOTS('',3,3,((#38747,#38748,#38749,#38750,#38751,
#38752,#38753,#38754,#38755,#38756,#38757,#38758,#38759,#38760,#38761,#38762,
#38763,#38764,#38765,#38766,#38767,#38768,#38769,#38770,#38771,#38772,#38773,
#38774,#38775,#38776,#38777,#38778,#38779,#38780,#38781,#38782,#38783,#38784,
#38785,#38786,#38787,#38788,#38789,#38790,#38791,#38792,#38793,#38794,#38795,
#38796,#38797,#38798,#38799,#38800,#38801,#38802,#38803,#38804,#38805,#38806,
#38807,#38808,#38809,#38810,#38811,#38812,#38813,#38814,#38815,#38816,#38817,
#38818,#38819,#38820,#38821,#38822,#38823,#38824,#38825,#38826,#38827,#38828,
#38829,#38830,#38831,#38832,#38833,#38834,#38835,#38836,#38837,#38838,#38839,
#38840,#38841,#38842,#38843,#38844,#38845,#38846,#38847,#38848,#38849,#38850,
#38851,#38852,#38853,#38854,#38855,#38856,#38857,#38858,#38859,#38860,#38861,
#38862,#38863,#38864,#38865,#38866,#38867,#38868,#38869,#38870,#38871,#38872,
#38873,#38874,#38875,#38876,#38877,#38878,#38879,#38880,#38881,#38882,#38883,
#38884,#38885,#38886,#38887,#38888,#38889,#38890,#38891,#38892,#38893,#38894,
#38895,#38896,#38897,#38898,#38899,#38900,#38901,#38902,#38903,#38904,#38905,
#38906,#38907,#38908,#38909,#38910,#38911,#38912,#38913,#38914,#38915,#38916,
#38917,#38918,#38919,#38920,#38921,#38922,#38923,#38924,#38925,#38926,#38927,
#38928,#38929,#38930,#38931,#38932,#38933,#38934,#38935,#38936,#38937,#38938,
#38939,#38940,#38941,#38942,#38943,#38944,#38945,#38946,#38947,#38948,#38949,
#38950,#38951,#38952,#38953,#38954,#38955,#38956,#38957,#38958,#38959,#38960,
#38961,#38962,#38963,#38964,#38965,#38966,#38967,#38968,#38969,#38970,#38971,
#38972,#38973,#38974,#38975,#38976,#38977,#38978,#38979,#38980,#38981,#38982,
#38983,#38984,#38985,#38986,#38987,#38988,#38989,#38990,#38991,#38992,#38993,
#38994,#38995,#38996,#38997,#38998,#38999,#39000,#39001,#39002,#39003,#39004,
#39005,#39006,#39007,#39008,#39009,#39010,#39011,#39012,#39013,#39014,#39015,
#39016,#39017,#39018,#39019,#39020,#39021,#39022,#39023,#39024,#39025,#39026,
#39027,#39028,#39029,#39030,#39031,#39032,#39033,#39034,#39035,#39036,#39037,
#39038,#39039,#39040,#39041,#39042,#39043,#39044,#39045,#39046,#39047,#39048,
#39049,#39050,#39051,#39052,#39053,#39054,#39055,#39056,#39057,#39058,#39059,
#39060,#39061,#39062,#39063,#39064,#39065,#39066,#39067,#39068,#39069,#39070,
#39071,#39072,#39073,#39074,#39075,#39076,#39077,#39078,#39079,#39080,#39081,
#39082,#39083,#39084,#39085,#39086,#39087,#39088,#39089,#39090,#39091,#39092,
#39093,#39094,#39095,#39096,#39097,#39098,#39099,#39100,#39101,#39102,#39103,
#39104,#39105,#39106,#39107,#39108,#39109,#39110,#39111,#39112,#39113,#39114,
#39115,#39116,#39117,#39118,#39119,#39120,#39121,#39122,#39123,#39124,#39125,
#39126,#39127,#39128,#39129,#39130,#39131,#39132,#39133,#39134,#39135,#39136,
#39137,#39138,#39139,#39140,#39141,#39142,#39143,#39144,#39145,#39146,#39147,
#39148,#39149,#39150,#39151,#39152,#39153,#39154,#39155,#39156,#39157,#39158,
#39159,#39160,#39161,#39162,#39163,#39164,#39165,#39166,#39167,#39168,#39169,
#39170,#39171,#39172,#39173,#39174,#39175,#39176,#39177,#39178,#39179,#39180,
#39181,#39182,#39183,#39184,#39185,#39186,#39187,#39188,#39189,#39190,#39191,
#39192,#39193,#39194,#39195,#39196,#39197,#39198,#39199,#39200,#39201,#39202,
#39203,#39204,#39205,#39206,#39207,#39208,#39209,#39210,#39211,#39212,#39213,
#39214,#39215,#39216,#39217,#39218,#39219,#39220,#39221,#39222,#39223,#39224,
#39225,#39226,#39227,#39228,#39229,#39230,#39231,#39232,#39233,#39234,#39235,
#39236,#39237,#39238,#39239,#39240,#39241,#39242,#39243,#39244),(#39245,
#39246,#39247,#39248,#39249,#39250,#39251,#39252,#39253,#39254,#39255,#39256,
#39257,#39258,#39259,#39260,#39261,#39262,#39263,#39264,#39265,#39266,#39267,
#39268,#39269,#39270,#39271,#39272,#39273,#39274,#39275,#39276,#39277,#39278,
#39279,#39280,#39281,#39282,#39283,#39284,#39285,#39286,#39287,#39288,#39289,
#39290,#39291,#39292,#39293,#39294,#39295,#39296,#39297,#39298,#39299,#39300,
#39301,#39302,#39303,#39304,#39305,#39306,#39307,#39308,#39309,#39310,#39311,
#39312,#39313,#39314,#39315,#39316,#39317,#39318,#39319,#39320,#39321,#39322,
#39323,#39324,#39325,#39326,#39327,#39328,#39329,#39330,#39331,#39332,#39333,
#39334,#39335,#39336,#39337,#39338,#39339,#39340,#39341,#39342,#39343,#39344,
#39345,#39346,#39347,#39348,#39349,#39350,#39351,#39352,#39353,#39354,#39355,
#39356,#39357,#39358,#39359,#39360,#39361,#39362,#39363,#39364,#39365,#39366,
#39367,#39368,#39369,#39370,#39371,#39372,#39373,#39374,#39375,#39376,#39377,
#39378,#39379,#39380,#39381,#39382,#39383,#39384,#39385,#39386,#39387,#39388,
#39389,#39390,#39391,#39392,#39393,#39394,#39395,#39396,#39397,#39398,#39399,
#39400,#39401,#39402,#39403,#39404,#39405,#39406,#39407,#39408,#39409,#39410,
#39411,#39412,#39413,#39414,#39415,#39416,#39417,#39418,#39419,#39420,#39421,
#39422,#39423,#39424,#39425,#39426,#39427,#39428,#39429,#39430,#39431,#39432,
#39433,#39434,#39435,#39436,#39437,#39438,#39439,#39440,#39441,#39442,#39443,
#39444,#39445,#39446,#39447,#39448,#39449,#39450,#39451,#39452,#39453,#39454,
#39455,#39456,#39457,#39458,#39459,#39460,#39461,#39462,#39463,#39464,#39465,
#39466,#39467,#39468,#39469,#39470,#39471,#39472,#39473,#39474,#39475,#39476,
#39477,#39478,#39479,#39480,#39481,#39482,#39483,#39484,#39485,#39486,#39487,
#39488,#39489,#39490,#39491,#39492,#39493,#39494,#39495,#39496,#39497,#39498,
#39499,#39500,#39501,#39502,#39503,#39504,#39505,#39506,#39507,#39508,#39509,
#39510,#39511,#39512,#39513,#39514,#39515,#39516,#39517,#39518,#39519,#39520,
#39521,#39522,#39523,#39524,#39525,#39526,#39527,#39528,#39529,#39530,#39531,
#39532,#39533,#39534,#39535,#39536,#39537,#39538,#39539,#39540,#39541,#39542,
#39543,#39544,#39545,#39546,#39547,#39548,#39549,#39550,#39551,#39552,#39553,
#39554,#39555,#39556,#39557,#39558,#39559,#39560,#39561,#39562,#39563,#39564,
#39565,#39566,#39567,#39568,#39569,#39570,#39571,#39572,#39573,#39574,#39575,
#39576,#39577,#39578,#39579,#39580,#39581,#39582,#39583,#39584,#39585,#39586,
#39587,#39588,#39589,#39590,#39591,#39592,#39593,#39594,#39595,#39596,#39597,
#39598,#39599,#39600,#39601,#39602,#39603,#39604,#39605,#39606,#39607,#39608,
#39609,#39610,#39611,#39612,#39613,#39614,#39615,#39616,#39617,#39618,#39619,
#39620,#39621,#39622,#39623,#39624,#39625,#39626,#39627,#39628,#39629,#39630,
#39631,#39632,#39633,#39634,#39635,#39636,#39637,#39638,#39639,#39640,#39641,
#39642,#39643,#39644,#39645,#39646,#39647,#39648,#39649,#39650,#39651,#39652,
#39653,#39654,#39655,#39656,#39657,#39658,#39659,#39660,#39661,#39662,#39663,
#39664,#39665,#39666,#39667,#39668,#39669,#39670,#39671,#39672,#39673,#39674,
#39675,#39676,#39677,#39678,#39679,#39680,#39681,#39682,#39683,#39684,#39685,
#39686,#39687,#39688,#39689,#39690,#39691,#39692,#39693,#39694,#39695,#39696,
#39697,#39698,#39699,#39700,#39701,#39702,#39703,#39704,#39705,#39706,#39707,
#39708,#39709,#39710,#39711,#39712,#39713,#39714,#39715,#39716,#39717,#39718,
#39719,#39720,#39721,#39722,#39723,#39724,#39725,#39726,#39727,#39728,#39729,
#39730,#39731,#39732,#39733,#39734,#39735,#39736,#39737,#39738,#39739,#39740,
#39741,#39742),(#39743,#39744,#39745,#39746,#39747,#39748,#39749,#39750,
#39751,#39752,#39753,#39754,#39755,#39756,#39757,#39758,#39759,#39760,#39761,
#39762,#39763,#39764,#39765,#39766,#39767,#39768,#39769,#39770,#39771,#39772,
#39773,#39774,#39775,#39776,#39777,#39778,#39779,#39780,#39781,#39782,#39783,
#39784,#39785,#39786,#39787,#39788,#39789,#39790,#39791,#39792,#39793,#39794,
#39795,#39796,#39797,#39798,#39799,#39800,#39801,#39802,#39803,#39804,#39805,
#39806,#39807,#39808,#39809,#39810,#39811,#39812,#39813,#39814,#39815,#39816,
#39817,#39818,#39819,#39820,#39821,#39822,#39823,#39824,#39825,#39826,#39827,
#39828,#39829,#39830,#39831,#39832,#39833,#39834,#39835,#39836,#39837,#39838,
#39839,#39840,#39841,#39842,#39843,#39844,#39845,#39846,#39847,#39848,#39849,
#39850,#39851,#39852,#39853,#39854,#39855,#39856,#39857,#39858,#39859,#39860,
#39861,#39862,#39863,#39864,#39865,#39866,#39867,#39868,#39869,#39870,#39871,
#39872,#39873,#39874,#39875,#39876,#39877,#39878,#39879,#39880,#39881,#39882,
#39883,#39884,#39885,#39886,#39887,#39888,#39889,#39890,#39891,#39892,#39893,
#39894,#39895,#39896,#39897,#39898,#39899,#39900,#39901,#39902,#39903,#39904,
#39905,#39906,#39907,#39908,#39909,#39910,#39911,#39912,#39913,#39914,#39915,
#39916,#39917,#39918,#39919,#39920,#39921,#39922,#39923,#39924,#39925,#39926,
#39927,#39928,#39929,#39930,#39931,#39932,#39933,#39934,#39935,#39936,#39937,
#39938,#39939,#39940,#39941,#39942,#39943,#39944,#39945,#39946,#39947,#39948,
#39949,#39950,#39951,#39952,#39953,#39954,#39955,#39956,#39957,#39958,#39959,
#39960,#39961,#39962,#39963,#39964,#39965,#39966,#39967,#39968,#39969,#39970,
#39971,#39972,#39973,#39974,#39975,#39976,#39977,#39978,#39979,#39980,#39981,
#39982,#39983,#39984,#39985,#39986,#39987,#39988,#39989,#39990,#39991,#39992,
#39993,#39994,#39995,#39996,#39997,#39998,#39999,#40000,#40001,#40002,#40003,
#40004,#40005,#40006,#40007,#40008,#40009,#40010,#40011,#40012,#40013,#40014,
#40015,#40016,#40017,#40018,#40019,#40020,#40021,#40022,#40023,#40024,#40025,
#40026,#40027,#40028,#40029,#40030,#40031,#40032,#40033,#40034,#40035,#40036,
#40037,#40038,#40039,#40040,#40041,#40042,#40043,#40044,#40045,#40046,#40047,
#40048,#40049,#40050,#40051,#40052,#40053,#40054,#40055,#40056,#40057,#40058,
#40059,#40060,#40061,#40062,#40063,#40064,#40065,#40066,#40067,#40068,#40069,
#40070,#40071,#40072,#40073,#40074,#40075,#40076,#40077,#40078,#40079,#40080,
#40081,#40082,#40083,#40084,#40085,#40086,#40087,#40088,#40089,#40090,#40091,
#40092,#40093,#40094,#40095,#40096,#40097,#40098,#40099,#40100,#40101,#40102,
#40103,#40104,#40105,#40106,#40107,#40108,#40109,#40110,#40111,#40112,#40113,
#40114,#40115,#40116,#40117,#40118,#40119,#40120,#40121,#40122,#40123,#40124,
#40125,#40126,#40127,#40128,#40129,#40130,#40131,#40132,#40133,#40134,#40135,
#40136,#40137,#40138,#40139,#40140,#40141,#40142,#40143,#40144,#40145,#40146,
#40147,#40148,#40149,#40150,#40151,#40152,#40153,#40154,#40155,#40156,#40157,
#40158,#40159,#40160,#40161,#40162,#40163,#40164,#40165,#40166,#40167,#40168,
#40169,#40170,#40171,#40172,#40173,#40174,#40175,#40176,#40177,#40178,#40179,
#40180,#40181,#40182,#40183,#40184,#40185,#40186,#40187,#40188,#40189,#40190,
#40191,#40192,#40193,#40194,#40195,#40196,#40197,#40198,#40199,#40200,#40201,
#40202,#40203,#40204,#40205,#40206,#40207,#40208,#40209,#40210,#40211,#40212,
#40213,#40214,#40215,#40216,#40217,#40218,#40219,#40220,#40221,#40222,#40223,
#40224,#40225,#40226,#40227,#40228,#40229,#40230,#40231,#40232,#40233,#40234,
#40235,#40236,#40237,#40238,#40239,#40240),(#40241,#40242,#40243,#40244,
#40245,#40246,#40247,#40248,#40249,#40250,#40251,#40252,#40253,#40254,#40255,
#40256,#40257,#40258,#40259,#40260,#40261,#40262,#40263,#40264,#40265,#40266,
#40267,#40268,#40269,#40270,#40271,#40272,#40273,#40274,#40275,#40276,#40277,
#40278,#40279,#40280,#40281,#40282,#40283,#40284,#40285,#40286,#40287,#40288,
#40289,#40290,#40291,#40292,#40293,#40294,#40295,#40296,#40297,#40298,#40299,
#40300,#40301,#40302,#40303,#40304,#40305,#40306,#40307,#40308,#40309,#40310,
#40311,#40312,#40313,#40314,#40315,#40316,#40317,#40318,#40319,#40320,#40321,
#40322,#40323,#40324,#40325,#40326,#40327,#40328,#40329,#40330,#40331,#40332,
#40333,#40334,#40335,#40336,#40337,#40338,#40339,#40340,#40341,#40342,#40343,
#40344,#40345,#40346,#40347,#40348,#40349,#40350,#40351,#40352,#40353,#40354,
#40355,#40356,#40357,#40358,#40359,#40360,#40361,#40362,#40363,#40364,#40365,
#40366,#40367,#40368,#40369,#40370,#40371,#40372,#40373,#40374,#40375,#40376,
#40377,#40378,#40379,#40380,#40381,#40382,#40383,#40384,#40385,#40386,#40387,
#40388,#40389,#40390,#40391,#40392,#40393,#40394,#40395,#40396,#40397,#40398,
#40399,#40400,#40401,#40402,#40403,#40404,#40405,#40406,#40407,#40408,#40409,
#40410,#40411,#40412,#40413,#40414,#40415,#40416,#40417,#40418,#40419,#40420,
#40421,#40422,#40423,#40424,#40425,#40426,#40427,#40428,#40429,#40430,#40431,
#40432,#40433,#40434,#40435,#40436,#40437,#40438,#40439,#40440,#40441,#40442,
#40443,#40444,#40445,#40446,#40447,#40448,#40449,#40450,#40451,#40452,#40453,
#40454,#40455,#40456,#40457,#40458,#40459,#40460,#40461,#40462,#40463,#40464,
#40465,#40466,#40467,#40468,#40469,#40470,#40471,#40472,#40473,#40474,#40475,
#40476,#40477,#40478,#40479,#40480,#40481,#40482,#40483,#40484,#40485,#40486,
#40487,#40488,#40489,#40490,#40491,#40492,#40493,#40494,#40495,#40496,#40497,
#40498,#40499,#40500,#40501,#40502,#40503,#40504,#40505,#40506,#40507,#40508,
#40509,#40510,#40511,#40512,#40513,#40514,#40515,#40516,#40517,#40518,#40519,
#40520,#40521,#40522,#40523,#40524,#40525,#40526,#40527,#40528,#40529,#40530,
#40531,#40532,#40533,#40534,#40535,#40536,#40537,#40538,#40539,#40540,#40541,
#40542,#40543,#40544,#40545,#40546,#40547,#40548,#40549,#40550,#40551,#40552,
#40553,#40554,#40555,#40556,#40557,#40558,#40559,#40560,#40561,#40562,#40563,
#40564,#40565,#40566,#40567,#40568,#40569,#40570,#40571,#40572,#40573,#40574,
#40575,#40576,#40577,#40578,#40579,#40580,#40581,#40582,#40583,#40584,#40585,
#40586,#40587,#40588,#40589,#40590,#40591,#40592,#40593,#40594,#40595,#40596,
#40597,#40598,#40599,#40600,#40601,#40602,#40603,#40604,#40605,#40606,#40607,
#40608,#40609,#40610,#40611,#40612,#40613,#40614,#40615,#40616,#40617,#40618,
#40619,#40620,#40621,#40622,#40623,#40624,#40625,#40626,#40627,#40628,#40629,
#40630,#40631,#40632,#40633,#40634,#40635,#40636,#40637,#40638,#40639,#40640,
#40641,#40642,#40643,#40644,#40645,#40646,#40647,#40648,#40649,#40650,#40651,
#40652,#40653,#40654,#40655,#40656,#40657,#40658,#40659,#40660,#40661,#40662,
#40663,#40664,#40665,#40666,#40667,#40668,#40669,#40670,#40671,#40672,#40673,
#40674,#40675,#40676,#40677,#40678,#40679,#40680,#40681,#40682,#40683,#40684,
#40685,#40686,#40687,#40688,#40689,#40690,#40691,#40692,#40693,#40694,#40695,
#40696,#40697,#40698,#40699,#40700,#40701,#40702,#40703,#40704,#40705,#40706,
#40707,#40708,#40709,#40710,#40711,#40712,#40713,#40714,#40715,#40716,#40717,
#40718,#40719,#40720,#40721,#40722,#40723,#40724,#40725,#40726,#40727,#40728,
#40729,#40730,#40731,#40732,#40733,#40734,#40735,#40736,#40737,#40738)),
 .UNSPECIFIED.,.F.,.F.,.F.,(4,4),(4,1,1,1,1,1,1,1,1,1,1,1,1,1,1,1,1,1,1,
1,1,1,1,1,1,1,1,1,1,1,1,1,1,1,1,1,1,1,1,1,1,1,1,1,1,1,1,1,1,1,1,1,1,1,1,
1,1,1,1,1,1,1,1,1,1,1,1,1,1,1,1,1,1,1,1,1,1,1,1,1,1,1,1,1,1,1,1,1,1,1,1,
1,1,1,1,1,1,1,1,1,1,1,1,1,1,1,1,1,1,1,1,1,1,1,1,1,1,1,1,1,1,1,1,1,1,1,1,
1,1,1,1,1,1,1,1,1,1,1,1,1,1,1,1,1,1,1,1,1,1,1,1,1,1,1,1,1,1,1,1,1,1,1,1,
1,1,1,1,1,1,1,1,1,1,1,1,1,1,1,1,1,1,1,1,1,1,1,1,1,1,1,1,1,1,1,1,1,1,1,1,
1,1,1,1,1,1,1,1,1,1,1,1,1,1,1,1,1,1,1,1,1,1,1,1,1,1,1,1,1,1,1,1,1,1,1,1,
1,1,1,1,1,1,1,1,1,1,1,1,1,1,1,1,1,1,1,1,1,1,1,1,1,1,1,1,1,1,1,1,1,1,1,1,
1,1,1,1,1,1,1,1,1,1,1,1,1,1,1,1,1,1,1,1,1,1,1,1,1,1,1,1,1,1,1,1,1,1,1,1,
1,1,1,1,1,1,1,1,1,1,1,1,1,1,1,1,1,1,1,1,1,1,1,1,1,1,1,1,1,1,1,1,1,1,1,1,
1,1,1,1,1,1,1,1,1,1,1,1,1,1,1,1,1,1,1,1,1,1,1,1,1,1,1,1,1,1,1,1,1,1,1,1,
1,1,1,1,1,1,1,1,1,1,1,1,1,1,1,1,1,1,1,1,1,1,1,1,1,1,1,1,1,1,1,1,1,1,1,1,
1,1,1,1,1,1,1,1,1,1,1,1,1,1,1,1,1,1,1,1,1,1,1,1,1,1,1,1,1,1,1,1,1,1,1,1,
1,1,1,1,1,1,1,1,1,1,1,1,1,1,1,1,1,1,1,1,1,1,1,1,1,1,1,1,1,1,1,1,1,1,1,1,
1,1,1,1,1,1,1,1,4),(0.,0.184512097253587),(8.98171729021681,9.48139635699984,
9.98107542378286,10.4807544905659,10.9804335573489,11.4801126241319,11.979791690915,
12.479470757698,12.979149824481,13.478828891264,13.9785079580471,14.4781870248301,
14.9778660916131,15.4775451583961,15.9772242251791,16.4769032919622,16.9765823587452,
17.4762614255282,17.9759404923112,18.4756195590943,18.9752986258773,19.4749776926603,
19.9746567594433,20.4743358262264,20.9740148930094,21.4736939597924,21.9733730265754,
22.4730520933585,22.9727311601415,23.4724102269245,23.9720892937075,24.4717683604905,
24.9714474272736,25.4711264940566,25.9708055608396,26.4704846276226,26.9701636944057,
27.4698427611887,27.9695218279717,28.4692008947547,28.9688799615378,29.4685590283208,
29.9682380951038,30.4679171618868,30.9675962286699,31.4672752954529,31.9669543622359,
32.4666334290189,32.966312495802,33.465991562585,33.965670629368,34.465349696151,
34.965028762934,35.4647078297171,35.9643868965001,36.4640659632831,36.9637450300661,
37.4634240968492,37.9631031636322,38.4627822304152,38.9624612971982,39.4621403639813,
39.9618194307643,40.4614984975473,40.9611775643303,41.4608566311134,41.9605356978964,
42.4602147646794,42.9598938314624,43.4595728982454,43.9592519650285,44.4589310318115,
44.9586100985945,45.4582891653775,45.9579682321606,46.4576472989436,46.9573263657266,
47.4570054325096,47.9566844992927,48.4563635660757,48.9560426328587,49.4557216996417,
49.9554007664248,50.4550798332078,50.9547588999908,51.4544379667738,51.9541170335568,
52.4537961003399,52.9534751671229,53.4531542339059,53.9528333006889,54.452512367472,
54.952191434255,55.451870501038,55.951549567821,56.4512286346041,56.9509077013871,
57.4505867681701,57.9502658349531,58.4499449017362,58.9496239685192,59.9489821020852,
60.9483402356513,61.9476983692173,62.9470565027834,63.9464146363494,64.9457727699155,
65.9451309034815,66.9444890370476,67.9438471706136,68.9432053041797,69.9425634377457,
70.9419215713118,71.9412797048778,72.9406378384438,73.9399959720099,74.9393541055759,
75.938712239142,76.938070372708,77.9374285062741,78.9367866398401,79.9361447734062,
80.9355029069722,81.9348610405383,82.9342191741043,83.9335773076704,84.9329354412364,
85.9322935748025,86.9316517083685,87.9310098419346,88.9303679755006,89.9297261090666,
90.9290842426327,91.9284423761987,92.9278005097648,93.9271586433308,94.9265167768969,
95.9258749104629,96.925233044029,97.924591177595,98.9239493111611,99.9233074447271,
100.922665578293,101.922023711859,102.921381845425,103.920739978991,104.920098112557,
105.919456246123,106.918814379689,107.918172513255,108.917530646822,109.916888780388,
110.916246913954,111.91560504752,112.914963181086,113.914321314652,114.913679448218,
115.913037581784,116.91239571535,117.911753848916,118.911111982482,119.910470116048,
120.909828249614,121.90918638318,122.908544516746,123.907902650312,124.907260783878,
125.906618917444,126.90597705101,127.905335184576,128.904693318142,129.904051451709,
130.903409585275,131.902767718841,132.902125852407,133.901483985973,134.900842119539,
135.900200253105,136.899558386671,137.898916520237,138.898274653803,139.897632787369,
140.896990920935,141.896349054501,142.895707188067,143.895065321633,144.894423455199,
145.893781588765,146.893139722331,147.892497855897,148.891855989463,149.891214123029,
150.890572256596,151.889930390162,152.889288523728,153.888646657294,154.88800479086,
155.887362924426,156.886721057992,157.886079191558,158.885437325124,159.88479545869,
160.884153592256,161.883511725822,162.882869859388,163.882227992954,164.88158612652,
165.880944260086,166.880302393652,167.879660527218,168.879018660784,169.87837679435,
170.877734927916,171.877093061483,172.876451195049,173.875809328615,174.875167462181,
175.874525595747,176.873883729313,177.873241862879,178.872599996445,179.871958130011,
180.871316263577,181.870674397143,182.870032530709,183.869390664275,184.868748797841,
185.868106931407,186.867465064973,187.866823198539,188.866181332105,189.865539465671,
190.864897599237,191.864255732803,192.86361386637,193.862971999936,194.862330133502,
195.861688267068,196.861046400634,197.8604045342,198.859762667766,199.859120801332,
200.858478934898,201.857837068464,202.85719520203,203.856553335596,204.855911469162,
205.855269602728,206.854627736294,207.85398586986,208.853344003426,209.852702136992,
210.852060270558,211.851418404124,212.85077653769,213.850134671257,214.849492804823,
215.848850938389,216.848209071955,217.847567205521,218.846925339087,219.846283472653,
220.845641606219,221.844999739785,222.844357873351,223.843716006917,224.843074140483,
225.842432274049,226.841790407615,227.841148541181,228.840506674747,229.839864808313,
230.839222941879,231.838581075445,232.837939209011,233.837297342577,234.836655476144,
235.83601360971,236.835371743276,237.834729876842,238.834088010408,239.833446143974,
240.83280427754,241.832162411106,242.831520544672,243.830878678238,244.830236811804,
245.82959494537,246.828953078936,247.828311212502,248.827669346068,249.827027479634,
250.8263856132,251.825743746766,252.825101880332,253.824460013898,254.823818147464,
255.82317628103,256.822534414597,257.821892548163,258.821250681729,259.820608815295,
260.819966948861,261.819325082427,262.818683215993,263.818041349559,264.817399483125,
265.816757616691,266.816115750257,267.815473883823,268.814832017389,269.814190150955,
270.813548284521,271.812906418087,272.812264551653,273.811622685219,274.810980818785,
275.810338952351,276.809697085917,277.809055219484,278.80841335305,279.807771486616,
280.807129620182,281.806487753748,282.805845887314,283.80520402088,284.804562154446,
285.803920288012,286.803278421578,287.802636555144,288.80199468871,289.801352822276,
290.800710955842,291.800069089408,292.799427222974,293.79878535654,294.798143490106,
295.797501623672,296.796859757238,297.796217890804,298.795576024371,299.794934157937,
300.794292291503,301.793650425069,302.793008558635,303.792366692201,304.791724825767,
305.791082959333,306.790441092899,307.789799226465,308.789157360031,309.788515493597,
310.787873627163,311.787231760729,312.786589894295,313.785948027861,314.785306161427,
315.784664294993,316.784022428559,317.783380562125,318.782738695691,319.782096829258,
320.781454962824,321.78081309639,322.780171229956,323.779529363522,324.778887497088,
325.778245630654,326.77760376422,327.776961897786,328.776320031352,329.775678164918,
330.775036298484,331.77439443205,332.773752565616,333.773110699182,334.772468832748,
335.771826966314,336.77118509988,337.770543233446,338.769901367012,339.769259500578,
340.768617634145,341.767975767711,342.767333901277,343.766692034843,344.766050168409,
345.765408301975,346.764766435541,347.764124569107,348.763482702673,349.762840836239,
350.762198969805,351.761557103371,352.760915236937,353.760273370503,354.259952437286,
354.759631504069,355.259310570852,355.758989637635,356.258668704418,356.758347771201,
357.258026837984,357.757705904767,358.25738497155,358.757064038333,359.256743105116,
359.756422171899,360.256101238682,360.755780305465,361.255459372248,361.755138439031,
362.254817505815,362.754496572598,363.254175639381,363.753854706164,364.253533772947,
364.75321283973,365.252891906513,365.752570973296,366.252250040079,366.751929106862,
367.251608173645,367.751287240428,368.250966307211,368.750645373994,369.250324440777,
369.75000350756,370.249682574343,370.749361641126,371.249040707909,371.748719774692,
372.248398841475,372.748077908258,373.247756975041,373.747436041824,374.247115108607,
374.74679417539,375.246473242173,375.746152308956,376.245831375739,376.745510442522,
377.245189509305,377.744868576088,378.244547642871,378.744226709654,379.243905776437,
379.74358484322,380.243263910003,380.742942976786,381.242622043569,381.742301110352,
382.241980177135,382.741659243918,383.241338310702,383.741017377485,384.240696444268,
384.740375511051,385.240054577834,385.739733644617,386.2394127114,386.739091778183,
387.238770844966,387.738449911749,388.238128978532,388.737808045315,389.237487112098,
389.737166178881,390.236845245664,390.736524312447,391.23620337923,391.735882446013,
392.235561512796,392.735240579579,393.234919646362,393.734598713145,394.234277779928,
394.733956846711,395.233635913494,395.733314980277,396.23299404706,396.732673113843,
397.232352180626,397.732031247409,398.231710314192,398.731389380975,399.231068447758,
399.730747514541,400.230426581324,400.730105648107,401.22978471489,401.729463781673,
402.229142848456,402.728821915239,403.228500982022,403.728180048805),
 .UNSPECIFIED.);
#14=B_SPLINE_SURFACE_WITH_KNOTS('',3,3,((#40832,#40833,#40834,#40835,#40836,
#40837,#40838,#40839,#40840,#40841,#40842,#40843,#40844,#40845,#40846,#40847,
#40848,#40849,#40850,#40851,#40852,#40853,#40854,#40855,#40856,#40857,#40858,
#40859,#40860,#40861,#40862,#40863,#40864,#40865,#40866,#40867,#40868,#40869,
#40870,#40871,#40872,#40873,#40874,#40875,#40876,#40877,#40878,#40879,#40880,
#40881,#40882,#40883,#40884,#40885,#40886,#40887,#40888,#40889,#40890,#40891,
#40892,#40893,#40894,#40895,#40896,#40897,#40898,#40899,#40900,#40901,#40902,
#40903,#40904,#40905,#40906,#40907,#40908,#40909,#40910,#40911,#40912,#40913,
#40914,#40915,#40916,#40917,#40918,#40919,#40920,#40921,#40922,#40923,#40924,
#40925,#40926,#40927,#40928,#40929,#40930,#40931,#40932,#40933,#40934,#40935,
#40936,#40937,#40938,#40939,#40940,#40941,#40942,#40943,#40944,#40945,#40946,
#40947,#40948,#40949,#40950,#40951,#40952,#40953,#40954,#40955,#40956,#40957,
#40958,#40959,#40960,#40961,#40962,#40963,#40964,#40965,#40966,#40967,#40968,
#40969,#40970,#40971,#40972,#40973,#40974,#40975,#40976,#40977,#40978,#40979,
#40980,#40981,#40982,#40983,#40984,#40985,#40986,#40987,#40988,#40989,#40990,
#40991,#40992,#40993,#40994,#40995,#40996,#40997,#40998,#40999,#41000,#41001,
#41002,#41003,#41004,#41005,#41006,#41007,#41008,#41009,#41010,#41011,#41012,
#41013,#41014,#41015,#41016,#41017,#41018,#41019,#41020,#41021,#41022,#41023,
#41024,#41025,#41026,#41027,#41028,#41029,#41030,#41031,#41032,#41033,#41034,
#41035,#41036,#41037,#41038,#41039,#41040,#41041,#41042,#41043,#41044,#41045,
#41046,#41047,#41048,#41049,#41050,#41051,#41052,#41053,#41054,#41055,#41056,
#41057,#41058,#41059,#41060,#41061,#41062,#41063,#41064,#41065,#41066,#41067,
#41068,#41069,#41070,#41071,#41072,#41073,#41074,#41075,#41076,#41077,#41078,
#41079,#41080,#41081,#41082,#41083,#41084,#41085,#41086,#41087,#41088,#41089,
#41090,#41091,#41092,#41093,#41094,#41095,#41096,#41097,#41098,#41099,#41100,
#41101,#41102,#41103,#41104,#41105,#41106,#41107,#41108,#41109,#41110,#41111,
#41112,#41113,#41114,#41115,#41116,#41117,#41118,#41119,#41120,#41121,#41122,
#41123,#41124,#41125,#41126,#41127,#41128,#41129,#41130,#41131,#41132,#41133,
#41134,#41135,#41136,#41137,#41138,#41139,#41140,#41141,#41142,#41143,#41144,
#41145,#41146,#41147,#41148,#41149,#41150,#41151,#41152,#41153,#41154,#41155,
#41156,#41157,#41158,#41159,#41160,#41161,#41162,#41163,#41164,#41165,#41166,
#41167,#41168,#41169,#41170,#41171,#41172,#41173,#41174,#41175,#41176,#41177,
#41178,#41179,#41180,#41181,#41182,#41183,#41184,#41185,#41186,#41187,#41188,
#41189,#41190,#41191,#41192,#41193,#41194,#41195,#41196,#41197,#41198,#41199,
#41200,#41201,#41202,#41203,#41204,#41205,#41206,#41207,#41208,#41209,#41210,
#41211,#41212,#41213,#41214,#41215,#41216,#41217,#41218,#41219,#41220,#41221,
#41222,#41223,#41224,#41225,#41226,#41227,#41228,#41229,#41230,#41231,#41232,
#41233,#41234,#41235,#41236,#41237,#41238,#41239,#41240,#41241,#41242,#41243,
#41244,#41245,#41246,#41247,#41248,#41249,#41250,#41251,#41252,#41253,#41254,
#41255,#41256,#41257,#41258,#41259,#41260,#41261,#41262,#41263,#41264,#41265,
#41266,#41267,#41268,#41269,#41270,#41271,#41272,#41273,#41274,#41275,#41276,
#41277,#41278,#41279,#41280,#41281,#41282,#41283,#41284,#41285,#41286,#41287,
#41288,#41289,#41290,#41291,#41292,#41293,#41294,#41295,#41296,#41297,#41298,
#41299,#41300,#41301,#41302,#41303,#41304,#41305,#41306,#41307,#41308,#41309,
#41310,#41311,#41312,#41313,#41314,#41315,#41316,#41317,#41318,#41319,#41320,
#41321,#41322,#41323,#41324,#41325,#41326,#41327,#41328,#41329),(#41330,
#41331,#41332,#41333,#41334,#41335,#41336,#41337,#41338,#41339,#41340,#41341,
#41342,#41343,#41344,#41345,#41346,#41347,#41348,#41349,#41350,#41351,#41352,
#41353,#41354,#41355,#41356,#41357,#41358,#41359,#41360,#41361,#41362,#41363,
#41364,#41365,#41366,#41367,#41368,#41369,#41370,#41371,#41372,#41373,#41374,
#41375,#41376,#41377,#41378,#41379,#41380,#41381,#41382,#41383,#41384,#41385,
#41386,#41387,#41388,#41389,#41390,#41391,#41392,#41393,#41394,#41395,#41396,
#41397,#41398,#41399,#41400,#41401,#41402,#41403,#41404,#41405,#41406,#41407,
#41408,#41409,#41410,#41411,#41412,#41413,#41414,#41415,#41416,#41417,#41418,
#41419,#41420,#41421,#41422,#41423,#41424,#41425,#41426,#41427,#41428,#41429,
#41430,#41431,#41432,#41433,#41434,#41435,#41436,#41437,#41438,#41439,#41440,
#41441,#41442,#41443,#41444,#41445,#41446,#41447,#41448,#41449,#41450,#41451,
#41452,#41453,#41454,#41455,#41456,#41457,#41458,#41459,#41460,#41461,#41462,
#41463,#41464,#41465,#41466,#41467,#41468,#41469,#41470,#41471,#41472,#41473,
#41474,#41475,#41476,#41477,#41478,#41479,#41480,#41481,#41482,#41483,#41484,
#41485,#41486,#41487,#41488,#41489,#41490,#41491,#41492,#41493,#41494,#41495,
#41496,#41497,#41498,#41499,#41500,#41501,#41502,#41503,#41504,#41505,#41506,
#41507,#41508,#41509,#41510,#41511,#41512,#41513,#41514,#41515,#41516,#41517,
#41518,#41519,#41520,#41521,#41522,#41523,#41524,#41525,#41526,#41527,#41528,
#41529,#41530,#41531,#41532,#41533,#41534,#41535,#41536,#41537,#41538,#41539,
#41540,#41541,#41542,#41543,#41544,#41545,#41546,#41547,#41548,#41549,#41550,
#41551,#41552,#41553,#41554,#41555,#41556,#41557,#41558,#41559,#41560,#41561,
#41562,#41563,#41564,#41565,#41566,#41567,#41568,#41569,#41570,#41571,#41572,
#41573,#41574,#41575,#41576,#41577,#41578,#41579,#41580,#41581,#41582,#41583,
#41584,#41585,#41586,#41587,#41588,#41589,#41590,#41591,#41592,#41593,#41594,
#41595,#41596,#41597,#41598,#41599,#41600,#41601,#41602,#41603,#41604,#41605,
#41606,#41607,#41608,#41609,#41610,#41611,#41612,#41613,#41614,#41615,#41616,
#41617,#41618,#41619,#41620,#41621,#41622,#41623,#41624,#41625,#41626,#41627,
#41628,#41629,#41630,#41631,#41632,#41633,#41634,#41635,#41636,#41637,#41638,
#41639,#41640,#41641,#41642,#41643,#41644,#41645,#41646,#41647,#41648,#41649,
#41650,#41651,#41652,#41653,#41654,#41655,#41656,#41657,#41658,#41659,#41660,
#41661,#41662,#41663,#41664,#41665,#41666,#41667,#41668,#41669,#41670,#41671,
#41672,#41673,#41674,#41675,#41676,#41677,#41678,#41679,#41680,#41681,#41682,
#41683,#41684,#41685,#41686,#41687,#41688,#41689,#41690,#41691,#41692,#41693,
#41694,#41695,#41696,#41697,#41698,#41699,#41700,#41701,#41702,#41703,#41704,
#41705,#41706,#41707,#41708,#41709,#41710,#41711,#41712,#41713,#41714,#41715,
#41716,#41717,#41718,#41719,#41720,#41721,#41722,#41723,#41724,#41725,#41726,
#41727,#41728,#41729,#41730,#41731,#41732,#41733,#41734,#41735,#41736,#41737,
#41738,#41739,#41740,#41741,#41742,#41743,#41744,#41745,#41746,#41747,#41748,
#41749,#41750,#41751,#41752,#41753,#41754,#41755,#41756,#41757,#41758,#41759,
#41760,#41761,#41762,#41763,#41764,#41765,#41766,#41767,#41768,#41769,#41770,
#41771,#41772,#41773,#41774,#41775,#41776,#41777,#41778,#41779,#41780,#41781,
#41782,#41783,#41784,#41785,#41786,#41787,#41788,#41789,#41790,#41791,#41792,
#41793,#41794,#41795,#41796,#41797,#41798,#41799,#41800,#41801,#41802,#41803,
#41804,#41805,#41806,#41807,#41808,#41809,#41810,#41811,#41812,#41813,#41814,
#41815,#41816,#41817,#41818,#41819,#41820,#41821,#41822,#41823,#41824,#41825,
#41826,#41827),(#41828,#41829,#41830,#41831,#41832,#41833,#41834,#41835,
#41836,#41837,#41838,#41839,#41840,#41841,#41842,#41843,#41844,#41845,#41846,
#41847,#41848,#41849,#41850,#41851,#41852,#41853,#41854,#41855,#41856,#41857,
#41858,#41859,#41860,#41861,#41862,#41863,#41864,#41865,#41866,#41867,#41868,
#41869,#41870,#41871,#41872,#41873,#41874,#41875,#41876,#41877,#41878,#41879,
#41880,#41881,#41882,#41883,#41884,#41885,#41886,#41887,#41888,#41889,#41890,
#41891,#41892,#41893,#41894,#41895,#41896,#41897,#41898,#41899,#41900,#41901,
#41902,#41903,#41904,#41905,#41906,#41907,#41908,#41909,#41910,#41911,#41912,
#41913,#41914,#41915,#41916,#41917,#41918,#41919,#41920,#41921,#41922,#41923,
#41924,#41925,#41926,#41927,#41928,#41929,#41930,#41931,#41932,#41933,#41934,
#41935,#41936,#41937,#41938,#41939,#41940,#41941,#41942,#41943,#41944,#41945,
#41946,#41947,#41948,#41949,#41950,#41951,#41952,#41953,#41954,#41955,#41956,
#41957,#41958,#41959,#41960,#41961,#41962,#41963,#41964,#41965,#41966,#41967,
#41968,#41969,#41970,#41971,#41972,#41973,#41974,#41975,#41976,#41977,#41978,
#41979,#41980,#41981,#41982,#41983,#41984,#41985,#41986,#41987,#41988,#41989,
#41990,#41991,#41992,#41993,#41994,#41995,#41996,#41997,#41998,#41999,#42000,
#42001,#42002,#42003,#42004,#42005,#42006,#42007,#42008,#42009,#42010,#42011,
#42012,#42013,#42014,#42015,#42016,#42017,#42018,#42019,#42020,#42021,#42022,
#42023,#42024,#42025,#42026,#42027,#42028,#42029,#42030,#42031,#42032,#42033,
#42034,#42035,#42036,#42037,#42038,#42039,#42040,#42041,#42042,#42043,#42044,
#42045,#42046,#42047,#42048,#42049,#42050,#42051,#42052,#42053,#42054,#42055,
#42056,#42057,#42058,#42059,#42060,#42061,#42062,#42063,#42064,#42065,#42066,
#42067,#42068,#42069,#42070,#42071,#42072,#42073,#42074,#42075,#42076,#42077,
#42078,#42079,#42080,#42081,#42082,#42083,#42084,#42085,#42086,#42087,#42088,
#42089,#42090,#42091,#42092,#42093,#42094,#42095,#42096,#42097,#42098,#42099,
#42100,#42101,#42102,#42103,#42104,#42105,#42106,#42107,#42108,#42109,#42110,
#42111,#42112,#42113,#42114,#42115,#42116,#42117,#42118,#42119,#42120,#42121,
#42122,#42123,#42124,#42125,#42126,#42127,#42128,#42129,#42130,#42131,#42132,
#42133,#42134,#42135,#42136,#42137,#42138,#42139,#42140,#42141,#42142,#42143,
#42144,#42145,#42146,#42147,#42148,#42149,#42150,#42151,#42152,#42153,#42154,
#42155,#42156,#42157,#42158,#42159,#42160,#42161,#42162,#42163,#42164,#42165,
#42166,#42167,#42168,#42169,#42170,#42171,#42172,#42173,#42174,#42175,#42176,
#42177,#42178,#42179,#42180,#42181,#42182,#42183,#42184,#42185,#42186,#42187,
#42188,#42189,#42190,#42191,#42192,#42193,#42194,#42195,#42196,#42197,#42198,
#42199,#42200,#42201,#42202,#42203,#42204,#42205,#42206,#42207,#42208,#42209,
#42210,#42211,#42212,#42213,#42214,#42215,#42216,#42217,#42218,#42219,#42220,
#42221,#42222,#42223,#42224,#42225,#42226,#42227,#42228,#42229,#42230,#42231,
#42232,#42233,#42234,#42235,#42236,#42237,#42238,#42239,#42240,#42241,#42242,
#42243,#42244,#42245,#42246,#42247,#42248,#42249,#42250,#42251,#42252,#42253,
#42254,#42255,#42256,#42257,#42258,#42259,#42260,#42261,#42262,#42263,#42264,
#42265,#42266,#42267,#42268,#42269,#42270,#42271,#42272,#42273,#42274,#42275,
#42276,#42277,#42278,#42279,#42280,#42281,#42282,#42283,#42284,#42285,#42286,
#42287,#42288,#42289,#42290,#42291,#42292,#42293,#42294,#42295,#42296,#42297,
#42298,#42299,#42300,#42301,#42302,#42303,#42304,#42305,#42306,#42307,#42308,
#42309,#42310,#42311,#42312,#42313,#42314,#42315,#42316,#42317,#42318,#42319,
#42320,#42321,#42322,#42323,#42324,#42325),(#42326,#42327,#42328,#42329,
#42330,#42331,#42332,#42333,#42334,#42335,#42336,#42337,#42338,#42339,#42340,
#42341,#42342,#42343,#42344,#42345,#42346,#42347,#42348,#42349,#42350,#42351,
#42352,#42353,#42354,#42355,#42356,#42357,#42358,#42359,#42360,#42361,#42362,
#42363,#42364,#42365,#42366,#42367,#42368,#42369,#42370,#42371,#42372,#42373,
#42374,#42375,#42376,#42377,#42378,#42379,#42380,#42381,#42382,#42383,#42384,
#42385,#42386,#42387,#42388,#42389,#42390,#42391,#42392,#42393,#42394,#42395,
#42396,#42397,#42398,#42399,#42400,#42401,#42402,#42403,#42404,#42405,#42406,
#42407,#42408,#42409,#42410,#42411,#42412,#42413,#42414,#42415,#42416,#42417,
#42418,#42419,#42420,#42421,#42422,#42423,#42424,#42425,#42426,#42427,#42428,
#42429,#42430,#42431,#42432,#42433,#42434,#42435,#42436,#42437,#42438,#42439,
#42440,#42441,#42442,#42443,#42444,#42445,#42446,#42447,#42448,#42449,#42450,
#42451,#42452,#42453,#42454,#42455,#42456,#42457,#42458,#42459,#42460,#42461,
#42462,#42463,#42464,#42465,#42466,#42467,#42468,#42469,#42470,#42471,#42472,
#42473,#42474,#42475,#42476,#42477,#42478,#42479,#42480,#42481,#42482,#42483,
#42484,#42485,#42486,#42487,#42488,#42489,#42490,#42491,#42492,#42493,#42494,
#42495,#42496,#42497,#42498,#42499,#42500,#42501,#42502,#42503,#42504,#42505,
#42506,#42507,#42508,#42509,#42510,#42511,#42512,#42513,#42514,#42515,#42516,
#42517,#42518,#42519,#42520,#42521,#42522,#42523,#42524,#42525,#42526,#42527,
#42528,#42529,#42530,#42531,#42532,#42533,#42534,#42535,#42536,#42537,#42538,
#42539,#42540,#42541,#42542,#42543,#42544,#42545,#42546,#42547,#42548,#42549,
#42550,#42551,#42552,#42553,#42554,#42555,#42556,#42557,#42558,#42559,#42560,
#42561,#42562,#42563,#42564,#42565,#42566,#42567,#42568,#42569,#42570,#42571,
#42572,#42573,#42574,#42575,#42576,#42577,#42578,#42579,#42580,#42581,#42582,
#42583,#42584,#42585,#42586,#42587,#42588,#42589,#42590,#42591,#42592,#42593,
#42594,#42595,#42596,#42597,#42598,#42599,#42600,#42601,#42602,#42603,#42604,
#42605,#42606,#42607,#42608,#42609,#42610,#42611,#42612,#42613,#42614,#42615,
#42616,#42617,#42618,#42619,#42620,#42621,#42622,#42623,#42624,#42625,#42626,
#42627,#42628,#42629,#42630,#42631,#42632,#42633,#42634,#42635,#42636,#42637,
#42638,#42639,#42640,#42641,#42642,#42643,#42644,#42645,#42646,#42647,#42648,
#42649,#42650,#42651,#42652,#42653,#42654,#42655,#42656,#42657,#42658,#42659,
#42660,#42661,#42662,#42663,#42664,#42665,#42666,#42667,#42668,#42669,#42670,
#42671,#42672,#42673,#42674,#42675,#42676,#42677,#42678,#42679,#42680,#42681,
#42682,#42683,#42684,#42685,#42686,#42687,#42688,#42689,#42690,#42691,#42692,
#42693,#42694,#42695,#42696,#42697,#42698,#42699,#42700,#42701,#42702,#42703,
#42704,#42705,#42706,#42707,#42708,#42709,#42710,#42711,#42712,#42713,#42714,
#42715,#42716,#42717,#42718,#42719,#42720,#42721,#42722,#42723,#42724,#42725,
#42726,#42727,#42728,#42729,#42730,#42731,#42732,#42733,#42734,#42735,#42736,
#42737,#42738,#42739,#42740,#42741,#42742,#42743,#42744,#42745,#42746,#42747,
#42748,#42749,#42750,#42751,#42752,#42753,#42754,#42755,#42756,#42757,#42758,
#42759,#42760,#42761,#42762,#42763,#42764,#42765,#42766,#42767,#42768,#42769,
#42770,#42771,#42772,#42773,#42774,#42775,#42776,#42777,#42778,#42779,#42780,
#42781,#42782,#42783,#42784,#42785,#42786,#42787,#42788,#42789,#42790,#42791,
#42792,#42793,#42794,#42795,#42796,#42797,#42798,#42799,#42800,#42801,#42802,
#42803,#42804,#42805,#42806,#42807,#42808,#42809,#42810,#42811,#42812,#42813,
#42814,#42815,#42816,#42817,#42818,#42819,#42820,#42821,#42822,#42823)),
 .UNSPECIFIED.,.F.,.F.,.F.,(4,4),(4,1,1,1,1,1,1,1,1,1,1,1,1,1,1,1,1,1,1,
1,1,1,1,1,1,1,1,1,1,1,1,1,1,1,1,1,1,1,1,1,1,1,1,1,1,1,1,1,1,1,1,1,1,1,1,
1,1,1,1,1,1,1,1,1,1,1,1,1,1,1,1,1,1,1,1,1,1,1,1,1,1,1,1,1,1,1,1,1,1,1,1,
1,1,1,1,1,1,1,1,1,1,1,1,1,1,1,1,1,1,1,1,1,1,1,1,1,1,1,1,1,1,1,1,1,1,1,1,
1,1,1,1,1,1,1,1,1,1,1,1,1,1,1,1,1,1,1,1,1,1,1,1,1,1,1,1,1,1,1,1,1,1,1,1,
1,1,1,1,1,1,1,1,1,1,1,1,1,1,1,1,1,1,1,1,1,1,1,1,1,1,1,1,1,1,1,1,1,1,1,1,
1,1,1,1,1,1,1,1,1,1,1,1,1,1,1,1,1,1,1,1,1,1,1,1,1,1,1,1,1,1,1,1,1,1,1,1,
1,1,1,1,1,1,1,1,1,1,1,1,1,1,1,1,1,1,1,1,1,1,1,1,1,1,1,1,1,1,1,1,1,1,1,1,
1,1,1,1,1,1,1,1,1,1,1,1,1,1,1,1,1,1,1,1,1,1,1,1,1,1,1,1,1,1,1,1,1,1,1,1,
1,1,1,1,1,1,1,1,1,1,1,1,1,1,1,1,1,1,1,1,1,1,1,1,1,1,1,1,1,1,1,1,1,1,1,1,
1,1,1,1,1,1,1,1,1,1,1,1,1,1,1,1,1,1,1,1,1,1,1,1,1,1,1,1,1,1,1,1,1,1,1,1,
1,1,1,1,1,1,1,1,1,1,1,1,1,1,1,1,1,1,1,1,1,1,1,1,1,1,1,1,1,1,1,1,1,1,1,1,
1,1,1,1,1,1,1,1,1,1,1,1,1,1,1,1,1,1,1,1,1,1,1,1,1,1,1,1,1,1,1,1,1,1,1,1,
1,1,1,1,1,1,1,1,1,1,1,1,1,1,1,1,1,1,1,1,1,1,1,1,1,1,1,1,1,1,1,1,1,1,1,1,
1,1,1,1,1,1,1,1,4),(0.,0.184512097253587),(12.0092477762453,12.5089268430284,
13.0086059098114,13.5082849765944,14.0079640433774,14.5076431101605,15.0073221769435,
15.5070012437265,16.0066803105095,16.5063593772925,17.0060384440756,17.5057175108586,
18.0053965776416,18.5050756444246,19.0047547112077,19.5044337779907,20.0041128447737,
20.5037919115567,21.0034709783398,21.5031500451228,22.0028291119058,22.5025081786888,
23.0021872454719,23.5018663122549,24.0015453790379,24.5012244458209,25.0009035126039,
25.500582579387,26.00026164617,26.499940712953,26.999619779736,27.4992988465191,
27.9989779133021,28.4986569800851,28.9983360468681,29.4980151136512,29.9976941804342,
30.4973732472172,30.9970523140002,31.4967313807832,31.9964104475663,32.4960895143493,
32.9957685811323,33.4954476479153,33.9951267146984,34.4948057814814,34.9944848482644,
35.4941639150474,35.9938429818305,36.4935220486135,36.9932011153965,37.4928801821795,
37.9925592489626,38.4922383157456,38.9919173825286,39.4915964493116,39.9912755160946,
40.4909545828777,40.9906336496607,41.4903127164437,41.9899917832267,42.4896708500098,
42.9893499167928,43.4890289835758,43.9887080503588,44.4883871171419,44.9880661839249,
45.4877452507079,45.9874243174909,46.4871033842739,46.986782451057,47.48646151784,
47.986140584623,48.485819651406,48.9854987181891,49.4851777849721,49.9848568517551,
50.4845359185381,50.9842149853212,51.4838940521042,51.9835731188872,52.4832521856702,
52.9829312524532,53.4826103192363,53.9822893860193,54.4819684528023,54.9816475195853,
55.4813265863684,55.9810056531514,56.4806847199344,56.9803637867174,57.4800428535005,
57.9797219202835,58.4794009870665,58.9790800538495,59.4787591206325,59.9784381874156,
60.4781172541986,60.9777963209816,61.4774753877646,61.9771544545477,62.9765125881137,
63.9758707216798,64.9752288552458,65.9745869888119,66.9739451223779,67.9733032559439,
68.97266138951,69.972019523076,70.9713776566421,71.9707357902081,72.9700939237742,
73.9694520573402,74.9688101909063,75.9681683244723,76.9675264580384,77.9668845916044,
78.9662427251705,79.9656008587365,80.9649589923026,81.9643171258686,82.9636752594347,
83.9630333930007,84.9623915265667,85.9617496601328,86.9611077936988,87.9604659272649,
88.9598240608309,89.959182194397,90.958540327963,91.9578984615291,92.9572565950951,
93.9566147286612,94.9559728622272,95.9553309957932,96.9546891293593,97.9540472629253,
98.9534053964914,99.9527635300574,100.952121663623,101.95147979719,102.950837930756,
103.950196064322,104.949554197888,105.948912331454,106.94827046502,107.947628598586,
108.946986732152,109.946344865718,110.945702999284,111.94506113285,112.944419266416,
113.943777399982,114.943135533548,115.942493667114,116.94185180068,117.941209934246,
118.940568067812,119.939926201378,120.939284334944,121.93864246851,122.938000602077,
123.937358735643,124.936716869209,125.936075002775,126.935433136341,127.934791269907,
128.934149403473,129.933507537039,130.932865670605,131.932223804171,132.931581937737,
133.930940071303,134.930298204869,135.929656338435,136.929014472001,137.928372605567,
138.927730739133,139.927088872699,140.926447006265,141.925805139831,142.925163273397,
143.924521406963,144.92387954053,145.923237674096,146.922595807662,147.921953941228,
148.921312074794,149.92067020836,150.920028341926,151.919386475492,152.918744609058,
153.918102742624,154.91746087619,155.916819009756,156.916177143322,157.915535276888,
158.914893410454,159.91425154402,160.913609677586,161.912967811152,162.912325944718,
163.911684078284,164.91104221185,165.910400345416,166.909758478983,167.909116612549,
168.908474746115,169.907832879681,170.907191013247,171.906549146813,172.905907280379,
173.905265413945,174.904623547511,175.903981681077,176.903339814643,177.902697948209,
178.902056081775,179.901414215341,180.900772348907,181.900130482473,182.899488616039,
183.898846749605,184.898204883171,185.897563016737,186.896921150303,187.89627928387,
188.895637417436,189.894995551002,190.894353684568,191.893711818134,192.8930699517,
193.892428085266,194.891786218832,195.891144352398,196.890502485964,197.88986061953,
198.889218753096,199.888576886662,200.887935020228,201.887293153794,202.88665128736,
203.886009420926,204.885367554492,205.884725688058,206.884083821624,207.88344195519,
208.882800088756,209.882158222323,210.881516355889,211.880874489455,212.880232623021,
213.879590756587,214.878948890153,215.878307023719,216.877665157285,217.877023290851,
218.876381424417,219.875739557983,220.875097691549,221.874455825115,222.873813958681,
223.873172092247,224.872530225813,225.871888359379,226.871246492945,227.870604626511,
228.869962760077,229.869320893643,230.86867902721,231.868037160776,232.867395294342,
233.866753427908,234.866111561474,235.86546969504,236.864827828606,237.864185962172,
238.863544095738,239.862902229304,240.86226036287,241.861618496436,242.860976630002,
243.860334763568,244.859692897134,245.8590510307,246.858409164266,247.857767297832,
248.857125431398,249.856483564964,250.85584169853,251.855199832097,252.854557965663,
253.853916099229,254.853274232795,255.852632366361,256.851990499927,257.851348633493,
258.850706767059,259.850064900625,260.849423034191,261.848781167757,262.848139301323,
263.847497434889,264.846855568455,265.846213702021,266.845571835587,267.844929969153,
268.844288102719,269.843646236285,270.843004369851,271.842362503417,272.841720636983,
273.84107877055,274.840436904116,275.839795037682,276.839153171248,277.838511304814,
278.83786943838,279.837227571946,280.836585705512,281.835943839078,282.835301972644,
283.83466010621,284.834018239776,285.833376373342,286.832734506908,287.832092640474,
288.83145077404,289.830808907606,290.830167041172,291.829525174738,292.828883308304,
293.82824144187,294.827599575437,295.826957709003,296.826315842569,297.825673976135,
298.825032109701,299.824390243267,300.823748376833,301.823106510399,302.822464643965,
303.821822777531,304.821180911097,305.820539044663,306.819897178229,307.819255311795,
308.818613445361,309.817971578927,310.817329712493,311.816687846059,312.816045979625,
313.815404113191,314.814762246757,315.814120380323,316.81347851389,317.812836647456,
318.812194781022,319.811552914588,320.810911048154,321.81026918172,322.809627315286,
323.808985448852,324.808343582418,325.807701715984,326.80705984955,327.806417983116,
328.805776116682,329.805134250248,330.804492383814,331.80385051738,332.803208650946,
333.802566784512,334.801924918078,335.801283051644,336.80064118521,337.799999318776,
338.799357452343,339.798715585909,340.798073719475,341.797431853041,342.796789986607,
343.796148120173,344.795506253739,345.794864387305,346.794222520871,347.793580654437,
348.792938788003,349.792296921569,350.791655055135,351.791013188701,352.790371322267,
353.789729455833,354.789087589399,355.788445722965,356.787803856531,357.287482923314,
357.787161990097,358.28684105688,358.786520123663,359.286199190446,359.78587825723,
360.285557324013,360.785236390796,361.284915457579,361.784594524362,362.284273591145,
362.783952657928,363.283631724711,363.783310791494,364.282989858277,364.78266892506,
365.282347991843,365.782027058626,366.281706125409,366.781385192192,367.281064258975,
367.780743325758,368.280422392541,368.780101459324,369.279780526107,369.77945959289,
370.279138659673,370.778817726456,371.278496793239,371.778175860022,372.277854926805,
372.777533993588,373.277213060371,373.776892127154,374.276571193937,374.77625026072,
375.275929327503,375.775608394286,376.275287461069,376.774966527852,377.274645594635,
377.774324661418,378.274003728201,378.773682794984,379.273361861767,379.77304092855,
380.272719995333,380.772399062117,381.2720781289,381.771757195683,382.271436262466,
382.771115329249,383.270794396032,383.770473462815,384.270152529598,384.769831596381,
385.269510663164,385.769189729947,386.26886879673,386.768547863513,387.268226930296,
387.767905997079,388.267585063862,388.767264130645,389.266943197428,389.766622264211,
390.266301330994,390.765980397777,391.26565946456,391.765338531343,392.265017598126,
392.764696664909,393.264375731692,393.764054798475,394.263733865258,394.763412932041,
395.263091998824,395.762771065607,396.26245013239,396.762129199173,397.261808265956,
397.761487332739,398.261166399522,398.760845466305,399.260524533088,399.760203599871,
400.259882666654,400.759561733437,401.25924080022,401.758919867003,402.258598933787,
402.75827800057,403.257957067353,403.757636134136,404.257315200919,404.756994267702,
405.256673334485,405.756352401268,406.256031468051,406.755710534834),
 .UNSPECIFIED.);
#628=B_SPLINE_CURVE_WITH_KNOTS('',3,(#33264,#33265,#33266,#33267,#33268,
#33269,#33270,#33271,#33272,#33273,#33274,#33275,#33276,#33277,#33278,#33279,
#33280,#33281,#33282),.UNSPECIFIED.,.F.,.F.,(4,3,3,3,3,3,4),(-3.69871549170445,
-3.49775346748116,-2.99807440069814,-2.49839533391511,-1.99871626713209,
-1.49903720034907,-1.00018350866767),.UNSPECIFIED.);
#629=B_SPLINE_CURVE_WITH_KNOTS('',3,(#33285,#33286,#33287,#33288),
 .UNSPECIFIED.,.F.,.F.,(4,4),(0.,0.443060670554495),.UNSPECIFIED.);
#630=B_SPLINE_CURVE_WITH_KNOTS('',3,(#33293,#33294,#33295,#33296,#33297,
#33298,#33299,#33300,#33301,#33302,#33303,#33304,#33305,#33306,#33307,#33308,
#33309,#33310,#33311,#33312,#33313,#33314,#33315,#33316,#33317,#33318,#33319,
#33320,#33321,#33322,#33323,#33324,#33325,#33326,#33327,#33328,#33329,#33330,
#33331,#33332),.UNSPECIFIED.,.F.,.F.,(4,3,3,3,3,3,3,3,3,3,3,3,3,4),(-9.98190079888403,
-9.49390226887744,-8.99422320209442,-8.4945441353114,-7.99486506852837,
-7.49518600174535,-6.99550693496233,-6.4958278681793,-5.99614880139628,
-5.49646973461325,-4.99679066783023,-4.49711160104721,-3.99743253426419,
-3.69871549170445),.UNSPECIFIED.);
#631=B_SPLINE_CURVE_WITH_KNOTS('',3,(#33333,#33334,#33335,#33336,#33337,
#33338,#33339,#33340,#33341,#33342,#33343,#33344,#33345,#33346,#33347,#33348,
#33349,#33350,#33351,#33352,#33353,#33354,#33355,#33356,#33357,#33358,#33359,
#33360,#33361,#33362,#33363,#33364,#33365,#33366,#33367,#33368,#33369,#33370,
#33371,#33372,#33373,#33374,#33375),.UNSPECIFIED.,.F.,.F.,(4,3,3,3,3,3,
3,3,3,3,3,3,3,3,4),(0.443060670554495,0.49967906678306,0.999358133566079,
1.4990372003491,1.99871626713212,2.49839533391514,2.99807440069816,3.49775346748117,
3.99743253426419,4.49711160104721,4.99679066783023,5.49646973461325,5.99614880139627,
6.49582786817929,6.72624597773408),.UNSPECIFIED.);
#632=B_SPLINE_CURVE_WITH_KNOTS('',3,(#33380,#33381,#33382,#33383,#33384,
#33385,#33386,#33387,#33388,#33389,#33390,#33391,#33392,#33393,#33394,#33395,
#33396,#33397,#33398,#33399,#33400,#33401,#33402,#33403,#33404,#33405,#33406,
#33407,#33408,#33409,#33410,#33411,#33412,#33413,#33414,#33415,#33416,#33417,
#33418,#33419,#33420,#33421,#33422),.UNSPECIFIED.,.F.,.F.,(4,3,3,3,3,3,
3,3,3,3,3,3,3,3,4),(-16.2650861060636,-15.9897301370567,-15.4900510702737,
-14.9903720034907,-14.4906929367077,-13.9910138699247,-13.4913348031416,
-12.9916557363586,-12.4919766695756,-11.9922976027926,-11.4926185360095,
-10.9929394692265,-10.4932604024435,-9.99358133566046,-9.98190079888403),
 .UNSPECIFIED.);
#633=B_SPLINE_CURVE_WITH_KNOTS('',3,(#33423,#33424,#33425,#33426,#33427,
#33428,#33429,#33430,#33431,#33432,#33433,#33434,#33435,#33436,#33437,#33438,
#33439,#33440,#33441,#33442,#33443,#33444,#33445,#33446,#33447,#33448,#33449,
#33450,#33451,#33452,#33453,#33454,#33455,#33456,#33457,#33458,#33459,#33460,
#33461,#33462,#33463,#33464,#33465),.UNSPECIFIED.,.F.,.F.,(4,3,3,3,3,3,
3,3,3,3,3,3,3,3,4),(6.72624597773408,6.99550693496231,7.49518600174534,
7.99486506852837,8.49454413531139,8.99422320209442,9.49390226887745,9.99358133566048,
10.4932604024435,10.9929394692265,11.4926185360096,11.9922976027926,12.4919766695756,
12.9916557363586,13.0094312849137),.UNSPECIFIED.);
#634=B_SPLINE_CURVE_WITH_KNOTS('',3,(#33470,#33471,#33472,#33473,#33474,
#33475,#33476,#33477,#33478,#33479,#33480,#33481,#33482,#33483,#33484,#33485,
#33486,#33487,#33488,#33489,#33490,#33491,#33492,#33493,#33494,#33495,#33496,
#33497,#33498,#33499,#33500,#33501,#33502,#33503,#33504,#33505,#33506,#33507,
#33508,#33509,#33510,#33511,#33512),.UNSPECIFIED.,.F.,.F.,(4,3,3,3,3,3,
3,3,3,3,3,3,3,3,4),(-22.5482714132432,-22.485558005236,-21.985878938453,
-21.48619987167,-20.986520804887,-20.486841738104,-19.9871626713209,-19.4874836045379,
-18.9878045377549,-18.4881254709719,-17.9884464041888,-17.4887673374058,
-16.9890882706228,-16.4894092038398,-16.2650861060636),.UNSPECIFIED.);
#635=B_SPLINE_CURVE_WITH_KNOTS('',3,(#33513,#33514,#33515,#33516,#33517,
#33518,#33519,#33520,#33521,#33522,#33523,#33524,#33525,#33526,#33527,#33528,
#33529,#33530,#33531,#33532,#33533,#33534,#33535,#33536,#33537,#33538,#33539,
#33540,#33541,#33542,#33543,#33544,#33545,#33546,#33547,#33548,#33549,#33550,
#33551,#33552),.UNSPECIFIED.,.F.,.F.,(4,3,3,3,3,3,3,3,3,3,3,3,3,4),(13.0094312849137,
13.4913348031417,13.9910138699247,14.4906929367077,14.9903720034907,15.4900510702737,
15.9897301370568,16.4894092038398,16.9890882706228,17.4887673374058,17.9884464041888,
18.4881254709718,18.9878045377549,19.2926165920933),.UNSPECIFIED.);
#636=B_SPLINE_CURVE_WITH_KNOTS('',3,(#33557,#33558,#33559,#33560,#33561,
#33562,#33563,#33564,#33565,#33566,#33567,#33568,#33569,#33570,#33571,#33572,
#33573,#33574,#33575,#33576,#33577,#33578,#33579,#33580,#33581,#33582,#33583,
#33584,#33585,#33586,#33587,#33588,#33589,#33590,#33591,#33592,#33593,#33594,
#33595,#33596),.UNSPECIFIED.,.F.,.F.,(4,3,3,3,3,3,3,3,3,3,3,3,3,4),(-28.8314567204228,
-28.4817068066323,-27.9820277398493,-27.4823486730663,-26.9826696062833,
-26.4829905395002,-25.9833114727172,-25.4836324059342,-24.9839533391512,
-24.4842742723681,-23.9845952055851,-23.4849161388021,-22.9852370720191,
-22.5482714132432),.UNSPECIFIED.);
#637=B_SPLINE_CURVE_WITH_KNOTS('',3,(#33597,#33598,#33599,#33600,#33601,
#33602,#33603,#33604,#33605,#33606,#33607,#33608,#33609,#33610,#33611,#33612,
#33613,#33614,#33615,#33616,#33617,#33618,#33619,#33620,#33621,#33622,#33623,
#33624,#33625,#33626,#33627,#33628,#33629,#33630,#33631,#33632,#33633,#33634,
#33635,#33636,#33637,#33638,#33639),.UNSPECIFIED.,.F.,.F.,(4,3,3,3,3,3,
3,3,3,3,3,3,3,3,4),(19.2926165920933,19.4874836045379,19.9871626713209,
20.4868417381039,20.986520804887,21.48619987167,21.985878938453,22.4855580052361,
22.9852370720191,23.4849161388021,23.9845952055851,24.4842742723682,24.9839533391512,
25.4836324059342,25.5758018992728),.UNSPECIFIED.);
#638=B_SPLINE_CURVE_WITH_KNOTS('',3,(#33644,#33645,#33646,#33647,#33648,
#33649,#33650,#33651,#33652,#33653,#33654,#33655,#33656,#33657,#33658,#33659,
#33660,#33661,#33662,#33663,#33664,#33665,#33666,#33667,#33668,#33669,#33670,
#33671,#33672,#33673,#33674,#33675,#33676,#33677,#33678,#33679,#33680,#33681,
#33682,#33683,#33684,#33685,#33686),.UNSPECIFIED.,.F.,.F.,(4,3,3,3,3,3,
3,3,3,3,3,3,3,3,4),(-35.1146420276024,-34.9775346748116,-34.4778556080286,
-33.9781765412456,-33.4784974744626,-32.9788184076795,-32.4791393408965,
-31.9794602741135,-31.4797812073305,-30.9801021405474,-30.4804230737644,
-29.9807440069814,-29.4810649401984,-28.9813858734153,-28.8314567204228),
 .UNSPECIFIED.);
#639=B_SPLINE_CURVE_WITH_KNOTS('',3,(#33687,#33688,#33689,#33690,#33691,
#33692,#33693,#33694,#33695,#33696,#33697,#33698,#33699,#33700,#33701,#33702,
#33703,#33704,#33705,#33706,#33707,#33708,#33709,#33710,#33711,#33712,#33713,
#33714,#33715,#33716,#33717,#33718,#33719,#33720,#33721,#33722,#33723,#33724,
#33725,#33726),.UNSPECIFIED.,.F.,.F.,(4,3,3,3,3,3,3,3,3,3,3,3,3,4),(25.5758018992728,
25.9833114727172,26.4829905395003,26.9826696062833,27.4823486730663,27.9820277398493,
28.4817068066324,28.9813858734154,29.4810649401984,29.9807440069814,30.4804230737645,
30.9801021405475,31.4797812073305,31.8589872064524),.UNSPECIFIED.);
#640=B_SPLINE_CURVE_WITH_KNOTS('',3,(#33731,#33732,#33733,#33734,#33735,
#33736,#33737,#33738,#33739,#33740,#33741,#33742,#33743,#33744,#33745,#33746,
#33747,#33748,#33749,#33750,#33751,#33752,#33753,#33754,#33755,#33756,#33757,
#33758,#33759,#33760,#33761,#33762,#33763,#33764,#33765,#33766,#33767,#33768,
#33769,#33770),.UNSPECIFIED.,.F.,.F.,(4,3,3,3,3,3,3,3,3,3,3,3,3,4),(-41.397827334782,
-40.9736834762079,-40.4740044094249,-39.9743253426419,-39.4746462758588,
-38.9749672090758,-38.4752881422928,-37.9756090755098,-37.4759300087267,
-36.9762509419437,-36.4765718751607,-35.9768928083777,-35.4772137415947,
-35.1146420276024),.UNSPECIFIED.);
#641=B_SPLINE_CURVE_WITH_KNOTS('',3,(#33771,#33772,#33773,#33774,#33775,
#33776,#33777,#33778,#33779,#33780,#33781,#33782,#33783,#33784,#33785,#33786,
#33787,#33788,#33789,#33790,#33791,#33792,#33793,#33794,#33795,#33796,#33797,
#33798,#33799,#33800,#33801,#33802,#33803,#33804,#33805,#33806,#33807,#33808,
#33809,#33810,#33811,#33812,#33813),.UNSPECIFIED.,.F.,.F.,(4,3,3,3,3,3,
3,3,3,3,3,3,3,3,4),(31.8589872064524,31.9794602741135,32.4791393408966,
32.9788184076796,33.4784974744626,33.9781765412456,34.4778556080286,34.9775346748117,
35.4772137415947,35.9768928083777,36.4765718751607,36.9762509419437,37.4759300087267,
37.9756090755098,38.142172513632),.UNSPECIFIED.);
#642=B_SPLINE_CURVE_WITH_KNOTS('',3,(#33818,#33819,#33820,#33821,#33822,
#33823,#33824,#33825,#33826,#33827,#33828,#33829,#33830,#33831,#33832,#33833,
#33834,#33835,#33836,#33837,#33838,#33839,#33840,#33841,#33842,#33843,#33844,
#33845,#33846,#33847,#33848,#33849,#33850,#33851,#33852,#33853,#33854,#33855,
#33856,#33857,#33858,#33859,#33860),.UNSPECIFIED.,.F.,.F.,(4,3,3,3,3,3,
3,3,3,3,3,3,3,3,4),(-47.6810126419616,-47.4695113443872,-46.9698322776042,
-46.4701532108212,-45.9704741440381,-45.4707950772551,-44.9711160104721,
-44.4714369436891,-43.971757876906,-43.472078810123,-42.97239974334,-42.472720676557,
-41.973041609774,-41.4733625429909,-41.397827334782),.UNSPECIFIED.);
#643=B_SPLINE_CURVE_WITH_KNOTS('',3,(#33861,#33862,#33863,#33864,#33865,
#33866,#33867,#33868,#33869,#33870,#33871,#33872,#33873,#33874,#33875,#33876,
#33877,#33878,#33879,#33880,#33881,#33882,#33883,#33884,#33885,#33886,#33887,
#33888,#33889,#33890,#33891,#33892,#33893,#33894,#33895,#33896,#33897,#33898,
#33899,#33900),.UNSPECIFIED.,.F.,.F.,(4,3,3,3,3,3,3,3,3,3,3,3,3,4),(38.142172513632,
38.4752881422928,38.9749672090758,39.4746462758589,39.9743253426419,40.4740044094249,
40.973683476208,41.473362542991,41.973041609774,42.472720676557,42.9723997433401,
43.4720788101231,43.9717578769061,44.4253578208116),.UNSPECIFIED.);
#644=B_SPLINE_CURVE_WITH_KNOTS('',3,(#33905,#33906,#33907,#33908,#33909,
#33910,#33911,#33912,#33913,#33914,#33915,#33916,#33917,#33918,#33919,#33920,
#33921,#33922,#33923,#33924,#33925,#33926,#33927,#33928,#33929,#33930,#33931,
#33932),.UNSPECIFIED.,.F.,.F.,(4,3,3,3,3,3,3,3,3,4),(-53.9641979491412,
-52.9659810790005,-51.9666229454344,-50.9672648118684,-49.9679066783023,
-49.4682276115193,-48.9685485447363,-48.4688694779533,-47.9691904111702,
-47.6810126419616),.UNSPECIFIED.);
#645=B_SPLINE_CURVE_WITH_KNOTS('',3,(#33933,#33934,#33935,#33936,#33937,
#33938,#33939,#33940,#33941,#33942,#33943,#33944,#33945,#33946,#33947,#33948,
#33949,#33950,#33951,#33952,#33953,#33954,#33955,#33956,#33957,#33958,#33959,
#33960,#33961,#33962,#33963,#33964,#33965,#33966,#33967,#33968,#33969,#33970,
#33971,#33972),.UNSPECIFIED.,.F.,.F.,(4,3,3,3,3,3,3,3,3,3,3,3,3,4),(44.4253578208116,
44.4714369436892,44.9711160104722,45.4707950772552,45.9704741440382,46.4701532108212,
46.9698322776042,47.4695113443873,47.9691904111703,48.4688694779533,48.9685485447363,
49.4682276115193,49.9679066783024,50.7085431279912),.UNSPECIFIED.);
#646=B_SPLINE_CURVE_WITH_KNOTS('',3,(#33977,#33978,#33979,#33980,#33981,
#33982,#33983,#33984,#33985,#33986,#33987,#33988,#33989,#33990,#33991,#33992,
#33993,#33994,#33995,#33996,#33997,#33998),.UNSPECIFIED.,.F.,.F.,(4,3,3,
3,3,3,3,4),(-60.2473832563207,-59.9614880139628,-58.9621298803968,-57.9627717468307,
-56.9634136132647,-55.9640554796986,-54.9646973461326,-53.9641979491412),
 .UNSPECIFIED.);
#647=B_SPLINE_CURVE_WITH_KNOTS('',3,(#33999,#34000,#34001,#34002,#34003,
#34004,#34005,#34006,#34007,#34008,#34009,#34010,#34011,#34012,#34013,#34014,
#34015,#34016,#34017,#34018,#34019,#34020,#34021,#34022,#34023),
 .UNSPECIFIED.,.F.,.F.,(4,3,3,3,3,3,3,3,4),(50.7085431279912,50.9672648118684,
51.9666229454345,52.9659810790005,53.9653392125666,54.9646973461326,55.9640554796987,
56.9634136132647,56.9917284351708),.UNSPECIFIED.);
#648=B_SPLINE_CURVE_WITH_KNOTS('',3,(#34028,#34029,#34030,#34031,#34032,
#34033,#34034,#34035,#34036,#34037,#34038,#34039,#34040,#34041,#34042,#34043,
#34044,#34045,#34046,#34047,#34048,#34049),.UNSPECIFIED.,.F.,.F.,(4,3,3,
3,3,3,3,4),(-66.5305685635003,-65.9576368153591,-64.958278681793,-63.958920548227,
-62.9595624146609,-61.9602042810949,-60.9608461475288,-60.2473832563207),
 .UNSPECIFIED.);
#649=B_SPLINE_CURVE_WITH_KNOTS('',3,(#34050,#34051,#34052,#34053,#34054,
#34055,#34056,#34057,#34058,#34059,#34060,#34061,#34062,#34063,#34064,#34065,
#34066,#34067,#34068,#34069,#34070,#34071),.UNSPECIFIED.,.F.,.F.,(4,3,3,
3,3,3,3,4),(56.9917284351708,57.9627717468308,58.9621298803968,59.9614880139629,
60.9608461475289,61.960204281095,62.959562414661,63.2749137423504),
 .UNSPECIFIED.);
#650=B_SPLINE_CURVE_WITH_KNOTS('',3,(#34076,#34077,#34078,#34079,#34080,
#34081,#34082,#34083,#34084,#34085,#34086,#34087,#34088,#34089,#34090,#34091,
#34092,#34093,#34094,#34095,#34096,#34097),.UNSPECIFIED.,.F.,.F.,(4,3,3,
3,3,3,3,4),(-72.8137538706799,-71.9537856167554,-70.9544274831893,-69.9550693496233,
-68.9557112160572,-67.9563530824912,-66.9569949489251,-66.5305685635003),
 .UNSPECIFIED.);
#651=B_SPLINE_CURVE_WITH_KNOTS('',3,(#34098,#34099,#34100,#34101,#34102,
#34103,#34104,#34105,#34106,#34107,#34108,#34109,#34110,#34111,#34112,#34113,
#34114,#34115,#34116,#34117,#34118,#34119),.UNSPECIFIED.,.F.,.F.,(4,3,3,
3,3,3,3,4),(63.2749137423504,63.958920548227,64.9582786817931,65.9576368153591,
66.9569949489252,67.9563530824912,68.9557112160573,69.55809904953),
 .UNSPECIFIED.);
#652=B_SPLINE_CURVE_WITH_KNOTS('',3,(#34124,#34125,#34126,#34127,#34128,
#34129,#34130,#34131,#34132,#34133,#34134,#34135,#34136,#34137,#34138,#34139,
#34140,#34141,#34142,#34143,#34144,#34145,#34146,#34147,#34148),
 .UNSPECIFIED.,.F.,.F.,(4,3,3,3,3,3,3,3,4),(-79.0969391778595,-78.9492925517177,
-77.9499344181516,-76.9505762845856,-75.9512181510195,-74.9518600174535,
-73.9525018838875,-72.9531437503214,-72.8137538706799),.UNSPECIFIED.);
#653=B_SPLINE_CURVE_WITH_KNOTS('',3,(#34149,#34150,#34151,#34152,#34153,
#34154,#34155,#34156,#34157,#34158,#34159,#34160,#34161,#34162,#34163,#34164,
#34165,#34166,#34167,#34168,#34169,#34170),.UNSPECIFIED.,.F.,.F.,(4,3,3,
3,3,3,3,4),(69.55809904953,69.9550693496233,70.9544274831893,71.9537856167554,
72.9531437503215,73.9525018838875,74.9518600174536,75.8412843567096),
 .UNSPECIFIED.);
#654=B_SPLINE_CURVE_WITH_KNOTS('',3,(#34175,#34176,#34177,#34178,#34179,
#34180,#34181,#34182,#34183,#34184,#34185,#34186,#34187,#34188,#34189,#34190,
#34191,#34192,#34193,#34194,#34195,#34196),.UNSPECIFIED.,.F.,.F.,(4,3,3,
3,3,3,3,4),(-85.3801244850391,-84.945441353114,-83.9460832195479,-82.9467250859819,
-81.9473669524158,-80.9480088188498,-79.9486506852837,-79.0969391778595),
 .UNSPECIFIED.);
#655=B_SPLINE_CURVE_WITH_KNOTS('',3,(#34197,#34198,#34199,#34200,#34201,
#34202,#34203,#34204,#34205,#34206,#34207,#34208,#34209,#34210,#34211,#34212,
#34213,#34214,#34215,#34216,#34217,#34218,#34219,#34220,#34221),
 .UNSPECIFIED.,.F.,.F.,(4,3,3,3,3,3,3,3,4),(75.8412843567096,75.9512181510196,
76.9505762845857,77.9499344181517,78.9492925517178,79.9486506852838,80.9480088188499,
81.9473669524159,82.1244696638892),.UNSPECIFIED.);
#656=B_SPLINE_CURVE_WITH_KNOTS('',3,(#34226,#34227,#34228,#34229,#34230,
#34231,#34232,#34233,#34234,#34235,#34236,#34237,#34238,#34239,#34240,#34241,
#34242,#34243,#34244,#34245,#34246,#34247),.UNSPECIFIED.,.F.,.F.,(4,3,3,
3,3,3,3,4),(-91.6633097922187,-90.9415901545102,-89.9422320209442,-88.9428738873782,
-87.9435157538121,-86.944157620246,-85.94479948668,-85.3801244850391),
 .UNSPECIFIED.);
#657=B_SPLINE_CURVE_WITH_KNOTS('',3,(#34248,#34249,#34250,#34251,#34252,
#34253,#34254,#34255,#34256,#34257,#34258,#34259,#34260,#34261,#34262,#34263,
#34264,#34265,#34266,#34267,#34268,#34269),.UNSPECIFIED.,.F.,.F.,(4,3,3,
3,3,3,3,4),(82.1244696638892,82.946725085982,83.946083219548,84.9454413531141,
85.9447994866801,86.9441576202461,87.9435157538122,88.4076549710687),
 .UNSPECIFIED.);
#658=B_SPLINE_CURVE_WITH_KNOTS('',3,(#34274,#34275,#34276,#34277,#34278,
#34279,#34280,#34281,#34282,#34283,#34284,#34285,#34286,#34287,#34288,#34289,
#34290,#34291,#34292,#34293,#34294,#34295,#34296,#34297,#34298),
 .UNSPECIFIED.,.F.,.F.,(4,3,3,3,3,3,3,3,4),(-97.9464950993983,-97.9370970894726,
-96.9377389559065,-95.9383808223405,-94.9390226887744,-93.9396645552084,
-92.9403064216423,-91.9409482880763,-91.6633097922187),.UNSPECIFIED.);
#659=B_SPLINE_CURVE_WITH_KNOTS('',3,(#34299,#34300,#34301,#34302,#34303,
#34304,#34305,#34306,#34307,#34308,#34309,#34310,#34311,#34312,#34313,#34314,
#34315,#34316,#34317,#34318,#34319,#34320),.UNSPECIFIED.,.F.,.F.,(4,3,3,
3,3,3,3,4),(88.4076549710687,88.9428738873782,89.9422320209442,90.9415901545103,
91.9409482880763,92.9403064216424,93.9396645552084,94.6908402782483),
 .UNSPECIFIED.);
#660=B_SPLINE_CURVE_WITH_KNOTS('',3,(#34325,#34326,#34327,#34328,#34329,
#34330,#34331,#34332,#34333,#34334,#34335,#34336,#34337,#34338,#34339,#34340,
#34341,#34342,#34343,#34344,#34345,#34346),.UNSPECIFIED.,.F.,.F.,(4,3,3,
3,3,3,3,4),(-104.229680406578,-103.933245890869,-102.933887757303,-101.934529623737,
-100.935171490171,-99.9358133566047,-98.9364552230386,-97.9464950993983),
 .UNSPECIFIED.);
#661=B_SPLINE_CURVE_WITH_KNOTS('',3,(#34347,#34348,#34349,#34350,#34351,
#34352,#34353,#34354,#34355,#34356,#34357,#34358,#34359,#34360,#34361,#34362,
#34363,#34364,#34365,#34366,#34367,#34368,#34369,#34370,#34371),
 .UNSPECIFIED.,.F.,.F.,(4,3,3,3,3,3,3,3,4),(94.6908402782483,94.9390226887745,
95.9383808223405,96.9377389559065,97.9370970894726,98.9364552230386,99.9358133566047,
100.935171490171,100.974025585428),.UNSPECIFIED.);
#662=B_SPLINE_CURVE_WITH_KNOTS('',3,(#34376,#34377,#34378,#34379,#34380,
#34381,#34382,#34383,#34384,#34385,#34386,#34387,#34388,#34389,#34390,#34391,
#34392,#34393,#34394,#34395,#34396,#34397),.UNSPECIFIED.,.F.,.F.,(4,3,3,
3,3,3,3,4),(-110.512865713757,-109.929394692265,-108.930036558699,-107.930678425133,
-106.931320291567,-105.931962158001,-104.932604024435,-104.229680406578),
 .UNSPECIFIED.);
#663=B_SPLINE_CURVE_WITH_KNOTS('',3,(#34398,#34399,#34400,#34401,#34402,
#34403,#34404,#34405,#34406,#34407,#34408,#34409,#34410,#34411,#34412,#34413,
#34414,#34415,#34416,#34417,#34418,#34419),.UNSPECIFIED.,.F.,.F.,(4,3,3,
3,3,3,3,4),(100.974025585428,101.934529623737,102.933887757303,103.933245890869,
104.932604024435,105.931962158001,106.931320291567,107.257210892608),
 .UNSPECIFIED.);
#664=B_SPLINE_CURVE_WITH_KNOTS('',3,(#34424,#34425,#34426,#34427,#34428,
#34429,#34430,#34431,#34432,#34433,#34434,#34435,#34436,#34437,#34438,#34439,
#34440,#34441,#34442,#34443,#34444,#34445),.UNSPECIFIED.,.F.,.F.,(4,3,3,
3,3,3,3,4),(-116.796051020937,-115.925543493661,-114.926185360095,-113.926827226529,
-112.927469092963,-111.928110959397,-110.928752825831,-110.512865713757),
 .UNSPECIFIED.);
#665=B_SPLINE_CURVE_WITH_KNOTS('',3,(#34446,#34447,#34448,#34449,#34450,
#34451,#34452,#34453,#34454,#34455,#34456,#34457,#34458,#34459,#34460,#34461,
#34462,#34463,#34464,#34465,#34466,#34467),.UNSPECIFIED.,.F.,.F.,(4,3,3,
3,3,3,3,4),(107.257210892608,107.930678425133,108.930036558699,109.929394692265,
110.928752825831,111.928110959397,112.927469092963,113.540396199787),
 .UNSPECIFIED.);
#666=B_SPLINE_CURVE_WITH_KNOTS('',3,(#34472,#34473,#34474,#34475,#34476,
#34477,#34478,#34479,#34480,#34481,#34482,#34483,#34484,#34485,#34486,#34487,
#34488,#34489,#34490,#34491,#34492,#34493,#34494,#34495,#34496),
 .UNSPECIFIED.,.F.,.F.,(4,3,3,3,3,3,3,3,4),(-123.079236328117,-122.921050428624,
-121.921692295058,-120.922334161492,-119.922976027926,-118.92361789436,
-117.924259760793,-116.924901627227,-116.796051020937),.UNSPECIFIED.);
#667=B_SPLINE_CURVE_WITH_KNOTS('',3,(#34497,#34498,#34499,#34500,#34501,
#34502,#34503,#34504,#34505,#34506,#34507,#34508,#34509,#34510,#34511,#34512,
#34513,#34514,#34515,#34516,#34517,#34518),.UNSPECIFIED.,.F.,.F.,(4,3,3,
3,3,3,3,4),(113.540396199787,113.926827226529,114.926185360095,115.925543493661,
116.924901627228,117.924259760794,118.92361789436,119.823581506967),
 .UNSPECIFIED.);
#668=B_SPLINE_CURVE_WITH_KNOTS('',3,(#34523,#34524,#34525,#34526,#34527,
#34528,#34529,#34530,#34531,#34532,#34533,#34534,#34535,#34536,#34537,#34538,
#34539,#34540,#34541,#34542,#34543,#34544),.UNSPECIFIED.,.F.,.F.,(4,3,3,
3,3,3,3,4),(-129.362421635296,-128.91719923002,-127.917841096454,-126.918482962888,
-125.919124829322,-124.919766695756,-123.92040856219,-123.079236328117),
 .UNSPECIFIED.);
#669=B_SPLINE_CURVE_WITH_KNOTS('',3,(#34545,#34546,#34547,#34548,#34549,
#34550,#34551,#34552,#34553,#34554,#34555,#34556,#34557,#34558,#34559,#34560,
#34561,#34562,#34563,#34564,#34565,#34566,#34567,#34568,#34569),
 .UNSPECIFIED.,.F.,.F.,(4,3,3,3,3,3,3,3,4),(119.823581506967,119.922976027926,
120.922334161492,121.921692295058,122.921050428624,123.92040856219,124.919766695756,
125.919124829322,126.106766814146),.UNSPECIFIED.);
#670=B_SPLINE_CURVE_WITH_KNOTS('',3,(#34574,#34575,#34576,#34577,#34578,
#34579,#34580,#34581,#34582,#34583,#34584,#34585,#34586,#34587,#34588,#34589,
#34590,#34591,#34592,#34593,#34594,#34595),.UNSPECIFIED.,.F.,.F.,(4,3,3,
3,3,3,3,4),(-135.645606942476,-134.913348031416,-133.91398989785,-132.914631764284,
-131.915273630718,-130.915915497152,-129.916557363586,-129.362421635296),
 .UNSPECIFIED.);
#671=B_SPLINE_CURVE_WITH_KNOTS('',3,(#34596,#34597,#34598,#34599,#34600,
#34601,#34602,#34603,#34604,#34605,#34606,#34607,#34608,#34609,#34610,#34611,
#34612,#34613,#34614,#34615,#34616,#34617),.UNSPECIFIED.,.F.,.F.,(4,3,3,
3,3,3,3,4),(126.106766814146,126.918482962888,127.917841096454,128.91719923002,
129.916557363586,130.915915497152,131.915273630718,132.389952121326),
 .UNSPECIFIED.);
#672=B_SPLINE_CURVE_WITH_KNOTS('',3,(#34622,#34623,#34624,#34625,#34626,
#34627,#34628,#34629,#34630,#34631,#34632,#34633,#34634,#34635,#34636,#34637,
#34638,#34639,#34640,#34641,#34642,#34643,#34644,#34645,#34646),
 .UNSPECIFIED.,.F.,.F.,(4,3,3,3,3,3,3,3,4),(-141.928792249655,-141.908854966379,
-140.909496832813,-139.910138699247,-138.91078056568,-137.911422432114,
-136.912064298548,-135.912706164982,-135.645606942476),.UNSPECIFIED.);
#673=B_SPLINE_CURVE_WITH_KNOTS('',3,(#34647,#34648,#34649,#34650,#34651,
#34652,#34653,#34654,#34655,#34656,#34657,#34658,#34659,#34660,#34661,#34662,
#34663,#34664,#34665,#34666,#34667,#34668),.UNSPECIFIED.,.F.,.F.,(4,3,3,
3,3,3,3,4),(132.389952121326,132.914631764284,133.91398989785,134.913348031416,
135.912706164982,136.912064298549,137.911422432115,138.673137428505),
 .UNSPECIFIED.);
#674=B_SPLINE_CURVE_WITH_KNOTS('',3,(#34673,#34674,#34675,#34676,#34677,
#34678,#34679,#34680,#34681,#34682,#34683,#34684,#34685,#34686,#34687,#34688,
#34689,#34690,#34691,#34692,#34693,#34694),.UNSPECIFIED.,.F.,.F.,(4,3,3,
3,3,3,3,4),(-148.211977556835,-147.905003767775,-146.905645634209,-145.906287500643,
-144.906929367077,-143.907571233511,-142.908213099945,-141.928792249655),
 .UNSPECIFIED.);
#675=B_SPLINE_CURVE_WITH_KNOTS('',3,(#34695,#34696,#34697,#34698,#34699,
#34700,#34701,#34702,#34703,#34704,#34705,#34706,#34707,#34708,#34709,#34710,
#34711,#34712,#34713,#34714,#34715,#34716,#34717,#34718,#34719),
 .UNSPECIFIED.,.F.,.F.,(4,3,3,3,3,3,3,3,4),(138.673137428505,138.910780565681,
139.910138699247,140.909496832813,141.908854966379,142.908213099945,143.907571233511,
144.906929367077,144.956322735685),.UNSPECIFIED.);
#676=B_SPLINE_CURVE_WITH_KNOTS('',3,(#34724,#34725,#34726,#34727,#34728,
#34729,#34730,#34731,#34732,#34733,#34734,#34735,#34736,#34737,#34738,#34739,
#34740,#34741,#34742,#34743,#34744,#34745),.UNSPECIFIED.,.F.,.F.,(4,3,3,
3,3,3,3,4),(-154.495162864015,-153.901152569171,-152.901794435605,-151.902436302039,
-150.903078168473,-149.903720034907,-148.904361901341,-148.211977556835),
 .UNSPECIFIED.);
#677=B_SPLINE_CURVE_WITH_KNOTS('',3,(#34746,#34747,#34748,#34749,#34750,
#34751,#34752,#34753,#34754,#34755,#34756,#34757,#34758,#34759,#34760,#34761,
#34762,#34763,#34764,#34765,#34766,#34767),.UNSPECIFIED.,.F.,.F.,(4,3,3,
3,3,3,3,4),(144.956322735685,145.906287500643,146.905645634209,147.905003767775,
148.904361901341,149.903720034907,150.903078168473,151.239508042865),
 .UNSPECIFIED.);
#678=B_SPLINE_CURVE_WITH_KNOTS('',3,(#34772,#34773,#34774,#34775,#34776,
#34777,#34778,#34779,#34780,#34781,#34782,#34783,#34784,#34785,#34786,#34787,
#34788,#34789,#34790,#34791,#34792,#34793),.UNSPECIFIED.,.F.,.F.,(4,3,3,
3,3,3,3,4),(-160.778348171194,-159.897301370567,-158.897943237001,-157.898585103435,
-156.899226969869,-155.899868836303,-154.900510702737,-154.495162864015),
 .UNSPECIFIED.);
#679=B_SPLINE_CURVE_WITH_KNOTS('',3,(#34794,#34795,#34796,#34797,#34798,
#34799,#34800,#34801,#34802,#34803,#34804,#34805,#34806,#34807,#34808,#34809,
#34810,#34811,#34812,#34813,#34814,#34815),.UNSPECIFIED.,.F.,.F.,(4,3,3,
3,3,3,3,4),(151.239508042865,151.902436302039,152.901794435605,153.901152569171,
154.900510702737,155.899868836303,156.899226969869,157.522693350044),
 .UNSPECIFIED.);
#680=B_SPLINE_CURVE_WITH_KNOTS('',3,(#34820,#34821,#34822,#34823,#34824,
#34825,#34826,#34827,#34828,#34829,#34830,#34831,#34832,#34833,#34834,#34835,
#34836,#34837,#34838,#34839,#34840,#34841,#34842,#34843,#34844),
 .UNSPECIFIED.,.F.,.F.,(4,3,3,3,3,3,3,3,4),(-167.061533478374,-166.89280830553,
-165.893450171964,-164.894092038398,-163.894733904832,-162.895375771266,
-161.8960176377,-160.896659504134,-160.778348171194),.UNSPECIFIED.);
#681=B_SPLINE_CURVE_WITH_KNOTS('',3,(#34845,#34846,#34847,#34848,#34849,
#34850,#34851,#34852,#34853,#34854,#34855,#34856,#34857,#34858,#34859,#34860,
#34861,#34862,#34863,#34864,#34865,#34866),.UNSPECIFIED.,.F.,.F.,(4,3,3,
3,3,3,3,4),(157.522693350044,157.898585103435,158.897943237002,159.897301370568,
160.896659504134,161.8960176377,162.895375771266,163.805878657224),
 .UNSPECIFIED.);
#682=B_SPLINE_CURVE_WITH_KNOTS('',3,(#34871,#34872,#34873,#34874,#34875,
#34876,#34877,#34878,#34879,#34880,#34881,#34882,#34883,#34884,#34885,#34886,
#34887,#34888,#34889,#34890,#34891,#34892),.UNSPECIFIED.,.F.,.F.,(4,3,3,
3,3,3,3,4),(-173.344718785553,-172.888957106926,-171.88959897336,-170.890240839794,
-169.890882706228,-168.891524572662,-167.892166439096,-167.061533478374),
 .UNSPECIFIED.);
#683=B_SPLINE_CURVE_WITH_KNOTS('',3,(#34893,#34894,#34895,#34896,#34897,
#34898,#34899,#34900,#34901,#34902,#34903,#34904,#34905,#34906,#34907,#34908,
#34909,#34910,#34911,#34912,#34913,#34914,#34915,#34916,#34917),
 .UNSPECIFIED.,.F.,.F.,(4,3,3,3,3,3,3,3,4),(163.805878657224,163.894733904832,
164.894092038398,165.893450171964,166.89280830553,167.892166439096,168.891524572662,
169.890882706228,170.089063964403),.UNSPECIFIED.);
#684=B_SPLINE_CURVE_WITH_KNOTS('',3,(#34922,#34923,#34924,#34925,#34926,
#34927,#34928,#34929,#34930,#34931,#34932,#34933,#34934,#34935,#34936,#34937,
#34938,#34939,#34940,#34941,#34942,#34943),.UNSPECIFIED.,.F.,.F.,(4,3,3,
3,3,3,3,4),(-179.627904092733,-178.885105908322,-177.885747774756,-176.88638964119,
-175.887031507624,-174.887673374058,-173.888315240492,-173.344718785553),
 .UNSPECIFIED.);
#685=B_SPLINE_CURVE_WITH_KNOTS('',3,(#34944,#34945,#34946,#34947,#34948,
#34949,#34950,#34951,#34952,#34953,#34954,#34955,#34956,#34957,#34958,#34959,
#34960,#34961,#34962,#34963,#34964,#34965),.UNSPECIFIED.,.F.,.F.,(4,3,3,
3,3,3,3,4),(170.089063964403,170.890240839794,171.88959897336,172.888957106926,
173.888315240492,174.887673374058,175.887031507624,176.372249271583),
 .UNSPECIFIED.);
#686=B_SPLINE_CURVE_WITH_KNOTS('',3,(#34970,#34971,#34972,#34973,#34974,
#34975,#34976,#34977,#34978,#34979,#34980,#34981,#34982,#34983,#34984,#34985,
#34986,#34987,#34988,#34989,#34990,#34991,#34992,#34993,#34994),
 .UNSPECIFIED.,.F.,.F.,(4,3,3,3,3,3,3,3,4),(-185.911089399912,-185.880612843285,
-184.881254709719,-183.881896576153,-182.882538442587,-181.88318030902,
-180.883822175454,-179.884464041888,-179.627904092733),.UNSPECIFIED.);
#687=B_SPLINE_CURVE_WITH_KNOTS('',3,(#34995,#34996,#34997,#34998,#34999,
#35000,#35001,#35002,#35003,#35004,#35005,#35006,#35007,#35008,#35009,#35010,
#35011,#35012,#35013,#35014,#35015,#35016),.UNSPECIFIED.,.F.,.F.,(4,3,3,
3,3,3,3,4),(176.372249271583,176.88638964119,177.885747774756,178.885105908322,
179.884464041889,180.883822175455,181.883180309021,182.655434578762),
 .UNSPECIFIED.);
#688=B_SPLINE_CURVE_WITH_KNOTS('',3,(#35021,#35022,#35023,#35024,#35025,
#35026,#35027,#35028,#35029,#35030,#35031,#35032,#35033,#35034,#35035,#35036,
#35037,#35038,#35039,#35040,#35041,#35042),.UNSPECIFIED.,.F.,.F.,(4,3,3,
3,3,3,3,4),(-192.194274707092,-191.876761644681,-190.877403511115,-189.878045377549,
-188.878687243983,-187.879329110417,-186.879970976851,-185.911089399912),
 .UNSPECIFIED.);
#689=B_SPLINE_CURVE_WITH_KNOTS('',3,(#35043,#35044,#35045,#35046,#35047,
#35048,#35049,#35050,#35051,#35052,#35053,#35054,#35055,#35056,#35057,#35058,
#35059,#35060,#35061,#35062,#35063,#35064,#35065,#35066,#35067),
 .UNSPECIFIED.,.F.,.F.,(4,3,3,3,3,3,3,3,4),(182.655434578762,182.882538442587,
183.881896576153,184.881254709719,185.880612843285,186.879970976851,187.879329110417,
188.878687243983,188.938619885942),.UNSPECIFIED.);
#690=B_SPLINE_CURVE_WITH_KNOTS('',3,(#35072,#35073,#35074,#35075,#35076,
#35077,#35078,#35079,#35080,#35081,#35082,#35083,#35084,#35085,#35086,#35087,
#35088,#35089,#35090,#35091,#35092,#35093),.UNSPECIFIED.,.F.,.F.,(4,3,3,
3,3,3,3,4),(-198.477460014271,-197.872910446077,-196.873552312511,-195.874194178945,
-194.874836045379,-193.875477911813,-192.876119778247,-192.194274707092),
 .UNSPECIFIED.);
#691=B_SPLINE_CURVE_WITH_KNOTS('',3,(#35094,#35095,#35096,#35097,#35098,
#35099,#35100,#35101,#35102,#35103,#35104,#35105,#35106,#35107,#35108,#35109,
#35110,#35111,#35112,#35113,#35114,#35115),.UNSPECIFIED.,.F.,.F.,(4,3,3,
3,3,3,3,4),(188.938619885942,189.878045377549,190.877403511115,191.876761644681,
192.876119778247,193.875477911813,194.874836045379,195.221805193122),
 .UNSPECIFIED.);
#692=B_SPLINE_CURVE_WITH_KNOTS('',3,(#35120,#35121,#35122,#35123,#35124,
#35125,#35126,#35127,#35128,#35129,#35130,#35131,#35132,#35133,#35134,#35135,
#35136,#35137,#35138,#35139,#35140,#35141),.UNSPECIFIED.,.F.,.F.,(4,3,3,
3,3,3,3,4),(-204.760645321451,-203.869059247473,-202.869701113907,-201.870342980341,
-200.870984846775,-199.871626713209,-198.872268579643,-198.477460014271),
 .UNSPECIFIED.);
#693=B_SPLINE_CURVE_WITH_KNOTS('',3,(#35142,#35143,#35144,#35145,#35146,
#35147,#35148,#35149,#35150,#35151,#35152,#35153,#35154,#35155,#35156,#35157,
#35158,#35159,#35160,#35161,#35162,#35163),.UNSPECIFIED.,.F.,.F.,(4,3,3,
3,3,3,3,4),(195.221805193122,195.874194178945,196.873552312511,197.872910446077,
198.872268579643,199.871626713209,200.870984846776,201.504990500301),
 .UNSPECIFIED.);
#694=B_SPLINE_CURVE_WITH_KNOTS('',3,(#35168,#35169,#35170,#35171,#35172,
#35173,#35174,#35175,#35176,#35177,#35178,#35179,#35180,#35181,#35182,#35183,
#35184,#35185,#35186,#35187,#35188,#35189,#35190,#35191,#35192),
 .UNSPECIFIED.,.F.,.F.,(4,3,3,3,3,3,3,3,4),(-211.043830628631,-210.864566182436,
-209.86520804887,-208.865849915304,-207.866491781738,-206.867133648172,
-205.867775514606,-204.86841738104,-204.760645321451),.UNSPECIFIED.);
#695=B_SPLINE_CURVE_WITH_KNOTS('',3,(#35193,#35194,#35195,#35196,#35197,
#35198,#35199,#35200,#35201,#35202,#35203,#35204,#35205,#35206,#35207,#35208,
#35209,#35210,#35211,#35212,#35213,#35214),.UNSPECIFIED.,.F.,.F.,(4,3,3,
3,3,3,3,4),(201.504990500301,201.870342980342,202.869701113908,203.869059247474,
204.86841738104,205.867775514606,206.867133648172,207.788175807481),
 .UNSPECIFIED.);
#696=B_SPLINE_CURVE_WITH_KNOTS('',3,(#35219,#35220,#35221,#35222,#35223,
#35224,#35225,#35226,#35227,#35228,#35229,#35230,#35231,#35232,#35233,#35234,
#35235,#35236,#35237,#35238,#35239,#35240),.UNSPECIFIED.,.F.,.F.,(4,3,3,
3,3,3,3,4),(-217.32701593581,-216.860714983832,-215.861356850266,-214.8619987167,
-213.862640583134,-212.863282449568,-211.863924316002,-211.043830628631),
 .UNSPECIFIED.);
#697=B_SPLINE_CURVE_WITH_KNOTS('',3,(#35241,#35242,#35243,#35244,#35245,
#35246,#35247,#35248,#35249,#35250,#35251,#35252,#35253,#35254,#35255,#35256,
#35257,#35258,#35259,#35260,#35261,#35262,#35263,#35264,#35265),
 .UNSPECIFIED.,.F.,.F.,(4,3,3,3,3,3,3,3,4),(207.788175807481,207.866491781738,
208.865849915304,209.86520804887,210.864566182436,211.863924316002,212.863282449568,
213.862640583134,214.07136111466),.UNSPECIFIED.);
#698=B_SPLINE_CURVE_WITH_KNOTS('',3,(#35270,#35271,#35272,#35273,#35274,
#35275,#35276,#35277,#35278,#35279,#35280,#35281,#35282,#35283,#35284,#35285,
#35286,#35287,#35288,#35289,#35290,#35291),.UNSPECIFIED.,.F.,.F.,(4,3,3,
3,3,3,3,4),(-223.61020124299,-222.856863785228,-221.857505651662,-220.858147518096,
-219.85878938453,-218.859431250964,-217.860073117398,-217.32701593581),
 .UNSPECIFIED.);
#699=B_SPLINE_CURVE_WITH_KNOTS('',3,(#35292,#35293,#35294,#35295,#35296,
#35297,#35298,#35299,#35300,#35301,#35302,#35303,#35304,#35305,#35306,#35307,
#35308,#35309,#35310,#35311,#35312,#35313),.UNSPECIFIED.,.F.,.F.,(4,3,3,
3,3,3,3,4),(214.07136111466,214.8619987167,215.861356850266,216.860714983832,
217.860073117398,218.859431250964,219.85878938453,220.35454642184),
 .UNSPECIFIED.);
#700=B_SPLINE_CURVE_WITH_KNOTS('',3,(#35318,#35319,#35320,#35321,#35322,
#35323,#35324,#35325,#35326,#35327,#35328,#35329,#35330,#35331,#35332,#35333,
#35334,#35335,#35336,#35337,#35338,#35339,#35340,#35341,#35342),
 .UNSPECIFIED.,.F.,.F.,(4,3,3,3,3,3,3,3,4),(-229.893386550169,-229.852370720191,
-228.853012586625,-227.853654453059,-226.854296319493,-225.854938185927,
-224.85558005236,-223.856221918794,-223.61020124299),.UNSPECIFIED.);
#701=B_SPLINE_CURVE_WITH_KNOTS('',3,(#35343,#35344,#35345,#35346,#35347,
#35348,#35349,#35350,#35351,#35352,#35353,#35354,#35355,#35356,#35357,#35358,
#35359,#35360,#35361,#35362,#35363,#35364),.UNSPECIFIED.,.F.,.F.,(4,3,3,
3,3,3,3,4),(220.35454642184,220.858147518096,221.857505651663,222.856863785229,
223.856221918795,224.855580052361,225.854938185927,226.637731729019),
 .UNSPECIFIED.);
#702=B_SPLINE_CURVE_WITH_KNOTS('',3,(#35369,#35370,#35371,#35372,#35373,
#35374,#35375,#35376,#35377,#35378,#35379,#35380,#35381,#35382,#35383,#35384,
#35385,#35386,#35387,#35388,#35389,#35390),.UNSPECIFIED.,.F.,.F.,(4,3,3,
3,3,3,3,4),(-236.176571857349,-235.848519521587,-234.849161388021,-233.849803254455,
-232.850445120889,-231.851086987323,-230.851728853757,-229.893386550169),
 .UNSPECIFIED.);
#703=B_SPLINE_CURVE_WITH_KNOTS('',3,(#35391,#35392,#35393,#35394,#35395,
#35396,#35397,#35398,#35399,#35400,#35401,#35402,#35403,#35404,#35405,#35406,
#35407,#35408,#35409,#35410,#35411,#35412,#35413,#35414,#35415),
 .UNSPECIFIED.,.F.,.F.,(4,3,3,3,3,3,3,3,4),(226.637731729019,226.854296319493,
227.853654453059,228.853012586625,229.852370720191,230.851728853757,231.851086987323,
232.850445120889,232.920917036199),.UNSPECIFIED.);
#704=B_SPLINE_CURVE_WITH_KNOTS('',3,(#35420,#35421,#35422,#35423,#35424,
#35425,#35426,#35427,#35428,#35429,#35430,#35431,#35432,#35433,#35434,#35435,
#35436,#35437,#35438,#35439,#35440,#35441),.UNSPECIFIED.,.F.,.F.,(4,3,3,
3,3,3,3,4),(-242.459757164528,-241.844668322983,-240.845310189417,-239.845952055851,
-238.846593922285,-237.847235788719,-236.847877655153,-236.176571857349),
 .UNSPECIFIED.);
#705=B_SPLINE_CURVE_WITH_KNOTS('',3,(#35442,#35443,#35444,#35445,#35446,
#35447,#35448,#35449,#35450,#35451,#35452,#35453,#35454,#35455,#35456,#35457,
#35458,#35459,#35460,#35461,#35462,#35463),.UNSPECIFIED.,.F.,.F.,(4,3,3,
3,3,3,3,4),(232.920917036199,233.849803254455,234.849161388021,235.848519521587,
236.847877655153,237.847235788719,238.846593922285,239.204102343378),
 .UNSPECIFIED.);
#706=B_SPLINE_CURVE_WITH_KNOTS('',3,(#35468,#35469,#35470,#35471,#35472,
#35473,#35474,#35475,#35476,#35477,#35478,#35479,#35480,#35481,#35482,#35483,
#35484,#35485,#35486,#35487,#35488,#35489),.UNSPECIFIED.,.F.,.F.,(4,3,3,
3,3,3,3,4),(-248.742942471708,-247.84081712438,-246.841458990814,-245.842100857247,
-244.842742723681,-243.843384590115,-242.844026456549,-242.459757164528),
 .UNSPECIFIED.);
#707=B_SPLINE_CURVE_WITH_KNOTS('',3,(#35490,#35491,#35492,#35493,#35494,
#35495,#35496,#35497,#35498,#35499,#35500,#35501,#35502,#35503,#35504,#35505,
#35506,#35507,#35508,#35509,#35510,#35511),.UNSPECIFIED.,.F.,.F.,(4,3,3,
3,3,3,3,4),(239.204102343378,239.845952055851,240.845310189417,241.844668322983,
242.84402645655,243.843384590116,244.842742723682,245.487287650558),
 .UNSPECIFIED.);
#708=B_SPLINE_CURVE_WITH_KNOTS('',3,(#35516,#35517,#35518,#35519,#35520,
#35521,#35522,#35523,#35524,#35525,#35526,#35527,#35528,#35529,#35530,#35531,
#35532,#35533,#35534,#35535,#35536,#35537,#35538,#35539,#35540),
 .UNSPECIFIED.,.F.,.F.,(4,3,3,3,3,3,3,3,4),(-255.026127778888,-254.836324059342,
-253.836965925776,-252.83760779221,-251.838249658644,-250.838891525078,
-249.839533391512,-248.840175257946,-248.742942471708),.UNSPECIFIED.);
#709=B_SPLINE_CURVE_WITH_KNOTS('',3,(#35541,#35542,#35543,#35544,#35545,
#35546,#35547,#35548,#35549,#35550,#35551,#35552,#35553,#35554,#35555,#35556,
#35557,#35558,#35559,#35560,#35561,#35562),.UNSPECIFIED.,.F.,.F.,(4,3,3,
3,3,3,3,4),(245.487287650558,245.842100857248,246.841458990814,247.84081712438,
248.840175257946,249.839533391512,250.838891525078,251.770472957738),
 .UNSPECIFIED.);
#710=B_SPLINE_CURVE_WITH_KNOTS('',3,(#35567,#35568,#35569,#35570,#35571,
#35572,#35573,#35574,#35575,#35576,#35577,#35578,#35579,#35580,#35581,#35582,
#35583,#35584,#35585,#35586,#35587,#35588),.UNSPECIFIED.,.F.,.F.,(4,3,3,
3,3,3,3,4),(-261.309313086067,-260.832472860738,-259.833114727172,-258.833756593606,
-257.83439846004,-256.835040326474,-255.835682192908,-255.026127778888),
 .UNSPECIFIED.);
#711=B_SPLINE_CURVE_WITH_KNOTS('',3,(#35589,#35590,#35591,#35592,#35593,
#35594,#35595,#35596,#35597,#35598,#35599,#35600,#35601,#35602,#35603,#35604,
#35605,#35606,#35607,#35608,#35609,#35610,#35611,#35612,#35613),
 .UNSPECIFIED.,.F.,.F.,(4,3,3,3,3,3,3,3,4),(251.770472957738,251.838249658644,
252.83760779221,253.836965925776,254.836324059342,255.835682192908,256.835040326474,
257.83439846004,258.053658264917),.UNSPECIFIED.);
#712=B_SPLINE_CURVE_WITH_KNOTS('',3,(#35618,#35619,#35620,#35621,#35622,
#35623,#35624,#35625,#35626,#35627,#35628,#35629,#35630,#35631,#35632,#35633,
#35634,#35635,#35636,#35637,#35638,#35639),.UNSPECIFIED.,.F.,.F.,(4,3,3,
3,3,3,3,4),(-267.592498393247,-266.828621662134,-265.829263528568,-264.829905395002,
-263.830547261436,-262.83118912787,-261.831830994304,-261.309313086067),
 .UNSPECIFIED.);
#713=B_SPLINE_CURVE_WITH_KNOTS('',3,(#35640,#35641,#35642,#35643,#35644,
#35645,#35646,#35647,#35648,#35649,#35650,#35651,#35652,#35653,#35654,#35655,
#35656,#35657,#35658,#35659,#35660,#35661),.UNSPECIFIED.,.F.,.F.,(4,3,3,
3,3,3,3,4),(258.053658264917,258.833756593606,259.833114727172,260.832472860738,
261.831830994304,262.83118912787,263.830547261436,264.336843572097),
 .UNSPECIFIED.);
#714=B_SPLINE_CURVE_WITH_KNOTS('',3,(#35666,#35667,#35668,#35669,#35670,
#35671,#35672,#35673,#35674,#35675,#35676,#35677,#35678,#35679,#35680,#35681,
#35682,#35683,#35684,#35685,#35686,#35687,#35688,#35689,#35690),
 .UNSPECIFIED.,.F.,.F.,(4,3,3,3,3,3,3,3,4),(-273.875683700426,-273.824128597097,
-272.824770463531,-271.825412329965,-270.826054196399,-269.826696062833,
-268.827337929266,-267.8279797957,-267.592498393247),.UNSPECIFIED.);
#715=B_SPLINE_CURVE_WITH_KNOTS('',3,(#35691,#35692,#35693,#35694,#35695,
#35696,#35697,#35698,#35699,#35700,#35701,#35702,#35703,#35704,#35705,#35706,
#35707,#35708,#35709,#35710,#35711,#35712),.UNSPECIFIED.,.F.,.F.,(4,3,3,
3,3,3,3,4),(264.336843572097,264.829905395003,265.829263528569,266.828621662135,
267.827979795701,268.827337929267,269.826696062833,270.620028879276),
 .UNSPECIFIED.);
#716=B_SPLINE_CURVE_WITH_KNOTS('',3,(#35717,#35718,#35719,#35720,#35721,
#35722,#35723,#35724,#35725,#35726,#35727,#35728,#35729,#35730,#35731,#35732,
#35733,#35734,#35735,#35736,#35737,#35738),.UNSPECIFIED.,.F.,.F.,(4,3,3,
3,3,3,3,4),(-280.158869007606,-279.820277398493,-278.820919264927,-277.821561131361,
-276.822202997795,-275.822844864229,-274.823486730663,-273.875683700426),
 .UNSPECIFIED.);
#717=B_SPLINE_CURVE_WITH_KNOTS('',3,(#35739,#35740,#35741,#35742,#35743,
#35744,#35745,#35746,#35747,#35748,#35749,#35750,#35751,#35752,#35753,#35754,
#35755,#35756,#35757,#35758,#35759,#35760,#35761,#35762,#35763),
 .UNSPECIFIED.,.F.,.F.,(4,3,3,3,3,3,3,3,4),(270.620028879276,270.826054196399,
271.825412329965,272.824770463531,273.824128597097,274.823486730663,275.822844864229,
276.822202997795,276.903214186456),.UNSPECIFIED.);
#718=B_SPLINE_CURVE_WITH_KNOTS('',3,(#35768,#35769,#35770,#35771,#35772,
#35773,#35774,#35775,#35776,#35777,#35778,#35779,#35780,#35781,#35782,#35783,
#35784,#35785,#35786,#35787,#35788,#35789),.UNSPECIFIED.,.F.,.F.,(4,3,3,
3,3,3,3,4),(-286.442054314785,-285.816426199889,-284.817068066323,-283.817709932757,
-282.818351799191,-281.818993665625,-280.819635532059,-280.158869007606),
 .UNSPECIFIED.);
#719=B_SPLINE_CURVE_WITH_KNOTS('',3,(#35790,#35791,#35792,#35793,#35794,
#35795,#35796,#35797,#35798,#35799,#35800,#35801,#35802,#35803,#35804,#35805,
#35806,#35807,#35808,#35809,#35810,#35811),.UNSPECIFIED.,.F.,.F.,(4,3,3,
3,3,3,3,4),(276.903214186456,277.821561131361,278.820919264927,279.820277398493,
280.819635532059,281.818993665625,282.818351799191,283.186399493635),
 .UNSPECIFIED.);
#720=B_SPLINE_CURVE_WITH_KNOTS('',3,(#35816,#35817,#35818,#35819,#35820,
#35821,#35822,#35823,#35824,#35825,#35826,#35827,#35828,#35829,#35830,#35831,
#35832,#35833,#35834,#35835,#35836,#35837),.UNSPECIFIED.,.F.,.F.,(4,3,3,
3,3,3,3,4),(-292.725239621965,-291.812575001286,-290.81321686772,-289.813858734153,
-288.814500600587,-287.815142467021,-286.815784333455,-286.442054314785),
 .UNSPECIFIED.);
#721=B_SPLINE_CURVE_WITH_KNOTS('',3,(#35838,#35839,#35840,#35841,#35842,
#35843,#35844,#35845,#35846,#35847,#35848,#35849,#35850,#35851,#35852,#35853,
#35854,#35855,#35856,#35857,#35858,#35859),.UNSPECIFIED.,.F.,.F.,(4,3,3,
3,3,3,3,4),(283.186399493635,283.817709932757,284.817068066323,285.81642619989,
286.815784333456,287.815142467022,288.814500600588,289.469584800815),
 .UNSPECIFIED.);
#722=B_SPLINE_CURVE_WITH_KNOTS('',3,(#35864,#35865,#35866,#35867,#35868,
#35869,#35870,#35871,#35872,#35873,#35874,#35875,#35876,#35877,#35878,#35879,
#35880,#35881,#35882,#35883,#35884,#35885,#35886,#35887,#35888),
 .UNSPECIFIED.,.F.,.F.,(4,3,3,3,3,3,3,3,4),(-299.008424929145,-298.808081936248,
-297.808723802682,-296.809365669116,-295.81000753555,-294.810649401984,
-293.811291268418,-292.811933134852,-292.725239621965),.UNSPECIFIED.);
#723=B_SPLINE_CURVE_WITH_KNOTS('',3,(#35889,#35890,#35891,#35892,#35893,
#35894,#35895,#35896,#35897,#35898,#35899,#35900,#35901,#35902,#35903,#35904,
#35905,#35906,#35907,#35908,#35909,#35910),.UNSPECIFIED.,.F.,.F.,(4,3,3,
3,3,3,3,4),(289.469584800815,289.813858734154,290.81321686772,291.812575001286,
292.811933134852,293.811291268418,294.810649401984,295.752770107995),
 .UNSPECIFIED.);
#724=B_SPLINE_CURVE_WITH_KNOTS('',3,(#35915,#35916,#35917,#35918,#35919,
#35920,#35921,#35922,#35923,#35924,#35925,#35926,#35927,#35928,#35929,#35930,
#35931,#35932,#35933,#35934,#35935,#35936),.UNSPECIFIED.,.F.,.F.,(4,3,3,
3,3,3,3,4),(-305.291610236324,-304.804230737644,-303.804872604078,-302.805514470512,
-301.806156336946,-300.80679820338,-299.807440069814,-299.008424929145),
 .UNSPECIFIED.);
#725=B_SPLINE_CURVE_WITH_KNOTS('',3,(#35937,#35938,#35939,#35940,#35941,
#35942,#35943,#35944,#35945,#35946,#35947,#35948,#35949,#35950,#35951,#35952,
#35953,#35954,#35955,#35956,#35957,#35958,#35959,#35960,#35961),
 .UNSPECIFIED.,.F.,.F.,(4,3,3,3,3,3,3,3,4),(295.752770107995,295.81000753555,
296.809365669116,297.808723802682,298.808081936248,299.807440069814,300.80679820338,
301.806156336946,302.035955415174),.UNSPECIFIED.);
#726=B_SPLINE_CURVE_WITH_KNOTS('',3,(#35966,#35967,#35968,#35969,#35970,
#35971,#35972,#35973,#35974,#35975,#35976,#35977,#35978,#35979,#35980,#35981,
#35982,#35983,#35984,#35985,#35986,#35987),.UNSPECIFIED.,.F.,.F.,(4,3,3,
3,3,3,3,4),(-311.574795543504,-310.80037953904,-309.801021405475,-308.801663271908,
-307.802305138342,-306.802947004776,-305.80358887121,-305.291610236324),
 .UNSPECIFIED.);
#727=B_SPLINE_CURVE_WITH_KNOTS('',3,(#35988,#35989,#35990,#35991,#35992,
#35993,#35994,#35995,#35996,#35997,#35998,#35999,#36000,#36001,#36002,#36003,
#36004,#36005,#36006,#36007,#36008,#36009),.UNSPECIFIED.,.F.,.F.,(4,3,3,
3,3,3,3,4),(302.035955415174,302.805514470512,303.804872604078,304.804230737644,
305.80358887121,306.802947004777,307.802305138343,308.319140722354),
 .UNSPECIFIED.);
#728=B_SPLINE_CURVE_WITH_KNOTS('',3,(#36014,#36015,#36016,#36017,#36018,
#36019,#36020,#36021,#36022,#36023,#36024,#36025,#36026,#36027,#36028,#36029,
#36030,#36031,#36032,#36033,#36034,#36035,#36036,#36037,#36038),
 .UNSPECIFIED.,.F.,.F.,(4,3,3,3,3,3,3,3,4),(-317.857980850683,-317.795886474003,
-316.796528340437,-315.797170206871,-314.797812073305,-313.798453939739,
-312.799095806173,-311.799737672607,-311.574795543504),.UNSPECIFIED.);
#729=B_SPLINE_CURVE_WITH_KNOTS('',3,(#36039,#36040,#36041,#36042,#36043,
#36044,#36045,#36046,#36047,#36048,#36049,#36050,#36051,#36052,#36053,#36054,
#36055,#36056,#36057,#36058,#36059,#36060),.UNSPECIFIED.,.F.,.F.,(4,3,3,
3,3,3,3,4),(308.319140722354,308.801663271909,309.801021405475,310.800379539041,
311.799737672607,312.799095806173,313.798453939739,314.602326029533),
 .UNSPECIFIED.);
#730=B_SPLINE_CURVE_WITH_KNOTS('',3,(#36065,#36066,#36067,#36068,#36069,
#36070,#36071,#36072,#36073,#36074,#36075,#36076,#36077,#36078,#36079,#36080,
#36081,#36082,#36083,#36084,#36085,#36086),.UNSPECIFIED.,.F.,.F.,(4,3,3,
3,3,3,3,4),(-324.141166157863,-323.792035275399,-322.792677141833,-321.793319008267,
-320.793960874701,-319.794602741135,-318.795244607569,-317.857980850683),
 .UNSPECIFIED.);
#731=B_SPLINE_CURVE_WITH_KNOTS('',3,(#36087,#36088,#36089,#36090,#36091,
#36092,#36093,#36094,#36095,#36096,#36097,#36098,#36099,#36100,#36101,#36102,
#36103,#36104,#36105,#36106,#36107,#36108,#36109,#36110,#36111),
 .UNSPECIFIED.,.F.,.F.,(4,3,3,3,3,3,3,3,4),(314.602326029533,314.797812073305,
315.797170206871,316.796528340437,317.795886474003,318.795244607569,319.794602741135,
320.793960874701,320.885511336713),.UNSPECIFIED.);
#732=B_SPLINE_CURVE_WITH_KNOTS('',3,(#36116,#36117,#36118,#36119,#36120,
#36121,#36122,#36123,#36124,#36125,#36126,#36127,#36128,#36129,#36130,#36131,
#36132,#36133,#36134,#36135,#36136,#36137),.UNSPECIFIED.,.F.,.F.,(4,3,3,
3,3,3,3,4),(-330.424351465042,-329.788184076795,-328.788825943229,-327.789467809663,
-326.790109676097,-325.790751542531,-324.791393408965,-324.141166157863),
 .UNSPECIFIED.);
#733=B_SPLINE_CURVE_WITH_KNOTS('',3,(#36138,#36139,#36140,#36141,#36142,
#36143,#36144,#36145,#36146,#36147,#36148,#36149,#36150,#36151,#36152,#36153,
#36154,#36155,#36156,#36157,#36158,#36159),.UNSPECIFIED.,.F.,.F.,(4,3,3,
3,3,3,3,4),(320.885511336713,321.793319008267,322.792677141833,323.792035275399,
324.791393408965,325.790751542531,326.790109676097,327.168696643892),
 .UNSPECIFIED.);
#734=B_SPLINE_CURVE_WITH_KNOTS('',3,(#36164,#36165,#36166,#36167,#36168,
#36169,#36170,#36171,#36172,#36173,#36174,#36175,#36176,#36177,#36178,#36179,
#36180,#36181,#36182,#36183,#36184,#36185),.UNSPECIFIED.,.F.,.F.,(4,3,3,
3,3,3,3,4),(-336.707536772222,-335.784332878192,-334.784974744626,-333.78561661106,
-332.786258477494,-331.786900343927,-330.787542210361,-330.424351465042),
 .UNSPECIFIED.);
#735=B_SPLINE_CURVE_WITH_KNOTS('',3,(#36186,#36187,#36188,#36189,#36190,
#36191,#36192,#36193,#36194,#36195,#36196,#36197,#36198,#36199,#36200,#36201,
#36202,#36203,#36204,#36205,#36206,#36207),.UNSPECIFIED.,.F.,.F.,(4,3,3,
3,3,3,3,4),(327.168696643892,327.789467809663,328.78882594323,329.788184076796,
330.787542210362,331.786900343928,332.786258477494,333.451881951072),
 .UNSPECIFIED.);
#736=B_SPLINE_CURVE_WITH_KNOTS('',3,(#36212,#36213,#36214,#36215,#36216,
#36217,#36218,#36219,#36220,#36221,#36222,#36223,#36224,#36225,#36226,#36227,
#36228,#36229,#36230,#36231,#36232,#36233,#36234,#36235,#36236),
 .UNSPECIFIED.,.F.,.F.,(4,3,3,3,3,3,3,3,4),(-342.990722079402,-342.779839813154,
-341.780481679588,-340.781123546022,-339.781765412456,-338.78240727889,
-337.783049145324,-336.783691011758,-336.707536772222),.UNSPECIFIED.);
#737=B_SPLINE_CURVE_WITH_KNOTS('',3,(#36237,#36238,#36239,#36240,#36241,
#36242,#36243,#36244,#36245,#36246,#36247,#36248,#36249,#36250,#36251,#36252,
#36253,#36254,#36255,#36256,#36257,#36258),.UNSPECIFIED.,.F.,.F.,(4,3,3,
3,3,3,3,4),(333.451881951072,333.78561661106,334.784974744626,335.784332878192,
336.783691011758,337.783049145324,338.78240727889,339.735067258252),
 .UNSPECIFIED.);
#738=B_SPLINE_CURVE_WITH_KNOTS('',3,(#36263,#36264,#36265,#36266,#36267,
#36268,#36269,#36270,#36271,#36272,#36273,#36274,#36275,#36276,#36277,#36278,
#36279,#36280,#36281,#36282,#36283,#36284,#36285,#36286,#36287,#36288,#36289,
#36290,#36291,#36292,#36293,#36294,#36295,#36296),.UNSPECIFIED.,.F.,.F.,
(4,3,3,3,3,3,3,3,3,3,3,4),(-349.273907386581,-348.77598861455,-348.276309547767,
-347.776630480984,-347.276951414201,-346.777272347418,-346.277593280635,
-345.777914213852,-345.278235147069,-344.778556080286,-343.77919794672,
-342.990722079402),.UNSPECIFIED.);
#739=B_SPLINE_CURVE_WITH_KNOTS('',3,(#36297,#36298,#36299,#36300,#36301,
#36302,#36303,#36304,#36305,#36306,#36307,#36308,#36309,#36310,#36311,#36312,
#36313,#36314,#36315,#36316,#36317,#36318,#36319,#36320,#36321,#36322,#36323,
#36324),.UNSPECIFIED.,.F.,.F.,(4,3,3,3,3,3,3,3,3,4),(339.735067258252,339.781765412456,
340.781123546022,341.780481679588,342.779839813154,343.77919794672,344.778556080286,
345.278235147069,345.777914213852,346.018252565431),.UNSPECIFIED.);
#740=B_SPLINE_CURVE_WITH_KNOTS('',3,(#36329,#36330,#36331,#36332,#36333,
#36334,#36335,#36336,#36337,#36338,#36339,#36340,#36341,#36342,#36343,#36344,
#36345,#36346,#36347,#36348,#36349,#36350,#36351,#36352,#36353,#36354,#36355,
#36356,#36357,#36358,#36359,#36360,#36361,#36362,#36363,#36364,#36365,#36366,
#36367,#36368,#36369,#36370,#36371),.UNSPECIFIED.,.F.,.F.,(4,3,3,3,3,3,
3,3,3,3,3,3,3,3,4),(-355.557092693761,-355.27181648273,-354.772137415947,
-354.272458349164,-353.77277928238,-353.273100215597,-352.773421148814,
-352.273742082031,-351.774063015248,-351.274383948465,-350.774704881682,
-350.275025814899,-349.775346748116,-349.275667681333,-349.273907386581),
 .UNSPECIFIED.);
#741=B_SPLINE_CURVE_WITH_KNOTS('',3,(#36372,#36373,#36374,#36375,#36376,
#36377,#36378,#36379,#36380,#36381,#36382,#36383,#36384,#36385,#36386,#36387,
#36388,#36389,#36390,#36391,#36392,#36393,#36394,#36395,#36396,#36397,#36398,
#36399,#36400,#36401,#36402,#36403,#36404,#36405,#36406,#36407,#36408,#36409,
#36410,#36411,#36412,#36413,#36414),.UNSPECIFIED.,.F.,.F.,(4,3,3,3,3,3,
3,3,3,3,3,3,3,3,4),(346.018252565431,346.277593280635,346.777272347418,
347.276951414201,347.776630480984,348.276309547767,348.77598861455,349.275667681334,
349.775346748116,350.2750258149,350.774704881683,351.274383948466,351.774063015249,
352.273742082032,352.301437872611),.UNSPECIFIED.);
#742=B_SPLINE_CURVE_WITH_KNOTS('',3,(#36419,#36420,#36421,#36422,#36423,
#36424,#36425,#36426,#36427,#36428,#36429,#36430,#36431,#36432,#36433,#36434,
#36435,#36436,#36437,#36438,#36439,#36440,#36441,#36442,#36443,#36444,#36445,
#36446,#36447,#36448,#36449,#36450,#36451,#36452,#36453,#36454,#36455,#36456,
#36457,#36458,#36459,#36460,#36461),.UNSPECIFIED.,.F.,.F.,(4,3,3,3,3,3,
3,3,3,3,3,3,3,3,4),(-361.84027800094,-361.767644350909,-361.267965284126,
-360.768286217343,-360.26860715056,-359.768928083777,-359.269249016994,
-358.769569950211,-358.269890883428,-357.770211816645,-357.270532749862,
-356.770853683079,-356.271174616296,-355.771495549513,-355.557092693761),
 .UNSPECIFIED.);
#743=B_SPLINE_CURVE_WITH_KNOTS('',3,(#36462,#36463,#36464,#36465,#36466,
#36467,#36468,#36469,#36470,#36471,#36472,#36473,#36474,#36475,#36476,#36477,
#36478,#36479,#36480,#36481,#36482,#36483,#36484,#36485,#36486,#36487,#36488,
#36489,#36490,#36491,#36492,#36493,#36494,#36495,#36496,#36497,#36498,#36499,
#36500,#36501),.UNSPECIFIED.,.F.,.F.,(4,3,3,3,3,3,3,3,3,3,3,3,3,4),(352.301437872611,
352.773421148815,353.273100215598,353.772779282381,354.272458349164,354.772137415947,
355.27181648273,355.771495549513,356.271174616296,356.770853683079,357.270532749862,
357.770211816645,358.269890883428,358.58462317979),.UNSPECIFIED.);
#744=B_SPLINE_CURVE_WITH_KNOTS('',3,(#36506,#36507,#36508,#36509,#36510,
#36511,#36512,#36513,#36514,#36515,#36516,#36517,#36518,#36519,#36520,#36521,
#36522,#36523,#36524,#36525,#36526,#36527,#36528,#36529,#36530,#36531,#36532,
#36533,#36534,#36535,#36536,#36537,#36538,#36539,#36540,#36541,#36542,#36543,
#36544,#36545),.UNSPECIFIED.,.F.,.F.,(4,3,3,3,3,3,3,3,3,3,3,3,3,4),(-368.12346330812,
-367.763793152305,-367.264114085522,-366.764435018739,-366.264755951956,
-365.765076885173,-365.26539781839,-364.765718751607,-364.266039684824,
-363.766360618041,-363.266681551258,-362.767002484475,-362.267323417692,
-361.84027800094),.UNSPECIFIED.);
#745=B_SPLINE_CURVE_WITH_KNOTS('',3,(#36546,#36547,#36548,#36549,#36550,
#36551,#36552,#36553,#36554,#36555,#36556,#36557,#36558,#36559,#36560,#36561,
#36562,#36563,#36564,#36565,#36566,#36567,#36568,#36569,#36570,#36571,#36572,
#36573,#36574,#36575,#36576,#36577,#36578,#36579,#36580,#36581,#36582,#36583,
#36584,#36585,#36586,#36587,#36588),.UNSPECIFIED.,.F.,.F.,(4,3,3,3,3,3,
3,3,3,3,3,3,3,3,4),(358.58462317979,358.769569950211,359.269249016994,359.768928083777,
360.26860715056,360.768286217343,361.267965284126,361.767644350909,362.267323417692,
362.767002484475,363.266681551258,363.766360618041,364.266039684824,364.765718751607,
364.86780848697),.UNSPECIFIED.);
#746=B_SPLINE_CURVE_WITH_KNOTS('',3,(#36593,#36594,#36595,#36596,#36597,
#36598,#36599,#36600,#36601,#36602,#36603,#36604,#36605,#36606,#36607,#36608,
#36609,#36610,#36611,#36612,#36613,#36614,#36615,#36616,#36617,#36618,#36619,
#36620,#36621,#36622,#36623,#36624,#36625,#36626,#36627,#36628,#36629,#36630,
#36631,#36632,#36633,#36634,#36635),.UNSPECIFIED.,.F.,.F.,(4,3,3,3,3,3,
3,3,3,3,3,3,3,3,4),(-374.406648615299,-374.259621020484,-373.759941953701,
-373.260262886918,-372.760583820135,-372.260904753352,-371.761225686569,
-371.261546619786,-370.761867553003,-370.26218848622,-369.762509419437,
-369.262830352654,-368.763151285871,-368.263472219088,-368.12346330812),
 .UNSPECIFIED.);
#747=B_SPLINE_CURVE_WITH_KNOTS('',3,(#36636,#36637,#36638,#36639,#36640,
#36641,#36642,#36643,#36644,#36645,#36646,#36647,#36648,#36649,#36650,#36651,
#36652,#36653,#36654,#36655,#36656,#36657,#36658,#36659,#36660,#36661,#36662,
#36663,#36664,#36665,#36666,#36667,#36668,#36669,#36670,#36671,#36672,#36673,
#36674,#36675),.UNSPECIFIED.,.F.,.F.,(4,3,3,3,3,3,3,3,3,3,3,3,3,4),(364.86780848697,
365.26539781839,365.765076885173,366.264755951956,366.764435018739,367.264114085522,
367.763793152305,368.263472219088,368.763151285871,369.262830352654,369.762509419437,
370.26218848622,370.761867553004,371.150993794149),.UNSPECIFIED.);
#748=B_SPLINE_CURVE_WITH_KNOTS('',3,(#36680,#36681,#36682,#36683,#36684,
#36685,#36686,#36687,#36688,#36689,#36690,#36691,#36692,#36693,#36694,#36695,
#36696,#36697,#36698,#36699,#36700,#36701,#36702,#36703,#36704,#36705,#36706,
#36707,#36708,#36709,#36710,#36711,#36712,#36713,#36714,#36715,#36716,#36717,
#36718,#36719),.UNSPECIFIED.,.F.,.F.,(4,3,3,3,3,3,3,3,3,3,3,3,3,4),(-380.689833922479,
-380.255769821881,-379.756090755098,-379.256411688315,-378.756732621532,
-378.257053554749,-377.757374487966,-377.257695421183,-376.7580163544,-376.258337287616,
-375.758658220834,-375.25897915405,-374.759300087267,-374.406648615299),
 .UNSPECIFIED.);
#749=B_SPLINE_CURVE_WITH_KNOTS('',3,(#36720,#36721,#36722,#36723,#36724,
#36725,#36726,#36727,#36728,#36729,#36730,#36731,#36732,#36733,#36734,#36735,
#36736,#36737,#36738,#36739,#36740,#36741,#36742,#36743,#36744,#36745,#36746,
#36747,#36748,#36749,#36750,#36751,#36752,#36753,#36754,#36755,#36756,#36757,
#36758,#36759,#36760,#36761,#36762),.UNSPECIFIED.,.F.,.F.,(4,3,3,3,3,3,
3,3,3,3,3,3,3,3,4),(371.150993794149,371.261546619787,371.76122568657,372.260904753353,
372.760583820136,373.260262886919,373.759941953702,374.259621020485,374.759300087268,
375.258979154051,375.758658220834,376.258337287617,376.7580163544,377.257695421183,
377.434179101329),.UNSPECIFIED.);
#750=B_SPLINE_CURVE_WITH_KNOTS('',3,(#36767,#36768,#36769,#36770,#36771,
#36772,#36773,#36774,#36775,#36776,#36777,#36778,#36779,#36780,#36781,#36782,
#36783,#36784,#36785,#36786,#36787,#36788,#36789,#36790,#36791,#36792,#36793,
#36794,#36795,#36796,#36797,#36798,#36799,#36800,#36801,#36802,#36803,#36804,
#36805,#36806,#36807,#36808,#36809),.UNSPECIFIED.,.F.,.F.,(4,3,3,3,3,3,
3,3,3,3,3,3,3,3,4),(-386.973019229658,-386.75159769006,-386.251918623277,
-385.752239556494,-385.252560489711,-384.752881422928,-384.253202356145,
-383.753523289362,-383.253844222579,-382.754165155796,-382.254486089013,
-381.75480702223,-381.255127955447,-380.755448888664,-380.689833922479),
 .UNSPECIFIED.);
#751=B_SPLINE_CURVE_WITH_KNOTS('',3,(#36810,#36811,#36812,#36813,#36814,
#36815,#36816,#36817,#36818,#36819,#36820,#36821,#36822,#36823,#36824,#36825,
#36826,#36827,#36828,#36829,#36830,#36831,#36832,#36833,#36834,#36835,#36836,
#36837,#36838,#36839,#36840,#36841,#36842,#36843,#36844,#36845,#36846,#36847,
#36848,#36849),.UNSPECIFIED.,.F.,.F.,(4,3,3,3,3,3,3,3,3,3,3,3,3,4),(377.434179101329,
377.757374487966,378.257053554749,378.756732621532,379.256411688315,379.756090755098,
380.255769821881,380.755448888664,381.255127955447,381.75480702223,382.254486089013,
382.754165155796,383.253844222579,383.717364408508),.UNSPECIFIED.);
#752=B_SPLINE_CURVE_WITH_KNOTS('',3,(#36854,#36855,#36856,#36857,#36858,
#36859,#36860,#36861,#36862,#36863,#36864,#36865,#36866,#36867,#36868,#36869,
#36870,#36871,#36872,#36873,#36874,#36875,#36876,#36877,#36878,#36879,#36880,
#36881,#36882,#36883,#36884,#36885,#36886,#36887,#36888,#36889,#36890,#36891,
#36892,#36893,#36894,#36895,#36896),.UNSPECIFIED.,.F.,.F.,(4,3,3,3,3,3,
3,3,3,3,3,3,3,3,4),(-393.256204536838,-393.247425558239,-392.747746491456,
-392.248067424673,-391.74838835789,-391.248709291107,-390.749030224324,
-390.249351157541,-389.749672090758,-389.249993023975,-388.750313957192,
-388.250634890409,-387.750955823626,-387.251276756843,-386.973019229658),
 .UNSPECIFIED.);
#753=B_SPLINE_CURVE_WITH_KNOTS('',3,(#36897,#36898,#36899,#36900,#36901,
#36902,#36903,#36904,#36905,#36906,#36907,#36908,#36909,#36910,#36911,#36912,
#36913,#36914,#36915,#36916,#36917,#36918,#36919,#36920,#36921,#36922,#36923,
#36924,#36925,#36926,#36927,#36928,#36929,#36930,#36931,#36932,#36933,#36934,
#36935,#36936,#36937,#36938,#36939),.UNSPECIFIED.,.F.,.F.,(4,3,3,3,3,3,
3,3,3,3,3,3,3,3,4),(383.717364408508,383.753523289362,384.253202356145,
384.752881422928,385.252560489711,385.752239556494,386.251918623277,386.75159769006,
387.251276756843,387.750955823626,388.250634890409,388.750313957192,389.249993023975,
389.749672090758,390.000549715688),.UNSPECIFIED.);
#754=B_SPLINE_CURVE_WITH_KNOTS('',3,(#36945,#36946,#36947,#36948),
 .UNSPECIFIED.,.F.,.F.,(4,4),(405.265452313083,405.755527026166),
 .UNSPECIFIED.);
#755=B_SPLINE_CURVE_WITH_KNOTS('',3,(#36954,#36955,#36956,#36957,#36958,
#36959,#36960,#36961,#36962,#36963,#36964,#36965,#36966,#36967,#36968,#36969,
#36970),.UNSPECIFIED.,.F.,.F.,(4,1,1,1,1,1,1,1,1,1,1,1,1,1,4),(398.982267005903,
399.260524533088,399.760203599871,400.259882666654,400.759561733437,401.25924080022,
401.758919867003,402.258598933787,402.75827800057,403.257957067353,403.757636134136,
404.257315200919,404.756994267702,405.256673334485,405.265452313083),
 .UNSPECIFIED.);
#756=B_SPLINE_CURVE_WITH_KNOTS('',3,(#36973,#36974,#36975,#36976,#36977,
#36978,#36979,#36980,#36981,#36982,#36983,#36984,#36985),.UNSPECIFIED.,
 .F.,.F.,(4,1,1,1,1,1,1,1,1,1,4),(398.982267005904,399.231068447758,399.730747514541,
400.230426581324,400.730105648107,401.22978471489,401.729463781673,402.229142848456,
402.728821915239,403.228500982022,403.728180048805),.UNSPECIFIED.);
#757=B_SPLINE_CURVE_WITH_KNOTS('',3,(#36990,#36991,#36992,#36993,#36994,
#36995,#36996,#36997,#36998,#36999,#37000,#37001,#37002,#37003,#37004,#37005,
#37006),.UNSPECIFIED.,.F.,.F.,(4,1,1,1,1,1,1,1,1,1,1,1,1,1,4),(392.699081698724,
392.764696664909,393.264375731692,393.764054798475,394.263733865258,394.763412932041,
395.263091998824,395.762771065607,396.26245013239,396.762129199173,397.261808265956,
397.761487332739,398.261166399522,398.760845466305,398.982267005903),
 .UNSPECIFIED.);
#758=B_SPLINE_CURVE_WITH_KNOTS('',3,(#37007,#37008,#37009,#37010,#37011,
#37012,#37013,#37014,#37015,#37016,#37017,#37018,#37019,#37020,#37021,#37022,
#37023),.UNSPECIFIED.,.F.,.F.,(4,1,1,1,1,1,1,1,1,1,1,1,1,1,4),(392.699081698724,
392.735240579579,393.234919646362,393.734598713145,394.234277779928,394.733956846711,
395.233635913494,395.733314980277,396.23299404706,396.732673113843,397.232352180626,
397.732031247409,398.231710314192,398.731389380975,398.982267005904),
 .UNSPECIFIED.);
#759=B_SPLINE_CURVE_WITH_KNOTS('',3,(#37028,#37029,#37030,#37031,#37032,
#37033,#37034,#37035,#37036,#37037,#37038,#37039,#37040,#37041,#37042,#37043),
 .UNSPECIFIED.,.F.,.F.,(4,1,1,1,1,1,1,1,1,1,1,1,1,4),(386.415896391544,
386.768547863513,387.268226930296,387.767905997079,388.267585063862,388.767264130645,
389.266943197428,389.766622264211,390.266301330994,390.765980397777,391.26565946456,
391.765338531343,392.265017598126,392.699081698724),.UNSPECIFIED.);
#760=B_SPLINE_CURVE_WITH_KNOTS('',3,(#37044,#37045,#37046,#37047,#37048,
#37049,#37050,#37051,#37052,#37053,#37054,#37055,#37056,#37057,#37058,#37059),
 .UNSPECIFIED.,.F.,.F.,(4,1,1,1,1,1,1,1,1,1,1,1,1,4),(386.415896391545,
386.739091778183,387.238770844966,387.738449911749,388.238128978532,388.737808045315,
389.237487112098,389.737166178881,390.236845245664,390.736524312447,391.23620337923,
391.735882446013,392.235561512796,392.699081698724),.UNSPECIFIED.);
#761=B_SPLINE_CURVE_WITH_KNOTS('',3,(#37064,#37065,#37066,#37067,#37068,
#37069,#37070,#37071,#37072,#37073,#37074,#37075,#37076,#37077,#37078,#37079,
#37080),.UNSPECIFIED.,.F.,.F.,(4,1,1,1,1,1,1,1,1,1,1,1,1,1,4),(380.132711084365,
380.272719995333,380.772399062117,381.2720781289,381.771757195683,382.271436262466,
382.771115329249,383.270794396032,383.770473462815,384.270152529598,384.769831596381,
385.269510663164,385.769189729947,386.26886879673,386.415896391544),
 .UNSPECIFIED.);
#762=B_SPLINE_CURVE_WITH_KNOTS('',3,(#37081,#37082,#37083,#37084,#37085,
#37086,#37087,#37088,#37089,#37090,#37091,#37092,#37093,#37094,#37095,#37096,
#37097),.UNSPECIFIED.,.F.,.F.,(4,1,1,1,1,1,1,1,1,1,1,1,1,1,4),(380.132711084365,
380.243263910003,380.742942976786,381.242622043569,381.742301110352,382.241980177135,
382.741659243918,383.241338310702,383.741017377485,384.240696444268,384.740375511051,
385.240054577834,385.739733644617,386.2394127114,386.415896391545),
 .UNSPECIFIED.);
#763=B_SPLINE_CURVE_WITH_KNOTS('',3,(#37102,#37103,#37104,#37105,#37106,
#37107,#37108,#37109,#37110,#37111,#37112,#37113,#37114,#37115,#37116,#37117),
 .UNSPECIFIED.,.F.,.F.,(4,1,1,1,1,1,1,1,1,1,1,1,1,4),(373.849525777185,
374.276571193937,374.77625026072,375.275929327503,375.775608394286,376.275287461069,
376.774966527852,377.274645594635,377.774324661418,378.274003728201,378.773682794984,
379.273361861767,379.77304092855,380.132711084365),.UNSPECIFIED.);
#764=B_SPLINE_CURVE_WITH_KNOTS('',3,(#37118,#37119,#37120,#37121,#37122,
#37123,#37124,#37125,#37126,#37127,#37128,#37129,#37130,#37131,#37132,#37133),
 .UNSPECIFIED.,.F.,.F.,(4,1,1,1,1,1,1,1,1,1,1,1,1,4),(373.849525777185,
374.247115108607,374.74679417539,375.246473242173,375.746152308956,376.245831375739,
376.745510442522,377.245189509305,377.744868576088,378.244547642871,378.744226709654,
379.243905776437,379.74358484322,380.132711084365),.UNSPECIFIED.);
#765=B_SPLINE_CURVE_WITH_KNOTS('',3,(#37138,#37139,#37140,#37141,#37142,
#37143,#37144,#37145,#37146,#37147,#37148,#37149,#37150,#37151,#37152,#37153,
#37154),.UNSPECIFIED.,.F.,.F.,(4,1,1,1,1,1,1,1,1,1,1,1,1,1,4),(367.566340470006,
367.780743325758,368.280422392541,368.780101459324,369.279780526107,369.77945959289,
370.279138659673,370.778817726456,371.278496793239,371.778175860022,372.277854926805,
372.777533993588,373.277213060371,373.776892127154,373.849525777185),
 .UNSPECIFIED.);
#766=B_SPLINE_CURVE_WITH_KNOTS('',3,(#37155,#37156,#37157,#37158,#37159,
#37160,#37161,#37162,#37163,#37164,#37165,#37166,#37167,#37168,#37169,#37170,
#37171),.UNSPECIFIED.,.F.,.F.,(4,1,1,1,1,1,1,1,1,1,1,1,1,1,4),(367.566340470006,
367.751287240428,368.250966307211,368.750645373994,369.250324440777,369.75000350756,
370.249682574343,370.749361641126,371.249040707909,371.748719774692,372.248398841475,
372.748077908258,373.247756975041,373.747436041824,373.849525777185),
 .UNSPECIFIED.);
#767=B_SPLINE_CURVE_WITH_KNOTS('',3,(#37176,#37177,#37178,#37179,#37180,
#37181,#37182,#37183,#37184,#37185,#37186,#37187,#37188,#37189,#37190,#37191,
#37192),.UNSPECIFIED.,.F.,.F.,(4,1,1,1,1,1,1,1,1,1,1,1,1,1,4),(361.283155162826,
361.284915457579,361.784594524362,362.284273591145,362.783952657928,363.283631724711,
363.783310791494,364.282989858277,364.78266892506,365.282347991843,365.782027058626,
366.281706125409,366.781385192192,367.281064258975,367.566340470006),
 .UNSPECIFIED.);
#768=B_SPLINE_CURVE_WITH_KNOTS('',3,(#37193,#37194,#37195,#37196,#37197,
#37198,#37199,#37200,#37201,#37202,#37203,#37204,#37205,#37206,#37207,#37208),
 .UNSPECIFIED.,.F.,.F.,(4,1,1,1,1,1,1,1,1,1,1,1,1,4),(361.283155162826,
361.755138439031,362.254817505815,362.754496572598,363.254175639381,363.753854706164,
364.253533772947,364.75321283973,365.252891906513,365.752570973296,366.252250040079,
366.751929106862,367.251608173645,367.566340470006),.UNSPECIFIED.);
#769=B_SPLINE_CURVE_WITH_KNOTS('',3,(#37213,#37214,#37215,#37216,#37217,
#37218,#37219,#37220,#37221,#37222,#37223,#37224,#37225,#37226),
 .UNSPECIFIED.,.F.,.F.,(4,1,1,1,1,1,1,1,1,1,1,4),(354.999969855646,355.788445722965,
356.787803856531,357.287482923314,357.787161990097,358.28684105688,358.786520123663,
359.286199190446,359.78587825723,360.285557324013,360.785236390796,361.283155162826),
 .UNSPECIFIED.);
#770=B_SPLINE_CURVE_WITH_KNOTS('',3,(#37227,#37228,#37229,#37230,#37231,
#37232,#37233,#37234,#37235,#37236,#37237,#37238,#37239,#37240,#37241,#37242,
#37243),.UNSPECIFIED.,.F.,.F.,(4,1,1,1,1,1,1,1,1,1,1,1,1,1,4),(354.999969855647,
355.259310570852,355.758989637635,356.258668704418,356.758347771201,357.258026837984,
357.757705904767,358.25738497155,358.757064038333,359.256743105116,359.756422171899,
360.256101238682,360.755780305465,361.255459372248,361.283155162826),
 .UNSPECIFIED.);
#771=B_SPLINE_CURVE_WITH_KNOTS('',3,(#37248,#37249,#37250,#37251,#37252,
#37253,#37254,#37255,#37256,#37257,#37258),.UNSPECIFIED.,.F.,.F.,(4,1,1,
1,1,1,1,1,4),(348.716784548467,348.792938788003,349.792296921569,350.791655055135,
351.791013188701,352.790371322267,353.789729455833,354.789087589399,354.999969855646),
 .UNSPECIFIED.);
#772=B_SPLINE_CURVE_WITH_KNOTS('',3,(#37259,#37260,#37261,#37262,#37263,
#37264,#37265,#37266,#37267,#37268,#37269,#37270),.UNSPECIFIED.,.F.,.F.,
(4,1,1,1,1,1,1,1,1,4),(348.716784548467,348.763482702673,349.762840836239,
350.762198969805,351.761557103371,352.760915236937,353.760273370503,354.259952437286,
354.759631504069,354.999969855647),.UNSPECIFIED.);
#773=B_SPLINE_CURVE_WITH_KNOTS('',3,(#37275,#37276,#37277,#37278,#37279,
#37280,#37281,#37282,#37283,#37284),.UNSPECIFIED.,.F.,.F.,(4,1,1,1,1,1,
1,4),(342.433599241287,342.796789986607,343.796148120173,344.795506253739,
345.794864387305,346.794222520871,347.793580654437,348.716784548467),
 .UNSPECIFIED.);
#774=B_SPLINE_CURVE_WITH_KNOTS('',3,(#37285,#37286,#37287,#37288,#37289,
#37290,#37291,#37292,#37293,#37294),.UNSPECIFIED.,.F.,.F.,(4,1,1,1,1,1,
1,4),(342.433599241288,342.767333901277,343.766692034843,344.766050168409,
345.765408301975,346.764766435541,347.764124569107,348.716784548467),
 .UNSPECIFIED.);
#775=B_SPLINE_CURVE_WITH_KNOTS('',3,(#37299,#37300,#37301,#37302,#37303,
#37304,#37305,#37306,#37307,#37308),.UNSPECIFIED.,.F.,.F.,(4,1,1,1,1,1,
1,4),(336.150413934108,336.80064118521,337.799999318776,338.799357452343,
339.798715585909,340.798073719475,341.797431853041,342.433599241287),
 .UNSPECIFIED.);
#776=B_SPLINE_CURVE_WITH_KNOTS('',3,(#37309,#37310,#37311,#37312,#37313,
#37314,#37315,#37316,#37317,#37318),.UNSPECIFIED.,.F.,.F.,(4,1,1,1,1,1,
1,4),(336.150413934108,336.77118509988,337.770543233446,338.769901367012,
339.769259500578,340.768617634145,341.767975767711,342.433599241288),
 .UNSPECIFIED.);
#777=B_SPLINE_CURVE_WITH_KNOTS('',3,(#37323,#37324,#37325,#37326,#37327,
#37328,#37329,#37330,#37331,#37332),.UNSPECIFIED.,.F.,.F.,(4,1,1,1,1,1,
1,4),(329.867228626928,330.804492383814,331.80385051738,332.803208650946,
333.802566784512,334.801924918078,335.801283051644,336.150413934108),
 .UNSPECIFIED.);
#778=B_SPLINE_CURVE_WITH_KNOTS('',3,(#37333,#37334,#37335,#37336,#37337,
#37338,#37339,#37340,#37341,#37342),.UNSPECIFIED.,.F.,.F.,(4,1,1,1,1,1,
1,4),(329.867228626928,330.775036298484,331.77439443205,332.773752565616,
333.773110699182,334.772468832748,335.771826966314,336.150413934108),
 .UNSPECIFIED.);
#779=B_SPLINE_CURVE_WITH_KNOTS('',3,(#37347,#37348,#37349,#37350,#37351,
#37352,#37353,#37354,#37355,#37356,#37357),.UNSPECIFIED.,.F.,.F.,(4,1,1,
1,1,1,1,1,4),(323.584043319749,323.808985448852,324.808343582418,325.807701715984,
326.80705984955,327.806417983116,328.805776116682,329.805134250248,329.867228626928),
 .UNSPECIFIED.);
#780=B_SPLINE_CURVE_WITH_KNOTS('',3,(#37358,#37359,#37360,#37361,#37362,
#37363,#37364,#37365,#37366,#37367,#37368),.UNSPECIFIED.,.F.,.F.,(4,1,1,
1,1,1,1,1,4),(323.584043319749,323.779529363522,324.778887497088,325.778245630654,
326.77760376422,327.776961897786,328.776320031352,329.775678164918,329.867228626928),
 .UNSPECIFIED.);
#781=B_SPLINE_CURVE_WITH_KNOTS('',3,(#37373,#37374,#37375,#37376,#37377,
#37378,#37379,#37380,#37381,#37382),.UNSPECIFIED.,.F.,.F.,(4,1,1,1,1,1,
1,4),(317.300858012569,317.812836647456,318.812194781022,319.811552914588,
320.810911048154,321.81026918172,322.809627315286,323.584043319749),
 .UNSPECIFIED.);
#782=B_SPLINE_CURVE_WITH_KNOTS('',3,(#37383,#37384,#37385,#37386,#37387,
#37388,#37389,#37390,#37391,#37392),.UNSPECIFIED.,.F.,.F.,(4,1,1,1,1,1,
1,4),(317.300858012569,317.783380562125,318.782738695691,319.782096829258,
320.781454962824,321.78081309639,322.780171229956,323.584043319749),
 .UNSPECIFIED.);
#783=B_SPLINE_CURVE_WITH_KNOTS('',3,(#37397,#37398,#37399,#37400,#37401,
#37402,#37403,#37404,#37405,#37406),.UNSPECIFIED.,.F.,.F.,(4,1,1,1,1,1,
1,4),(311.017672705389,311.816687846059,312.816045979625,313.815404113191,
314.814762246757,315.814120380323,316.81347851389,317.300858012569),
 .UNSPECIFIED.);
#784=B_SPLINE_CURVE_WITH_KNOTS('',3,(#37407,#37408,#37409,#37410,#37411,
#37412,#37413,#37414,#37415,#37416),.UNSPECIFIED.,.F.,.F.,(4,1,1,1,1,1,
1,4),(311.01767270539,311.787231760729,312.786589894295,313.785948027861,
314.785306161427,315.784664294993,316.784022428559,317.300858012569),
 .UNSPECIFIED.);
#785=B_SPLINE_CURVE_WITH_KNOTS('',3,(#37421,#37422,#37423,#37424,#37425,
#37426,#37427,#37428,#37429,#37430,#37431),.UNSPECIFIED.,.F.,.F.,(4,1,1,
1,1,1,1,1,4),(304.73448739821,304.821180911097,305.820539044663,306.819897178229,
307.819255311795,308.818613445361,309.817971578927,310.817329712493,311.017672705389),
 .UNSPECIFIED.);
#786=B_SPLINE_CURVE_WITH_KNOTS('',3,(#37432,#37433,#37434,#37435,#37436,
#37437,#37438,#37439,#37440,#37441,#37442),.UNSPECIFIED.,.F.,.F.,(4,1,1,
1,1,1,1,1,4),(304.73448739821,304.791724825767,305.791082959333,306.790441092899,
307.789799226465,308.789157360031,309.788515493597,310.787873627163,311.01767270539),
 .UNSPECIFIED.);
#787=B_SPLINE_CURVE_WITH_KNOTS('',3,(#37447,#37448,#37449,#37450,#37451,
#37452,#37453,#37454,#37455,#37456),.UNSPECIFIED.,.F.,.F.,(4,1,1,1,1,1,
1,4),(298.45130209103,298.825032109701,299.824390243267,300.823748376833,
301.823106510399,302.822464643965,303.821822777531,304.73448739821),
 .UNSPECIFIED.);
#788=B_SPLINE_CURVE_WITH_KNOTS('',3,(#37457,#37458,#37459,#37460,#37461,
#37462,#37463,#37464,#37465,#37466),.UNSPECIFIED.,.F.,.F.,(4,1,1,1,1,1,
1,4),(298.451302091031,298.795576024371,299.794934157937,300.794292291503,
301.793650425069,302.793008558635,303.792366692201,304.73448739821),
 .UNSPECIFIED.);
#789=B_SPLINE_CURVE_WITH_KNOTS('',3,(#37471,#37472,#37473,#37474,#37475,
#37476,#37477,#37478,#37479,#37480),.UNSPECIFIED.,.F.,.F.,(4,1,1,1,1,1,
1,4),(292.168116783851,292.828883308304,293.82824144187,294.827599575437,
295.826957709003,296.826315842569,297.825673976135,298.45130209103),
 .UNSPECIFIED.);
#790=B_SPLINE_CURVE_WITH_KNOTS('',3,(#37481,#37482,#37483,#37484,#37485,
#37486,#37487,#37488,#37489,#37490),.UNSPECIFIED.,.F.,.F.,(4,1,1,1,1,1,
1,4),(292.168116783851,292.799427222974,293.79878535654,294.798143490106,
295.797501623672,296.796859757238,297.796217890804,298.451302091031),
 .UNSPECIFIED.);
#791=B_SPLINE_CURVE_WITH_KNOTS('',3,(#37495,#37496,#37497,#37498,#37499,
#37500,#37501,#37502,#37503,#37504),.UNSPECIFIED.,.F.,.F.,(4,1,1,1,1,1,
1,4),(285.884931476671,286.832734506908,287.832092640474,288.83145077404,
289.830808907606,290.830167041172,291.829525174738,292.168116783851),
 .UNSPECIFIED.);
#792=B_SPLINE_CURVE_WITH_KNOTS('',3,(#37505,#37506,#37507,#37508,#37509,
#37510,#37511,#37512,#37513,#37514),.UNSPECIFIED.,.F.,.F.,(4,1,1,1,1,1,
1,4),(285.884931476672,286.803278421578,287.802636555144,288.80199468871,
289.801352822276,290.800710955842,291.800069089408,292.168116783851),
 .UNSPECIFIED.);
#793=B_SPLINE_CURVE_WITH_KNOTS('',3,(#37519,#37520,#37521,#37522,#37523,
#37524,#37525,#37526,#37527,#37528,#37529),.UNSPECIFIED.,.F.,.F.,(4,1,1,
1,1,1,1,1,4),(279.601746169492,279.837227571946,280.836585705512,281.835943839078,
282.835301972644,283.83466010621,284.834018239776,285.833376373342,285.884931476671),
 .UNSPECIFIED.);
#794=B_SPLINE_CURVE_WITH_KNOTS('',3,(#37530,#37531,#37532,#37533,#37534,
#37535,#37536,#37537,#37538,#37539,#37540),.UNSPECIFIED.,.F.,.F.,(4,1,1,
1,1,1,1,1,4),(279.601746169492,279.807771486616,280.807129620182,281.806487753748,
282.805845887314,283.80520402088,284.804562154446,285.803920288012,285.884931476672),
 .UNSPECIFIED.);
#795=B_SPLINE_CURVE_WITH_KNOTS('',3,(#37545,#37546,#37547,#37548,#37549,
#37550,#37551,#37552,#37553,#37554),.UNSPECIFIED.,.F.,.F.,(4,1,1,1,1,1,
1,4),(273.318560862312,273.84107877055,274.840436904116,275.839795037682,
276.839153171248,277.838511304814,278.83786943838,279.601746169492),
 .UNSPECIFIED.);
#796=B_SPLINE_CURVE_WITH_KNOTS('',3,(#37555,#37556,#37557,#37558,#37559,
#37560,#37561,#37562,#37563,#37564),.UNSPECIFIED.,.F.,.F.,(4,1,1,1,1,1,
1,4),(273.318560862312,273.811622685219,274.810980818785,275.810338952351,
276.809697085917,277.809055219484,278.80841335305,279.601746169492),
 .UNSPECIFIED.);
#797=B_SPLINE_CURVE_WITH_KNOTS('',3,(#37569,#37570,#37571,#37572,#37573,
#37574,#37575,#37576,#37577,#37578),.UNSPECIFIED.,.F.,.F.,(4,1,1,1,1,1,
1,4),(267.035375555133,267.844929969153,268.844288102719,269.843646236285,
270.843004369851,271.842362503417,272.841720636983,273.318560862312),
 .UNSPECIFIED.);
#798=B_SPLINE_CURVE_WITH_KNOTS('',3,(#37579,#37580,#37581,#37582,#37583,
#37584,#37585,#37586,#37587,#37588),.UNSPECIFIED.,.F.,.F.,(4,1,1,1,1,1,
1,4),(267.035375555133,267.815473883823,268.814832017389,269.814190150955,
270.813548284521,271.812906418087,272.812264551653,273.318560862312),
 .UNSPECIFIED.);
#799=B_SPLINE_CURVE_WITH_KNOTS('',3,(#37593,#37594,#37595,#37596,#37597,
#37598,#37599,#37600,#37601,#37602,#37603),.UNSPECIFIED.,.F.,.F.,(4,1,1,
1,1,1,1,1,4),(260.752190247953,260.849423034191,261.848781167757,262.848139301323,
263.847497434889,264.846855568455,265.846213702021,266.845571835587,267.035375555133),
 .UNSPECIFIED.);
#800=B_SPLINE_CURVE_WITH_KNOTS('',3,(#37604,#37605,#37606,#37607,#37608,
#37609,#37610,#37611,#37612,#37613,#37614),.UNSPECIFIED.,.F.,.F.,(4,1,1,
1,1,1,1,1,4),(260.752190247953,260.819966948861,261.819325082427,262.818683215993,
263.818041349559,264.817399483125,265.816757616691,266.816115750257,267.035375555133),
 .UNSPECIFIED.);
#801=B_SPLINE_CURVE_WITH_KNOTS('',3,(#37619,#37620,#37621,#37622,#37623,
#37624,#37625,#37626,#37627,#37628),.UNSPECIFIED.,.F.,.F.,(4,1,1,1,1,1,
1,4),(254.469004940773,254.853274232795,255.852632366361,256.851990499927,
257.851348633493,258.850706767059,259.850064900625,260.752190247953),
 .UNSPECIFIED.);
#802=B_SPLINE_CURVE_WITH_KNOTS('',3,(#37629,#37630,#37631,#37632,#37633,
#37634,#37635,#37636,#37637,#37638),.UNSPECIFIED.,.F.,.F.,(4,1,1,1,1,1,
1,4),(254.469004940774,254.823818147464,255.82317628103,256.822534414597,
257.821892548163,258.821250681729,259.820608815295,260.752190247953),
 .UNSPECIFIED.);
#803=B_SPLINE_CURVE_WITH_KNOTS('',3,(#37643,#37644,#37645,#37646,#37647,
#37648,#37649,#37650,#37651,#37652),.UNSPECIFIED.,.F.,.F.,(4,1,1,1,1,1,
1,4),(248.185819633594,248.857125431398,249.856483564964,250.85584169853,
251.855199832097,252.854557965663,253.853916099229,254.469004940773),
 .UNSPECIFIED.);
#804=B_SPLINE_CURVE_WITH_KNOTS('',3,(#37653,#37654,#37655,#37656,#37657,
#37658,#37659,#37660,#37661,#37662),.UNSPECIFIED.,.F.,.F.,(4,1,1,1,1,1,
1,4),(248.185819633594,248.827669346068,249.827027479634,250.8263856132,
251.825743746766,252.825101880332,253.824460013898,254.469004940774),
 .UNSPECIFIED.);
#805=B_SPLINE_CURVE_WITH_KNOTS('',3,(#37667,#37668,#37669,#37670,#37671,
#37672,#37673,#37674,#37675,#37676),.UNSPECIFIED.,.F.,.F.,(4,1,1,1,1,1,
1,4),(241.902634326414,242.860976630002,243.860334763568,244.859692897134,
245.8590510307,246.858409164266,247.857767297832,248.185819633594),
 .UNSPECIFIED.);
#806=B_SPLINE_CURVE_WITH_KNOTS('',3,(#37677,#37678,#37679,#37680,#37681,
#37682,#37683,#37684,#37685,#37686),.UNSPECIFIED.,.F.,.F.,(4,1,1,1,1,1,
1,4),(241.902634326415,242.831520544672,243.830878678238,244.830236811804,
245.82959494537,246.828953078936,247.828311212502,248.185819633594),
 .UNSPECIFIED.);
#807=B_SPLINE_CURVE_WITH_KNOTS('',3,(#37691,#37692,#37693,#37694,#37695,
#37696,#37697,#37698,#37699,#37700,#37701),.UNSPECIFIED.,.F.,.F.,(4,1,1,
1,1,1,1,1,4),(235.619449019235,235.86546969504,236.864827828606,237.864185962172,
238.863544095738,239.862902229304,240.86226036287,241.861618496436,241.902634326414),
 .UNSPECIFIED.);
#808=B_SPLINE_CURVE_WITH_KNOTS('',3,(#37702,#37703,#37704,#37705,#37706,
#37707,#37708,#37709,#37710,#37711,#37712),.UNSPECIFIED.,.F.,.F.,(4,1,1,
1,1,1,1,1,4),(235.619449019235,235.83601360971,236.835371743276,237.834729876842,
238.834088010408,239.833446143974,240.83280427754,241.832162411106,241.902634326415),
 .UNSPECIFIED.);
#809=B_SPLINE_CURVE_WITH_KNOTS('',3,(#37717,#37718,#37719,#37720,#37721,
#37722,#37723,#37724,#37725,#37726),.UNSPECIFIED.,.F.,.F.,(4,1,1,1,1,1,
1,4),(229.336263712055,229.869320893643,230.86867902721,231.868037160776,
232.867395294342,233.866753427908,234.866111561474,235.619449019235),
 .UNSPECIFIED.);
#810=B_SPLINE_CURVE_WITH_KNOTS('',3,(#37727,#37728,#37729,#37730,#37731,
#37732,#37733,#37734,#37735,#37736),.UNSPECIFIED.,.F.,.F.,(4,1,1,1,1,1,
1,4),(229.336263712055,229.839864808313,230.839222941879,231.838581075445,
232.837939209011,233.837297342577,234.836655476144,235.619449019235),
 .UNSPECIFIED.);
#811=B_SPLINE_CURVE_WITH_KNOTS('',3,(#37741,#37742,#37743,#37744,#37745,
#37746,#37747,#37748,#37749,#37750),.UNSPECIFIED.,.F.,.F.,(4,1,1,1,1,1,
1,4),(223.053078404876,223.873172092247,224.872530225813,225.871888359379,
226.871246492945,227.870604626511,228.869962760077,229.336263712055),
 .UNSPECIFIED.);
#812=B_SPLINE_CURVE_WITH_KNOTS('',3,(#37751,#37752,#37753,#37754,#37755,
#37756,#37757,#37758,#37759,#37760),.UNSPECIFIED.,.F.,.F.,(4,1,1,1,1,1,
1,4),(223.053078404876,223.843716006917,224.843074140483,225.842432274049,
226.841790407615,227.841148541181,228.840506674747,229.336263712055),
 .UNSPECIFIED.);
#813=B_SPLINE_CURVE_WITH_KNOTS('',3,(#37765,#37766,#37767,#37768,#37769,
#37770,#37771,#37772,#37773,#37774,#37775),.UNSPECIFIED.,.F.,.F.,(4,1,1,
1,1,1,1,1,4),(216.769893097696,216.877665157285,217.877023290851,218.876381424417,
219.875739557983,220.875097691549,221.874455825115,222.873813958681,223.053078404876),
 .UNSPECIFIED.);
#814=B_SPLINE_CURVE_WITH_KNOTS('',3,(#37776,#37777,#37778,#37779,#37780,
#37781,#37782,#37783,#37784,#37785,#37786),.UNSPECIFIED.,.F.,.F.,(4,1,1,
1,1,1,1,1,4),(216.769893097696,216.848209071955,217.847567205521,218.846925339087,
219.846283472653,220.845641606219,221.844999739785,222.844357873351,223.053078404876),
 .UNSPECIFIED.);
#815=B_SPLINE_CURVE_WITH_KNOTS('',3,(#37791,#37792,#37793,#37794,#37795,
#37796,#37797,#37798,#37799,#37800),.UNSPECIFIED.,.F.,.F.,(4,1,1,1,1,1,
1,4),(210.486707790516,210.881516355889,211.880874489455,212.880232623021,
213.879590756587,214.878948890153,215.878307023719,216.769893097696),
 .UNSPECIFIED.);
#816=B_SPLINE_CURVE_WITH_KNOTS('',3,(#37801,#37802,#37803,#37804,#37805,
#37806,#37807,#37808,#37809,#37810),.UNSPECIFIED.,.F.,.F.,(4,1,1,1,1,1,
1,4),(210.486707790517,210.852060270558,211.851418404124,212.85077653769,
213.850134671257,214.849492804823,215.848850938389,216.769893097696),
 .UNSPECIFIED.);
#817=B_SPLINE_CURVE_WITH_KNOTS('',3,(#37815,#37816,#37817,#37818,#37819,
#37820,#37821,#37822,#37823,#37824),.UNSPECIFIED.,.F.,.F.,(4,1,1,1,1,1,
1,4),(204.203522483337,204.885367554492,205.884725688058,206.884083821624,
207.88344195519,208.882800088756,209.882158222323,210.486707790516),
 .UNSPECIFIED.);
#818=B_SPLINE_CURVE_WITH_KNOTS('',3,(#37825,#37826,#37827,#37828,#37829,
#37830,#37831,#37832,#37833,#37834),.UNSPECIFIED.,.F.,.F.,(4,1,1,1,1,1,
1,4),(204.203522483337,204.855911469162,205.855269602728,206.854627736294,
207.85398586986,208.853344003426,209.852702136992,210.486707790517),
 .UNSPECIFIED.);
#819=B_SPLINE_CURVE_WITH_KNOTS('',3,(#37839,#37840,#37841,#37842,#37843,
#37844,#37845,#37846,#37847,#37848),.UNSPECIFIED.,.F.,.F.,(4,1,1,1,1,1,
1,4),(197.920337176157,198.889218753096,199.888576886662,200.887935020228,
201.887293153794,202.88665128736,203.886009420926,204.203522483337),
 .UNSPECIFIED.);
#820=B_SPLINE_CURVE_WITH_KNOTS('',3,(#37849,#37850,#37851,#37852,#37853,
#37854,#37855,#37856,#37857,#37858),.UNSPECIFIED.,.F.,.F.,(4,1,1,1,1,1,
1,4),(197.920337176158,198.859762667766,199.859120801332,200.858478934898,
201.857837068464,202.85719520203,203.856553335596,204.203522483337),
 .UNSPECIFIED.);
#821=B_SPLINE_CURVE_WITH_KNOTS('',3,(#37863,#37864,#37865,#37866,#37867,
#37868,#37869,#37870,#37871,#37872,#37873),.UNSPECIFIED.,.F.,.F.,(4,1,1,
1,1,1,1,1,4),(191.637151868978,191.893711818134,192.8930699517,193.892428085266,
194.891786218832,195.891144352398,196.890502485964,197.88986061953,197.920337176157),
 .UNSPECIFIED.);
#822=B_SPLINE_CURVE_WITH_KNOTS('',3,(#37874,#37875,#37876,#37877,#37878,
#37879,#37880,#37881,#37882,#37883,#37884),.UNSPECIFIED.,.F.,.F.,(4,1,1,
1,1,1,1,1,4),(191.637151868978,191.864255732803,192.86361386637,193.862971999936,
194.862330133502,195.861688267068,196.861046400634,197.8604045342,197.920337176158),
 .UNSPECIFIED.);
#823=B_SPLINE_CURVE_WITH_KNOTS('',3,(#37889,#37890,#37891,#37892,#37893,
#37894,#37895,#37896,#37897,#37898),.UNSPECIFIED.,.F.,.F.,(4,1,1,1,1,1,
1,4),(185.353966561798,185.897563016737,186.896921150303,187.89627928387,
188.895637417436,189.894995551002,190.894353684568,191.637151868978),
 .UNSPECIFIED.);
#824=B_SPLINE_CURVE_WITH_KNOTS('',3,(#37899,#37900,#37901,#37902,#37903,
#37904,#37905,#37906,#37907,#37908),.UNSPECIFIED.,.F.,.F.,(4,1,1,1,1,1,
1,4),(185.353966561799,185.868106931407,186.867465064973,187.866823198539,
188.866181332105,189.865539465671,190.864897599237,191.637151868978),
 .UNSPECIFIED.);
#825=B_SPLINE_CURVE_WITH_KNOTS('',3,(#37913,#37914,#37915,#37916,#37917,
#37918,#37919,#37920,#37921,#37922),.UNSPECIFIED.,.F.,.F.,(4,1,1,1,1,1,
1,4),(179.070781254619,179.901414215341,180.900772348907,181.900130482473,
182.899488616039,183.898846749605,184.898204883171,185.353966561798),
 .UNSPECIFIED.);
#826=B_SPLINE_CURVE_WITH_KNOTS('',3,(#37923,#37924,#37925,#37926,#37927,
#37928,#37929,#37930,#37931,#37932),.UNSPECIFIED.,.F.,.F.,(4,1,1,1,1,1,
1,4),(179.070781254619,179.871958130011,180.871316263577,181.870674397143,
182.870032530709,183.869390664275,184.868748797841,185.353966561799),
 .UNSPECIFIED.);
#827=B_SPLINE_CURVE_WITH_KNOTS('',3,(#37937,#37938,#37939,#37940,#37941,
#37942,#37943,#37944,#37945,#37946,#37947),.UNSPECIFIED.,.F.,.F.,(4,1,1,
1,1,1,1,1,4),(172.787595947439,172.905907280379,173.905265413945,174.904623547511,
175.903981681077,176.903339814643,177.902697948209,178.902056081775,179.070781254619),
 .UNSPECIFIED.);
#828=B_SPLINE_CURVE_WITH_KNOTS('',3,(#37948,#37949,#37950,#37951,#37952,
#37953,#37954,#37955,#37956,#37957,#37958),.UNSPECIFIED.,.F.,.F.,(4,1,1,
1,1,1,1,1,4),(172.787595947439,172.876451195049,173.875809328615,174.875167462181,
175.874525595747,176.873883729313,177.873241862879,178.872599996445,179.070781254619),
 .UNSPECIFIED.);
#829=B_SPLINE_CURVE_WITH_KNOTS('',3,(#37963,#37964,#37965,#37966,#37967,
#37968,#37969,#37970,#37971,#37972),.UNSPECIFIED.,.F.,.F.,(4,1,1,1,1,1,
1,4),(166.504410640259,166.909758478983,167.909116612549,168.908474746115,
169.907832879681,170.907191013247,171.906549146813,172.787595947439),
 .UNSPECIFIED.);
#830=B_SPLINE_CURVE_WITH_KNOTS('',3,(#37973,#37974,#37975,#37976,#37977,
#37978,#37979,#37980,#37981,#37982),.UNSPECIFIED.,.F.,.F.,(4,1,1,1,1,1,
1,4),(166.50441064026,166.880302393652,167.879660527218,168.879018660784,
169.87837679435,170.877734927916,171.877093061483,172.787595947439),
 .UNSPECIFIED.);
#831=B_SPLINE_CURVE_WITH_KNOTS('',3,(#37987,#37988,#37989,#37990,#37991,
#37992,#37993,#37994,#37995,#37996),.UNSPECIFIED.,.F.,.F.,(4,1,1,1,1,1,
1,4),(160.22122533308,160.913609677586,161.912967811152,162.912325944718,
163.911684078284,164.91104221185,165.910400345416,166.504410640259),
 .UNSPECIFIED.);
#832=B_SPLINE_CURVE_WITH_KNOTS('',3,(#37997,#37998,#37999,#38000,#38001,
#38002,#38003,#38004,#38005,#38006),.UNSPECIFIED.,.F.,.F.,(4,1,1,1,1,1,
1,4),(160.22122533308,160.884153592256,161.883511725822,162.882869859388,
163.882227992954,164.88158612652,165.880944260086,166.50441064026),
 .UNSPECIFIED.);
#833=B_SPLINE_CURVE_WITH_KNOTS('',3,(#38011,#38012,#38013,#38014,#38015,
#38016,#38017,#38018,#38019,#38020),.UNSPECIFIED.,.F.,.F.,(4,1,1,1,1,1,
1,4),(153.9380400259,154.91746087619,155.916819009756,156.916177143322,
157.915535276888,158.914893410454,159.91425154402,160.22122533308),
 .UNSPECIFIED.);
#834=B_SPLINE_CURVE_WITH_KNOTS('',3,(#38021,#38022,#38023,#38024,#38025,
#38026,#38027,#38028,#38029,#38030),.UNSPECIFIED.,.F.,.F.,(4,1,1,1,1,1,
1,4),(153.938040025901,154.88800479086,155.887362924426,156.886721057992,
157.886079191558,158.885437325124,159.88479545869,160.22122533308),
 .UNSPECIFIED.);
#835=B_SPLINE_CURVE_WITH_KNOTS('',3,(#38035,#38036,#38037,#38038,#38039,
#38040,#38041,#38042,#38043,#38044,#38045),.UNSPECIFIED.,.F.,.F.,(4,1,1,
1,1,1,1,1,4),(147.654854718721,147.921953941228,148.921312074794,149.92067020836,
150.920028341926,151.919386475492,152.918744609058,153.918102742624,153.9380400259),
 .UNSPECIFIED.);
#836=B_SPLINE_CURVE_WITH_KNOTS('',3,(#38046,#38047,#38048,#38049,#38050,
#38051,#38052,#38053,#38054,#38055,#38056),.UNSPECIFIED.,.F.,.F.,(4,1,1,
1,1,1,1,1,4),(147.654854718721,147.892497855897,148.891855989463,149.891214123029,
150.890572256596,151.889930390162,152.889288523728,153.888646657294,153.938040025901),
 .UNSPECIFIED.);
#837=B_SPLINE_CURVE_WITH_KNOTS('',3,(#38061,#38062,#38063,#38064,#38065,
#38066,#38067,#38068,#38069,#38070),.UNSPECIFIED.,.F.,.F.,(4,1,1,1,1,1,
1,4),(141.371669411541,141.925805139831,142.925163273397,143.924521406963,
144.92387954053,145.923237674096,146.922595807662,147.654854718721),
 .UNSPECIFIED.);
#838=B_SPLINE_CURVE_WITH_KNOTS('',3,(#38071,#38072,#38073,#38074,#38075,
#38076,#38077,#38078,#38079,#38080),.UNSPECIFIED.,.F.,.F.,(4,1,1,1,1,1,
1,4),(141.371669411542,141.896349054501,142.895707188067,143.895065321633,
144.894423455199,145.893781588765,146.893139722331,147.654854718721),
 .UNSPECIFIED.);
#839=B_SPLINE_CURVE_WITH_KNOTS('',3,(#38085,#38086,#38087,#38088,#38089,
#38090,#38091,#38092,#38093,#38094),.UNSPECIFIED.,.F.,.F.,(4,1,1,1,1,1,
1,4),(135.088484104362,135.929656338435,136.929014472001,137.928372605567,
138.927730739133,139.927088872699,140.926447006265,141.371669411541),
 .UNSPECIFIED.);
#840=B_SPLINE_CURVE_WITH_KNOTS('',3,(#38095,#38096,#38097,#38098,#38099,
#38100,#38101,#38102,#38103,#38104),.UNSPECIFIED.,.F.,.F.,(4,1,1,1,1,1,
1,4),(135.088484104362,135.900200253105,136.899558386671,137.898916520237,
138.898274653803,139.897632787369,140.896990920935,141.371669411542),
 .UNSPECIFIED.);
#841=B_SPLINE_CURVE_WITH_KNOTS('',3,(#38109,#38110,#38111,#38112,#38113,
#38114,#38115,#38116,#38117,#38118,#38119),.UNSPECIFIED.,.F.,.F.,(4,1,1,
1,1,1,1,1,4),(128.805298797182,128.934149403473,129.933507537039,130.932865670605,
131.932223804171,132.931581937737,133.930940071303,134.930298204869,135.088484104362),
 .UNSPECIFIED.);
#842=B_SPLINE_CURVE_WITH_KNOTS('',3,(#38120,#38121,#38122,#38123,#38124,
#38125,#38126,#38127,#38128,#38129,#38130),.UNSPECIFIED.,.F.,.F.,(4,1,1,
1,1,1,1,1,4),(128.805298797182,128.904693318142,129.904051451709,130.903409585275,
131.902767718841,132.902125852407,133.901483985973,134.900842119539,135.088484104362),
 .UNSPECIFIED.);
#843=B_SPLINE_CURVE_WITH_KNOTS('',3,(#38135,#38136,#38137,#38138,#38139,
#38140,#38141,#38142,#38143,#38144),.UNSPECIFIED.,.F.,.F.,(4,1,1,1,1,1,
1,4),(122.522113490002,122.938000602077,123.937358735643,124.936716869209,
125.936075002775,126.935433136341,127.934791269907,128.805298797182),
 .UNSPECIFIED.);
#844=B_SPLINE_CURVE_WITH_KNOTS('',3,(#38145,#38146,#38147,#38148,#38149,
#38150,#38151,#38152,#38153,#38154),.UNSPECIFIED.,.F.,.F.,(4,1,1,1,1,1,
1,4),(122.522113490003,122.908544516746,123.907902650312,124.907260783878,
125.906618917444,126.90597705101,127.905335184576,128.805298797182),
 .UNSPECIFIED.);
#845=B_SPLINE_CURVE_WITH_KNOTS('',3,(#38159,#38160,#38161,#38162,#38163,
#38164,#38165,#38166,#38167,#38168),.UNSPECIFIED.,.F.,.F.,(4,1,1,1,1,1,
1,4),(116.238928182823,116.94185180068,117.941209934246,118.940568067812,
119.939926201378,120.939284334944,121.93864246851,122.522113490002),
 .UNSPECIFIED.);
#846=B_SPLINE_CURVE_WITH_KNOTS('',3,(#38169,#38170,#38171,#38172,#38173,
#38174,#38175,#38176,#38177,#38178),.UNSPECIFIED.,.F.,.F.,(4,1,1,1,1,1,
1,4),(116.238928182823,116.91239571535,117.911753848916,118.911111982482,
119.910470116048,120.909828249614,121.90918638318,122.522113490003),
 .UNSPECIFIED.);
#847=B_SPLINE_CURVE_WITH_KNOTS('',3,(#38183,#38184,#38185,#38186,#38187,
#38188,#38189,#38190,#38191,#38192),.UNSPECIFIED.,.F.,.F.,(4,1,1,1,1,1,
1,4),(109.955742875643,110.945702999284,111.94506113285,112.944419266416,
113.943777399982,114.943135533548,115.942493667114,116.238928182823),
 .UNSPECIFIED.);
#848=B_SPLINE_CURVE_WITH_KNOTS('',3,(#38193,#38194,#38195,#38196,#38197,
#38198,#38199,#38200,#38201,#38202),.UNSPECIFIED.,.F.,.F.,(4,1,1,1,1,1,
1,4),(109.955742875644,110.916246913954,111.91560504752,112.914963181086,
113.914321314652,114.913679448218,115.913037581784,116.238928182823),
 .UNSPECIFIED.);
#849=B_SPLINE_CURVE_WITH_KNOTS('',3,(#38207,#38208,#38209,#38210,#38211,
#38212,#38213,#38214,#38215,#38216,#38217),.UNSPECIFIED.,.F.,.F.,(4,1,1,
1,1,1,1,1,4),(103.672557568464,103.950196064322,104.949554197888,105.948912331454,
106.94827046502,107.947628598586,108.946986732152,109.946344865718,109.955742875643),
 .UNSPECIFIED.);
#850=B_SPLINE_CURVE_WITH_KNOTS('',3,(#38218,#38219,#38220,#38221,#38222,
#38223,#38224,#38225,#38226,#38227,#38228),.UNSPECIFIED.,.F.,.F.,(4,1,1,
1,1,1,1,1,4),(103.672557568464,103.920739978991,104.920098112557,105.919456246123,
106.918814379689,107.918172513255,108.917530646822,109.916888780388,109.955742875644),
 .UNSPECIFIED.);
#851=B_SPLINE_CURVE_WITH_KNOTS('',3,(#38233,#38234,#38235,#38236,#38237,
#38238,#38239,#38240,#38241,#38242),.UNSPECIFIED.,.F.,.F.,(4,1,1,1,1,1,
1,4),(97.3893722612841,97.9540472629253,98.9534053964914,99.9527635300574,
100.952121663623,101.95147979719,102.950837930756,103.672557568464),
 .UNSPECIFIED.);
#852=B_SPLINE_CURVE_WITH_KNOTS('',3,(#38243,#38244,#38245,#38246,#38247,
#38248,#38249,#38250,#38251,#38252),.UNSPECIFIED.,.F.,.F.,(4,1,1,1,1,1,
1,4),(97.3893722612845,97.924591177595,98.9239493111611,99.9233074447271,
100.922665578293,101.922023711859,102.921381845425,103.672557568464),
 .UNSPECIFIED.);
#853=B_SPLINE_CURVE_WITH_KNOTS('',3,(#38257,#38258,#38259,#38260,#38261,
#38262,#38263,#38264,#38265,#38266),.UNSPECIFIED.,.F.,.F.,(4,1,1,1,1,1,
1,4),(91.1061869541045,91.9578984615291,92.9572565950951,93.9566147286612,
94.9559728622272,95.9553309957932,96.9546891293593,97.3893722612841),
 .UNSPECIFIED.);
#854=B_SPLINE_CURVE_WITH_KNOTS('',3,(#38267,#38268,#38269,#38270,#38271,
#38272,#38273,#38274,#38275,#38276),.UNSPECIFIED.,.F.,.F.,(4,1,1,1,1,1,
1,4),(91.1061869541048,91.9284423761987,92.9278005097648,93.9271586433308,
94.9265167768969,95.9258749104629,96.925233044029,97.3893722612845),
 .UNSPECIFIED.);
#855=B_SPLINE_CURVE_WITH_KNOTS('',3,(#38281,#38282,#38283,#38284,#38285,
#38286,#38287,#38288,#38289,#38290,#38291),.UNSPECIFIED.,.F.,.F.,(4,1,1,
1,1,1,1,1,4),(84.8230016469249,84.9623915265667,85.9617496601328,86.9611077936988,
87.9604659272649,88.9598240608309,89.959182194397,90.958540327963,91.1061869541045),
 .UNSPECIFIED.);
#856=B_SPLINE_CURVE_WITH_KNOTS('',3,(#38292,#38293,#38294,#38295,#38296,
#38297,#38298,#38299,#38300,#38301,#38302),.UNSPECIFIED.,.F.,.F.,(4,1,1,
1,1,1,1,1,4),(84.8230016469253,84.9329354412364,85.9322935748025,86.9316517083685,
87.9310098419346,88.9303679755006,89.9297261090666,90.9290842426327,91.1061869541048),
 .UNSPECIFIED.);
#857=B_SPLINE_CURVE_WITH_KNOTS('',3,(#38307,#38308,#38309,#38310,#38311,
#38312,#38313,#38314,#38315,#38316),.UNSPECIFIED.,.F.,.F.,(4,1,1,1,1,1,
1,4),(78.5398163397454,78.9662427251705,79.9656008587365,80.9649589923026,
81.9643171258686,82.9636752594347,83.9630333930007,84.8230016469249),
 .UNSPECIFIED.);
#858=B_SPLINE_CURVE_WITH_KNOTS('',3,(#38317,#38318,#38319,#38320,#38321,
#38322,#38323,#38324,#38325,#38326),.UNSPECIFIED.,.F.,.F.,(4,1,1,1,1,1,
1,4),(78.5398163397457,78.9367866398401,79.9361447734062,80.9355029069722,
81.9348610405383,82.9342191741043,83.9335773076704,84.8230016469253),
 .UNSPECIFIED.);
#859=B_SPLINE_CURVE_WITH_KNOTS('',3,(#38331,#38332,#38333,#38334,#38335,
#38336,#38337,#38338,#38339,#38340),.UNSPECIFIED.,.F.,.F.,(4,1,1,1,1,1,
1,4),(72.2566310325658,72.9700939237742,73.9694520573402,74.9688101909063,
75.9681683244723,76.9675264580384,77.9668845916044,78.5398163397454),
 .UNSPECIFIED.);
#860=B_SPLINE_CURVE_WITH_KNOTS('',3,(#38341,#38342,#38343,#38344,#38345,
#38346,#38347,#38348,#38349,#38350),.UNSPECIFIED.,.F.,.F.,(4,1,1,1,1,1,
1,4),(72.2566310325661,72.9406378384438,73.9399959720099,74.9393541055759,
75.938712239142,76.938070372708,77.9374285062741,78.5398163397457),
 .UNSPECIFIED.);
#861=B_SPLINE_CURVE_WITH_KNOTS('',3,(#38355,#38356,#38357,#38358,#38359,
#38360,#38361,#38362,#38363,#38364,#38365),.UNSPECIFIED.,.F.,.F.,(4,1,1,
1,1,1,1,1,4),(65.9734457253862,65.9745869888119,66.9739451223779,67.9733032559439,
68.97266138951,69.972019523076,70.9713776566421,71.9707357902081,72.2566310325658),
 .UNSPECIFIED.);
#862=B_SPLINE_CURVE_WITH_KNOTS('',3,(#38366,#38367,#38368,#38369,#38370,
#38371,#38372,#38373,#38374,#38375),.UNSPECIFIED.,.F.,.F.,(4,1,1,1,1,1,
1,4),(65.9734457253865,66.9444890370476,67.9438471706136,68.9432053041797,
69.9425634377457,70.9419215713118,71.9412797048778,72.2566310325661),
 .UNSPECIFIED.);
#863=B_SPLINE_CURVE_WITH_KNOTS('',3,(#38380,#38381,#38382,#38383,#38384,
#38385,#38386,#38387,#38388,#38389,#38390,#38391),.UNSPECIFIED.,.F.,.F.,
(4,1,1,1,1,1,1,1,1,4),(59.6902604182066,59.9784381874156,60.4781172541986,
60.9777963209816,61.4774753877646,61.9771544545477,62.9765125881137,63.9758707216798,
64.9752288552458,65.9734457253862),.UNSPECIFIED.);
#864=B_SPLINE_CURVE_WITH_KNOTS('',3,(#38392,#38393,#38394,#38395,#38396,
#38397,#38398,#38399,#38400,#38401,#38402),.UNSPECIFIED.,.F.,.F.,(4,1,1,
1,1,1,1,1,4),(59.6902604182069,59.9489821020852,60.9483402356513,61.9476983692173,
62.9470565027834,63.9464146363494,64.9457727699155,65.9451309034815,65.9734457253865),
 .UNSPECIFIED.);
#865=B_SPLINE_CURVE_WITH_KNOTS('',3,(#38407,#38408,#38409,#38410,#38411,
#38412,#38413,#38414,#38415,#38416,#38417,#38418,#38419,#38420,#38421,#38422,
#38423),.UNSPECIFIED.,.F.,.F.,(4,1,1,1,1,1,1,1,1,1,1,1,1,1,4),(53.407075111027,
53.4826103192363,53.9822893860193,54.4819684528023,54.9816475195853,55.4813265863684,
55.9810056531514,56.4806847199344,56.9803637867174,57.4800428535005,57.9797219202835,
58.4794009870665,58.9790800538495,59.4787591206325,59.6902604182066),
 .UNSPECIFIED.);
#866=B_SPLINE_CURVE_WITH_KNOTS('',3,(#38424,#38425,#38426,#38427,#38428,
#38429,#38430,#38431,#38432,#38433,#38434,#38435,#38436,#38437,#38438,#38439),
 .UNSPECIFIED.,.F.,.F.,(4,1,1,1,1,1,1,1,1,1,1,1,1,4),(53.4070751110273,
53.4531542339059,53.9528333006889,54.452512367472,54.952191434255,55.451870501038,
55.951549567821,56.4512286346041,56.9509077013871,57.4505867681701,57.9502658349531,
58.4499449017362,58.9496239685192,59.6902604182069),.UNSPECIFIED.);
#867=B_SPLINE_CURVE_WITH_KNOTS('',3,(#38444,#38445,#38446,#38447,#38448,
#38449,#38450,#38451,#38452,#38453,#38454,#38455,#38456,#38457,#38458,#38459),
 .UNSPECIFIED.,.F.,.F.,(4,1,1,1,1,1,1,1,1,1,1,1,1,4),(47.1238898038474,
47.48646151784,47.986140584623,48.485819651406,48.9854987181891,49.4851777849721,
49.9848568517551,50.4845359185381,50.9842149853212,51.4838940521042,51.9835731188872,
52.4832521856702,52.9829312524532,53.407075111027),.UNSPECIFIED.);
#868=B_SPLINE_CURVE_WITH_KNOTS('',3,(#38460,#38461,#38462,#38463,#38464,
#38465,#38466,#38467,#38468,#38469,#38470,#38471,#38472,#38473,#38474,#38475),
 .UNSPECIFIED.,.F.,.F.,(4,1,1,1,1,1,1,1,1,1,1,1,1,4),(47.1238898038477,
47.4570054325096,47.9566844992927,48.4563635660757,48.9560426328587,49.4557216996417,
49.9554007664248,50.4550798332078,50.9547588999908,51.4544379667738,51.9541170335568,
52.4537961003399,52.9534751671229,53.4070751110273),.UNSPECIFIED.);
#869=B_SPLINE_CURVE_WITH_KNOTS('',3,(#38480,#38481,#38482,#38483,#38484,
#38485,#38486,#38487,#38488,#38489,#38490,#38491,#38492,#38493,#38494,#38495,
#38496),.UNSPECIFIED.,.F.,.F.,(4,1,1,1,1,1,1,1,1,1,1,1,1,1,4),(40.8407044966678,
40.9906336496607,41.4903127164437,41.9899917832267,42.4896708500098,42.9893499167928,
43.4890289835758,43.9887080503588,44.4883871171419,44.9880661839249,45.4877452507079,
45.9874243174909,46.4871033842739,46.986782451057,47.1238898038474),
 .UNSPECIFIED.);
#870=B_SPLINE_CURVE_WITH_KNOTS('',3,(#38497,#38498,#38499,#38500,#38501,
#38502,#38503,#38504,#38505,#38506,#38507,#38508,#38509,#38510,#38511,#38512,
#38513),.UNSPECIFIED.,.F.,.F.,(4,1,1,1,1,1,1,1,1,1,1,1,1,1,4),(40.8407044966681,
40.9611775643303,41.4608566311134,41.9605356978964,42.4602147646794,42.9598938314624,
43.4595728982454,43.9592519650285,44.4589310318115,44.9586100985945,45.4582891653775,
45.9579682321606,46.4576472989436,46.9573263657266,47.1238898038477),
 .UNSPECIFIED.);
#871=B_SPLINE_CURVE_WITH_KNOTS('',3,(#38518,#38519,#38520,#38521,#38522,
#38523,#38524,#38525,#38526,#38527,#38528,#38529,#38530,#38531,#38532,#38533),
 .UNSPECIFIED.,.F.,.F.,(4,1,1,1,1,1,1,1,1,1,1,1,1,4),(34.5575191894882,
34.9944848482644,35.4941639150474,35.9938429818305,36.4935220486135,36.9932011153965,
37.4928801821795,37.9925592489626,38.4922383157456,38.9919173825286,39.4915964493116,
39.9912755160946,40.4909545828777,40.8407044966678),.UNSPECIFIED.);
#872=B_SPLINE_CURVE_WITH_KNOTS('',3,(#38534,#38535,#38536,#38537,#38538,
#38539,#38540,#38541,#38542,#38543,#38544,#38545,#38546,#38547,#38548,#38549),
 .UNSPECIFIED.,.F.,.F.,(4,1,1,1,1,1,1,1,1,1,1,1,1,4),(34.5575191894886,
34.965028762934,35.4647078297171,35.9643868965001,36.4640659632831,36.9637450300661,
37.4634240968492,37.9631031636322,38.4627822304152,38.9624612971982,39.4621403639813,
39.9618194307643,40.4614984975473,40.8407044966681),.UNSPECIFIED.);
#873=B_SPLINE_CURVE_WITH_KNOTS('',3,(#38554,#38555,#38556,#38557,#38558,
#38559,#38560,#38561,#38562,#38563,#38564,#38565,#38566,#38567,#38568,#38569,
#38570),.UNSPECIFIED.,.F.,.F.,(4,1,1,1,1,1,1,1,1,1,1,1,1,1,4),(28.2743338823086,
28.4986569800851,28.9983360468681,29.4980151136512,29.9976941804342,30.4973732472172,
30.9970523140002,31.4967313807832,31.9964104475663,32.4960895143493,32.9957685811323,
33.4954476479153,33.9951267146984,34.4948057814814,34.5575191894882),
 .UNSPECIFIED.);
#874=B_SPLINE_CURVE_WITH_KNOTS('',3,(#38571,#38572,#38573,#38574,#38575,
#38576,#38577,#38578,#38579,#38580,#38581,#38582,#38583,#38584,#38585,#38586,
#38587),.UNSPECIFIED.,.F.,.F.,(4,1,1,1,1,1,1,1,1,1,1,1,1,1,4),(28.2743338823089,
28.4692008947547,28.9688799615378,29.4685590283208,29.9682380951038,30.4679171618868,
30.9675962286699,31.4672752954529,31.9669543622359,32.4666334290189,32.966312495802,
33.465991562585,33.965670629368,34.465349696151,34.5575191894886),
 .UNSPECIFIED.);
#875=B_SPLINE_CURVE_WITH_KNOTS('',3,(#38592,#38593,#38594,#38595,#38596,
#38597,#38598,#38599,#38600,#38601,#38602,#38603,#38604,#38605,#38606,#38607,
#38608),.UNSPECIFIED.,.F.,.F.,(4,1,1,1,1,1,1,1,1,1,1,1,1,1,4),(21.991148575129,
22.0028291119058,22.5025081786888,23.0021872454719,23.5018663122549,24.0015453790379,
24.5012244458209,25.0009035126039,25.500582579387,26.00026164617,26.499940712953,
26.999619779736,27.4992988465191,27.9989779133021,28.2743338823086),
 .UNSPECIFIED.);
#876=B_SPLINE_CURVE_WITH_KNOTS('',3,(#38609,#38610,#38611,#38612,#38613,
#38614,#38615,#38616,#38617,#38618,#38619,#38620,#38621,#38622,#38623,#38624),
 .UNSPECIFIED.,.F.,.F.,(4,1,1,1,1,1,1,1,1,1,1,1,1,4),(21.9911485751294,
22.4730520933585,22.9727311601415,23.4724102269245,23.9720892937075,24.4717683604905,
24.9714474272736,25.4711264940566,25.9708055608396,26.4704846276226,26.9701636944057,
27.4698427611887,27.9695218279717,28.2743338823089),.UNSPECIFIED.);
#877=B_SPLINE_CURVE_WITH_KNOTS('',3,(#38629,#38630,#38631,#38632,#38633,
#38634,#38635,#38636,#38637,#38638,#38639,#38640,#38641,#38642,#38643,#38644),
 .UNSPECIFIED.,.F.,.F.,(4,1,1,1,1,1,1,1,1,1,1,1,1,4),(15.7079632679495,
16.0066803105095,16.5063593772925,17.0060384440756,17.5057175108586,18.0053965776416,
18.5050756444246,19.0047547112077,19.5044337779907,20.0041128447737,20.5037919115567,
21.0034709783398,21.5031500451228,21.991148575129),.UNSPECIFIED.);
#878=B_SPLINE_CURVE_WITH_KNOTS('',3,(#38645,#38646,#38647,#38648,#38649,
#38650,#38651,#38652,#38653,#38654,#38655,#38656,#38657,#38658,#38659,#38660,
#38661),.UNSPECIFIED.,.F.,.F.,(4,1,1,1,1,1,1,1,1,1,1,1,1,1,4),(15.7079632679498,
15.9772242251791,16.4769032919622,16.9765823587452,17.4762614255282,17.9759404923112,
18.4756195590943,18.9752986258773,19.4749776926603,19.9746567594433,20.4743358262264,
20.9740148930094,21.4736939597924,21.9733730265754,21.9911485751294),
 .UNSPECIFIED.);
#879=B_SPLINE_CURVE_WITH_KNOTS('',3,(#38666,#38667,#38668,#38669,#38670,
#38671,#38672,#38673,#38674,#38675,#38676,#38677,#38678,#38679,#38680,#38681,
#38682,#38683,#38684,#38685,#38686,#38687,#38688,#38689,#38690,#38691,#38692,
#38693,#38694,#38695,#38696,#38697,#38698,#38699,#38700,#38701,#38702),
 .UNSPECIFIED.,.F.,.F.,(4,3,3,3,3,3,3,3,3,3,3,3,4),(0.,0.000373494560508806,
0.0620760815771024,0.112839239637108,0.153038169722591,0.175804963675793,
0.247183842626883,0.319084136954533,0.344742425233931,0.363606980156396,
0.439518700737557,0.51795432283266,0.534785019937482),.UNSPECIFIED.);
#880=B_SPLINE_CURVE_WITH_KNOTS('',3,(#38704,#38705,#38706,#38707,#38708,
#38709,#38710,#38711,#38712,#38713,#38714,#38715,#38716,#38717,#38718,#38719,
#38720,#38721,#38722,#38723,#38724,#38725,#38726,#38727,#38728,#38729,#38730,
#38731,#38732,#38733,#38734,#38735,#38736,#38737,#38738,#38739,#38740),
 .UNSPECIFIED.,.F.,.F.,(4,3,3,3,3,3,3,3,3,3,3,3,4),(0.,0.000511892384038064,
0.078754853834616,0.155070466132989,0.20164291816609,0.227017770490094,
0.290460834304131,0.352619921814331,0.383703668213755,0.403796492255862,
0.466621120797767,0.52704524650008,0.539097184344933),.UNSPECIFIED.);
#881=B_SPLINE_CURVE_WITH_KNOTS('',3,(#40740,#40741,#40742,#40743,#40744,
#40745,#40746,#40747,#40748,#40749,#40750,#40751,#40752,#40753,#40754,#40755,
#40756,#40757,#40758,#40759,#40760,#40761,#40762,#40763,#40764,#40765,#40766,
#40767,#40768,#40769,#40770,#40771,#40772,#40773,#40774,#40775,#40776,#40777,
#40778,#40779),.UNSPECIFIED.,.F.,.F.,(4,3,3,3,3,3,3,3,3,3,3,3,3,4),(-0.53478501993692,
-0.534277081309421,-0.456439695901019,-0.38064245929011,-0.348102919117109,
-0.328886681298388,-0.258595553176405,-0.246742105655551,-0.185056579241663,
-0.163339235199672,-0.143463957830519,-0.0808484674142256,-0.0206857924044652,
0.),.UNSPECIFIED.);
#882=B_SPLINE_CURVE_WITH_KNOTS('',3,(#40780,#40781,#40782,#40783,#40784,
#40785,#40786,#40787,#40788,#40789,#40790,#40791,#40792,#40793,#40794,#40795,
#40796,#40797,#40798,#40799,#40800,#40801,#40802,#40803,#40804),
 .UNSPECIFIED.,.F.,.F.,(4,3,3,3,3,3,3,3,4),(390.000549715688,390.249351157541,
390.749030224325,391.248709291108,391.748388357891,392.248067424674,392.747746491457,
393.24742555824,393.746279249921),.UNSPECIFIED.);
#883=B_SPLINE_CURVE_WITH_KNOTS('',3,(#40805,#40806,#40807,#40808,#40809,
#40810,#40811,#40812,#40813,#40814,#40815,#40816,#40817,#40818,#40819),
 .UNSPECIFIED.,.F.,.F.,(4,1,1,1,1,1,1,1,1,1,1,1,4),(9.98190079888485,10.4807544905659,
10.9804335573489,11.4801126241319,11.979791690915,12.479470757698,12.979149824481,
13.478828891264,13.9785079580471,14.4781870248301,14.9778660916131,15.4775451583961,
15.7079632679498),.UNSPECIFIED.);
#884=B_SPLINE_CURVE_WITH_KNOTS('',3,(#40821,#40822,#40823,#40824,#40825,
#40826,#40827,#40828,#40829,#40830,#40831),.UNSPECIFIED.,.F.,.F.,(4,1,1,
1,1,1,1,1,4),(12.0092477762453,12.5089268430284,13.0086059098114,13.5082849765944,
14.0079640433774,14.5076431101605,15.0073221769435,15.5070012437265,15.7079632679495),
 .UNSPECIFIED.);
#885=B_SPLINE_CURVE_WITH_KNOTS('',3,(#42825,#42826,#42827,#42828,#42829,
#42830,#42831,#42832,#42833,#42834,#42835,#42836,#42837,#42838,#42839,#42840,
#42841,#42842,#42843,#42844,#42845,#42846,#42847,#42848,#42849,#42850,#42851,
#42852,#42853,#42854,#42855,#42856,#42857,#42858,#42859,#42860,#42861,#42862,
#42863,#42864),.UNSPECIFIED.,.F.,.F.,(4,3,3,3,3,3,3,3,3,3,3,3,3,4),(-0.539097184344981,
-0.538720824057998,-0.476544551511477,-0.429912347101587,-0.401091234701428,
-0.381803774975435,-0.313681369269712,-0.290015733871917,-0.24230273417063,
-0.214804629165427,-0.192593514291413,-0.116696500404398,-0.0381316372362206,
0.),.UNSPECIFIED.);
#886=B_SPLINE_CURVE_WITH_KNOTS('',3,(#42865,#42866,#42867,#42868,#42869,
#42870,#42871,#42872,#42873,#42874),.UNSPECIFIED.,.F.,.F.,(4,3,3,4),(-394.746462758588,
-394.246783691805,-393.747104625022,-393.256204536838),.UNSPECIFIED.);
#1034=SHAPE_REPRESENTATION_RELATIONSHIP('SRR','None',#43851,#1094);
#1094=ADVANCED_BREP_SHAPE_REPRESENTATION('',(#1238),#43511);
#1169=STYLED_ITEM('',(#44209),#1238);
#1238=MANIFOLD_SOLID_BREP('Body1',#18612);
#1565=FACE_BOUND('',#4491,.T.);
#1566=FACE_BOUND('',#4503,.T.);
#1567=FACE_BOUND('',#4506,.T.);
#1568=FACE_BOUND('',#4509,.T.);
#2110=PLANE('',#21029);
#2111=PLANE('',#21034);
#2112=PLANE('',#21036);
#2113=PLANE('',#21037);
#2114=PLANE('',#21039);
#2115=PLANE('',#21040);
#2116=PLANE('',#21041);
#2117=PLANE('',#21046);
#2118=PLANE('',#21047);
#2119=PLANE('',#21052);
#2999=FACE_OUTER_BOUND('',#4364,.T.);
#3000=FACE_OUTER_BOUND('',#4365,.T.);
#3001=FACE_OUTER_BOUND('',#4366,.T.);
#3002=FACE_OUTER_BOUND('',#4367,.T.);
#3003=FACE_OUTER_BOUND('',#4368,.T.);
#3004=FACE_OUTER_BOUND('',#4369,.T.);
#3005=FACE_OUTER_BOUND('',#4370,.T.);
#3006=FACE_OUTER_BOUND('',#4371,.T.);
#3007=FACE_OUTER_BOUND('',#4372,.T.);
#3008=FACE_OUTER_BOUND('',#4373,.T.);
#3009=FACE_OUTER_BOUND('',#4374,.T.);
#3010=FACE_OUTER_BOUND('',#4375,.T.);
#3011=FACE_OUTER_BOUND('',#4376,.T.);
#3012=FACE_OUTER_BOUND('',#4377,.T.);
#3013=FACE_OUTER_BOUND('',#4378,.T.);
#3014=FACE_OUTER_BOUND('',#4379,.T.);
#3015=FACE_OUTER_BOUND('',#4380,.T.);
#3016=FACE_OUTER_BOUND('',#4381,.T.);
#3017=FACE_OUTER_BOUND('',#4382,.T.);
#3018=FACE_OUTER_BOUND('',#4383,.T.);
#3019=FACE_OUTER_BOUND('',#4384,.T.);
#3020=FACE_OUTER_BOUND('',#4385,.T.);
#3021=FACE_OUTER_BOUND('',#4386,.T.);
#3022=FACE_OUTER_BOUND('',#4387,.T.);
#3023=FACE_OUTER_BOUND('',#4388,.T.);
#3024=FACE_OUTER_BOUND('',#4389,.T.);
#3025=FACE_OUTER_BOUND('',#4390,.T.);
#3026=FACE_OUTER_BOUND('',#4391,.T.);
#3027=FACE_OUTER_BOUND('',#4392,.T.);
#3028=FACE_OUTER_BOUND('',#4393,.T.);
#3029=FACE_OUTER_BOUND('',#4394,.T.);
#3030=FACE_OUTER_BOUND('',#4395,.T.);
#3031=FACE_OUTER_BOUND('',#4396,.T.);
#3032=FACE_OUTER_BOUND('',#4397,.T.);
#3033=FACE_OUTER_BOUND('',#4398,.T.);
#3034=FACE_OUTER_BOUND('',#4399,.T.);
#3035=FACE_OUTER_BOUND('',#4400,.T.);
#3036=FACE_OUTER_BOUND('',#4401,.T.);
#3037=FACE_OUTER_BOUND('',#4402,.T.);
#3038=FACE_OUTER_BOUND('',#4403,.T.);
#3039=FACE_OUTER_BOUND('',#4404,.T.);
#3040=FACE_OUTER_BOUND('',#4405,.T.);
#3041=FACE_OUTER_BOUND('',#4406,.T.);
#3042=FACE_OUTER_BOUND('',#4407,.T.);
#3043=FACE_OUTER_BOUND('',#4408,.T.);
#3044=FACE_OUTER_BOUND('',#4409,.T.);
#3045=FACE_OUTER_BOUND('',#4410,.T.);
#3046=FACE_OUTER_BOUND('',#4411,.T.);
#3047=FACE_OUTER_BOUND('',#4412,.T.);
#3048=FACE_OUTER_BOUND('',#4413,.T.);
#3049=FACE_OUTER_BOUND('',#4414,.T.);
#3050=FACE_OUTER_BOUND('',#4415,.T.);
#3051=FACE_OUTER_BOUND('',#4416,.T.);
#3052=FACE_OUTER_BOUND('',#4417,.T.);
#3053=FACE_OUTER_BOUND('',#4418,.T.);
#3054=FACE_OUTER_BOUND('',#4419,.T.);
#3055=FACE_OUTER_BOUND('',#4420,.T.);
#3056=FACE_OUTER_BOUND('',#4421,.T.);
#3057=FACE_OUTER_BOUND('',#4422,.T.);
#3058=FACE_OUTER_BOUND('',#4423,.T.);
#3059=FACE_OUTER_BOUND('',#4424,.T.);
#3060=FACE_OUTER_BOUND('',#4425,.T.);
#3061=FACE_OUTER_BOUND('',#4426,.T.);
#3062=FACE_OUTER_BOUND('',#4427,.T.);
#3063=FACE_OUTER_BOUND('',#4428,.T.);
#3064=FACE_OUTER_BOUND('',#4429,.T.);
#3065=FACE_OUTER_BOUND('',#4430,.T.);
#3066=FACE_OUTER_BOUND('',#4431,.T.);
#3067=FACE_OUTER_BOUND('',#4432,.T.);
#3068=FACE_OUTER_BOUND('',#4433,.T.);
#3069=FACE_OUTER_BOUND('',#4434,.T.);
#3070=FACE_OUTER_BOUND('',#4435,.T.);
#3071=FACE_OUTER_BOUND('',#4436,.T.);
#3072=FACE_OUTER_BOUND('',#4437,.T.);
#3073=FACE_OUTER_BOUND('',#4438,.T.);
#3074=FACE_OUTER_BOUND('',#4439,.T.);
#3075=FACE_OUTER_BOUND('',#4440,.T.);
#3076=FACE_OUTER_BOUND('',#4441,.T.);
#3077=FACE_OUTER_BOUND('',#4442,.T.);
#3078=FACE_OUTER_BOUND('',#4443,.T.);
#3079=FACE_OUTER_BOUND('',#4444,.T.);
#3080=FACE_OUTER_BOUND('',#4445,.T.);
#3081=FACE_OUTER_BOUND('',#4446,.T.);
#3082=FACE_OUTER_BOUND('',#4447,.T.);
#3083=FACE_OUTER_BOUND('',#4448,.T.);
#3084=FACE_OUTER_BOUND('',#4449,.T.);
#3085=FACE_OUTER_BOUND('',#4450,.T.);
#3086=FACE_OUTER_BOUND('',#4451,.T.);
#3087=FACE_OUTER_BOUND('',#4452,.T.);
#3088=FACE_OUTER_BOUND('',#4453,.T.);
#3089=FACE_OUTER_BOUND('',#4454,.T.);
#3090=FACE_OUTER_BOUND('',#4455,.T.);
#3091=FACE_OUTER_BOUND('',#4456,.T.);
#3092=FACE_OUTER_BOUND('',#4457,.T.);
#3093=FACE_OUTER_BOUND('',#4458,.T.);
#3094=FACE_OUTER_BOUND('',#4459,.T.);
#3095=FACE_OUTER_BOUND('',#4460,.T.);
#3096=FACE_OUTER_BOUND('',#4461,.T.);
#3097=FACE_OUTER_BOUND('',#4462,.T.);
#3098=FACE_OUTER_BOUND('',#4463,.T.);
#3099=FACE_OUTER_BOUND('',#4464,.T.);
#3100=FACE_OUTER_BOUND('',#4465,.T.);
#3101=FACE_OUTER_BOUND('',#4466,.T.);
#3102=FACE_OUTER_BOUND('',#4467,.T.);
#3103=FACE_OUTER_BOUND('',#4468,.T.);
#3104=FACE_OUTER_BOUND('',#4469,.T.);
#3105=FACE_OUTER_BOUND('',#4470,.T.);
#3106=FACE_OUTER_BOUND('',#4471,.T.);
#3107=FACE_OUTER_BOUND('',#4472,.T.);
#3108=FACE_OUTER_BOUND('',#4473,.T.);
#3109=FACE_OUTER_BOUND('',#4474,.T.);
#3110=FACE_OUTER_BOUND('',#4475,.T.);
#3111=FACE_OUTER_BOUND('',#4476,.T.);
#3112=FACE_OUTER_BOUND('',#4477,.T.);
#3113=FACE_OUTER_BOUND('',#4478,.T.);
#3114=FACE_OUTER_BOUND('',#4479,.T.);
#3115=FACE_OUTER_BOUND('',#4480,.T.);
#3116=FACE_OUTER_BOUND('',#4481,.T.);
#3117=FACE_OUTER_BOUND('',#4482,.T.);
#3118=FACE_OUTER_BOUND('',#4483,.T.);
#3119=FACE_OUTER_BOUND('',#4484,.T.);
#3120=FACE_OUTER_BOUND('',#4485,.T.);
#3121=FACE_OUTER_BOUND('',#4486,.T.);
#3122=FACE_OUTER_BOUND('',#4487,.T.);
#3123=FACE_OUTER_BOUND('',#4488,.T.);
#3124=FACE_OUTER_BOUND('',#4489,.T.);
#3125=FACE_OUTER_BOUND('',#4490,.T.);
#3126=FACE_OUTER_BOUND('',#4492,.T.);
#3127=FACE_OUTER_BOUND('',#4493,.T.);
#3128=FACE_OUTER_BOUND('',#4494,.T.);
#3129=FACE_OUTER_BOUND('',#4495,.T.);
#3130=FACE_OUTER_BOUND('',#4496,.T.);
#3131=FACE_OUTER_BOUND('',#4497,.T.);
#3132=FACE_OUTER_BOUND('',#4498,.T.);
#3133=FACE_OUTER_BOUND('',#4499,.T.);
#3134=FACE_OUTER_BOUND('',#4500,.T.);
#3135=FACE_OUTER_BOUND('',#4501,.T.);
#3136=FACE_OUTER_BOUND('',#4502,.T.);
#3137=FACE_OUTER_BOUND('',#4504,.T.);
#3138=FACE_OUTER_BOUND('',#4505,.T.);
#3139=FACE_OUTER_BOUND('',#4507,.T.);
#3140=FACE_OUTER_BOUND('',#4508,.T.);
#3141=FACE_OUTER_BOUND('',#4510,.T.);
#4364=EDGE_LOOP('',(#15973,#15974,#15975,#15976));
#4365=EDGE_LOOP('',(#15977,#15978,#15979,#15980));
#4366=EDGE_LOOP('',(#15981,#15982,#15983,#15984));
#4367=EDGE_LOOP('',(#15985,#15986,#15987,#15988));
#4368=EDGE_LOOP('',(#15989,#15990,#15991,#15992));
#4369=EDGE_LOOP('',(#15993,#15994,#15995,#15996));
#4370=EDGE_LOOP('',(#15997,#15998,#15999,#16000));
#4371=EDGE_LOOP('',(#16001,#16002,#16003,#16004));
#4372=EDGE_LOOP('',(#16005,#16006,#16007,#16008));
#4373=EDGE_LOOP('',(#16009,#16010,#16011,#16012));
#4374=EDGE_LOOP('',(#16013,#16014,#16015,#16016));
#4375=EDGE_LOOP('',(#16017,#16018,#16019,#16020));
#4376=EDGE_LOOP('',(#16021,#16022,#16023,#16024));
#4377=EDGE_LOOP('',(#16025,#16026,#16027,#16028));
#4378=EDGE_LOOP('',(#16029,#16030,#16031,#16032));
#4379=EDGE_LOOP('',(#16033,#16034,#16035,#16036));
#4380=EDGE_LOOP('',(#16037,#16038,#16039,#16040));
#4381=EDGE_LOOP('',(#16041,#16042,#16043,#16044));
#4382=EDGE_LOOP('',(#16045,#16046,#16047,#16048));
#4383=EDGE_LOOP('',(#16049,#16050,#16051,#16052));
#4384=EDGE_LOOP('',(#16053,#16054,#16055,#16056));
#4385=EDGE_LOOP('',(#16057,#16058,#16059,#16060));
#4386=EDGE_LOOP('',(#16061,#16062,#16063,#16064));
#4387=EDGE_LOOP('',(#16065,#16066,#16067,#16068));
#4388=EDGE_LOOP('',(#16069,#16070,#16071,#16072));
#4389=EDGE_LOOP('',(#16073,#16074,#16075,#16076));
#4390=EDGE_LOOP('',(#16077,#16078,#16079,#16080));
#4391=EDGE_LOOP('',(#16081,#16082,#16083,#16084));
#4392=EDGE_LOOP('',(#16085,#16086,#16087,#16088));
#4393=EDGE_LOOP('',(#16089,#16090,#16091,#16092));
#4394=EDGE_LOOP('',(#16093,#16094,#16095,#16096));
#4395=EDGE_LOOP('',(#16097,#16098,#16099,#16100));
#4396=EDGE_LOOP('',(#16101,#16102,#16103,#16104));
#4397=EDGE_LOOP('',(#16105,#16106,#16107,#16108));
#4398=EDGE_LOOP('',(#16109,#16110,#16111,#16112));
#4399=EDGE_LOOP('',(#16113,#16114,#16115,#16116));
#4400=EDGE_LOOP('',(#16117,#16118,#16119,#16120));
#4401=EDGE_LOOP('',(#16121,#16122,#16123,#16124));
#4402=EDGE_LOOP('',(#16125,#16126,#16127,#16128));
#4403=EDGE_LOOP('',(#16129,#16130,#16131,#16132));
#4404=EDGE_LOOP('',(#16133,#16134,#16135,#16136));
#4405=EDGE_LOOP('',(#16137,#16138,#16139,#16140));
#4406=EDGE_LOOP('',(#16141,#16142,#16143,#16144));
#4407=EDGE_LOOP('',(#16145,#16146,#16147,#16148));
#4408=EDGE_LOOP('',(#16149,#16150,#16151,#16152));
#4409=EDGE_LOOP('',(#16153,#16154,#16155,#16156));
#4410=EDGE_LOOP('',(#16157,#16158,#16159,#16160));
#4411=EDGE_LOOP('',(#16161,#16162,#16163,#16164));
#4412=EDGE_LOOP('',(#16165,#16166,#16167,#16168));
#4413=EDGE_LOOP('',(#16169,#16170,#16171,#16172));
#4414=EDGE_LOOP('',(#16173,#16174,#16175,#16176));
#4415=EDGE_LOOP('',(#16177,#16178,#16179,#16180));
#4416=EDGE_LOOP('',(#16181,#16182,#16183,#16184));
#4417=EDGE_LOOP('',(#16185,#16186,#16187,#16188));
#4418=EDGE_LOOP('',(#16189,#16190,#16191,#16192));
#4419=EDGE_LOOP('',(#16193,#16194,#16195,#16196));
#4420=EDGE_LOOP('',(#16197,#16198,#16199,#16200));
#4421=EDGE_LOOP('',(#16201,#16202,#16203,#16204));
#4422=EDGE_LOOP('',(#16205,#16206,#16207,#16208));
#4423=EDGE_LOOP('',(#16209,#16210,#16211,#16212));
#4424=EDGE_LOOP('',(#16213,#16214,#16215,#16216));
#4425=EDGE_LOOP('',(#16217,#16218,#16219,#16220));
#4426=EDGE_LOOP('',(#16221,#16222,#16223,#16224));
#4427=EDGE_LOOP('',(#16225,#16226,#16227));
#4428=EDGE_LOOP('',(#16228,#16229,#16230,#16231,#16232));
#4429=EDGE_LOOP('',(#16233,#16234,#16235,#16236));
#4430=EDGE_LOOP('',(#16237,#16238,#16239,#16240));
#4431=EDGE_LOOP('',(#16241,#16242,#16243,#16244));
#4432=EDGE_LOOP('',(#16245,#16246,#16247,#16248));
#4433=EDGE_LOOP('',(#16249,#16250,#16251,#16252));
#4434=EDGE_LOOP('',(#16253,#16254,#16255,#16256));
#4435=EDGE_LOOP('',(#16257,#16258,#16259,#16260));
#4436=EDGE_LOOP('',(#16261,#16262,#16263,#16264));
#4437=EDGE_LOOP('',(#16265,#16266,#16267,#16268));
#4438=EDGE_LOOP('',(#16269,#16270,#16271,#16272));
#4439=EDGE_LOOP('',(#16273,#16274,#16275,#16276));
#4440=EDGE_LOOP('',(#16277,#16278,#16279,#16280));
#4441=EDGE_LOOP('',(#16281,#16282,#16283,#16284));
#4442=EDGE_LOOP('',(#16285,#16286,#16287,#16288));
#4443=EDGE_LOOP('',(#16289,#16290,#16291,#16292));
#4444=EDGE_LOOP('',(#16293,#16294,#16295,#16296));
#4445=EDGE_LOOP('',(#16297,#16298,#16299,#16300));
#4446=EDGE_LOOP('',(#16301,#16302,#16303,#16304));
#4447=EDGE_LOOP('',(#16305,#16306,#16307,#16308));
#4448=EDGE_LOOP('',(#16309,#16310,#16311,#16312));
#4449=EDGE_LOOP('',(#16313,#16314,#16315,#16316));
#4450=EDGE_LOOP('',(#16317,#16318,#16319,#16320));
#4451=EDGE_LOOP('',(#16321,#16322,#16323,#16324));
#4452=EDGE_LOOP('',(#16325,#16326,#16327,#16328));
#4453=EDGE_LOOP('',(#16329,#16330,#16331,#16332));
#4454=EDGE_LOOP('',(#16333,#16334,#16335,#16336));
#4455=EDGE_LOOP('',(#16337,#16338,#16339,#16340));
#4456=EDGE_LOOP('',(#16341,#16342,#16343,#16344));
#4457=EDGE_LOOP('',(#16345,#16346,#16347,#16348));
#4458=EDGE_LOOP('',(#16349,#16350,#16351,#16352));
#4459=EDGE_LOOP('',(#16353,#16354,#16355,#16356));
#4460=EDGE_LOOP('',(#16357,#16358,#16359,#16360));
#4461=EDGE_LOOP('',(#16361,#16362,#16363,#16364));
#4462=EDGE_LOOP('',(#16365,#16366,#16367,#16368));
#4463=EDGE_LOOP('',(#16369,#16370,#16371,#16372));
#4464=EDGE_LOOP('',(#16373,#16374,#16375,#16376));
#4465=EDGE_LOOP('',(#16377,#16378,#16379,#16380));
#4466=EDGE_LOOP('',(#16381,#16382,#16383,#16384));
#4467=EDGE_LOOP('',(#16385,#16386,#16387,#16388));
#4468=EDGE_LOOP('',(#16389,#16390,#16391,#16392));
#4469=EDGE_LOOP('',(#16393,#16394,#16395,#16396));
#4470=EDGE_LOOP('',(#16397,#16398,#16399,#16400));
#4471=EDGE_LOOP('',(#16401,#16402,#16403,#16404));
#4472=EDGE_LOOP('',(#16405,#16406,#16407,#16408));
#4473=EDGE_LOOP('',(#16409,#16410,#16411,#16412));
#4474=EDGE_LOOP('',(#16413,#16414,#16415,#16416));
#4475=EDGE_LOOP('',(#16417,#16418,#16419,#16420));
#4476=EDGE_LOOP('',(#16421,#16422,#16423,#16424));
#4477=EDGE_LOOP('',(#16425,#16426,#16427,#16428));
#4478=EDGE_LOOP('',(#16429,#16430,#16431,#16432));
#4479=EDGE_LOOP('',(#16433,#16434,#16435,#16436));
#4480=EDGE_LOOP('',(#16437,#16438,#16439,#16440));
#4481=EDGE_LOOP('',(#16441,#16442,#16443,#16444));
#4482=EDGE_LOOP('',(#16445,#16446,#16447,#16448));
#4483=EDGE_LOOP('',(#16449,#16450,#16451,#16452));
#4484=EDGE_LOOP('',(#16453,#16454,#16455,#16456));
#4485=EDGE_LOOP('',(#16457,#16458,#16459,#16460));
#4486=EDGE_LOOP('',(#16461,#16462,#16463,#16464));
#4487=EDGE_LOOP('',(#16465,#16466,#16467,#16468));
#4488=EDGE_LOOP('',(#16469,#16470,#16471,#16472));
#4489=EDGE_LOOP('',(#16473,#16474,#16475,#16476));
#4490=EDGE_LOOP('',(#16477));
#4491=EDGE_LOOP('',(#16478,#16479,#16480,#16481));
#4492=EDGE_LOOP('',(#16482,#16483,#16484,#16485));
#4493=EDGE_LOOP('',(#16486));
#4494=EDGE_LOOP('',(#16487,#16488,#16489,#16490,#16491,#16492,#16493,#16494,
#16495,#16496,#16497,#16498,#16499,#16500,#16501,#16502,#16503,#16504,#16505,
#16506,#16507,#16508,#16509,#16510,#16511,#16512,#16513,#16514,#16515,#16516,
#16517,#16518,#16519,#16520,#16521,#16522,#16523,#16524,#16525,#16526,#16527,
#16528,#16529,#16530,#16531,#16532,#16533,#16534,#16535,#16536,#16537,#16538,
#16539,#16540,#16541,#16542,#16543,#16544,#16545,#16546,#16547,#16548,#16549,
#16550,#16551,#16552,#16553,#16554,#16555,#16556,#16557,#16558,#16559,#16560,
#16561,#16562,#16563,#16564,#16565,#16566,#16567,#16568,#16569,#16570,#16571,
#16572,#16573,#16574,#16575,#16576,#16577,#16578,#16579,#16580,#16581,#16582,
#16583,#16584,#16585,#16586,#16587,#16588,#16589,#16590,#16591,#16592,#16593,
#16594,#16595,#16596,#16597,#16598,#16599,#16600,#16601,#16602,#16603,#16604,
#16605,#16606,#16607,#16608,#16609,#16610,#16611,#16612,#16613,#16614,#16615));
#4495=EDGE_LOOP('',(#16616,#16617,#16618,#16619));
#4496=EDGE_LOOP('',(#16620,#16621,#16622,#16623,#16624,#16625,#16626,#16627,
#16628,#16629,#16630,#16631,#16632,#16633,#16634,#16635,#16636,#16637,#16638,
#16639,#16640,#16641,#16642,#16643,#16644,#16645,#16646,#16647,#16648,#16649,
#16650,#16651,#16652,#16653,#16654,#16655,#16656,#16657,#16658,#16659,#16660,
#16661,#16662,#16663,#16664,#16665,#16666,#16667,#16668,#16669,#16670,#16671,
#16672,#16673,#16674,#16675,#16676,#16677,#16678,#16679,#16680,#16681,#16682,
#16683,#16684,#16685,#16686,#16687,#16688,#16689,#16690,#16691,#16692,#16693,
#16694,#16695,#16696,#16697,#16698,#16699,#16700,#16701,#16702,#16703,#16704,
#16705,#16706,#16707,#16708,#16709,#16710,#16711,#16712,#16713,#16714,#16715,
#16716,#16717,#16718,#16719,#16720,#16721,#16722,#16723,#16724,#16725,#16726,
#16727,#16728,#16729,#16730,#16731,#16732,#16733,#16734,#16735,#16736,#16737,
#16738,#16739,#16740,#16741,#16742,#16743,#16744,#16745,#16746,#16747,#16748,
#16749));
#4497=EDGE_LOOP('',(#16750,#16751,#16752,#16753));
#4498=EDGE_LOOP('',(#16754,#16755,#16756,#16757));
#4499=EDGE_LOOP('',(#16758,#16759,#16760,#16761));
#4500=EDGE_LOOP('',(#16762,#16763,#16764,#16765));
#4501=EDGE_LOOP('',(#16766,#16767,#16768,#16769));
#4502=EDGE_LOOP('',(#16770,#16771,#16772,#16773));
#4503=EDGE_LOOP('',(#16774,#16775,#16776,#16777));
#4504=EDGE_LOOP('',(#16778));
#4505=EDGE_LOOP('',(#16779));
#4506=EDGE_LOOP('',(#16780,#16781,#16782,#16783,#16784));
#4507=EDGE_LOOP('',(#16785,#16786,#16787,#16788));
#4508=EDGE_LOOP('',(#16789));
#4509=EDGE_LOOP('',(#16790));
#4510=EDGE_LOOP('',(#16791,#16792,#16793,#16794));
#5798=LINE('',#33262,#7230);
#5799=LINE('',#33292,#7231);
#5800=LINE('',#33379,#7232);
#5801=LINE('',#33469,#7233);
#5802=LINE('',#33556,#7234);
#5803=LINE('',#33643,#7235);
#5804=LINE('',#33730,#7236);
#5805=LINE('',#33817,#7237);
#5806=LINE('',#33904,#7238);
#5807=LINE('',#33976,#7239);
#5808=LINE('',#34027,#7240);
#5809=LINE('',#34075,#7241);
#5810=LINE('',#34123,#7242);
#5811=LINE('',#34174,#7243);
#5812=LINE('',#34225,#7244);
#5813=LINE('',#34273,#7245);
#5814=LINE('',#34324,#7246);
#5815=LINE('',#34375,#7247);
#5816=LINE('',#34423,#7248);
#5817=LINE('',#34471,#7249);
#5818=LINE('',#34522,#7250);
#5819=LINE('',#34573,#7251);
#5820=LINE('',#34621,#7252);
#5821=LINE('',#34672,#7253);
#5822=LINE('',#34723,#7254);
#5823=LINE('',#34771,#7255);
#5824=LINE('',#34819,#7256);
#5825=LINE('',#34870,#7257);
#5826=LINE('',#34921,#7258);
#5827=LINE('',#34969,#7259);
#5828=LINE('',#35020,#7260);
#5829=LINE('',#35071,#7261);
#5830=LINE('',#35119,#7262);
#5831=LINE('',#35167,#7263);
#5832=LINE('',#35218,#7264);
#5833=LINE('',#35269,#7265);
#5834=LINE('',#35317,#7266);
#5835=LINE('',#35368,#7267);
#5836=LINE('',#35419,#7268);
#5837=LINE('',#35467,#7269);
#5838=LINE('',#35515,#7270);
#5839=LINE('',#35566,#7271);
#5840=LINE('',#35617,#7272);
#5841=LINE('',#35665,#7273);
#5842=LINE('',#35716,#7274);
#5843=LINE('',#35767,#7275);
#5844=LINE('',#35815,#7276);
#5845=LINE('',#35863,#7277);
#5846=LINE('',#35914,#7278);
#5847=LINE('',#35965,#7279);
#5848=LINE('',#36013,#7280);
#5849=LINE('',#36064,#7281);
#5850=LINE('',#36115,#7282);
#5851=LINE('',#36163,#7283);
#5852=LINE('',#36211,#7284);
#5853=LINE('',#36262,#7285);
#5854=LINE('',#36328,#7286);
#5855=LINE('',#36418,#7287);
#5856=LINE('',#36505,#7288);
#5857=LINE('',#36592,#7289);
#5858=LINE('',#36679,#7290);
#5859=LINE('',#36766,#7291);
#5860=LINE('',#36853,#7292);
#5861=LINE('',#36943,#7293);
#5862=LINE('',#36953,#7294);
#5863=LINE('',#36989,#7295);
#5864=LINE('',#37027,#7296);
#5865=LINE('',#37063,#7297);
#5866=LINE('',#37101,#7298);
#5867=LINE('',#37137,#7299);
#5868=LINE('',#37175,#7300);
#5869=LINE('',#37212,#7301);
#5870=LINE('',#37247,#7302);
#5871=LINE('',#37274,#7303);
#5872=LINE('',#37298,#7304);
#5873=LINE('',#37322,#7305);
#5874=LINE('',#37346,#7306);
#5875=LINE('',#37372,#7307);
#5876=LINE('',#37396,#7308);
#5877=LINE('',#37420,#7309);
#5878=LINE('',#37446,#7310);
#5879=LINE('',#37470,#7311);
#5880=LINE('',#37494,#7312);
#5881=LINE('',#37518,#7313);
#5882=LINE('',#37544,#7314);
#5883=LINE('',#37568,#7315);
#5884=LINE('',#37592,#7316);
#5885=LINE('',#37618,#7317);
#5886=LINE('',#37642,#7318);
#5887=LINE('',#37666,#7319);
#5888=LINE('',#37690,#7320);
#5889=LINE('',#37716,#7321);
#5890=LINE('',#37740,#7322);
#5891=LINE('',#37764,#7323);
#5892=LINE('',#37790,#7324);
#5893=LINE('',#37814,#7325);
#5894=LINE('',#37838,#7326);
#5895=LINE('',#37862,#7327);
#5896=LINE('',#37888,#7328);
#5897=LINE('',#37912,#7329);
#5898=LINE('',#37936,#7330);
#5899=LINE('',#37962,#7331);
#5900=LINE('',#37986,#7332);
#5901=LINE('',#38010,#7333);
#5902=LINE('',#38034,#7334);
#5903=LINE('',#38060,#7335);
#5904=LINE('',#38084,#7336);
#5905=LINE('',#38108,#7337);
#5906=LINE('',#38134,#7338);
#5907=LINE('',#38158,#7339);
#5908=LINE('',#38182,#7340);
#5909=LINE('',#38206,#7341);
#5910=LINE('',#38232,#7342);
#5911=LINE('',#38256,#7343);
#5912=LINE('',#38280,#7344);
#5913=LINE('',#38306,#7345);
#5914=LINE('',#38330,#7346);
#5915=LINE('',#38354,#7347);
#5916=LINE('',#38379,#7348);
#5917=LINE('',#38406,#7349);
#5918=LINE('',#38443,#7350);
#5919=LINE('',#38479,#7351);
#5920=LINE('',#38517,#7352);
#5921=LINE('',#38553,#7353);
#5922=LINE('',#38591,#7354);
#5923=LINE('',#38628,#7355);
#5924=LINE('',#38744,#7356);
#5925=LINE('',#42878,#7357);
#5926=LINE('',#42880,#7358);
#5927=LINE('',#42882,#7359);
#5928=LINE('',#42883,#7360);
#5929=LINE('',#42888,#7361);
#5930=LINE('',#42889,#7362);
#5931=LINE('',#42892,#7363);
#5932=LINE('',#42893,#7364);
#5933=LINE('',#42896,#7365);
#5934=LINE('',#42897,#7366);
#5935=LINE('',#42904,#7367);
#5936=LINE('',#42914,#7368);
#7230=VECTOR('',#25622,0.6);
#7231=VECTOR('',#25627,0.6);
#7232=VECTOR('',#25630,0.6);
#7233=VECTOR('',#25633,0.6);
#7234=VECTOR('',#25636,0.6);
#7235=VECTOR('',#25639,0.6);
#7236=VECTOR('',#25642,0.6);
#7237=VECTOR('',#25645,0.6);
#7238=VECTOR('',#25648,0.6);
#7239=VECTOR('',#25651,0.6);
#7240=VECTOR('',#25654,0.6);
#7241=VECTOR('',#25657,0.6);
#7242=VECTOR('',#25660,0.6);
#7243=VECTOR('',#25663,0.6);
#7244=VECTOR('',#25666,0.6);
#7245=VECTOR('',#25669,0.6);
#7246=VECTOR('',#25672,0.6);
#7247=VECTOR('',#25675,0.6);
#7248=VECTOR('',#25678,0.6);
#7249=VECTOR('',#25681,0.6);
#7250=VECTOR('',#25684,0.6);
#7251=VECTOR('',#25687,0.6);
#7252=VECTOR('',#25690,0.6);
#7253=VECTOR('',#25693,0.6);
#7254=VECTOR('',#25696,0.6);
#7255=VECTOR('',#25699,0.6);
#7256=VECTOR('',#25702,0.6);
#7257=VECTOR('',#25705,0.6);
#7258=VECTOR('',#25708,0.6);
#7259=VECTOR('',#25711,0.6);
#7260=VECTOR('',#25714,0.6);
#7261=VECTOR('',#25717,0.6);
#7262=VECTOR('',#25720,0.6);
#7263=VECTOR('',#25723,0.6);
#7264=VECTOR('',#25726,0.6);
#7265=VECTOR('',#25729,0.6);
#7266=VECTOR('',#25732,0.6);
#7267=VECTOR('',#25735,0.6);
#7268=VECTOR('',#25738,0.6);
#7269=VECTOR('',#25741,0.6);
#7270=VECTOR('',#25744,0.6);
#7271=VECTOR('',#25747,0.6);
#7272=VECTOR('',#25750,0.6);
#7273=VECTOR('',#25753,0.6);
#7274=VECTOR('',#25756,0.6);
#7275=VECTOR('',#25759,0.6);
#7276=VECTOR('',#25762,0.6);
#7277=VECTOR('',#25765,0.6);
#7278=VECTOR('',#25768,0.6);
#7279=VECTOR('',#25771,0.6);
#7280=VECTOR('',#25774,0.6);
#7281=VECTOR('',#25777,0.6);
#7282=VECTOR('',#25780,0.6);
#7283=VECTOR('',#25783,0.6);
#7284=VECTOR('',#25786,0.6);
#7285=VECTOR('',#25789,0.6);
#7286=VECTOR('',#25792,0.6);
#7287=VECTOR('',#25795,0.6);
#7288=VECTOR('',#25798,0.6);
#7289=VECTOR('',#25801,0.6);
#7290=VECTOR('',#25804,0.6);
#7291=VECTOR('',#25807,0.6);
#7292=VECTOR('',#25810,0.6);
#7293=VECTOR('',#25813,0.415875);
#7294=VECTOR('',#25818,0.415875);
#7295=VECTOR('',#25823,0.415875);
#7296=VECTOR('',#25826,0.415875);
#7297=VECTOR('',#25829,0.415875);
#7298=VECTOR('',#25832,0.415875);
#7299=VECTOR('',#25835,0.415875);
#7300=VECTOR('',#25838,0.415875);
#7301=VECTOR('',#25841,0.415875);
#7302=VECTOR('',#25844,0.415875);
#7303=VECTOR('',#25847,0.415875);
#7304=VECTOR('',#25850,0.415875);
#7305=VECTOR('',#25853,0.415875);
#7306=VECTOR('',#25856,0.415875);
#7307=VECTOR('',#25859,0.415875);
#7308=VECTOR('',#25862,0.415875);
#7309=VECTOR('',#25865,0.415875);
#7310=VECTOR('',#25868,0.415875);
#7311=VECTOR('',#25871,0.415875);
#7312=VECTOR('',#25874,0.415875);
#7313=VECTOR('',#25877,0.415875);
#7314=VECTOR('',#25880,0.415875);
#7315=VECTOR('',#25883,0.415875);
#7316=VECTOR('',#25886,0.415875);
#7317=VECTOR('',#25889,0.415875);
#7318=VECTOR('',#25892,0.415875);
#7319=VECTOR('',#25895,0.415875);
#7320=VECTOR('',#25898,0.415875);
#7321=VECTOR('',#25901,0.415875);
#7322=VECTOR('',#25904,0.415875);
#7323=VECTOR('',#25907,0.415875);
#7324=VECTOR('',#25910,0.415875);
#7325=VECTOR('',#25913,0.415875);
#7326=VECTOR('',#25916,0.415875);
#7327=VECTOR('',#25919,0.415875);
#7328=VECTOR('',#25922,0.415875);
#7329=VECTOR('',#25925,0.415875);
#7330=VECTOR('',#25928,0.415875);
#7331=VECTOR('',#25931,0.415875);
#7332=VECTOR('',#25934,0.415875);
#7333=VECTOR('',#25937,0.415875);
#7334=VECTOR('',#25940,0.415875);
#7335=VECTOR('',#25943,0.415875);
#7336=VECTOR('',#25946,0.415875);
#7337=VECTOR('',#25949,0.415875);
#7338=VECTOR('',#25952,0.415875);
#7339=VECTOR('',#25955,0.415875);
#7340=VECTOR('',#25958,0.415875);
#7341=VECTOR('',#25961,0.415875);
#7342=VECTOR('',#25964,0.415875);
#7343=VECTOR('',#25967,0.415875);
#7344=VECTOR('',#25970,0.415875);
#7345=VECTOR('',#25973,0.415875);
#7346=VECTOR('',#25976,0.415875);
#7347=VECTOR('',#25979,0.415875);
#7348=VECTOR('',#25982,0.415875);
#7349=VECTOR('',#25985,0.415875);
#7350=VECTOR('',#25988,0.415875);
#7351=VECTOR('',#25991,0.415875);
#7352=VECTOR('',#25994,0.415875);
#7353=VECTOR('',#25997,0.415875);
#7354=VECTOR('',#26000,0.415875);
#7355=VECTOR('',#26003,0.415875);
#7356=VECTOR('',#26012,0.6);
#7357=VECTOR('',#26021,1.);
#7358=VECTOR('',#26022,1.);
#7359=VECTOR('',#26023,1.);
#7360=VECTOR('',#26024,1.);
#7361=VECTOR('',#26029,1.);
#7362=VECTOR('',#26030,1.);
#7363=VECTOR('',#26033,1.);
#7364=VECTOR('',#26034,1.);
#7365=VECTOR('',#26037,1.);
#7366=VECTOR('',#26038,1.);
#7367=VECTOR('',#26047,1.);
#7368=VECTOR('',#26062,1.35);
#8079=CIRCLE('',#20901,0.5941);
#8080=CIRCLE('',#20965,0.415875);
#8081=CIRCLE('',#20967,0.415875);
#8082=CIRCLE('',#21030,0.6);
#8083=CIRCLE('',#21031,0.415875);
#8084=CIRCLE('',#21033,0.6);
#8085=CIRCLE('',#21038,1.);
#8086=CIRCLE('',#21042,1.);
#8087=CIRCLE('',#21044,1.);
#8088=CIRCLE('',#21045,1.);
#8089=CIRCLE('',#21048,1.35);
#8090=CIRCLE('',#21049,0.5941);
#8091=CIRCLE('',#21051,1.35);
#9397=VERTEX_POINT('',#33260);
#9398=VERTEX_POINT('',#33261);
#9399=VERTEX_POINT('',#33263);
#9400=VERTEX_POINT('',#33283);
#9401=VERTEX_POINT('',#33290);
#9402=VERTEX_POINT('',#33291);
#9403=VERTEX_POINT('',#33377);
#9404=VERTEX_POINT('',#33378);
#9405=VERTEX_POINT('',#33467);
#9406=VERTEX_POINT('',#33468);
#9407=VERTEX_POINT('',#33554);
#9408=VERTEX_POINT('',#33555);
#9409=VERTEX_POINT('',#33641);
#9410=VERTEX_POINT('',#33642);
#9411=VERTEX_POINT('',#33728);
#9412=VERTEX_POINT('',#33729);
#9413=VERTEX_POINT('',#33815);
#9414=VERTEX_POINT('',#33816);
#9415=VERTEX_POINT('',#33902);
#9416=VERTEX_POINT('',#33903);
#9417=VERTEX_POINT('',#33974);
#9418=VERTEX_POINT('',#33975);
#9419=VERTEX_POINT('',#34025);
#9420=VERTEX_POINT('',#34026);
#9421=VERTEX_POINT('',#34073);
#9422=VERTEX_POINT('',#34074);
#9423=VERTEX_POINT('',#34121);
#9424=VERTEX_POINT('',#34122);
#9425=VERTEX_POINT('',#34172);
#9426=VERTEX_POINT('',#34173);
#9427=VERTEX_POINT('',#34223);
#9428=VERTEX_POINT('',#34224);
#9429=VERTEX_POINT('',#34271);
#9430=VERTEX_POINT('',#34272);
#9431=VERTEX_POINT('',#34322);
#9432=VERTEX_POINT('',#34323);
#9433=VERTEX_POINT('',#34373);
#9434=VERTEX_POINT('',#34374);
#9435=VERTEX_POINT('',#34421);
#9436=VERTEX_POINT('',#34422);
#9437=VERTEX_POINT('',#34469);
#9438=VERTEX_POINT('',#34470);
#9439=VERTEX_POINT('',#34520);
#9440=VERTEX_POINT('',#34521);
#9441=VERTEX_POINT('',#34571);
#9442=VERTEX_POINT('',#34572);
#9443=VERTEX_POINT('',#34619);
#9444=VERTEX_POINT('',#34620);
#9445=VERTEX_POINT('',#34670);
#9446=VERTEX_POINT('',#34671);
#9447=VERTEX_POINT('',#34721);
#9448=VERTEX_POINT('',#34722);
#9449=VERTEX_POINT('',#34769);
#9450=VERTEX_POINT('',#34770);
#9451=VERTEX_POINT('',#34817);
#9452=VERTEX_POINT('',#34818);
#9453=VERTEX_POINT('',#34868);
#9454=VERTEX_POINT('',#34869);
#9455=VERTEX_POINT('',#34919);
#9456=VERTEX_POINT('',#34920);
#9457=VERTEX_POINT('',#34967);
#9458=VERTEX_POINT('',#34968);
#9459=VERTEX_POINT('',#35018);
#9460=VERTEX_POINT('',#35019);
#9461=VERTEX_POINT('',#35069);
#9462=VERTEX_POINT('',#35070);
#9463=VERTEX_POINT('',#35117);
#9464=VERTEX_POINT('',#35118);
#9465=VERTEX_POINT('',#35165);
#9466=VERTEX_POINT('',#35166);
#9467=VERTEX_POINT('',#35216);
#9468=VERTEX_POINT('',#35217);
#9469=VERTEX_POINT('',#35267);
#9470=VERTEX_POINT('',#35268);
#9471=VERTEX_POINT('',#35315);
#9472=VERTEX_POINT('',#35316);
#9473=VERTEX_POINT('',#35366);
#9474=VERTEX_POINT('',#35367);
#9475=VERTEX_POINT('',#35417);
#9476=VERTEX_POINT('',#35418);
#9477=VERTEX_POINT('',#35465);
#9478=VERTEX_POINT('',#35466);
#9479=VERTEX_POINT('',#35513);
#9480=VERTEX_POINT('',#35514);
#9481=VERTEX_POINT('',#35564);
#9482=VERTEX_POINT('',#35565);
#9483=VERTEX_POINT('',#35615);
#9484=VERTEX_POINT('',#35616);
#9485=VERTEX_POINT('',#35663);
#9486=VERTEX_POINT('',#35664);
#9487=VERTEX_POINT('',#35714);
#9488=VERTEX_POINT('',#35715);
#9489=VERTEX_POINT('',#35765);
#9490=VERTEX_POINT('',#35766);
#9491=VERTEX_POINT('',#35813);
#9492=VERTEX_POINT('',#35814);
#9493=VERTEX_POINT('',#35861);
#9494=VERTEX_POINT('',#35862);
#9495=VERTEX_POINT('',#35912);
#9496=VERTEX_POINT('',#35913);
#9497=VERTEX_POINT('',#35963);
#9498=VERTEX_POINT('',#35964);
#9499=VERTEX_POINT('',#36011);
#9500=VERTEX_POINT('',#36012);
#9501=VERTEX_POINT('',#36062);
#9502=VERTEX_POINT('',#36063);
#9503=VERTEX_POINT('',#36113);
#9504=VERTEX_POINT('',#36114);
#9505=VERTEX_POINT('',#36161);
#9506=VERTEX_POINT('',#36162);
#9507=VERTEX_POINT('',#36209);
#9508=VERTEX_POINT('',#36210);
#9509=VERTEX_POINT('',#36260);
#9510=VERTEX_POINT('',#36261);
#9511=VERTEX_POINT('',#36326);
#9512=VERTEX_POINT('',#36327);
#9513=VERTEX_POINT('',#36416);
#9514=VERTEX_POINT('',#36417);
#9515=VERTEX_POINT('',#36503);
#9516=VERTEX_POINT('',#36504);
#9517=VERTEX_POINT('',#36590);
#9518=VERTEX_POINT('',#36591);
#9519=VERTEX_POINT('',#36677);
#9520=VERTEX_POINT('',#36678);
#9521=VERTEX_POINT('',#36764);
#9522=VERTEX_POINT('',#36765);
#9523=VERTEX_POINT('',#36851);
#9524=VERTEX_POINT('',#36852);
#9525=VERTEX_POINT('',#36941);
#9526=VERTEX_POINT('',#36942);
#9527=VERTEX_POINT('',#36944);
#9528=VERTEX_POINT('',#36951);
#9529=VERTEX_POINT('',#36952);
#9530=VERTEX_POINT('',#36971);
#9531=VERTEX_POINT('',#36987);
#9532=VERTEX_POINT('',#36988);
#9533=VERTEX_POINT('',#37025);
#9534=VERTEX_POINT('',#37026);
#9535=VERTEX_POINT('',#37061);
#9536=VERTEX_POINT('',#37062);
#9537=VERTEX_POINT('',#37099);
#9538=VERTEX_POINT('',#37100);
#9539=VERTEX_POINT('',#37135);
#9540=VERTEX_POINT('',#37136);
#9541=VERTEX_POINT('',#37173);
#9542=VERTEX_POINT('',#37174);
#9543=VERTEX_POINT('',#37210);
#9544=VERTEX_POINT('',#37211);
#9545=VERTEX_POINT('',#37245);
#9546=VERTEX_POINT('',#37246);
#9547=VERTEX_POINT('',#37272);
#9548=VERTEX_POINT('',#37273);
#9549=VERTEX_POINT('',#37296);
#9550=VERTEX_POINT('',#37297);
#9551=VERTEX_POINT('',#37320);
#9552=VERTEX_POINT('',#37321);
#9553=VERTEX_POINT('',#37344);
#9554=VERTEX_POINT('',#37345);
#9555=VERTEX_POINT('',#37370);
#9556=VERTEX_POINT('',#37371);
#9557=VERTEX_POINT('',#37394);
#9558=VERTEX_POINT('',#37395);
#9559=VERTEX_POINT('',#37418);
#9560=VERTEX_POINT('',#37419);
#9561=VERTEX_POINT('',#37444);
#9562=VERTEX_POINT('',#37445);
#9563=VERTEX_POINT('',#37468);
#9564=VERTEX_POINT('',#37469);
#9565=VERTEX_POINT('',#37492);
#9566=VERTEX_POINT('',#37493);
#9567=VERTEX_POINT('',#37516);
#9568=VERTEX_POINT('',#37517);
#9569=VERTEX_POINT('',#37542);
#9570=VERTEX_POINT('',#37543);
#9571=VERTEX_POINT('',#37566);
#9572=VERTEX_POINT('',#37567);
#9573=VERTEX_POINT('',#37590);
#9574=VERTEX_POINT('',#37591);
#9575=VERTEX_POINT('',#37616);
#9576=VERTEX_POINT('',#37617);
#9577=VERTEX_POINT('',#37640);
#9578=VERTEX_POINT('',#37641);
#9579=VERTEX_POINT('',#37664);
#9580=VERTEX_POINT('',#37665);
#9581=VERTEX_POINT('',#37688);
#9582=VERTEX_POINT('',#37689);
#9583=VERTEX_POINT('',#37714);
#9584=VERTEX_POINT('',#37715);
#9585=VERTEX_POINT('',#37738);
#9586=VERTEX_POINT('',#37739);
#9587=VERTEX_POINT('',#37762);
#9588=VERTEX_POINT('',#37763);
#9589=VERTEX_POINT('',#37788);
#9590=VERTEX_POINT('',#37789);
#9591=VERTEX_POINT('',#37812);
#9592=VERTEX_POINT('',#37813);
#9593=VERTEX_POINT('',#37836);
#9594=VERTEX_POINT('',#37837);
#9595=VERTEX_POINT('',#37860);
#9596=VERTEX_POINT('',#37861);
#9597=VERTEX_POINT('',#37886);
#9598=VERTEX_POINT('',#37887);
#9599=VERTEX_POINT('',#37910);
#9600=VERTEX_POINT('',#37911);
#9601=VERTEX_POINT('',#37934);
#9602=VERTEX_POINT('',#37935);
#9603=VERTEX_POINT('',#37960);
#9604=VERTEX_POINT('',#37961);
#9605=VERTEX_POINT('',#37984);
#9606=VERTEX_POINT('',#37985);
#9607=VERTEX_POINT('',#38008);
#9608=VERTEX_POINT('',#38009);
#9609=VERTEX_POINT('',#38032);
#9610=VERTEX_POINT('',#38033);
#9611=VERTEX_POINT('',#38058);
#9612=VERTEX_POINT('',#38059);
#9613=VERTEX_POINT('',#38082);
#9614=VERTEX_POINT('',#38083);
#9615=VERTEX_POINT('',#38106);
#9616=VERTEX_POINT('',#38107);
#9617=VERTEX_POINT('',#38132);
#9618=VERTEX_POINT('',#38133);
#9619=VERTEX_POINT('',#38156);
#9620=VERTEX_POINT('',#38157);
#9621=VERTEX_POINT('',#38180);
#9622=VERTEX_POINT('',#38181);
#9623=VERTEX_POINT('',#38204);
#9624=VERTEX_POINT('',#38205);
#9625=VERTEX_POINT('',#38230);
#9626=VERTEX_POINT('',#38231);
#9627=VERTEX_POINT('',#38254);
#9628=VERTEX_POINT('',#38255);
#9629=VERTEX_POINT('',#38278);
#9630=VERTEX_POINT('',#38279);
#9631=VERTEX_POINT('',#38304);
#9632=VERTEX_POINT('',#38305);
#9633=VERTEX_POINT('',#38328);
#9634=VERTEX_POINT('',#38329);
#9635=VERTEX_POINT('',#38352);
#9636=VERTEX_POINT('',#38353);
#9637=VERTEX_POINT('',#38377);
#9638=VERTEX_POINT('',#38378);
#9639=VERTEX_POINT('',#38404);
#9640=VERTEX_POINT('',#38405);
#9641=VERTEX_POINT('',#38441);
#9642=VERTEX_POINT('',#38442);
#9643=VERTEX_POINT('',#38477);
#9644=VERTEX_POINT('',#38478);
#9645=VERTEX_POINT('',#38515);
#9646=VERTEX_POINT('',#38516);
#9647=VERTEX_POINT('',#38551);
#9648=VERTEX_POINT('',#38552);
#9649=VERTEX_POINT('',#38589);
#9650=VERTEX_POINT('',#38590);
#9651=VERTEX_POINT('',#38626);
#9652=VERTEX_POINT('',#38627);
#9653=VERTEX_POINT('',#38663);
#9654=VERTEX_POINT('',#38665);
#9655=VERTEX_POINT('',#38703);
#9656=VERTEX_POINT('',#38743);
#9657=VERTEX_POINT('',#40739);
#9658=VERTEX_POINT('',#42824);
#9659=VERTEX_POINT('',#42876);
#9660=VERTEX_POINT('',#42877);
#9661=VERTEX_POINT('',#42879);
#9662=VERTEX_POINT('',#42881);
#9663=VERTEX_POINT('',#42885);
#9664=VERTEX_POINT('',#42887);
#9665=VERTEX_POINT('',#42891);
#9666=VERTEX_POINT('',#42895);
#9667=VERTEX_POINT('',#42901);
#9668=VERTEX_POINT('',#42903);
#9669=VERTEX_POINT('',#42908);
#9670=VERTEX_POINT('',#42912);
#11651=EDGE_CURVE('',#9397,#9398,#5798,.T.);
#11652=EDGE_CURVE('',#9397,#9399,#628,.T.);
#11653=EDGE_CURVE('',#9399,#9400,#8079,.F.);
#11654=EDGE_CURVE('',#9400,#9398,#629,.T.);
#11655=EDGE_CURVE('',#9401,#9402,#5799,.T.);
#11656=EDGE_CURVE('',#9401,#9397,#630,.T.);
#11657=EDGE_CURVE('',#9398,#9402,#631,.T.);
#11658=EDGE_CURVE('',#9403,#9404,#5800,.T.);
#11659=EDGE_CURVE('',#9403,#9401,#632,.T.);
#11660=EDGE_CURVE('',#9402,#9404,#633,.T.);
#11661=EDGE_CURVE('',#9405,#9406,#5801,.T.);
#11662=EDGE_CURVE('',#9405,#9403,#634,.T.);
#11663=EDGE_CURVE('',#9404,#9406,#635,.T.);
#11664=EDGE_CURVE('',#9407,#9408,#5802,.T.);
#11665=EDGE_CURVE('',#9407,#9405,#636,.T.);
#11666=EDGE_CURVE('',#9406,#9408,#637,.T.);
#11667=EDGE_CURVE('',#9409,#9410,#5803,.T.);
#11668=EDGE_CURVE('',#9409,#9407,#638,.T.);
#11669=EDGE_CURVE('',#9408,#9410,#639,.T.);
#11670=EDGE_CURVE('',#9411,#9412,#5804,.T.);
#11671=EDGE_CURVE('',#9411,#9409,#640,.T.);
#11672=EDGE_CURVE('',#9410,#9412,#641,.T.);
#11673=EDGE_CURVE('',#9413,#9414,#5805,.T.);
#11674=EDGE_CURVE('',#9413,#9411,#642,.T.);
#11675=EDGE_CURVE('',#9412,#9414,#643,.T.);
#11676=EDGE_CURVE('',#9415,#9416,#5806,.T.);
#11677=EDGE_CURVE('',#9415,#9413,#644,.T.);
#11678=EDGE_CURVE('',#9414,#9416,#645,.T.);
#11679=EDGE_CURVE('',#9417,#9418,#5807,.T.);
#11680=EDGE_CURVE('',#9417,#9415,#646,.T.);
#11681=EDGE_CURVE('',#9416,#9418,#647,.T.);
#11682=EDGE_CURVE('',#9419,#9420,#5808,.T.);
#11683=EDGE_CURVE('',#9419,#9417,#648,.T.);
#11684=EDGE_CURVE('',#9418,#9420,#649,.T.);
#11685=EDGE_CURVE('',#9421,#9422,#5809,.T.);
#11686=EDGE_CURVE('',#9421,#9419,#650,.T.);
#11687=EDGE_CURVE('',#9420,#9422,#651,.T.);
#11688=EDGE_CURVE('',#9423,#9424,#5810,.T.);
#11689=EDGE_CURVE('',#9423,#9421,#652,.T.);
#11690=EDGE_CURVE('',#9422,#9424,#653,.T.);
#11691=EDGE_CURVE('',#9425,#9426,#5811,.T.);
#11692=EDGE_CURVE('',#9425,#9423,#654,.T.);
#11693=EDGE_CURVE('',#9424,#9426,#655,.T.);
#11694=EDGE_CURVE('',#9427,#9428,#5812,.T.);
#11695=EDGE_CURVE('',#9427,#9425,#656,.T.);
#11696=EDGE_CURVE('',#9426,#9428,#657,.T.);
#11697=EDGE_CURVE('',#9429,#9430,#5813,.T.);
#11698=EDGE_CURVE('',#9429,#9427,#658,.T.);
#11699=EDGE_CURVE('',#9428,#9430,#659,.T.);
#11700=EDGE_CURVE('',#9431,#9432,#5814,.T.);
#11701=EDGE_CURVE('',#9431,#9429,#660,.T.);
#11702=EDGE_CURVE('',#9430,#9432,#661,.T.);
#11703=EDGE_CURVE('',#9433,#9434,#5815,.T.);
#11704=EDGE_CURVE('',#9433,#9431,#662,.T.);
#11705=EDGE_CURVE('',#9432,#9434,#663,.T.);
#11706=EDGE_CURVE('',#9435,#9436,#5816,.T.);
#11707=EDGE_CURVE('',#9435,#9433,#664,.T.);
#11708=EDGE_CURVE('',#9434,#9436,#665,.T.);
#11709=EDGE_CURVE('',#9437,#9438,#5817,.T.);
#11710=EDGE_CURVE('',#9437,#9435,#666,.T.);
#11711=EDGE_CURVE('',#9436,#9438,#667,.T.);
#11712=EDGE_CURVE('',#9439,#9440,#5818,.T.);
#11713=EDGE_CURVE('',#9439,#9437,#668,.T.);
#11714=EDGE_CURVE('',#9438,#9440,#669,.T.);
#11715=EDGE_CURVE('',#9441,#9442,#5819,.T.);
#11716=EDGE_CURVE('',#9441,#9439,#670,.T.);
#11717=EDGE_CURVE('',#9440,#9442,#671,.T.);
#11718=EDGE_CURVE('',#9443,#9444,#5820,.T.);
#11719=EDGE_CURVE('',#9443,#9441,#672,.T.);
#11720=EDGE_CURVE('',#9442,#9444,#673,.T.);
#11721=EDGE_CURVE('',#9445,#9446,#5821,.T.);
#11722=EDGE_CURVE('',#9445,#9443,#674,.T.);
#11723=EDGE_CURVE('',#9444,#9446,#675,.T.);
#11724=EDGE_CURVE('',#9447,#9448,#5822,.T.);
#11725=EDGE_CURVE('',#9447,#9445,#676,.T.);
#11726=EDGE_CURVE('',#9446,#9448,#677,.T.);
#11727=EDGE_CURVE('',#9449,#9450,#5823,.T.);
#11728=EDGE_CURVE('',#9449,#9447,#678,.T.);
#11729=EDGE_CURVE('',#9448,#9450,#679,.T.);
#11730=EDGE_CURVE('',#9451,#9452,#5824,.T.);
#11731=EDGE_CURVE('',#9451,#9449,#680,.T.);
#11732=EDGE_CURVE('',#9450,#9452,#681,.T.);
#11733=EDGE_CURVE('',#9453,#9454,#5825,.T.);
#11734=EDGE_CURVE('',#9453,#9451,#682,.T.);
#11735=EDGE_CURVE('',#9452,#9454,#683,.T.);
#11736=EDGE_CURVE('',#9455,#9456,#5826,.T.);
#11737=EDGE_CURVE('',#9455,#9453,#684,.T.);
#11738=EDGE_CURVE('',#9454,#9456,#685,.T.);
#11739=EDGE_CURVE('',#9457,#9458,#5827,.T.);
#11740=EDGE_CURVE('',#9457,#9455,#686,.T.);
#11741=EDGE_CURVE('',#9456,#9458,#687,.T.);
#11742=EDGE_CURVE('',#9459,#9460,#5828,.T.);
#11743=EDGE_CURVE('',#9459,#9457,#688,.T.);
#11744=EDGE_CURVE('',#9458,#9460,#689,.T.);
#11745=EDGE_CURVE('',#9461,#9462,#5829,.T.);
#11746=EDGE_CURVE('',#9461,#9459,#690,.T.);
#11747=EDGE_CURVE('',#9460,#9462,#691,.T.);
#11748=EDGE_CURVE('',#9463,#9464,#5830,.T.);
#11749=EDGE_CURVE('',#9463,#9461,#692,.T.);
#11750=EDGE_CURVE('',#9462,#9464,#693,.T.);
#11751=EDGE_CURVE('',#9465,#9466,#5831,.T.);
#11752=EDGE_CURVE('',#9465,#9463,#694,.T.);
#11753=EDGE_CURVE('',#9464,#9466,#695,.T.);
#11754=EDGE_CURVE('',#9467,#9468,#5832,.T.);
#11755=EDGE_CURVE('',#9467,#9465,#696,.T.);
#11756=EDGE_CURVE('',#9466,#9468,#697,.T.);
#11757=EDGE_CURVE('',#9469,#9470,#5833,.T.);
#11758=EDGE_CURVE('',#9469,#9467,#698,.T.);
#11759=EDGE_CURVE('',#9468,#9470,#699,.T.);
#11760=EDGE_CURVE('',#9471,#9472,#5834,.T.);
#11761=EDGE_CURVE('',#9471,#9469,#700,.T.);
#11762=EDGE_CURVE('',#9470,#9472,#701,.T.);
#11763=EDGE_CURVE('',#9473,#9474,#5835,.T.);
#11764=EDGE_CURVE('',#9473,#9471,#702,.T.);
#11765=EDGE_CURVE('',#9472,#9474,#703,.T.);
#11766=EDGE_CURVE('',#9475,#9476,#5836,.T.);
#11767=EDGE_CURVE('',#9475,#9473,#704,.T.);
#11768=EDGE_CURVE('',#9474,#9476,#705,.T.);
#11769=EDGE_CURVE('',#9477,#9478,#5837,.T.);
#11770=EDGE_CURVE('',#9477,#9475,#706,.T.);
#11771=EDGE_CURVE('',#9476,#9478,#707,.T.);
#11772=EDGE_CURVE('',#9479,#9480,#5838,.T.);
#11773=EDGE_CURVE('',#9479,#9477,#708,.T.);
#11774=EDGE_CURVE('',#9478,#9480,#709,.T.);
#11775=EDGE_CURVE('',#9481,#9482,#5839,.T.);
#11776=EDGE_CURVE('',#9481,#9479,#710,.T.);
#11777=EDGE_CURVE('',#9480,#9482,#711,.T.);
#11778=EDGE_CURVE('',#9483,#9484,#5840,.T.);
#11779=EDGE_CURVE('',#9483,#9481,#712,.T.);
#11780=EDGE_CURVE('',#9482,#9484,#713,.T.);
#11781=EDGE_CURVE('',#9485,#9486,#5841,.T.);
#11782=EDGE_CURVE('',#9485,#9483,#714,.T.);
#11783=EDGE_CURVE('',#9484,#9486,#715,.T.);
#11784=EDGE_CURVE('',#9487,#9488,#5842,.T.);
#11785=EDGE_CURVE('',#9487,#9485,#716,.T.);
#11786=EDGE_CURVE('',#9486,#9488,#717,.T.);
#11787=EDGE_CURVE('',#9489,#9490,#5843,.T.);
#11788=EDGE_CURVE('',#9489,#9487,#718,.T.);
#11789=EDGE_CURVE('',#9488,#9490,#719,.T.);
#11790=EDGE_CURVE('',#9491,#9492,#5844,.T.);
#11791=EDGE_CURVE('',#9491,#9489,#720,.T.);
#11792=EDGE_CURVE('',#9490,#9492,#721,.T.);
#11793=EDGE_CURVE('',#9493,#9494,#5845,.T.);
#11794=EDGE_CURVE('',#9493,#9491,#722,.T.);
#11795=EDGE_CURVE('',#9492,#9494,#723,.T.);
#11796=EDGE_CURVE('',#9495,#9496,#5846,.T.);
#11797=EDGE_CURVE('',#9495,#9493,#724,.T.);
#11798=EDGE_CURVE('',#9494,#9496,#725,.T.);
#11799=EDGE_CURVE('',#9497,#9498,#5847,.T.);
#11800=EDGE_CURVE('',#9497,#9495,#726,.T.);
#11801=EDGE_CURVE('',#9496,#9498,#727,.T.);
#11802=EDGE_CURVE('',#9499,#9500,#5848,.T.);
#11803=EDGE_CURVE('',#9499,#9497,#728,.T.);
#11804=EDGE_CURVE('',#9498,#9500,#729,.T.);
#11805=EDGE_CURVE('',#9501,#9502,#5849,.T.);
#11806=EDGE_CURVE('',#9501,#9499,#730,.T.);
#11807=EDGE_CURVE('',#9500,#9502,#731,.T.);
#11808=EDGE_CURVE('',#9503,#9504,#5850,.T.);
#11809=EDGE_CURVE('',#9503,#9501,#732,.T.);
#11810=EDGE_CURVE('',#9502,#9504,#733,.T.);
#11811=EDGE_CURVE('',#9505,#9506,#5851,.T.);
#11812=EDGE_CURVE('',#9505,#9503,#734,.T.);
#11813=EDGE_CURVE('',#9504,#9506,#735,.T.);
#11814=EDGE_CURVE('',#9507,#9508,#5852,.T.);
#11815=EDGE_CURVE('',#9507,#9505,#736,.T.);
#11816=EDGE_CURVE('',#9506,#9508,#737,.T.);
#11817=EDGE_CURVE('',#9509,#9510,#5853,.T.);
#11818=EDGE_CURVE('',#9509,#9507,#738,.T.);
#11819=EDGE_CURVE('',#9508,#9510,#739,.T.);
#11820=EDGE_CURVE('',#9511,#9512,#5854,.T.);
#11821=EDGE_CURVE('',#9511,#9509,#740,.T.);
#11822=EDGE_CURVE('',#9510,#9512,#741,.T.);
#11823=EDGE_CURVE('',#9513,#9514,#5855,.T.);
#11824=EDGE_CURVE('',#9513,#9511,#742,.T.);
#11825=EDGE_CURVE('',#9512,#9514,#743,.T.);
#11826=EDGE_CURVE('',#9515,#9516,#5856,.T.);
#11827=EDGE_CURVE('',#9515,#9513,#744,.T.);
#11828=EDGE_CURVE('',#9514,#9516,#745,.T.);
#11829=EDGE_CURVE('',#9517,#9518,#5857,.T.);
#11830=EDGE_CURVE('',#9517,#9515,#746,.T.);
#11831=EDGE_CURVE('',#9516,#9518,#747,.T.);
#11832=EDGE_CURVE('',#9519,#9520,#5858,.T.);
#11833=EDGE_CURVE('',#9519,#9517,#748,.T.);
#11834=EDGE_CURVE('',#9518,#9520,#749,.T.);
#11835=EDGE_CURVE('',#9521,#9522,#5859,.T.);
#11836=EDGE_CURVE('',#9521,#9519,#750,.T.);
#11837=EDGE_CURVE('',#9520,#9522,#751,.T.);
#11838=EDGE_CURVE('',#9523,#9524,#5860,.T.);
#11839=EDGE_CURVE('',#9523,#9521,#752,.T.);
#11840=EDGE_CURVE('',#9522,#9524,#753,.T.);
#11841=EDGE_CURVE('',#9525,#9526,#5861,.T.);
#11842=EDGE_CURVE('',#9525,#9527,#754,.T.);
#11843=EDGE_CURVE('',#9526,#9527,#8080,.T.);
#11844=EDGE_CURVE('',#9528,#9529,#5862,.T.);
#11845=EDGE_CURVE('',#9528,#9525,#755,.T.);
#11846=EDGE_CURVE('',#9530,#9526,#8081,.T.);
#11847=EDGE_CURVE('',#9529,#9530,#756,.T.);
#11848=EDGE_CURVE('',#9531,#9532,#5863,.T.);
#11849=EDGE_CURVE('',#9531,#9528,#757,.T.);
#11850=EDGE_CURVE('',#9532,#9529,#758,.T.);
#11851=EDGE_CURVE('',#9533,#9534,#5864,.T.);
#11852=EDGE_CURVE('',#9533,#9531,#759,.T.);
#11853=EDGE_CURVE('',#9534,#9532,#760,.T.);
#11854=EDGE_CURVE('',#9535,#9536,#5865,.T.);
#11855=EDGE_CURVE('',#9535,#9533,#761,.T.);
#11856=EDGE_CURVE('',#9536,#9534,#762,.T.);
#11857=EDGE_CURVE('',#9537,#9538,#5866,.T.);
#11858=EDGE_CURVE('',#9537,#9535,#763,.T.);
#11859=EDGE_CURVE('',#9538,#9536,#764,.T.);
#11860=EDGE_CURVE('',#9539,#9540,#5867,.T.);
#11861=EDGE_CURVE('',#9539,#9537,#765,.T.);
#11862=EDGE_CURVE('',#9540,#9538,#766,.T.);
#11863=EDGE_CURVE('',#9541,#9542,#5868,.T.);
#11864=EDGE_CURVE('',#9541,#9539,#767,.T.);
#11865=EDGE_CURVE('',#9542,#9540,#768,.T.);
#11866=EDGE_CURVE('',#9543,#9544,#5869,.T.);
#11867=EDGE_CURVE('',#9543,#9541,#769,.T.);
#11868=EDGE_CURVE('',#9544,#9542,#770,.T.);
#11869=EDGE_CURVE('',#9545,#9546,#5870,.T.);
#11870=EDGE_CURVE('',#9545,#9543,#771,.T.);
#11871=EDGE_CURVE('',#9546,#9544,#772,.T.);
#11872=EDGE_CURVE('',#9547,#9548,#5871,.T.);
#11873=EDGE_CURVE('',#9547,#9545,#773,.T.);
#11874=EDGE_CURVE('',#9548,#9546,#774,.T.);
#11875=EDGE_CURVE('',#9549,#9550,#5872,.T.);
#11876=EDGE_CURVE('',#9549,#9547,#775,.T.);
#11877=EDGE_CURVE('',#9550,#9548,#776,.T.);
#11878=EDGE_CURVE('',#9551,#9552,#5873,.T.);
#11879=EDGE_CURVE('',#9551,#9549,#777,.T.);
#11880=EDGE_CURVE('',#9552,#9550,#778,.T.);
#11881=EDGE_CURVE('',#9553,#9554,#5874,.T.);
#11882=EDGE_CURVE('',#9553,#9551,#779,.T.);
#11883=EDGE_CURVE('',#9554,#9552,#780,.T.);
#11884=EDGE_CURVE('',#9555,#9556,#5875,.T.);
#11885=EDGE_CURVE('',#9555,#9553,#781,.T.);
#11886=EDGE_CURVE('',#9556,#9554,#782,.T.);
#11887=EDGE_CURVE('',#9557,#9558,#5876,.T.);
#11888=EDGE_CURVE('',#9557,#9555,#783,.T.);
#11889=EDGE_CURVE('',#9558,#9556,#784,.T.);
#11890=EDGE_CURVE('',#9559,#9560,#5877,.T.);
#11891=EDGE_CURVE('',#9559,#9557,#785,.T.);
#11892=EDGE_CURVE('',#9560,#9558,#786,.T.);
#11893=EDGE_CURVE('',#9561,#9562,#5878,.T.);
#11894=EDGE_CURVE('',#9561,#9559,#787,.T.);
#11895=EDGE_CURVE('',#9562,#9560,#788,.T.);
#11896=EDGE_CURVE('',#9563,#9564,#5879,.T.);
#11897=EDGE_CURVE('',#9563,#9561,#789,.T.);
#11898=EDGE_CURVE('',#9564,#9562,#790,.T.);
#11899=EDGE_CURVE('',#9565,#9566,#5880,.T.);
#11900=EDGE_CURVE('',#9565,#9563,#791,.T.);
#11901=EDGE_CURVE('',#9566,#9564,#792,.T.);
#11902=EDGE_CURVE('',#9567,#9568,#5881,.T.);
#11903=EDGE_CURVE('',#9567,#9565,#793,.T.);
#11904=EDGE_CURVE('',#9568,#9566,#794,.T.);
#11905=EDGE_CURVE('',#9569,#9570,#5882,.T.);
#11906=EDGE_CURVE('',#9569,#9567,#795,.T.);
#11907=EDGE_CURVE('',#9570,#9568,#796,.T.);
#11908=EDGE_CURVE('',#9571,#9572,#5883,.T.);
#11909=EDGE_CURVE('',#9571,#9569,#797,.T.);
#11910=EDGE_CURVE('',#9572,#9570,#798,.T.);
#11911=EDGE_CURVE('',#9573,#9574,#5884,.T.);
#11912=EDGE_CURVE('',#9573,#9571,#799,.T.);
#11913=EDGE_CURVE('',#9574,#9572,#800,.T.);
#11914=EDGE_CURVE('',#9575,#9576,#5885,.T.);
#11915=EDGE_CURVE('',#9575,#9573,#801,.T.);
#11916=EDGE_CURVE('',#9576,#9574,#802,.T.);
#11917=EDGE_CURVE('',#9577,#9578,#5886,.T.);
#11918=EDGE_CURVE('',#9577,#9575,#803,.T.);
#11919=EDGE_CURVE('',#9578,#9576,#804,.T.);
#11920=EDGE_CURVE('',#9579,#9580,#5887,.T.);
#11921=EDGE_CURVE('',#9579,#9577,#805,.T.);
#11922=EDGE_CURVE('',#9580,#9578,#806,.T.);
#11923=EDGE_CURVE('',#9581,#9582,#5888,.T.);
#11924=EDGE_CURVE('',#9581,#9579,#807,.T.);
#11925=EDGE_CURVE('',#9582,#9580,#808,.T.);
#11926=EDGE_CURVE('',#9583,#9584,#5889,.T.);
#11927=EDGE_CURVE('',#9583,#9581,#809,.T.);
#11928=EDGE_CURVE('',#9584,#9582,#810,.T.);
#11929=EDGE_CURVE('',#9585,#9586,#5890,.T.);
#11930=EDGE_CURVE('',#9585,#9583,#811,.T.);
#11931=EDGE_CURVE('',#9586,#9584,#812,.T.);
#11932=EDGE_CURVE('',#9587,#9588,#5891,.T.);
#11933=EDGE_CURVE('',#9587,#9585,#813,.T.);
#11934=EDGE_CURVE('',#9588,#9586,#814,.T.);
#11935=EDGE_CURVE('',#9589,#9590,#5892,.T.);
#11936=EDGE_CURVE('',#9589,#9587,#815,.T.);
#11937=EDGE_CURVE('',#9590,#9588,#816,.T.);
#11938=EDGE_CURVE('',#9591,#9592,#5893,.T.);
#11939=EDGE_CURVE('',#9591,#9589,#817,.T.);
#11940=EDGE_CURVE('',#9592,#9590,#818,.T.);
#11941=EDGE_CURVE('',#9593,#9594,#5894,.T.);
#11942=EDGE_CURVE('',#9593,#9591,#819,.T.);
#11943=EDGE_CURVE('',#9594,#9592,#820,.T.);
#11944=EDGE_CURVE('',#9595,#9596,#5895,.T.);
#11945=EDGE_CURVE('',#9595,#9593,#821,.T.);
#11946=EDGE_CURVE('',#9596,#9594,#822,.T.);
#11947=EDGE_CURVE('',#9597,#9598,#5896,.T.);
#11948=EDGE_CURVE('',#9597,#9595,#823,.T.);
#11949=EDGE_CURVE('',#9598,#9596,#824,.T.);
#11950=EDGE_CURVE('',#9599,#9600,#5897,.T.);
#11951=EDGE_CURVE('',#9599,#9597,#825,.T.);
#11952=EDGE_CURVE('',#9600,#9598,#826,.T.);
#11953=EDGE_CURVE('',#9601,#9602,#5898,.T.);
#11954=EDGE_CURVE('',#9601,#9599,#827,.T.);
#11955=EDGE_CURVE('',#9602,#9600,#828,.T.);
#11956=EDGE_CURVE('',#9603,#9604,#5899,.T.);
#11957=EDGE_CURVE('',#9603,#9601,#829,.T.);
#11958=EDGE_CURVE('',#9604,#9602,#830,.T.);
#11959=EDGE_CURVE('',#9605,#9606,#5900,.T.);
#11960=EDGE_CURVE('',#9605,#9603,#831,.T.);
#11961=EDGE_CURVE('',#9606,#9604,#832,.T.);
#11962=EDGE_CURVE('',#9607,#9608,#5901,.T.);
#11963=EDGE_CURVE('',#9607,#9605,#833,.T.);
#11964=EDGE_CURVE('',#9608,#9606,#834,.T.);
#11965=EDGE_CURVE('',#9609,#9610,#5902,.T.);
#11966=EDGE_CURVE('',#9609,#9607,#835,.T.);
#11967=EDGE_CURVE('',#9610,#9608,#836,.T.);
#11968=EDGE_CURVE('',#9611,#9612,#5903,.T.);
#11969=EDGE_CURVE('',#9611,#9609,#837,.T.);
#11970=EDGE_CURVE('',#9612,#9610,#838,.T.);
#11971=EDGE_CURVE('',#9613,#9614,#5904,.T.);
#11972=EDGE_CURVE('',#9613,#9611,#839,.T.);
#11973=EDGE_CURVE('',#9614,#9612,#840,.T.);
#11974=EDGE_CURVE('',#9615,#9616,#5905,.T.);
#11975=EDGE_CURVE('',#9615,#9613,#841,.T.);
#11976=EDGE_CURVE('',#9616,#9614,#842,.T.);
#11977=EDGE_CURVE('',#9617,#9618,#5906,.T.);
#11978=EDGE_CURVE('',#9617,#9615,#843,.T.);
#11979=EDGE_CURVE('',#9618,#9616,#844,.T.);
#11980=EDGE_CURVE('',#9619,#9620,#5907,.T.);
#11981=EDGE_CURVE('',#9619,#9617,#845,.T.);
#11982=EDGE_CURVE('',#9620,#9618,#846,.T.);
#11983=EDGE_CURVE('',#9621,#9622,#5908,.T.);
#11984=EDGE_CURVE('',#9621,#9619,#847,.T.);
#11985=EDGE_CURVE('',#9622,#9620,#848,.T.);
#11986=EDGE_CURVE('',#9623,#9624,#5909,.T.);
#11987=EDGE_CURVE('',#9623,#9621,#849,.T.);
#11988=EDGE_CURVE('',#9624,#9622,#850,.T.);
#11989=EDGE_CURVE('',#9625,#9626,#5910,.T.);
#11990=EDGE_CURVE('',#9625,#9623,#851,.T.);
#11991=EDGE_CURVE('',#9626,#9624,#852,.T.);
#11992=EDGE_CURVE('',#9627,#9628,#5911,.T.);
#11993=EDGE_CURVE('',#9627,#9625,#853,.T.);
#11994=EDGE_CURVE('',#9628,#9626,#854,.T.);
#11995=EDGE_CURVE('',#9629,#9630,#5912,.T.);
#11996=EDGE_CURVE('',#9629,#9627,#855,.T.);
#11997=EDGE_CURVE('',#9630,#9628,#856,.T.);
#11998=EDGE_CURVE('',#9631,#9632,#5913,.T.);
#11999=EDGE_CURVE('',#9631,#9629,#857,.T.);
#12000=EDGE_CURVE('',#9632,#9630,#858,.T.);
#12001=EDGE_CURVE('',#9633,#9634,#5914,.T.);
#12002=EDGE_CURVE('',#9633,#9631,#859,.T.);
#12003=EDGE_CURVE('',#9634,#9632,#860,.T.);
#12004=EDGE_CURVE('',#9635,#9636,#5915,.T.);
#12005=EDGE_CURVE('',#9635,#9633,#861,.T.);
#12006=EDGE_CURVE('',#9636,#9634,#862,.T.);
#12007=EDGE_CURVE('',#9637,#9638,#5916,.T.);
#12008=EDGE_CURVE('',#9637,#9635,#863,.T.);
#12009=EDGE_CURVE('',#9638,#9636,#864,.T.);
#12010=EDGE_CURVE('',#9639,#9640,#5917,.T.);
#12011=EDGE_CURVE('',#9639,#9637,#865,.T.);
#12012=EDGE_CURVE('',#9640,#9638,#866,.T.);
#12013=EDGE_CURVE('',#9641,#9642,#5918,.T.);
#12014=EDGE_CURVE('',#9641,#9639,#867,.T.);
#12015=EDGE_CURVE('',#9642,#9640,#868,.T.);
#12016=EDGE_CURVE('',#9643,#9644,#5919,.T.);
#12017=EDGE_CURVE('',#9643,#9641,#869,.T.);
#12018=EDGE_CURVE('',#9644,#9642,#870,.T.);
#12019=EDGE_CURVE('',#9645,#9646,#5920,.T.);
#12020=EDGE_CURVE('',#9645,#9643,#871,.T.);
#12021=EDGE_CURVE('',#9646,#9644,#872,.T.);
#12022=EDGE_CURVE('',#9647,#9648,#5921,.T.);
#12023=EDGE_CURVE('',#9647,#9645,#873,.T.);
#12024=EDGE_CURVE('',#9648,#9646,#874,.T.);
#12025=EDGE_CURVE('',#9649,#9650,#5922,.T.);
#12026=EDGE_CURVE('',#9649,#9647,#875,.T.);
#12027=EDGE_CURVE('',#9650,#9648,#876,.T.);
#12028=EDGE_CURVE('',#9651,#9652,#5923,.T.);
#12029=EDGE_CURVE('',#9651,#9649,#877,.T.);
#12030=EDGE_CURVE('',#9652,#9650,#878,.T.);
#12031=EDGE_CURVE('',#9653,#9653,#8082,.T.);
#12032=EDGE_CURVE('',#9654,#9400,#879,.T.);
#12033=EDGE_CURVE('',#9399,#9655,#880,.T.);
#12034=EDGE_CURVE('',#9655,#9654,#8083,.T.);
#12035=EDGE_CURVE('',#9653,#9656,#5924,.T.);
#12036=EDGE_CURVE('',#9656,#9656,#8084,.T.);
#12037=EDGE_CURVE('',#9657,#9530,#881,.T.);
#12038=EDGE_CURVE('',#9524,#9657,#882,.T.);
#12039=EDGE_CURVE('',#9654,#9652,#883,.T.);
#12040=EDGE_CURVE('',#9655,#9651,#884,.T.);
#12041=EDGE_CURVE('',#9527,#9658,#885,.T.);
#12042=EDGE_CURVE('',#9658,#9523,#886,.T.);
#12043=EDGE_CURVE('',#9659,#9660,#5925,.T.);
#12044=EDGE_CURVE('',#9659,#9661,#5926,.T.);
#12045=EDGE_CURVE('',#9662,#9661,#5927,.T.);
#12046=EDGE_CURVE('',#9660,#9662,#5928,.T.);
#12047=EDGE_CURVE('',#9660,#9663,#8085,.T.);
#12048=EDGE_CURVE('',#9662,#9664,#5929,.T.);
#12049=EDGE_CURVE('',#9664,#9663,#5930,.T.);
#12050=EDGE_CURVE('',#9661,#9665,#5931,.T.);
#12051=EDGE_CURVE('',#9664,#9665,#5932,.T.);
#12052=EDGE_CURVE('',#9663,#9666,#5933,.T.);
#12053=EDGE_CURVE('',#9665,#9666,#5934,.T.);
#12054=EDGE_CURVE('',#9666,#9659,#8086,.T.);
#12055=EDGE_CURVE('',#9667,#9667,#8087,.T.);
#12056=EDGE_CURVE('',#9667,#9668,#5935,.T.);
#12057=EDGE_CURVE('',#9668,#9668,#8088,.T.);
#12058=EDGE_CURVE('',#9669,#9669,#8089,.T.);
#12059=EDGE_CURVE('',#9658,#9657,#8090,.F.);
#12060=EDGE_CURVE('',#9670,#9670,#8091,.T.);
#12061=EDGE_CURVE('',#9670,#9669,#5936,.T.);
#15973=ORIENTED_EDGE('',*,*,#11651,.F.);
#15974=ORIENTED_EDGE('',*,*,#11652,.T.);
#15975=ORIENTED_EDGE('',*,*,#11653,.T.);
#15976=ORIENTED_EDGE('',*,*,#11654,.T.);
#15977=ORIENTED_EDGE('',*,*,#11655,.F.);
#15978=ORIENTED_EDGE('',*,*,#11656,.T.);
#15979=ORIENTED_EDGE('',*,*,#11651,.T.);
#15980=ORIENTED_EDGE('',*,*,#11657,.T.);
#15981=ORIENTED_EDGE('',*,*,#11658,.F.);
#15982=ORIENTED_EDGE('',*,*,#11659,.T.);
#15983=ORIENTED_EDGE('',*,*,#11655,.T.);
#15984=ORIENTED_EDGE('',*,*,#11660,.T.);
#15985=ORIENTED_EDGE('',*,*,#11661,.F.);
#15986=ORIENTED_EDGE('',*,*,#11662,.T.);
#15987=ORIENTED_EDGE('',*,*,#11658,.T.);
#15988=ORIENTED_EDGE('',*,*,#11663,.T.);
#15989=ORIENTED_EDGE('',*,*,#11664,.F.);
#15990=ORIENTED_EDGE('',*,*,#11665,.T.);
#15991=ORIENTED_EDGE('',*,*,#11661,.T.);
#15992=ORIENTED_EDGE('',*,*,#11666,.T.);
#15993=ORIENTED_EDGE('',*,*,#11667,.F.);
#15994=ORIENTED_EDGE('',*,*,#11668,.T.);
#15995=ORIENTED_EDGE('',*,*,#11664,.T.);
#15996=ORIENTED_EDGE('',*,*,#11669,.T.);
#15997=ORIENTED_EDGE('',*,*,#11670,.F.);
#15998=ORIENTED_EDGE('',*,*,#11671,.T.);
#15999=ORIENTED_EDGE('',*,*,#11667,.T.);
#16000=ORIENTED_EDGE('',*,*,#11672,.T.);
#16001=ORIENTED_EDGE('',*,*,#11673,.F.);
#16002=ORIENTED_EDGE('',*,*,#11674,.T.);
#16003=ORIENTED_EDGE('',*,*,#11670,.T.);
#16004=ORIENTED_EDGE('',*,*,#11675,.T.);
#16005=ORIENTED_EDGE('',*,*,#11676,.F.);
#16006=ORIENTED_EDGE('',*,*,#11677,.T.);
#16007=ORIENTED_EDGE('',*,*,#11673,.T.);
#16008=ORIENTED_EDGE('',*,*,#11678,.T.);
#16009=ORIENTED_EDGE('',*,*,#11679,.F.);
#16010=ORIENTED_EDGE('',*,*,#11680,.T.);
#16011=ORIENTED_EDGE('',*,*,#11676,.T.);
#16012=ORIENTED_EDGE('',*,*,#11681,.T.);
#16013=ORIENTED_EDGE('',*,*,#11682,.F.);
#16014=ORIENTED_EDGE('',*,*,#11683,.T.);
#16015=ORIENTED_EDGE('',*,*,#11679,.T.);
#16016=ORIENTED_EDGE('',*,*,#11684,.T.);
#16017=ORIENTED_EDGE('',*,*,#11685,.F.);
#16018=ORIENTED_EDGE('',*,*,#11686,.T.);
#16019=ORIENTED_EDGE('',*,*,#11682,.T.);
#16020=ORIENTED_EDGE('',*,*,#11687,.T.);
#16021=ORIENTED_EDGE('',*,*,#11688,.F.);
#16022=ORIENTED_EDGE('',*,*,#11689,.T.);
#16023=ORIENTED_EDGE('',*,*,#11685,.T.);
#16024=ORIENTED_EDGE('',*,*,#11690,.T.);
#16025=ORIENTED_EDGE('',*,*,#11691,.F.);
#16026=ORIENTED_EDGE('',*,*,#11692,.T.);
#16027=ORIENTED_EDGE('',*,*,#11688,.T.);
#16028=ORIENTED_EDGE('',*,*,#11693,.T.);
#16029=ORIENTED_EDGE('',*,*,#11694,.F.);
#16030=ORIENTED_EDGE('',*,*,#11695,.T.);
#16031=ORIENTED_EDGE('',*,*,#11691,.T.);
#16032=ORIENTED_EDGE('',*,*,#11696,.T.);
#16033=ORIENTED_EDGE('',*,*,#11697,.F.);
#16034=ORIENTED_EDGE('',*,*,#11698,.T.);
#16035=ORIENTED_EDGE('',*,*,#11694,.T.);
#16036=ORIENTED_EDGE('',*,*,#11699,.T.);
#16037=ORIENTED_EDGE('',*,*,#11700,.F.);
#16038=ORIENTED_EDGE('',*,*,#11701,.T.);
#16039=ORIENTED_EDGE('',*,*,#11697,.T.);
#16040=ORIENTED_EDGE('',*,*,#11702,.T.);
#16041=ORIENTED_EDGE('',*,*,#11703,.F.);
#16042=ORIENTED_EDGE('',*,*,#11704,.T.);
#16043=ORIENTED_EDGE('',*,*,#11700,.T.);
#16044=ORIENTED_EDGE('',*,*,#11705,.T.);
#16045=ORIENTED_EDGE('',*,*,#11706,.F.);
#16046=ORIENTED_EDGE('',*,*,#11707,.T.);
#16047=ORIENTED_EDGE('',*,*,#11703,.T.);
#16048=ORIENTED_EDGE('',*,*,#11708,.T.);
#16049=ORIENTED_EDGE('',*,*,#11709,.F.);
#16050=ORIENTED_EDGE('',*,*,#11710,.T.);
#16051=ORIENTED_EDGE('',*,*,#11706,.T.);
#16052=ORIENTED_EDGE('',*,*,#11711,.T.);
#16053=ORIENTED_EDGE('',*,*,#11712,.F.);
#16054=ORIENTED_EDGE('',*,*,#11713,.T.);
#16055=ORIENTED_EDGE('',*,*,#11709,.T.);
#16056=ORIENTED_EDGE('',*,*,#11714,.T.);
#16057=ORIENTED_EDGE('',*,*,#11715,.F.);
#16058=ORIENTED_EDGE('',*,*,#11716,.T.);
#16059=ORIENTED_EDGE('',*,*,#11712,.T.);
#16060=ORIENTED_EDGE('',*,*,#11717,.T.);
#16061=ORIENTED_EDGE('',*,*,#11718,.F.);
#16062=ORIENTED_EDGE('',*,*,#11719,.T.);
#16063=ORIENTED_EDGE('',*,*,#11715,.T.);
#16064=ORIENTED_EDGE('',*,*,#11720,.T.);
#16065=ORIENTED_EDGE('',*,*,#11721,.F.);
#16066=ORIENTED_EDGE('',*,*,#11722,.T.);
#16067=ORIENTED_EDGE('',*,*,#11718,.T.);
#16068=ORIENTED_EDGE('',*,*,#11723,.T.);
#16069=ORIENTED_EDGE('',*,*,#11724,.F.);
#16070=ORIENTED_EDGE('',*,*,#11725,.T.);
#16071=ORIENTED_EDGE('',*,*,#11721,.T.);
#16072=ORIENTED_EDGE('',*,*,#11726,.T.);
#16073=ORIENTED_EDGE('',*,*,#11727,.F.);
#16074=ORIENTED_EDGE('',*,*,#11728,.T.);
#16075=ORIENTED_EDGE('',*,*,#11724,.T.);
#16076=ORIENTED_EDGE('',*,*,#11729,.T.);
#16077=ORIENTED_EDGE('',*,*,#11730,.F.);
#16078=ORIENTED_EDGE('',*,*,#11731,.T.);
#16079=ORIENTED_EDGE('',*,*,#11727,.T.);
#16080=ORIENTED_EDGE('',*,*,#11732,.T.);
#16081=ORIENTED_EDGE('',*,*,#11733,.F.);
#16082=ORIENTED_EDGE('',*,*,#11734,.T.);
#16083=ORIENTED_EDGE('',*,*,#11730,.T.);
#16084=ORIENTED_EDGE('',*,*,#11735,.T.);
#16085=ORIENTED_EDGE('',*,*,#11736,.F.);
#16086=ORIENTED_EDGE('',*,*,#11737,.T.);
#16087=ORIENTED_EDGE('',*,*,#11733,.T.);
#16088=ORIENTED_EDGE('',*,*,#11738,.T.);
#16089=ORIENTED_EDGE('',*,*,#11739,.F.);
#16090=ORIENTED_EDGE('',*,*,#11740,.T.);
#16091=ORIENTED_EDGE('',*,*,#11736,.T.);
#16092=ORIENTED_EDGE('',*,*,#11741,.T.);
#16093=ORIENTED_EDGE('',*,*,#11742,.F.);
#16094=ORIENTED_EDGE('',*,*,#11743,.T.);
#16095=ORIENTED_EDGE('',*,*,#11739,.T.);
#16096=ORIENTED_EDGE('',*,*,#11744,.T.);
#16097=ORIENTED_EDGE('',*,*,#11745,.F.);
#16098=ORIENTED_EDGE('',*,*,#11746,.T.);
#16099=ORIENTED_EDGE('',*,*,#11742,.T.);
#16100=ORIENTED_EDGE('',*,*,#11747,.T.);
#16101=ORIENTED_EDGE('',*,*,#11748,.F.);
#16102=ORIENTED_EDGE('',*,*,#11749,.T.);
#16103=ORIENTED_EDGE('',*,*,#11745,.T.);
#16104=ORIENTED_EDGE('',*,*,#11750,.T.);
#16105=ORIENTED_EDGE('',*,*,#11751,.F.);
#16106=ORIENTED_EDGE('',*,*,#11752,.T.);
#16107=ORIENTED_EDGE('',*,*,#11748,.T.);
#16108=ORIENTED_EDGE('',*,*,#11753,.T.);
#16109=ORIENTED_EDGE('',*,*,#11754,.F.);
#16110=ORIENTED_EDGE('',*,*,#11755,.T.);
#16111=ORIENTED_EDGE('',*,*,#11751,.T.);
#16112=ORIENTED_EDGE('',*,*,#11756,.T.);
#16113=ORIENTED_EDGE('',*,*,#11757,.F.);
#16114=ORIENTED_EDGE('',*,*,#11758,.T.);
#16115=ORIENTED_EDGE('',*,*,#11754,.T.);
#16116=ORIENTED_EDGE('',*,*,#11759,.T.);
#16117=ORIENTED_EDGE('',*,*,#11760,.F.);
#16118=ORIENTED_EDGE('',*,*,#11761,.T.);
#16119=ORIENTED_EDGE('',*,*,#11757,.T.);
#16120=ORIENTED_EDGE('',*,*,#11762,.T.);
#16121=ORIENTED_EDGE('',*,*,#11763,.F.);
#16122=ORIENTED_EDGE('',*,*,#11764,.T.);
#16123=ORIENTED_EDGE('',*,*,#11760,.T.);
#16124=ORIENTED_EDGE('',*,*,#11765,.T.);
#16125=ORIENTED_EDGE('',*,*,#11766,.F.);
#16126=ORIENTED_EDGE('',*,*,#11767,.T.);
#16127=ORIENTED_EDGE('',*,*,#11763,.T.);
#16128=ORIENTED_EDGE('',*,*,#11768,.T.);
#16129=ORIENTED_EDGE('',*,*,#11769,.F.);
#16130=ORIENTED_EDGE('',*,*,#11770,.T.);
#16131=ORIENTED_EDGE('',*,*,#11766,.T.);
#16132=ORIENTED_EDGE('',*,*,#11771,.T.);
#16133=ORIENTED_EDGE('',*,*,#11772,.F.);
#16134=ORIENTED_EDGE('',*,*,#11773,.T.);
#16135=ORIENTED_EDGE('',*,*,#11769,.T.);
#16136=ORIENTED_EDGE('',*,*,#11774,.T.);
#16137=ORIENTED_EDGE('',*,*,#11775,.F.);
#16138=ORIENTED_EDGE('',*,*,#11776,.T.);
#16139=ORIENTED_EDGE('',*,*,#11772,.T.);
#16140=ORIENTED_EDGE('',*,*,#11777,.T.);
#16141=ORIENTED_EDGE('',*,*,#11778,.F.);
#16142=ORIENTED_EDGE('',*,*,#11779,.T.);
#16143=ORIENTED_EDGE('',*,*,#11775,.T.);
#16144=ORIENTED_EDGE('',*,*,#11780,.T.);
#16145=ORIENTED_EDGE('',*,*,#11781,.F.);
#16146=ORIENTED_EDGE('',*,*,#11782,.T.);
#16147=ORIENTED_EDGE('',*,*,#11778,.T.);
#16148=ORIENTED_EDGE('',*,*,#11783,.T.);
#16149=ORIENTED_EDGE('',*,*,#11784,.F.);
#16150=ORIENTED_EDGE('',*,*,#11785,.T.);
#16151=ORIENTED_EDGE('',*,*,#11781,.T.);
#16152=ORIENTED_EDGE('',*,*,#11786,.T.);
#16153=ORIENTED_EDGE('',*,*,#11787,.F.);
#16154=ORIENTED_EDGE('',*,*,#11788,.T.);
#16155=ORIENTED_EDGE('',*,*,#11784,.T.);
#16156=ORIENTED_EDGE('',*,*,#11789,.T.);
#16157=ORIENTED_EDGE('',*,*,#11790,.F.);
#16158=ORIENTED_EDGE('',*,*,#11791,.T.);
#16159=ORIENTED_EDGE('',*,*,#11787,.T.);
#16160=ORIENTED_EDGE('',*,*,#11792,.T.);
#16161=ORIENTED_EDGE('',*,*,#11793,.F.);
#16162=ORIENTED_EDGE('',*,*,#11794,.T.);
#16163=ORIENTED_EDGE('',*,*,#11790,.T.);
#16164=ORIENTED_EDGE('',*,*,#11795,.T.);
#16165=ORIENTED_EDGE('',*,*,#11796,.F.);
#16166=ORIENTED_EDGE('',*,*,#11797,.T.);
#16167=ORIENTED_EDGE('',*,*,#11793,.T.);
#16168=ORIENTED_EDGE('',*,*,#11798,.T.);
#16169=ORIENTED_EDGE('',*,*,#11799,.F.);
#16170=ORIENTED_EDGE('',*,*,#11800,.T.);
#16171=ORIENTED_EDGE('',*,*,#11796,.T.);
#16172=ORIENTED_EDGE('',*,*,#11801,.T.);
#16173=ORIENTED_EDGE('',*,*,#11802,.F.);
#16174=ORIENTED_EDGE('',*,*,#11803,.T.);
#16175=ORIENTED_EDGE('',*,*,#11799,.T.);
#16176=ORIENTED_EDGE('',*,*,#11804,.T.);
#16177=ORIENTED_EDGE('',*,*,#11805,.F.);
#16178=ORIENTED_EDGE('',*,*,#11806,.T.);
#16179=ORIENTED_EDGE('',*,*,#11802,.T.);
#16180=ORIENTED_EDGE('',*,*,#11807,.T.);
#16181=ORIENTED_EDGE('',*,*,#11808,.F.);
#16182=ORIENTED_EDGE('',*,*,#11809,.T.);
#16183=ORIENTED_EDGE('',*,*,#11805,.T.);
#16184=ORIENTED_EDGE('',*,*,#11810,.T.);
#16185=ORIENTED_EDGE('',*,*,#11811,.F.);
#16186=ORIENTED_EDGE('',*,*,#11812,.T.);
#16187=ORIENTED_EDGE('',*,*,#11808,.T.);
#16188=ORIENTED_EDGE('',*,*,#11813,.T.);
#16189=ORIENTED_EDGE('',*,*,#11814,.F.);
#16190=ORIENTED_EDGE('',*,*,#11815,.T.);
#16191=ORIENTED_EDGE('',*,*,#11811,.T.);
#16192=ORIENTED_EDGE('',*,*,#11816,.T.);
#16193=ORIENTED_EDGE('',*,*,#11817,.F.);
#16194=ORIENTED_EDGE('',*,*,#11818,.T.);
#16195=ORIENTED_EDGE('',*,*,#11814,.T.);
#16196=ORIENTED_EDGE('',*,*,#11819,.T.);
#16197=ORIENTED_EDGE('',*,*,#11820,.F.);
#16198=ORIENTED_EDGE('',*,*,#11821,.T.);
#16199=ORIENTED_EDGE('',*,*,#11817,.T.);
#16200=ORIENTED_EDGE('',*,*,#11822,.T.);
#16201=ORIENTED_EDGE('',*,*,#11823,.F.);
#16202=ORIENTED_EDGE('',*,*,#11824,.T.);
#16203=ORIENTED_EDGE('',*,*,#11820,.T.);
#16204=ORIENTED_EDGE('',*,*,#11825,.T.);
#16205=ORIENTED_EDGE('',*,*,#11826,.F.);
#16206=ORIENTED_EDGE('',*,*,#11827,.T.);
#16207=ORIENTED_EDGE('',*,*,#11823,.T.);
#16208=ORIENTED_EDGE('',*,*,#11828,.T.);
#16209=ORIENTED_EDGE('',*,*,#11829,.F.);
#16210=ORIENTED_EDGE('',*,*,#11830,.T.);
#16211=ORIENTED_EDGE('',*,*,#11826,.T.);
#16212=ORIENTED_EDGE('',*,*,#11831,.T.);
#16213=ORIENTED_EDGE('',*,*,#11832,.F.);
#16214=ORIENTED_EDGE('',*,*,#11833,.T.);
#16215=ORIENTED_EDGE('',*,*,#11829,.T.);
#16216=ORIENTED_EDGE('',*,*,#11834,.T.);
#16217=ORIENTED_EDGE('',*,*,#11835,.F.);
#16218=ORIENTED_EDGE('',*,*,#11836,.T.);
#16219=ORIENTED_EDGE('',*,*,#11832,.T.);
#16220=ORIENTED_EDGE('',*,*,#11837,.T.);
#16221=ORIENTED_EDGE('',*,*,#11838,.F.);
#16222=ORIENTED_EDGE('',*,*,#11839,.T.);
#16223=ORIENTED_EDGE('',*,*,#11835,.T.);
#16224=ORIENTED_EDGE('',*,*,#11840,.T.);
#16225=ORIENTED_EDGE('',*,*,#11841,.F.);
#16226=ORIENTED_EDGE('',*,*,#11842,.T.);
#16227=ORIENTED_EDGE('',*,*,#11843,.F.);
#16228=ORIENTED_EDGE('',*,*,#11844,.F.);
#16229=ORIENTED_EDGE('',*,*,#11845,.T.);
#16230=ORIENTED_EDGE('',*,*,#11841,.T.);
#16231=ORIENTED_EDGE('',*,*,#11846,.F.);
#16232=ORIENTED_EDGE('',*,*,#11847,.F.);
#16233=ORIENTED_EDGE('',*,*,#11848,.F.);
#16234=ORIENTED_EDGE('',*,*,#11849,.T.);
#16235=ORIENTED_EDGE('',*,*,#11844,.T.);
#16236=ORIENTED_EDGE('',*,*,#11850,.F.);
#16237=ORIENTED_EDGE('',*,*,#11851,.F.);
#16238=ORIENTED_EDGE('',*,*,#11852,.T.);
#16239=ORIENTED_EDGE('',*,*,#11848,.T.);
#16240=ORIENTED_EDGE('',*,*,#11853,.F.);
#16241=ORIENTED_EDGE('',*,*,#11854,.F.);
#16242=ORIENTED_EDGE('',*,*,#11855,.T.);
#16243=ORIENTED_EDGE('',*,*,#11851,.T.);
#16244=ORIENTED_EDGE('',*,*,#11856,.F.);
#16245=ORIENTED_EDGE('',*,*,#11857,.F.);
#16246=ORIENTED_EDGE('',*,*,#11858,.T.);
#16247=ORIENTED_EDGE('',*,*,#11854,.T.);
#16248=ORIENTED_EDGE('',*,*,#11859,.F.);
#16249=ORIENTED_EDGE('',*,*,#11860,.F.);
#16250=ORIENTED_EDGE('',*,*,#11861,.T.);
#16251=ORIENTED_EDGE('',*,*,#11857,.T.);
#16252=ORIENTED_EDGE('',*,*,#11862,.F.);
#16253=ORIENTED_EDGE('',*,*,#11863,.F.);
#16254=ORIENTED_EDGE('',*,*,#11864,.T.);
#16255=ORIENTED_EDGE('',*,*,#11860,.T.);
#16256=ORIENTED_EDGE('',*,*,#11865,.F.);
#16257=ORIENTED_EDGE('',*,*,#11866,.F.);
#16258=ORIENTED_EDGE('',*,*,#11867,.T.);
#16259=ORIENTED_EDGE('',*,*,#11863,.T.);
#16260=ORIENTED_EDGE('',*,*,#11868,.F.);
#16261=ORIENTED_EDGE('',*,*,#11869,.F.);
#16262=ORIENTED_EDGE('',*,*,#11870,.T.);
#16263=ORIENTED_EDGE('',*,*,#11866,.T.);
#16264=ORIENTED_EDGE('',*,*,#11871,.F.);
#16265=ORIENTED_EDGE('',*,*,#11872,.F.);
#16266=ORIENTED_EDGE('',*,*,#11873,.T.);
#16267=ORIENTED_EDGE('',*,*,#11869,.T.);
#16268=ORIENTED_EDGE('',*,*,#11874,.F.);
#16269=ORIENTED_EDGE('',*,*,#11875,.F.);
#16270=ORIENTED_EDGE('',*,*,#11876,.T.);
#16271=ORIENTED_EDGE('',*,*,#11872,.T.);
#16272=ORIENTED_EDGE('',*,*,#11877,.F.);
#16273=ORIENTED_EDGE('',*,*,#11878,.F.);
#16274=ORIENTED_EDGE('',*,*,#11879,.T.);
#16275=ORIENTED_EDGE('',*,*,#11875,.T.);
#16276=ORIENTED_EDGE('',*,*,#11880,.F.);
#16277=ORIENTED_EDGE('',*,*,#11881,.F.);
#16278=ORIENTED_EDGE('',*,*,#11882,.T.);
#16279=ORIENTED_EDGE('',*,*,#11878,.T.);
#16280=ORIENTED_EDGE('',*,*,#11883,.F.);
#16281=ORIENTED_EDGE('',*,*,#11884,.F.);
#16282=ORIENTED_EDGE('',*,*,#11885,.T.);
#16283=ORIENTED_EDGE('',*,*,#11881,.T.);
#16284=ORIENTED_EDGE('',*,*,#11886,.F.);
#16285=ORIENTED_EDGE('',*,*,#11887,.F.);
#16286=ORIENTED_EDGE('',*,*,#11888,.T.);
#16287=ORIENTED_EDGE('',*,*,#11884,.T.);
#16288=ORIENTED_EDGE('',*,*,#11889,.F.);
#16289=ORIENTED_EDGE('',*,*,#11890,.F.);
#16290=ORIENTED_EDGE('',*,*,#11891,.T.);
#16291=ORIENTED_EDGE('',*,*,#11887,.T.);
#16292=ORIENTED_EDGE('',*,*,#11892,.F.);
#16293=ORIENTED_EDGE('',*,*,#11893,.F.);
#16294=ORIENTED_EDGE('',*,*,#11894,.T.);
#16295=ORIENTED_EDGE('',*,*,#11890,.T.);
#16296=ORIENTED_EDGE('',*,*,#11895,.F.);
#16297=ORIENTED_EDGE('',*,*,#11896,.F.);
#16298=ORIENTED_EDGE('',*,*,#11897,.T.);
#16299=ORIENTED_EDGE('',*,*,#11893,.T.);
#16300=ORIENTED_EDGE('',*,*,#11898,.F.);
#16301=ORIENTED_EDGE('',*,*,#11899,.F.);
#16302=ORIENTED_EDGE('',*,*,#11900,.T.);
#16303=ORIENTED_EDGE('',*,*,#11896,.T.);
#16304=ORIENTED_EDGE('',*,*,#11901,.F.);
#16305=ORIENTED_EDGE('',*,*,#11902,.F.);
#16306=ORIENTED_EDGE('',*,*,#11903,.T.);
#16307=ORIENTED_EDGE('',*,*,#11899,.T.);
#16308=ORIENTED_EDGE('',*,*,#11904,.F.);
#16309=ORIENTED_EDGE('',*,*,#11905,.F.);
#16310=ORIENTED_EDGE('',*,*,#11906,.T.);
#16311=ORIENTED_EDGE('',*,*,#11902,.T.);
#16312=ORIENTED_EDGE('',*,*,#11907,.F.);
#16313=ORIENTED_EDGE('',*,*,#11908,.F.);
#16314=ORIENTED_EDGE('',*,*,#11909,.T.);
#16315=ORIENTED_EDGE('',*,*,#11905,.T.);
#16316=ORIENTED_EDGE('',*,*,#11910,.F.);
#16317=ORIENTED_EDGE('',*,*,#11911,.F.);
#16318=ORIENTED_EDGE('',*,*,#11912,.T.);
#16319=ORIENTED_EDGE('',*,*,#11908,.T.);
#16320=ORIENTED_EDGE('',*,*,#11913,.F.);
#16321=ORIENTED_EDGE('',*,*,#11914,.F.);
#16322=ORIENTED_EDGE('',*,*,#11915,.T.);
#16323=ORIENTED_EDGE('',*,*,#11911,.T.);
#16324=ORIENTED_EDGE('',*,*,#11916,.F.);
#16325=ORIENTED_EDGE('',*,*,#11917,.F.);
#16326=ORIENTED_EDGE('',*,*,#11918,.T.);
#16327=ORIENTED_EDGE('',*,*,#11914,.T.);
#16328=ORIENTED_EDGE('',*,*,#11919,.F.);
#16329=ORIENTED_EDGE('',*,*,#11920,.F.);
#16330=ORIENTED_EDGE('',*,*,#11921,.T.);
#16331=ORIENTED_EDGE('',*,*,#11917,.T.);
#16332=ORIENTED_EDGE('',*,*,#11922,.F.);
#16333=ORIENTED_EDGE('',*,*,#11923,.F.);
#16334=ORIENTED_EDGE('',*,*,#11924,.T.);
#16335=ORIENTED_EDGE('',*,*,#11920,.T.);
#16336=ORIENTED_EDGE('',*,*,#11925,.F.);
#16337=ORIENTED_EDGE('',*,*,#11926,.F.);
#16338=ORIENTED_EDGE('',*,*,#11927,.T.);
#16339=ORIENTED_EDGE('',*,*,#11923,.T.);
#16340=ORIENTED_EDGE('',*,*,#11928,.F.);
#16341=ORIENTED_EDGE('',*,*,#11929,.F.);
#16342=ORIENTED_EDGE('',*,*,#11930,.T.);
#16343=ORIENTED_EDGE('',*,*,#11926,.T.);
#16344=ORIENTED_EDGE('',*,*,#11931,.F.);
#16345=ORIENTED_EDGE('',*,*,#11932,.F.);
#16346=ORIENTED_EDGE('',*,*,#11933,.T.);
#16347=ORIENTED_EDGE('',*,*,#11929,.T.);
#16348=ORIENTED_EDGE('',*,*,#11934,.F.);
#16349=ORIENTED_EDGE('',*,*,#11935,.F.);
#16350=ORIENTED_EDGE('',*,*,#11936,.T.);
#16351=ORIENTED_EDGE('',*,*,#11932,.T.);
#16352=ORIENTED_EDGE('',*,*,#11937,.F.);
#16353=ORIENTED_EDGE('',*,*,#11938,.F.);
#16354=ORIENTED_EDGE('',*,*,#11939,.T.);
#16355=ORIENTED_EDGE('',*,*,#11935,.T.);
#16356=ORIENTED_EDGE('',*,*,#11940,.F.);
#16357=ORIENTED_EDGE('',*,*,#11941,.F.);
#16358=ORIENTED_EDGE('',*,*,#11942,.T.);
#16359=ORIENTED_EDGE('',*,*,#11938,.T.);
#16360=ORIENTED_EDGE('',*,*,#11943,.F.);
#16361=ORIENTED_EDGE('',*,*,#11944,.F.);
#16362=ORIENTED_EDGE('',*,*,#11945,.T.);
#16363=ORIENTED_EDGE('',*,*,#11941,.T.);
#16364=ORIENTED_EDGE('',*,*,#11946,.F.);
#16365=ORIENTED_EDGE('',*,*,#11947,.F.);
#16366=ORIENTED_EDGE('',*,*,#11948,.T.);
#16367=ORIENTED_EDGE('',*,*,#11944,.T.);
#16368=ORIENTED_EDGE('',*,*,#11949,.F.);
#16369=ORIENTED_EDGE('',*,*,#11950,.F.);
#16370=ORIENTED_EDGE('',*,*,#11951,.T.);
#16371=ORIENTED_EDGE('',*,*,#11947,.T.);
#16372=ORIENTED_EDGE('',*,*,#11952,.F.);
#16373=ORIENTED_EDGE('',*,*,#11953,.F.);
#16374=ORIENTED_EDGE('',*,*,#11954,.T.);
#16375=ORIENTED_EDGE('',*,*,#11950,.T.);
#16376=ORIENTED_EDGE('',*,*,#11955,.F.);
#16377=ORIENTED_EDGE('',*,*,#11956,.F.);
#16378=ORIENTED_EDGE('',*,*,#11957,.T.);
#16379=ORIENTED_EDGE('',*,*,#11953,.T.);
#16380=ORIENTED_EDGE('',*,*,#11958,.F.);
#16381=ORIENTED_EDGE('',*,*,#11959,.F.);
#16382=ORIENTED_EDGE('',*,*,#11960,.T.);
#16383=ORIENTED_EDGE('',*,*,#11956,.T.);
#16384=ORIENTED_EDGE('',*,*,#11961,.F.);
#16385=ORIENTED_EDGE('',*,*,#11962,.F.);
#16386=ORIENTED_EDGE('',*,*,#11963,.T.);
#16387=ORIENTED_EDGE('',*,*,#11959,.T.);
#16388=ORIENTED_EDGE('',*,*,#11964,.F.);
#16389=ORIENTED_EDGE('',*,*,#11965,.F.);
#16390=ORIENTED_EDGE('',*,*,#11966,.T.);
#16391=ORIENTED_EDGE('',*,*,#11962,.T.);
#16392=ORIENTED_EDGE('',*,*,#11967,.F.);
#16393=ORIENTED_EDGE('',*,*,#11968,.F.);
#16394=ORIENTED_EDGE('',*,*,#11969,.T.);
#16395=ORIENTED_EDGE('',*,*,#11965,.T.);
#16396=ORIENTED_EDGE('',*,*,#11970,.F.);
#16397=ORIENTED_EDGE('',*,*,#11971,.F.);
#16398=ORIENTED_EDGE('',*,*,#11972,.T.);
#16399=ORIENTED_EDGE('',*,*,#11968,.T.);
#16400=ORIENTED_EDGE('',*,*,#11973,.F.);
#16401=ORIENTED_EDGE('',*,*,#11974,.F.);
#16402=ORIENTED_EDGE('',*,*,#11975,.T.);
#16403=ORIENTED_EDGE('',*,*,#11971,.T.);
#16404=ORIENTED_EDGE('',*,*,#11976,.F.);
#16405=ORIENTED_EDGE('',*,*,#11977,.F.);
#16406=ORIENTED_EDGE('',*,*,#11978,.T.);
#16407=ORIENTED_EDGE('',*,*,#11974,.T.);
#16408=ORIENTED_EDGE('',*,*,#11979,.F.);
#16409=ORIENTED_EDGE('',*,*,#11980,.F.);
#16410=ORIENTED_EDGE('',*,*,#11981,.T.);
#16411=ORIENTED_EDGE('',*,*,#11977,.T.);
#16412=ORIENTED_EDGE('',*,*,#11982,.F.);
#16413=ORIENTED_EDGE('',*,*,#11983,.F.);
#16414=ORIENTED_EDGE('',*,*,#11984,.T.);
#16415=ORIENTED_EDGE('',*,*,#11980,.T.);
#16416=ORIENTED_EDGE('',*,*,#11985,.F.);
#16417=ORIENTED_EDGE('',*,*,#11986,.F.);
#16418=ORIENTED_EDGE('',*,*,#11987,.T.);
#16419=ORIENTED_EDGE('',*,*,#11983,.T.);
#16420=ORIENTED_EDGE('',*,*,#11988,.F.);
#16421=ORIENTED_EDGE('',*,*,#11989,.F.);
#16422=ORIENTED_EDGE('',*,*,#11990,.T.);
#16423=ORIENTED_EDGE('',*,*,#11986,.T.);
#16424=ORIENTED_EDGE('',*,*,#11991,.F.);
#16425=ORIENTED_EDGE('',*,*,#11992,.F.);
#16426=ORIENTED_EDGE('',*,*,#11993,.T.);
#16427=ORIENTED_EDGE('',*,*,#11989,.T.);
#16428=ORIENTED_EDGE('',*,*,#11994,.F.);
#16429=ORIENTED_EDGE('',*,*,#11995,.F.);
#16430=ORIENTED_EDGE('',*,*,#11996,.T.);
#16431=ORIENTED_EDGE('',*,*,#11992,.T.);
#16432=ORIENTED_EDGE('',*,*,#11997,.F.);
#16433=ORIENTED_EDGE('',*,*,#11998,.F.);
#16434=ORIENTED_EDGE('',*,*,#11999,.T.);
#16435=ORIENTED_EDGE('',*,*,#11995,.T.);
#16436=ORIENTED_EDGE('',*,*,#12000,.F.);
#16437=ORIENTED_EDGE('',*,*,#12001,.F.);
#16438=ORIENTED_EDGE('',*,*,#12002,.T.);
#16439=ORIENTED_EDGE('',*,*,#11998,.T.);
#16440=ORIENTED_EDGE('',*,*,#12003,.F.);
#16441=ORIENTED_EDGE('',*,*,#12004,.F.);
#16442=ORIENTED_EDGE('',*,*,#12005,.T.);
#16443=ORIENTED_EDGE('',*,*,#12001,.T.);
#16444=ORIENTED_EDGE('',*,*,#12006,.F.);
#16445=ORIENTED_EDGE('',*,*,#12007,.F.);
#16446=ORIENTED_EDGE('',*,*,#12008,.T.);
#16447=ORIENTED_EDGE('',*,*,#12004,.T.);
#16448=ORIENTED_EDGE('',*,*,#12009,.F.);
#16449=ORIENTED_EDGE('',*,*,#12010,.F.);
#16450=ORIENTED_EDGE('',*,*,#12011,.T.);
#16451=ORIENTED_EDGE('',*,*,#12007,.T.);
#16452=ORIENTED_EDGE('',*,*,#12012,.F.);
#16453=ORIENTED_EDGE('',*,*,#12013,.F.);
#16454=ORIENTED_EDGE('',*,*,#12014,.T.);
#16455=ORIENTED_EDGE('',*,*,#12010,.T.);
#16456=ORIENTED_EDGE('',*,*,#12015,.F.);
#16457=ORIENTED_EDGE('',*,*,#12016,.F.);
#16458=ORIENTED_EDGE('',*,*,#12017,.T.);
#16459=ORIENTED_EDGE('',*,*,#12013,.T.);
#16460=ORIENTED_EDGE('',*,*,#12018,.F.);
#16461=ORIENTED_EDGE('',*,*,#12019,.F.);
#16462=ORIENTED_EDGE('',*,*,#12020,.T.);
#16463=ORIENTED_EDGE('',*,*,#12016,.T.);
#16464=ORIENTED_EDGE('',*,*,#12021,.F.);
#16465=ORIENTED_EDGE('',*,*,#12022,.F.);
#16466=ORIENTED_EDGE('',*,*,#12023,.T.);
#16467=ORIENTED_EDGE('',*,*,#12019,.T.);
#16468=ORIENTED_EDGE('',*,*,#12024,.F.);
#16469=ORIENTED_EDGE('',*,*,#12025,.F.);
#16470=ORIENTED_EDGE('',*,*,#12026,.T.);
#16471=ORIENTED_EDGE('',*,*,#12022,.T.);
#16472=ORIENTED_EDGE('',*,*,#12027,.F.);
#16473=ORIENTED_EDGE('',*,*,#12028,.F.);
#16474=ORIENTED_EDGE('',*,*,#12029,.T.);
#16475=ORIENTED_EDGE('',*,*,#12025,.T.);
#16476=ORIENTED_EDGE('',*,*,#12030,.F.);
#16477=ORIENTED_EDGE('',*,*,#12031,.T.);
#16478=ORIENTED_EDGE('',*,*,#12032,.T.);
#16479=ORIENTED_EDGE('',*,*,#11653,.F.);
#16480=ORIENTED_EDGE('',*,*,#12033,.T.);
#16481=ORIENTED_EDGE('',*,*,#12034,.T.);
#16482=ORIENTED_EDGE('',*,*,#12031,.F.);
#16483=ORIENTED_EDGE('',*,*,#12035,.T.);
#16484=ORIENTED_EDGE('',*,*,#12036,.T.);
#16485=ORIENTED_EDGE('',*,*,#12035,.F.);
#16486=ORIENTED_EDGE('',*,*,#12036,.F.);
#16487=ORIENTED_EDGE('',*,*,#12037,.F.);
#16488=ORIENTED_EDGE('',*,*,#12038,.F.);
#16489=ORIENTED_EDGE('',*,*,#11840,.F.);
#16490=ORIENTED_EDGE('',*,*,#11837,.F.);
#16491=ORIENTED_EDGE('',*,*,#11834,.F.);
#16492=ORIENTED_EDGE('',*,*,#11831,.F.);
#16493=ORIENTED_EDGE('',*,*,#11828,.F.);
#16494=ORIENTED_EDGE('',*,*,#11825,.F.);
#16495=ORIENTED_EDGE('',*,*,#11822,.F.);
#16496=ORIENTED_EDGE('',*,*,#11819,.F.);
#16497=ORIENTED_EDGE('',*,*,#11816,.F.);
#16498=ORIENTED_EDGE('',*,*,#11813,.F.);
#16499=ORIENTED_EDGE('',*,*,#11810,.F.);
#16500=ORIENTED_EDGE('',*,*,#11807,.F.);
#16501=ORIENTED_EDGE('',*,*,#11804,.F.);
#16502=ORIENTED_EDGE('',*,*,#11801,.F.);
#16503=ORIENTED_EDGE('',*,*,#11798,.F.);
#16504=ORIENTED_EDGE('',*,*,#11795,.F.);
#16505=ORIENTED_EDGE('',*,*,#11792,.F.);
#16506=ORIENTED_EDGE('',*,*,#11789,.F.);
#16507=ORIENTED_EDGE('',*,*,#11786,.F.);
#16508=ORIENTED_EDGE('',*,*,#11783,.F.);
#16509=ORIENTED_EDGE('',*,*,#11780,.F.);
#16510=ORIENTED_EDGE('',*,*,#11777,.F.);
#16511=ORIENTED_EDGE('',*,*,#11774,.F.);
#16512=ORIENTED_EDGE('',*,*,#11771,.F.);
#16513=ORIENTED_EDGE('',*,*,#11768,.F.);
#16514=ORIENTED_EDGE('',*,*,#11765,.F.);
#16515=ORIENTED_EDGE('',*,*,#11762,.F.);
#16516=ORIENTED_EDGE('',*,*,#11759,.F.);
#16517=ORIENTED_EDGE('',*,*,#11756,.F.);
#16518=ORIENTED_EDGE('',*,*,#11753,.F.);
#16519=ORIENTED_EDGE('',*,*,#11750,.F.);
#16520=ORIENTED_EDGE('',*,*,#11747,.F.);
#16521=ORIENTED_EDGE('',*,*,#11744,.F.);
#16522=ORIENTED_EDGE('',*,*,#11741,.F.);
#16523=ORIENTED_EDGE('',*,*,#11738,.F.);
#16524=ORIENTED_EDGE('',*,*,#11735,.F.);
#16525=ORIENTED_EDGE('',*,*,#11732,.F.);
#16526=ORIENTED_EDGE('',*,*,#11729,.F.);
#16527=ORIENTED_EDGE('',*,*,#11726,.F.);
#16528=ORIENTED_EDGE('',*,*,#11723,.F.);
#16529=ORIENTED_EDGE('',*,*,#11720,.F.);
#16530=ORIENTED_EDGE('',*,*,#11717,.F.);
#16531=ORIENTED_EDGE('',*,*,#11714,.F.);
#16532=ORIENTED_EDGE('',*,*,#11711,.F.);
#16533=ORIENTED_EDGE('',*,*,#11708,.F.);
#16534=ORIENTED_EDGE('',*,*,#11705,.F.);
#16535=ORIENTED_EDGE('',*,*,#11702,.F.);
#16536=ORIENTED_EDGE('',*,*,#11699,.F.);
#16537=ORIENTED_EDGE('',*,*,#11696,.F.);
#16538=ORIENTED_EDGE('',*,*,#11693,.F.);
#16539=ORIENTED_EDGE('',*,*,#11690,.F.);
#16540=ORIENTED_EDGE('',*,*,#11687,.F.);
#16541=ORIENTED_EDGE('',*,*,#11684,.F.);
#16542=ORIENTED_EDGE('',*,*,#11681,.F.);
#16543=ORIENTED_EDGE('',*,*,#11678,.F.);
#16544=ORIENTED_EDGE('',*,*,#11675,.F.);
#16545=ORIENTED_EDGE('',*,*,#11672,.F.);
#16546=ORIENTED_EDGE('',*,*,#11669,.F.);
#16547=ORIENTED_EDGE('',*,*,#11666,.F.);
#16548=ORIENTED_EDGE('',*,*,#11663,.F.);
#16549=ORIENTED_EDGE('',*,*,#11660,.F.);
#16550=ORIENTED_EDGE('',*,*,#11657,.F.);
#16551=ORIENTED_EDGE('',*,*,#11654,.F.);
#16552=ORIENTED_EDGE('',*,*,#12032,.F.);
#16553=ORIENTED_EDGE('',*,*,#12039,.T.);
#16554=ORIENTED_EDGE('',*,*,#12030,.T.);
#16555=ORIENTED_EDGE('',*,*,#12027,.T.);
#16556=ORIENTED_EDGE('',*,*,#12024,.T.);
#16557=ORIENTED_EDGE('',*,*,#12021,.T.);
#16558=ORIENTED_EDGE('',*,*,#12018,.T.);
#16559=ORIENTED_EDGE('',*,*,#12015,.T.);
#16560=ORIENTED_EDGE('',*,*,#12012,.T.);
#16561=ORIENTED_EDGE('',*,*,#12009,.T.);
#16562=ORIENTED_EDGE('',*,*,#12006,.T.);
#16563=ORIENTED_EDGE('',*,*,#12003,.T.);
#16564=ORIENTED_EDGE('',*,*,#12000,.T.);
#16565=ORIENTED_EDGE('',*,*,#11997,.T.);
#16566=ORIENTED_EDGE('',*,*,#11994,.T.);
#16567=ORIENTED_EDGE('',*,*,#11991,.T.);
#16568=ORIENTED_EDGE('',*,*,#11988,.T.);
#16569=ORIENTED_EDGE('',*,*,#11985,.T.);
#16570=ORIENTED_EDGE('',*,*,#11982,.T.);
#16571=ORIENTED_EDGE('',*,*,#11979,.T.);
#16572=ORIENTED_EDGE('',*,*,#11976,.T.);
#16573=ORIENTED_EDGE('',*,*,#11973,.T.);
#16574=ORIENTED_EDGE('',*,*,#11970,.T.);
#16575=ORIENTED_EDGE('',*,*,#11967,.T.);
#16576=ORIENTED_EDGE('',*,*,#11964,.T.);
#16577=ORIENTED_EDGE('',*,*,#11961,.T.);
#16578=ORIENTED_EDGE('',*,*,#11958,.T.);
#16579=ORIENTED_EDGE('',*,*,#11955,.T.);
#16580=ORIENTED_EDGE('',*,*,#11952,.T.);
#16581=ORIENTED_EDGE('',*,*,#11949,.T.);
#16582=ORIENTED_EDGE('',*,*,#11946,.T.);
#16583=ORIENTED_EDGE('',*,*,#11943,.T.);
#16584=ORIENTED_EDGE('',*,*,#11940,.T.);
#16585=ORIENTED_EDGE('',*,*,#11937,.T.);
#16586=ORIENTED_EDGE('',*,*,#11934,.T.);
#16587=ORIENTED_EDGE('',*,*,#11931,.T.);
#16588=ORIENTED_EDGE('',*,*,#11928,.T.);
#16589=ORIENTED_EDGE('',*,*,#11925,.T.);
#16590=ORIENTED_EDGE('',*,*,#11922,.T.);
#16591=ORIENTED_EDGE('',*,*,#11919,.T.);
#16592=ORIENTED_EDGE('',*,*,#11916,.T.);
#16593=ORIENTED_EDGE('',*,*,#11913,.T.);
#16594=ORIENTED_EDGE('',*,*,#11910,.T.);
#16595=ORIENTED_EDGE('',*,*,#11907,.T.);
#16596=ORIENTED_EDGE('',*,*,#11904,.T.);
#16597=ORIENTED_EDGE('',*,*,#11901,.T.);
#16598=ORIENTED_EDGE('',*,*,#11898,.T.);
#16599=ORIENTED_EDGE('',*,*,#11895,.T.);
#16600=ORIENTED_EDGE('',*,*,#11892,.T.);
#16601=ORIENTED_EDGE('',*,*,#11889,.T.);
#16602=ORIENTED_EDGE('',*,*,#11886,.T.);
#16603=ORIENTED_EDGE('',*,*,#11883,.T.);
#16604=ORIENTED_EDGE('',*,*,#11880,.T.);
#16605=ORIENTED_EDGE('',*,*,#11877,.T.);
#16606=ORIENTED_EDGE('',*,*,#11874,.T.);
#16607=ORIENTED_EDGE('',*,*,#11871,.T.);
#16608=ORIENTED_EDGE('',*,*,#11868,.T.);
#16609=ORIENTED_EDGE('',*,*,#11865,.T.);
#16610=ORIENTED_EDGE('',*,*,#11862,.T.);
#16611=ORIENTED_EDGE('',*,*,#11859,.T.);
#16612=ORIENTED_EDGE('',*,*,#11856,.T.);
#16613=ORIENTED_EDGE('',*,*,#11853,.T.);
#16614=ORIENTED_EDGE('',*,*,#11850,.T.);
#16615=ORIENTED_EDGE('',*,*,#11847,.T.);
#16616=ORIENTED_EDGE('',*,*,#12028,.T.);
#16617=ORIENTED_EDGE('',*,*,#12039,.F.);
#16618=ORIENTED_EDGE('',*,*,#12034,.F.);
#16619=ORIENTED_EDGE('',*,*,#12040,.T.);
#16620=ORIENTED_EDGE('',*,*,#12041,.F.);
#16621=ORIENTED_EDGE('',*,*,#11842,.F.);
#16622=ORIENTED_EDGE('',*,*,#11845,.F.);
#16623=ORIENTED_EDGE('',*,*,#11849,.F.);
#16624=ORIENTED_EDGE('',*,*,#11852,.F.);
#16625=ORIENTED_EDGE('',*,*,#11855,.F.);
#16626=ORIENTED_EDGE('',*,*,#11858,.F.);
#16627=ORIENTED_EDGE('',*,*,#11861,.F.);
#16628=ORIENTED_EDGE('',*,*,#11864,.F.);
#16629=ORIENTED_EDGE('',*,*,#11867,.F.);
#16630=ORIENTED_EDGE('',*,*,#11870,.F.);
#16631=ORIENTED_EDGE('',*,*,#11873,.F.);
#16632=ORIENTED_EDGE('',*,*,#11876,.F.);
#16633=ORIENTED_EDGE('',*,*,#11879,.F.);
#16634=ORIENTED_EDGE('',*,*,#11882,.F.);
#16635=ORIENTED_EDGE('',*,*,#11885,.F.);
#16636=ORIENTED_EDGE('',*,*,#11888,.F.);
#16637=ORIENTED_EDGE('',*,*,#11891,.F.);
#16638=ORIENTED_EDGE('',*,*,#11894,.F.);
#16639=ORIENTED_EDGE('',*,*,#11897,.F.);
#16640=ORIENTED_EDGE('',*,*,#11900,.F.);
#16641=ORIENTED_EDGE('',*,*,#11903,.F.);
#16642=ORIENTED_EDGE('',*,*,#11906,.F.);
#16643=ORIENTED_EDGE('',*,*,#11909,.F.);
#16644=ORIENTED_EDGE('',*,*,#11912,.F.);
#16645=ORIENTED_EDGE('',*,*,#11915,.F.);
#16646=ORIENTED_EDGE('',*,*,#11918,.F.);
#16647=ORIENTED_EDGE('',*,*,#11921,.F.);
#16648=ORIENTED_EDGE('',*,*,#11924,.F.);
#16649=ORIENTED_EDGE('',*,*,#11927,.F.);
#16650=ORIENTED_EDGE('',*,*,#11930,.F.);
#16651=ORIENTED_EDGE('',*,*,#11933,.F.);
#16652=ORIENTED_EDGE('',*,*,#11936,.F.);
#16653=ORIENTED_EDGE('',*,*,#11939,.F.);
#16654=ORIENTED_EDGE('',*,*,#11942,.F.);
#16655=ORIENTED_EDGE('',*,*,#11945,.F.);
#16656=ORIENTED_EDGE('',*,*,#11948,.F.);
#16657=ORIENTED_EDGE('',*,*,#11951,.F.);
#16658=ORIENTED_EDGE('',*,*,#11954,.F.);
#16659=ORIENTED_EDGE('',*,*,#11957,.F.);
#16660=ORIENTED_EDGE('',*,*,#11960,.F.);
#16661=ORIENTED_EDGE('',*,*,#11963,.F.);
#16662=ORIENTED_EDGE('',*,*,#11966,.F.);
#16663=ORIENTED_EDGE('',*,*,#11969,.F.);
#16664=ORIENTED_EDGE('',*,*,#11972,.F.);
#16665=ORIENTED_EDGE('',*,*,#11975,.F.);
#16666=ORIENTED_EDGE('',*,*,#11978,.F.);
#16667=ORIENTED_EDGE('',*,*,#11981,.F.);
#16668=ORIENTED_EDGE('',*,*,#11984,.F.);
#16669=ORIENTED_EDGE('',*,*,#11987,.F.);
#16670=ORIENTED_EDGE('',*,*,#11990,.F.);
#16671=ORIENTED_EDGE('',*,*,#11993,.F.);
#16672=ORIENTED_EDGE('',*,*,#11996,.F.);
#16673=ORIENTED_EDGE('',*,*,#11999,.F.);
#16674=ORIENTED_EDGE('',*,*,#12002,.F.);
#16675=ORIENTED_EDGE('',*,*,#12005,.F.);
#16676=ORIENTED_EDGE('',*,*,#12008,.F.);
#16677=ORIENTED_EDGE('',*,*,#12011,.F.);
#16678=ORIENTED_EDGE('',*,*,#12014,.F.);
#16679=ORIENTED_EDGE('',*,*,#12017,.F.);
#16680=ORIENTED_EDGE('',*,*,#12020,.F.);
#16681=ORIENTED_EDGE('',*,*,#12023,.F.);
#16682=ORIENTED_EDGE('',*,*,#12026,.F.);
#16683=ORIENTED_EDGE('',*,*,#12029,.F.);
#16684=ORIENTED_EDGE('',*,*,#12040,.F.);
#16685=ORIENTED_EDGE('',*,*,#12033,.F.);
#16686=ORIENTED_EDGE('',*,*,#11652,.F.);
#16687=ORIENTED_EDGE('',*,*,#11656,.F.);
#16688=ORIENTED_EDGE('',*,*,#11659,.F.);
#16689=ORIENTED_EDGE('',*,*,#11662,.F.);
#16690=ORIENTED_EDGE('',*,*,#11665,.F.);
#16691=ORIENTED_EDGE('',*,*,#11668,.F.);
#16692=ORIENTED_EDGE('',*,*,#11671,.F.);
#16693=ORIENTED_EDGE('',*,*,#11674,.F.);
#16694=ORIENTED_EDGE('',*,*,#11677,.F.);
#16695=ORIENTED_EDGE('',*,*,#11680,.F.);
#16696=ORIENTED_EDGE('',*,*,#11683,.F.);
#16697=ORIENTED_EDGE('',*,*,#11686,.F.);
#16698=ORIENTED_EDGE('',*,*,#11689,.F.);
#16699=ORIENTED_EDGE('',*,*,#11692,.F.);
#16700=ORIENTED_EDGE('',*,*,#11695,.F.);
#16701=ORIENTED_EDGE('',*,*,#11698,.F.);
#16702=ORIENTED_EDGE('',*,*,#11701,.F.);
#16703=ORIENTED_EDGE('',*,*,#11704,.F.);
#16704=ORIENTED_EDGE('',*,*,#11707,.F.);
#16705=ORIENTED_EDGE('',*,*,#11710,.F.);
#16706=ORIENTED_EDGE('',*,*,#11713,.F.);
#16707=ORIENTED_EDGE('',*,*,#11716,.F.);
#16708=ORIENTED_EDGE('',*,*,#11719,.F.);
#16709=ORIENTED_EDGE('',*,*,#11722,.F.);
#16710=ORIENTED_EDGE('',*,*,#11725,.F.);
#16711=ORIENTED_EDGE('',*,*,#11728,.F.);
#16712=ORIENTED_EDGE('',*,*,#11731,.F.);
#16713=ORIENTED_EDGE('',*,*,#11734,.F.);
#16714=ORIENTED_EDGE('',*,*,#11737,.F.);
#16715=ORIENTED_EDGE('',*,*,#11740,.F.);
#16716=ORIENTED_EDGE('',*,*,#11743,.F.);
#16717=ORIENTED_EDGE('',*,*,#11746,.F.);
#16718=ORIENTED_EDGE('',*,*,#11749,.F.);
#16719=ORIENTED_EDGE('',*,*,#11752,.F.);
#16720=ORIENTED_EDGE('',*,*,#11755,.F.);
#16721=ORIENTED_EDGE('',*,*,#11758,.F.);
#16722=ORIENTED_EDGE('',*,*,#11761,.F.);
#16723=ORIENTED_EDGE('',*,*,#11764,.F.);
#16724=ORIENTED_EDGE('',*,*,#11767,.F.);
#16725=ORIENTED_EDGE('',*,*,#11770,.F.);
#16726=ORIENTED_EDGE('',*,*,#11773,.F.);
#16727=ORIENTED_EDGE('',*,*,#11776,.F.);
#16728=ORIENTED_EDGE('',*,*,#11779,.F.);
#16729=ORIENTED_EDGE('',*,*,#11782,.F.);
#16730=ORIENTED_EDGE('',*,*,#11785,.F.);
#16731=ORIENTED_EDGE('',*,*,#11788,.F.);
#16732=ORIENTED_EDGE('',*,*,#11791,.F.);
#16733=ORIENTED_EDGE('',*,*,#11794,.F.);
#16734=ORIENTED_EDGE('',*,*,#11797,.F.);
#16735=ORIENTED_EDGE('',*,*,#11800,.F.);
#16736=ORIENTED_EDGE('',*,*,#11803,.F.);
#16737=ORIENTED_EDGE('',*,*,#11806,.F.);
#16738=ORIENTED_EDGE('',*,*,#11809,.F.);
#16739=ORIENTED_EDGE('',*,*,#11812,.F.);
#16740=ORIENTED_EDGE('',*,*,#11815,.F.);
#16741=ORIENTED_EDGE('',*,*,#11818,.F.);
#16742=ORIENTED_EDGE('',*,*,#11821,.F.);
#16743=ORIENTED_EDGE('',*,*,#11824,.F.);
#16744=ORIENTED_EDGE('',*,*,#11827,.F.);
#16745=ORIENTED_EDGE('',*,*,#11830,.F.);
#16746=ORIENTED_EDGE('',*,*,#11833,.F.);
#16747=ORIENTED_EDGE('',*,*,#11836,.F.);
#16748=ORIENTED_EDGE('',*,*,#11839,.F.);
#16749=ORIENTED_EDGE('',*,*,#12042,.F.);
#16750=ORIENTED_EDGE('',*,*,#12043,.F.);
#16751=ORIENTED_EDGE('',*,*,#12044,.T.);
#16752=ORIENTED_EDGE('',*,*,#12045,.F.);
#16753=ORIENTED_EDGE('',*,*,#12046,.F.);
#16754=ORIENTED_EDGE('',*,*,#12047,.F.);
#16755=ORIENTED_EDGE('',*,*,#12046,.T.);
#16756=ORIENTED_EDGE('',*,*,#12048,.T.);
#16757=ORIENTED_EDGE('',*,*,#12049,.T.);
#16758=ORIENTED_EDGE('',*,*,#12048,.F.);
#16759=ORIENTED_EDGE('',*,*,#12045,.T.);
#16760=ORIENTED_EDGE('',*,*,#12050,.T.);
#16761=ORIENTED_EDGE('',*,*,#12051,.F.);
#16762=ORIENTED_EDGE('',*,*,#12052,.F.);
#16763=ORIENTED_EDGE('',*,*,#12049,.F.);
#16764=ORIENTED_EDGE('',*,*,#12051,.T.);
#16765=ORIENTED_EDGE('',*,*,#12053,.T.);
#16766=ORIENTED_EDGE('',*,*,#12054,.F.);
#16767=ORIENTED_EDGE('',*,*,#12053,.F.);
#16768=ORIENTED_EDGE('',*,*,#12050,.F.);
#16769=ORIENTED_EDGE('',*,*,#12044,.F.);
#16770=ORIENTED_EDGE('',*,*,#12055,.F.);
#16771=ORIENTED_EDGE('',*,*,#12056,.T.);
#16772=ORIENTED_EDGE('',*,*,#12057,.F.);
#16773=ORIENTED_EDGE('',*,*,#12056,.F.);
#16774=ORIENTED_EDGE('',*,*,#12052,.T.);
#16775=ORIENTED_EDGE('',*,*,#12054,.T.);
#16776=ORIENTED_EDGE('',*,*,#12043,.T.);
#16777=ORIENTED_EDGE('',*,*,#12047,.T.);
#16778=ORIENTED_EDGE('',*,*,#12055,.T.);
#16779=ORIENTED_EDGE('',*,*,#12058,.F.);
#16780=ORIENTED_EDGE('',*,*,#12059,.T.);
#16781=ORIENTED_EDGE('',*,*,#12037,.T.);
#16782=ORIENTED_EDGE('',*,*,#11846,.T.);
#16783=ORIENTED_EDGE('',*,*,#11843,.T.);
#16784=ORIENTED_EDGE('',*,*,#12041,.T.);
#16785=ORIENTED_EDGE('',*,*,#12060,.F.);
#16786=ORIENTED_EDGE('',*,*,#12061,.T.);
#16787=ORIENTED_EDGE('',*,*,#12058,.T.);
#16788=ORIENTED_EDGE('',*,*,#12061,.F.);
#16789=ORIENTED_EDGE('',*,*,#12060,.T.);
#16790=ORIENTED_EDGE('',*,*,#12057,.T.);
#16791=ORIENTED_EDGE('',*,*,#11838,.T.);
#16792=ORIENTED_EDGE('',*,*,#12038,.T.);
#16793=ORIENTED_EDGE('',*,*,#12059,.F.);
#16794=ORIENTED_EDGE('',*,*,#12042,.T.);
#17344=CYLINDRICAL_SURFACE('',#20900,0.5941);
#17345=CYLINDRICAL_SURFACE('',#20902,0.5941);
#17346=CYLINDRICAL_SURFACE('',#20903,0.5941);
#17347=CYLINDRICAL_SURFACE('',#20904,0.5941);
#17348=CYLINDRICAL_SURFACE('',#20905,0.5941);
#17349=CYLINDRICAL_SURFACE('',#20906,0.5941);
#17350=CYLINDRICAL_SURFACE('',#20907,0.5941);
#17351=CYLINDRICAL_SURFACE('',#20908,0.5941);
#17352=CYLINDRICAL_SURFACE('',#20909,0.5941);
#17353=CYLINDRICAL_SURFACE('',#20910,0.5941);
#17354=CYLINDRICAL_SURFACE('',#20911,0.5941);
#17355=CYLINDRICAL_SURFACE('',#20912,0.5941);
#17356=CYLINDRICAL_SURFACE('',#20913,0.5941);
#17357=CYLINDRICAL_SURFACE('',#20914,0.5941);
#17358=CYLINDRICAL_SURFACE('',#20915,0.5941);
#17359=CYLINDRICAL_SURFACE('',#20916,0.5941);
#17360=CYLINDRICAL_SURFACE('',#20917,0.5941);
#17361=CYLINDRICAL_SURFACE('',#20918,0.5941);
#17362=CYLINDRICAL_SURFACE('',#20919,0.5941);
#17363=CYLINDRICAL_SURFACE('',#20920,0.5941);
#17364=CYLINDRICAL_SURFACE('',#20921,0.5941);
#17365=CYLINDRICAL_SURFACE('',#20922,0.5941);
#17366=CYLINDRICAL_SURFACE('',#20923,0.5941);
#17367=CYLINDRICAL_SURFACE('',#20924,0.5941);
#17368=CYLINDRICAL_SURFACE('',#20925,0.5941);
#17369=CYLINDRICAL_SURFACE('',#20926,0.5941);
#17370=CYLINDRICAL_SURFACE('',#20927,0.5941);
#17371=CYLINDRICAL_SURFACE('',#20928,0.5941);
#17372=CYLINDRICAL_SURFACE('',#20929,0.5941);
#17373=CYLINDRICAL_SURFACE('',#20930,0.5941);
#17374=CYLINDRICAL_SURFACE('',#20931,0.5941);
#17375=CYLINDRICAL_SURFACE('',#20932,0.5941);
#17376=CYLINDRICAL_SURFACE('',#20933,0.5941);
#17377=CYLINDRICAL_SURFACE('',#20934,0.5941);
#17378=CYLINDRICAL_SURFACE('',#20935,0.5941);
#17379=CYLINDRICAL_SURFACE('',#20936,0.5941);
#17380=CYLINDRICAL_SURFACE('',#20937,0.5941);
#17381=CYLINDRICAL_SURFACE('',#20938,0.5941);
#17382=CYLINDRICAL_SURFACE('',#20939,0.5941);
#17383=CYLINDRICAL_SURFACE('',#20940,0.5941);
#17384=CYLINDRICAL_SURFACE('',#20941,0.5941);
#17385=CYLINDRICAL_SURFACE('',#20942,0.5941);
#17386=CYLINDRICAL_SURFACE('',#20943,0.5941);
#17387=CYLINDRICAL_SURFACE('',#20944,0.5941);
#17388=CYLINDRICAL_SURFACE('',#20945,0.5941);
#17389=CYLINDRICAL_SURFACE('',#20946,0.5941);
#17390=CYLINDRICAL_SURFACE('',#20947,0.5941);
#17391=CYLINDRICAL_SURFACE('',#20948,0.5941);
#17392=CYLINDRICAL_SURFACE('',#20949,0.5941);
#17393=CYLINDRICAL_SURFACE('',#20950,0.5941);
#17394=CYLINDRICAL_SURFACE('',#20951,0.5941);
#17395=CYLINDRICAL_SURFACE('',#20952,0.5941);
#17396=CYLINDRICAL_SURFACE('',#20953,0.5941);
#17397=CYLINDRICAL_SURFACE('',#20954,0.5941);
#17398=CYLINDRICAL_SURFACE('',#20955,0.5941);
#17399=CYLINDRICAL_SURFACE('',#20956,0.5941);
#17400=CYLINDRICAL_SURFACE('',#20957,0.5941);
#17401=CYLINDRICAL_SURFACE('',#20958,0.5941);
#17402=CYLINDRICAL_SURFACE('',#20959,0.5941);
#17403=CYLINDRICAL_SURFACE('',#20960,0.5941);
#17404=CYLINDRICAL_SURFACE('',#20961,0.5941);
#17405=CYLINDRICAL_SURFACE('',#20962,0.5941);
#17406=CYLINDRICAL_SURFACE('',#20963,0.5941);
#17407=CYLINDRICAL_SURFACE('',#20964,0.415875);
#17408=CYLINDRICAL_SURFACE('',#20966,0.415875);
#17409=CYLINDRICAL_SURFACE('',#20968,0.415875);
#17410=CYLINDRICAL_SURFACE('',#20969,0.415875);
#17411=CYLINDRICAL_SURFACE('',#20970,0.415875);
#17412=CYLINDRICAL_SURFACE('',#20971,0.415875);
#17413=CYLINDRICAL_SURFACE('',#20972,0.415875);
#17414=CYLINDRICAL_SURFACE('',#20973,0.415875);
#17415=CYLINDRICAL_SURFACE('',#20974,0.415875);
#17416=CYLINDRICAL_SURFACE('',#20975,0.415875);
#17417=CYLINDRICAL_SURFACE('',#20976,0.415875);
#17418=CYLINDRICAL_SURFACE('',#20977,0.415875);
#17419=CYLINDRICAL_SURFACE('',#20978,0.415875);
#17420=CYLINDRICAL_SURFACE('',#20979,0.415875);
#17421=CYLINDRICAL_SURFACE('',#20980,0.415875);
#17422=CYLINDRICAL_SURFACE('',#20981,0.415875);
#17423=CYLINDRICAL_SURFACE('',#20982,0.415875);
#17424=CYLINDRICAL_SURFACE('',#20983,0.415875);
#17425=CYLINDRICAL_SURFACE('',#20984,0.415875);
#17426=CYLINDRICAL_SURFACE('',#20985,0.415875);
#17427=CYLINDRICAL_SURFACE('',#20986,0.415875);
#17428=CYLINDRICAL_SURFACE('',#20987,0.415875);
#17429=CYLINDRICAL_SURFACE('',#20988,0.415875);
#17430=CYLINDRICAL_SURFACE('',#20989,0.415875);
#17431=CYLINDRICAL_SURFACE('',#20990,0.415875);
#17432=CYLINDRICAL_SURFACE('',#20991,0.415875);
#17433=CYLINDRICAL_SURFACE('',#20992,0.415875);
#17434=CYLINDRICAL_SURFACE('',#20993,0.415875);
#17435=CYLINDRICAL_SURFACE('',#20994,0.415875);
#17436=CYLINDRICAL_SURFACE('',#20995,0.415875);
#17437=CYLINDRICAL_SURFACE('',#20996,0.415875);
#17438=CYLINDRICAL_SURFACE('',#20997,0.415875);
#17439=CYLINDRICAL_SURFACE('',#20998,0.415875);
#17440=CYLINDRICAL_SURFACE('',#20999,0.415875);
#17441=CYLINDRICAL_SURFACE('',#21000,0.415875);
#17442=CYLINDRICAL_SURFACE('',#21001,0.415875);
#17443=CYLINDRICAL_SURFACE('',#21002,0.415875);
#17444=CYLINDRICAL_SURFACE('',#21003,0.415875);
#17445=CYLINDRICAL_SURFACE('',#21004,0.415875);
#17446=CYLINDRICAL_SURFACE('',#21005,0.415875);
#17447=CYLINDRICAL_SURFACE('',#21006,0.415875);
#17448=CYLINDRICAL_SURFACE('',#21007,0.415875);
#17449=CYLINDRICAL_SURFACE('',#21008,0.415875);
#17450=CYLINDRICAL_SURFACE('',#21009,0.415875);
#17451=CYLINDRICAL_SURFACE('',#21010,0.415875);
#17452=CYLINDRICAL_SURFACE('',#21011,0.415875);
#17453=CYLINDRICAL_SURFACE('',#21012,0.415875);
#17454=CYLINDRICAL_SURFACE('',#21013,0.415875);
#17455=CYLINDRICAL_SURFACE('',#21014,0.415875);
#17456=CYLINDRICAL_SURFACE('',#21015,0.415875);
#17457=CYLINDRICAL_SURFACE('',#21016,0.415875);
#17458=CYLINDRICAL_SURFACE('',#21017,0.415875);
#17459=CYLINDRICAL_SURFACE('',#21018,0.415875);
#17460=CYLINDRICAL_SURFACE('',#21019,0.415875);
#17461=CYLINDRICAL_SURFACE('',#21020,0.415875);
#17462=CYLINDRICAL_SURFACE('',#21021,0.415875);
#17463=CYLINDRICAL_SURFACE('',#21022,0.415875);
#17464=CYLINDRICAL_SURFACE('',#21023,0.415875);
#17465=CYLINDRICAL_SURFACE('',#21024,0.415875);
#17466=CYLINDRICAL_SURFACE('',#21025,0.415875);
#17467=CYLINDRICAL_SURFACE('',#21026,0.415875);
#17468=CYLINDRICAL_SURFACE('',#21027,0.415875);
#17469=CYLINDRICAL_SURFACE('',#21028,0.415875);
#17470=CYLINDRICAL_SURFACE('',#21032,0.6);
#17471=CYLINDRICAL_SURFACE('',#21035,0.415875);
#17472=CYLINDRICAL_SURFACE('',#21043,1.);
#17473=CYLINDRICAL_SURFACE('',#21050,1.35);
#17474=CYLINDRICAL_SURFACE('',#21053,0.5941);
#18323=ADVANCED_FACE('',(#2999),#17344,.T.);
#18324=ADVANCED_FACE('',(#3000),#17345,.T.);
#18325=ADVANCED_FACE('',(#3001),#17346,.T.);
#18326=ADVANCED_FACE('',(#3002),#17347,.T.);
#18327=ADVANCED_FACE('',(#3003),#17348,.T.);
#18328=ADVANCED_FACE('',(#3004),#17349,.T.);
#18329=ADVANCED_FACE('',(#3005),#17350,.T.);
#18330=ADVANCED_FACE('',(#3006),#17351,.T.);
#18331=ADVANCED_FACE('',(#3007),#17352,.T.);
#18332=ADVANCED_FACE('',(#3008),#17353,.T.);
#18333=ADVANCED_FACE('',(#3009),#17354,.T.);
#18334=ADVANCED_FACE('',(#3010),#17355,.T.);
#18335=ADVANCED_FACE('',(#3011),#17356,.T.);
#18336=ADVANCED_FACE('',(#3012),#17357,.T.);
#18337=ADVANCED_FACE('',(#3013),#17358,.T.);
#18338=ADVANCED_FACE('',(#3014),#17359,.T.);
#18339=ADVANCED_FACE('',(#3015),#17360,.T.);
#18340=ADVANCED_FACE('',(#3016),#17361,.T.);
#18341=ADVANCED_FACE('',(#3017),#17362,.T.);
#18342=ADVANCED_FACE('',(#3018),#17363,.T.);
#18343=ADVANCED_FACE('',(#3019),#17364,.T.);
#18344=ADVANCED_FACE('',(#3020),#17365,.T.);
#18345=ADVANCED_FACE('',(#3021),#17366,.T.);
#18346=ADVANCED_FACE('',(#3022),#17367,.T.);
#18347=ADVANCED_FACE('',(#3023),#17368,.T.);
#18348=ADVANCED_FACE('',(#3024),#17369,.T.);
#18349=ADVANCED_FACE('',(#3025),#17370,.T.);
#18350=ADVANCED_FACE('',(#3026),#17371,.T.);
#18351=ADVANCED_FACE('',(#3027),#17372,.T.);
#18352=ADVANCED_FACE('',(#3028),#17373,.T.);
#18353=ADVANCED_FACE('',(#3029),#17374,.T.);
#18354=ADVANCED_FACE('',(#3030),#17375,.T.);
#18355=ADVANCED_FACE('',(#3031),#17376,.T.);
#18356=ADVANCED_FACE('',(#3032),#17377,.T.);
#18357=ADVANCED_FACE('',(#3033),#17378,.T.);
#18358=ADVANCED_FACE('',(#3034),#17379,.T.);
#18359=ADVANCED_FACE('',(#3035),#17380,.T.);
#18360=ADVANCED_FACE('',(#3036),#17381,.T.);
#18361=ADVANCED_FACE('',(#3037),#17382,.T.);
#18362=ADVANCED_FACE('',(#3038),#17383,.T.);
#18363=ADVANCED_FACE('',(#3039),#17384,.T.);
#18364=ADVANCED_FACE('',(#3040),#17385,.T.);
#18365=ADVANCED_FACE('',(#3041),#17386,.T.);
#18366=ADVANCED_FACE('',(#3042),#17387,.T.);
#18367=ADVANCED_FACE('',(#3043),#17388,.T.);
#18368=ADVANCED_FACE('',(#3044),#17389,.T.);
#18369=ADVANCED_FACE('',(#3045),#17390,.T.);
#18370=ADVANCED_FACE('',(#3046),#17391,.T.);
#18371=ADVANCED_FACE('',(#3047),#17392,.T.);
#18372=ADVANCED_FACE('',(#3048),#17393,.T.);
#18373=ADVANCED_FACE('',(#3049),#17394,.T.);
#18374=ADVANCED_FACE('',(#3050),#17395,.T.);
#18375=ADVANCED_FACE('',(#3051),#17396,.T.);
#18376=ADVANCED_FACE('',(#3052),#17397,.T.);
#18377=ADVANCED_FACE('',(#3053),#17398,.T.);
#18378=ADVANCED_FACE('',(#3054),#17399,.T.);
#18379=ADVANCED_FACE('',(#3055),#17400,.T.);
#18380=ADVANCED_FACE('',(#3056),#17401,.T.);
#18381=ADVANCED_FACE('',(#3057),#17402,.T.);
#18382=ADVANCED_FACE('',(#3058),#17403,.T.);
#18383=ADVANCED_FACE('',(#3059),#17404,.T.);
#18384=ADVANCED_FACE('',(#3060),#17405,.T.);
#18385=ADVANCED_FACE('',(#3061),#17406,.T.);
#18386=ADVANCED_FACE('',(#3062),#17407,.T.);
#18387=ADVANCED_FACE('',(#3063),#17408,.T.);
#18388=ADVANCED_FACE('',(#3064),#17409,.T.);
#18389=ADVANCED_FACE('',(#3065),#17410,.T.);
#18390=ADVANCED_FACE('',(#3066),#17411,.T.);
#18391=ADVANCED_FACE('',(#3067),#17412,.T.);
#18392=ADVANCED_FACE('',(#3068),#17413,.T.);
#18393=ADVANCED_FACE('',(#3069),#17414,.T.);
#18394=ADVANCED_FACE('',(#3070),#17415,.T.);
#18395=ADVANCED_FACE('',(#3071),#17416,.T.);
#18396=ADVANCED_FACE('',(#3072),#17417,.T.);
#18397=ADVANCED_FACE('',(#3073),#17418,.T.);
#18398=ADVANCED_FACE('',(#3074),#17419,.T.);
#18399=ADVANCED_FACE('',(#3075),#17420,.T.);
#18400=ADVANCED_FACE('',(#3076),#17421,.T.);
#18401=ADVANCED_FACE('',(#3077),#17422,.T.);
#18402=ADVANCED_FACE('',(#3078),#17423,.T.);
#18403=ADVANCED_FACE('',(#3079),#17424,.T.);
#18404=ADVANCED_FACE('',(#3080),#17425,.T.);
#18405=ADVANCED_FACE('',(#3081),#17426,.T.);
#18406=ADVANCED_FACE('',(#3082),#17427,.T.);
#18407=ADVANCED_FACE('',(#3083),#17428,.T.);
#18408=ADVANCED_FACE('',(#3084),#17429,.T.);
#18409=ADVANCED_FACE('',(#3085),#17430,.T.);
#18410=ADVANCED_FACE('',(#3086),#17431,.T.);
#18411=ADVANCED_FACE('',(#3087),#17432,.T.);
#18412=ADVANCED_FACE('',(#3088),#17433,.T.);
#18413=ADVANCED_FACE('',(#3089),#17434,.T.);
#18414=ADVANCED_FACE('',(#3090),#17435,.T.);
#18415=ADVANCED_FACE('',(#3091),#17436,.T.);
#18416=ADVANCED_FACE('',(#3092),#17437,.T.);
#18417=ADVANCED_FACE('',(#3093),#17438,.T.);
#18418=ADVANCED_FACE('',(#3094),#17439,.T.);
#18419=ADVANCED_FACE('',(#3095),#17440,.T.);
#18420=ADVANCED_FACE('',(#3096),#17441,.T.);
#18421=ADVANCED_FACE('',(#3097),#17442,.T.);
#18422=ADVANCED_FACE('',(#3098),#17443,.T.);
#18423=ADVANCED_FACE('',(#3099),#17444,.T.);
#18424=ADVANCED_FACE('',(#3100),#17445,.T.);
#18425=ADVANCED_FACE('',(#3101),#17446,.T.);
#18426=ADVANCED_FACE('',(#3102),#17447,.T.);
#18427=ADVANCED_FACE('',(#3103),#17448,.T.);
#18428=ADVANCED_FACE('',(#3104),#17449,.T.);
#18429=ADVANCED_FACE('',(#3105),#17450,.T.);
#18430=ADVANCED_FACE('',(#3106),#17451,.T.);
#18431=ADVANCED_FACE('',(#3107),#17452,.T.);
#18432=ADVANCED_FACE('',(#3108),#17453,.T.);
#18433=ADVANCED_FACE('',(#3109),#17454,.T.);
#18434=ADVANCED_FACE('',(#3110),#17455,.T.);
#18435=ADVANCED_FACE('',(#3111),#17456,.T.);
#18436=ADVANCED_FACE('',(#3112),#17457,.T.);
#18437=ADVANCED_FACE('',(#3113),#17458,.T.);
#18438=ADVANCED_FACE('',(#3114),#17459,.T.);
#18439=ADVANCED_FACE('',(#3115),#17460,.T.);
#18440=ADVANCED_FACE('',(#3116),#17461,.T.);
#18441=ADVANCED_FACE('',(#3117),#17462,.T.);
#18442=ADVANCED_FACE('',(#3118),#17463,.T.);
#18443=ADVANCED_FACE('',(#3119),#17464,.T.);
#18444=ADVANCED_FACE('',(#3120),#17465,.T.);
#18445=ADVANCED_FACE('',(#3121),#17466,.T.);
#18446=ADVANCED_FACE('',(#3122),#17467,.T.);
#18447=ADVANCED_FACE('',(#3123),#17468,.T.);
#18448=ADVANCED_FACE('',(#3124),#17469,.T.);
#18449=ADVANCED_FACE('',(#3125,#1565),#2110,.T.);
#18450=ADVANCED_FACE('',(#3126),#17470,.T.);
#18451=ADVANCED_FACE('',(#3127),#2111,.F.);
#18452=ADVANCED_FACE('',(#3128),#13,.F.);
#18453=ADVANCED_FACE('',(#3129),#17471,.T.);
#18454=ADVANCED_FACE('',(#3130),#14,.F.);
#18455=ADVANCED_FACE('',(#3131),#2112,.F.);
#18456=ADVANCED_FACE('',(#3132),#2113,.T.);
#18457=ADVANCED_FACE('',(#3133),#2114,.F.);
#18458=ADVANCED_FACE('',(#3134),#2115,.F.);
#18459=ADVANCED_FACE('',(#3135),#2116,.F.);
#18460=ADVANCED_FACE('',(#3136,#1566),#17472,.T.);
#18461=ADVANCED_FACE('',(#3137),#2117,.T.);
#18462=ADVANCED_FACE('',(#3138,#1567),#2118,.F.);
#18463=ADVANCED_FACE('',(#3139),#17473,.T.);
#18464=ADVANCED_FACE('',(#3140,#1568),#2119,.T.);
#18465=ADVANCED_FACE('',(#3141),#17474,.T.);
#18612=CLOSED_SHELL('',(#18323,#18324,#18325,#18326,#18327,#18328,#18329,
#18330,#18331,#18332,#18333,#18334,#18335,#18336,#18337,#18338,#18339,#18340,
#18341,#18342,#18343,#18344,#18345,#18346,#18347,#18348,#18349,#18350,#18351,
#18352,#18353,#18354,#18355,#18356,#18357,#18358,#18359,#18360,#18361,#18362,
#18363,#18364,#18365,#18366,#18367,#18368,#18369,#18370,#18371,#18372,#18373,
#18374,#18375,#18376,#18377,#18378,#18379,#18380,#18381,#18382,#18383,#18384,
#18385,#18386,#18387,#18388,#18389,#18390,#18391,#18392,#18393,#18394,#18395,
#18396,#18397,#18398,#18399,#18400,#18401,#18402,#18403,#18404,#18405,#18406,
#18407,#18408,#18409,#18410,#18411,#18412,#18413,#18414,#18415,#18416,#18417,
#18418,#18419,#18420,#18421,#18422,#18423,#18424,#18425,#18426,#18427,#18428,
#18429,#18430,#18431,#18432,#18433,#18434,#18435,#18436,#18437,#18438,#18439,
#18440,#18441,#18442,#18443,#18444,#18445,#18446,#18447,#18448,#18449,#18450,
#18451,#18452,#18453,#18454,#18455,#18456,#18457,#18458,#18459,#18460,#18461,
#18462,#18463,#18464,#18465));
#20899=AXIS2_PLACEMENT_3D('',#33258,#25618,#25619);
#20900=AXIS2_PLACEMENT_3D('',#33259,#25620,#25621);
#20901=AXIS2_PLACEMENT_3D('',#33284,#25623,#25624);
#20902=AXIS2_PLACEMENT_3D('',#33289,#25625,#25626);
#20903=AXIS2_PLACEMENT_3D('',#33376,#25628,#25629);
#20904=AXIS2_PLACEMENT_3D('',#33466,#25631,#25632);
#20905=AXIS2_PLACEMENT_3D('',#33553,#25634,#25635);
#20906=AXIS2_PLACEMENT_3D('',#33640,#25637,#25638);
#20907=AXIS2_PLACEMENT_3D('',#33727,#25640,#25641);
#20908=AXIS2_PLACEMENT_3D('',#33814,#25643,#25644);
#20909=AXIS2_PLACEMENT_3D('',#33901,#25646,#25647);
#20910=AXIS2_PLACEMENT_3D('',#33973,#25649,#25650);
#20911=AXIS2_PLACEMENT_3D('',#34024,#25652,#25653);
#20912=AXIS2_PLACEMENT_3D('',#34072,#25655,#25656);
#20913=AXIS2_PLACEMENT_3D('',#34120,#25658,#25659);
#20914=AXIS2_PLACEMENT_3D('',#34171,#25661,#25662);
#20915=AXIS2_PLACEMENT_3D('',#34222,#25664,#25665);
#20916=AXIS2_PLACEMENT_3D('',#34270,#25667,#25668);
#20917=AXIS2_PLACEMENT_3D('',#34321,#25670,#25671);
#20918=AXIS2_PLACEMENT_3D('',#34372,#25673,#25674);
#20919=AXIS2_PLACEMENT_3D('',#34420,#25676,#25677);
#20920=AXIS2_PLACEMENT_3D('',#34468,#25679,#25680);
#20921=AXIS2_PLACEMENT_3D('',#34519,#25682,#25683);
#20922=AXIS2_PLACEMENT_3D('',#34570,#25685,#25686);
#20923=AXIS2_PLACEMENT_3D('',#34618,#25688,#25689);
#20924=AXIS2_PLACEMENT_3D('',#34669,#25691,#25692);
#20925=AXIS2_PLACEMENT_3D('',#34720,#25694,#25695);
#20926=AXIS2_PLACEMENT_3D('',#34768,#25697,#25698);
#20927=AXIS2_PLACEMENT_3D('',#34816,#25700,#25701);
#20928=AXIS2_PLACEMENT_3D('',#34867,#25703,#25704);
#20929=AXIS2_PLACEMENT_3D('',#34918,#25706,#25707);
#20930=AXIS2_PLACEMENT_3D('',#34966,#25709,#25710);
#20931=AXIS2_PLACEMENT_3D('',#35017,#25712,#25713);
#20932=AXIS2_PLACEMENT_3D('',#35068,#25715,#25716);
#20933=AXIS2_PLACEMENT_3D('',#35116,#25718,#25719);
#20934=AXIS2_PLACEMENT_3D('',#35164,#25721,#25722);
#20935=AXIS2_PLACEMENT_3D('',#35215,#25724,#25725);
#20936=AXIS2_PLACEMENT_3D('',#35266,#25727,#25728);
#20937=AXIS2_PLACEMENT_3D('',#35314,#25730,#25731);
#20938=AXIS2_PLACEMENT_3D('',#35365,#25733,#25734);
#20939=AXIS2_PLACEMENT_3D('',#35416,#25736,#25737);
#20940=AXIS2_PLACEMENT_3D('',#35464,#25739,#25740);
#20941=AXIS2_PLACEMENT_3D('',#35512,#25742,#25743);
#20942=AXIS2_PLACEMENT_3D('',#35563,#25745,#25746);
#20943=AXIS2_PLACEMENT_3D('',#35614,#25748,#25749);
#20944=AXIS2_PLACEMENT_3D('',#35662,#25751,#25752);
#20945=AXIS2_PLACEMENT_3D('',#35713,#25754,#25755);
#20946=AXIS2_PLACEMENT_3D('',#35764,#25757,#25758);
#20947=AXIS2_PLACEMENT_3D('',#35812,#25760,#25761);
#20948=AXIS2_PLACEMENT_3D('',#35860,#25763,#25764);
#20949=AXIS2_PLACEMENT_3D('',#35911,#25766,#25767);
#20950=AXIS2_PLACEMENT_3D('',#35962,#25769,#25770);
#20951=AXIS2_PLACEMENT_3D('',#36010,#25772,#25773);
#20952=AXIS2_PLACEMENT_3D('',#36061,#25775,#25776);
#20953=AXIS2_PLACEMENT_3D('',#36112,#25778,#25779);
#20954=AXIS2_PLACEMENT_3D('',#36160,#25781,#25782);
#20955=AXIS2_PLACEMENT_3D('',#36208,#25784,#25785);
#20956=AXIS2_PLACEMENT_3D('',#36259,#25787,#25788);
#20957=AXIS2_PLACEMENT_3D('',#36325,#25790,#25791);
#20958=AXIS2_PLACEMENT_3D('',#36415,#25793,#25794);
#20959=AXIS2_PLACEMENT_3D('',#36502,#25796,#25797);
#20960=AXIS2_PLACEMENT_3D('',#36589,#25799,#25800);
#20961=AXIS2_PLACEMENT_3D('',#36676,#25802,#25803);
#20962=AXIS2_PLACEMENT_3D('',#36763,#25805,#25806);
#20963=AXIS2_PLACEMENT_3D('',#36850,#25808,#25809);
#20964=AXIS2_PLACEMENT_3D('',#36940,#25811,#25812);
#20965=AXIS2_PLACEMENT_3D('',#36949,#25814,#25815);
#20966=AXIS2_PLACEMENT_3D('',#36950,#25816,#25817);
#20967=AXIS2_PLACEMENT_3D('',#36972,#25819,#25820);
#20968=AXIS2_PLACEMENT_3D('',#36986,#25821,#25822);
#20969=AXIS2_PLACEMENT_3D('',#37024,#25824,#25825);
#20970=AXIS2_PLACEMENT_3D('',#37060,#25827,#25828);
#20971=AXIS2_PLACEMENT_3D('',#37098,#25830,#25831);
#20972=AXIS2_PLACEMENT_3D('',#37134,#25833,#25834);
#20973=AXIS2_PLACEMENT_3D('',#37172,#25836,#25837);
#20974=AXIS2_PLACEMENT_3D('',#37209,#25839,#25840);
#20975=AXIS2_PLACEMENT_3D('',#37244,#25842,#25843);
#20976=AXIS2_PLACEMENT_3D('',#37271,#25845,#25846);
#20977=AXIS2_PLACEMENT_3D('',#37295,#25848,#25849);
#20978=AXIS2_PLACEMENT_3D('',#37319,#25851,#25852);
#20979=AXIS2_PLACEMENT_3D('',#37343,#25854,#25855);
#20980=AXIS2_PLACEMENT_3D('',#37369,#25857,#25858);
#20981=AXIS2_PLACEMENT_3D('',#37393,#25860,#25861);
#20982=AXIS2_PLACEMENT_3D('',#37417,#25863,#25864);
#20983=AXIS2_PLACEMENT_3D('',#37443,#25866,#25867);
#20984=AXIS2_PLACEMENT_3D('',#37467,#25869,#25870);
#20985=AXIS2_PLACEMENT_3D('',#37491,#25872,#25873);
#20986=AXIS2_PLACEMENT_3D('',#37515,#25875,#25876);
#20987=AXIS2_PLACEMENT_3D('',#37541,#25878,#25879);
#20988=AXIS2_PLACEMENT_3D('',#37565,#25881,#25882);
#20989=AXIS2_PLACEMENT_3D('',#37589,#25884,#25885);
#20990=AXIS2_PLACEMENT_3D('',#37615,#25887,#25888);
#20991=AXIS2_PLACEMENT_3D('',#37639,#25890,#25891);
#20992=AXIS2_PLACEMENT_3D('',#37663,#25893,#25894);
#20993=AXIS2_PLACEMENT_3D('',#37687,#25896,#25897);
#20994=AXIS2_PLACEMENT_3D('',#37713,#25899,#25900);
#20995=AXIS2_PLACEMENT_3D('',#37737,#25902,#25903);
#20996=AXIS2_PLACEMENT_3D('',#37761,#25905,#25906);
#20997=AXIS2_PLACEMENT_3D('',#37787,#25908,#25909);
#20998=AXIS2_PLACEMENT_3D('',#37811,#25911,#25912);
#20999=AXIS2_PLACEMENT_3D('',#37835,#25914,#25915);
#21000=AXIS2_PLACEMENT_3D('',#37859,#25917,#25918);
#21001=AXIS2_PLACEMENT_3D('',#37885,#25920,#25921);
#21002=AXIS2_PLACEMENT_3D('',#37909,#25923,#25924);
#21003=AXIS2_PLACEMENT_3D('',#37933,#25926,#25927);
#21004=AXIS2_PLACEMENT_3D('',#37959,#25929,#25930);
#21005=AXIS2_PLACEMENT_3D('',#37983,#25932,#25933);
#21006=AXIS2_PLACEMENT_3D('',#38007,#25935,#25936);
#21007=AXIS2_PLACEMENT_3D('',#38031,#25938,#25939);
#21008=AXIS2_PLACEMENT_3D('',#38057,#25941,#25942);
#21009=AXIS2_PLACEMENT_3D('',#38081,#25944,#25945);
#21010=AXIS2_PLACEMENT_3D('',#38105,#25947,#25948);
#21011=AXIS2_PLACEMENT_3D('',#38131,#25950,#25951);
#21012=AXIS2_PLACEMENT_3D('',#38155,#25953,#25954);
#21013=AXIS2_PLACEMENT_3D('',#38179,#25956,#25957);
#21014=AXIS2_PLACEMENT_3D('',#38203,#25959,#25960);
#21015=AXIS2_PLACEMENT_3D('',#38229,#25962,#25963);
#21016=AXIS2_PLACEMENT_3D('',#38253,#25965,#25966);
#21017=AXIS2_PLACEMENT_3D('',#38277,#25968,#25969);
#21018=AXIS2_PLACEMENT_3D('',#38303,#25971,#25972);
#21019=AXIS2_PLACEMENT_3D('',#38327,#25974,#25975);
#21020=AXIS2_PLACEMENT_3D('',#38351,#25977,#25978);
#21021=AXIS2_PLACEMENT_3D('',#38376,#25980,#25981);
#21022=AXIS2_PLACEMENT_3D('',#38403,#25983,#25984);
#21023=AXIS2_PLACEMENT_3D('',#38440,#25986,#25987);
#21024=AXIS2_PLACEMENT_3D('',#38476,#25989,#25990);
#21025=AXIS2_PLACEMENT_3D('',#38514,#25992,#25993);
#21026=AXIS2_PLACEMENT_3D('',#38550,#25995,#25996);
#21027=AXIS2_PLACEMENT_3D('',#38588,#25998,#25999);
#21028=AXIS2_PLACEMENT_3D('',#38625,#26001,#26002);
#21029=AXIS2_PLACEMENT_3D('',#38662,#26004,#26005);
#21030=AXIS2_PLACEMENT_3D('',#38664,#26006,#26007);
#21031=AXIS2_PLACEMENT_3D('',#38741,#26008,#26009);
#21032=AXIS2_PLACEMENT_3D('',#38742,#26010,#26011);
#21033=AXIS2_PLACEMENT_3D('',#38745,#26013,#26014);
#21034=AXIS2_PLACEMENT_3D('',#38746,#26015,#26016);
#21035=AXIS2_PLACEMENT_3D('',#40820,#26017,#26018);
#21036=AXIS2_PLACEMENT_3D('',#42875,#26019,#26020);
#21037=AXIS2_PLACEMENT_3D('',#42884,#26025,#26026);
#21038=AXIS2_PLACEMENT_3D('',#42886,#26027,#26028);
#21039=AXIS2_PLACEMENT_3D('',#42890,#26031,#26032);
#21040=AXIS2_PLACEMENT_3D('',#42894,#26035,#26036);
#21041=AXIS2_PLACEMENT_3D('',#42898,#26039,#26040);
#21042=AXIS2_PLACEMENT_3D('',#42899,#26041,#26042);
#21043=AXIS2_PLACEMENT_3D('',#42900,#26043,#26044);
#21044=AXIS2_PLACEMENT_3D('',#42902,#26045,#26046);
#21045=AXIS2_PLACEMENT_3D('',#42905,#26048,#26049);
#21046=AXIS2_PLACEMENT_3D('',#42906,#26050,#26051);
#21047=AXIS2_PLACEMENT_3D('',#42907,#26052,#26053);
#21048=AXIS2_PLACEMENT_3D('',#42909,#26054,#26055);
#21049=AXIS2_PLACEMENT_3D('',#42910,#26056,#26057);
#21050=AXIS2_PLACEMENT_3D('',#42911,#26058,#26059);
#21051=AXIS2_PLACEMENT_3D('',#42913,#26060,#26061);
#21052=AXIS2_PLACEMENT_3D('',#42915,#26063,#26064);
#21053=AXIS2_PLACEMENT_3D('',#42916,#26065,#26066);
#25618=DIRECTION('axis',(0.,0.,1.));
#25619=DIRECTION('refdir',(1.,0.,0.));
#25620=DIRECTION('center_axis',(1.,0.,0.));
#25621=DIRECTION('ref_axis',(0.,0.975560628713931,0.219730425074181));
#25622=DIRECTION('',(-1.,0.,0.));
#25623=DIRECTION('center_axis',(-1.,0.,0.));
#25624=DIRECTION('ref_axis',(0.,0.,-1.));
#25625=DIRECTION('center_axis',(1.,0.,0.));
#25626=DIRECTION('ref_axis',(0.,0.,-1.));
#25627=DIRECTION('',(-1.,0.,0.));
#25628=DIRECTION('center_axis',(1.,0.,0.));
#25629=DIRECTION('ref_axis',(0.,0.,-1.));
#25630=DIRECTION('',(-1.,0.,0.));
#25631=DIRECTION('center_axis',(1.,0.,0.));
#25632=DIRECTION('ref_axis',(0.,0.,-1.));
#25633=DIRECTION('',(-1.,0.,0.));
#25634=DIRECTION('center_axis',(1.,0.,0.));
#25635=DIRECTION('ref_axis',(0.,0.,-1.));
#25636=DIRECTION('',(-1.,0.,0.));
#25637=DIRECTION('center_axis',(1.,0.,0.));
#25638=DIRECTION('ref_axis',(0.,0.,-1.));
#25639=DIRECTION('',(-1.,0.,0.));
#25640=DIRECTION('center_axis',(1.,0.,0.));
#25641=DIRECTION('ref_axis',(0.,0.,-1.));
#25642=DIRECTION('',(-1.,0.,0.));
#25643=DIRECTION('center_axis',(1.,0.,0.));
#25644=DIRECTION('ref_axis',(0.,0.,-1.));
#25645=DIRECTION('',(-1.,0.,0.));
#25646=DIRECTION('center_axis',(1.,0.,0.));
#25647=DIRECTION('ref_axis',(0.,0.,-1.));
#25648=DIRECTION('',(-1.,0.,0.));
#25649=DIRECTION('center_axis',(1.,0.,0.));
#25650=DIRECTION('ref_axis',(0.,0.,-1.));
#25651=DIRECTION('',(-1.,0.,0.));
#25652=DIRECTION('center_axis',(1.,0.,0.));
#25653=DIRECTION('ref_axis',(0.,0.,-1.));
#25654=DIRECTION('',(-1.,0.,0.));
#25655=DIRECTION('center_axis',(1.,0.,0.));
#25656=DIRECTION('ref_axis',(0.,0.,-1.));
#25657=DIRECTION('',(-1.,0.,0.));
#25658=DIRECTION('center_axis',(1.,0.,0.));
#25659=DIRECTION('ref_axis',(0.,0.,-1.));
#25660=DIRECTION('',(-1.,0.,0.));
#25661=DIRECTION('center_axis',(1.,0.,0.));
#25662=DIRECTION('ref_axis',(0.,0.,-1.));
#25663=DIRECTION('',(-1.,0.,0.));
#25664=DIRECTION('center_axis',(1.,0.,0.));
#25665=DIRECTION('ref_axis',(0.,0.,-1.));
#25666=DIRECTION('',(-1.,0.,0.));
#25667=DIRECTION('center_axis',(1.,0.,0.));
#25668=DIRECTION('ref_axis',(0.,0.,-1.));
#25669=DIRECTION('',(-1.,0.,0.));
#25670=DIRECTION('center_axis',(1.,0.,0.));
#25671=DIRECTION('ref_axis',(0.,0.,-1.));
#25672=DIRECTION('',(-1.,0.,0.));
#25673=DIRECTION('center_axis',(1.,0.,0.));
#25674=DIRECTION('ref_axis',(0.,0.,-1.));
#25675=DIRECTION('',(-1.,0.,0.));
#25676=DIRECTION('center_axis',(1.,0.,0.));
#25677=DIRECTION('ref_axis',(0.,0.,-1.));
#25678=DIRECTION('',(-1.,0.,0.));
#25679=DIRECTION('center_axis',(1.,0.,0.));
#25680=DIRECTION('ref_axis',(0.,0.,-1.));
#25681=DIRECTION('',(-1.,0.,0.));
#25682=DIRECTION('center_axis',(1.,0.,0.));
#25683=DIRECTION('ref_axis',(0.,0.,-1.));
#25684=DIRECTION('',(-1.,0.,0.));
#25685=DIRECTION('center_axis',(1.,0.,0.));
#25686=DIRECTION('ref_axis',(0.,0.,-1.));
#25687=DIRECTION('',(-1.,0.,0.));
#25688=DIRECTION('center_axis',(1.,0.,0.));
#25689=DIRECTION('ref_axis',(0.,0.,-1.));
#25690=DIRECTION('',(-1.,0.,0.));
#25691=DIRECTION('center_axis',(1.,0.,0.));
#25692=DIRECTION('ref_axis',(0.,0.,-1.));
#25693=DIRECTION('',(-1.,0.,0.));
#25694=DIRECTION('center_axis',(1.,0.,0.));
#25695=DIRECTION('ref_axis',(0.,0.,-1.));
#25696=DIRECTION('',(-1.,0.,0.));
#25697=DIRECTION('center_axis',(1.,0.,0.));
#25698=DIRECTION('ref_axis',(0.,0.,-1.));
#25699=DIRECTION('',(-1.,0.,0.));
#25700=DIRECTION('center_axis',(1.,0.,0.));
#25701=DIRECTION('ref_axis',(0.,0.,-1.));
#25702=DIRECTION('',(-1.,0.,0.));
#25703=DIRECTION('center_axis',(1.,0.,0.));
#25704=DIRECTION('ref_axis',(0.,0.,-1.));
#25705=DIRECTION('',(-1.,0.,0.));
#25706=DIRECTION('center_axis',(1.,0.,0.));
#25707=DIRECTION('ref_axis',(0.,0.,-1.));
#25708=DIRECTION('',(-1.,0.,0.));
#25709=DIRECTION('center_axis',(1.,0.,0.));
#25710=DIRECTION('ref_axis',(0.,0.,-1.));
#25711=DIRECTION('',(-1.,0.,0.));
#25712=DIRECTION('center_axis',(1.,0.,0.));
#25713=DIRECTION('ref_axis',(0.,0.,-1.));
#25714=DIRECTION('',(-1.,0.,0.));
#25715=DIRECTION('center_axis',(1.,0.,0.));
#25716=DIRECTION('ref_axis',(0.,0.,-1.));
#25717=DIRECTION('',(-1.,0.,0.));
#25718=DIRECTION('center_axis',(1.,0.,0.));
#25719=DIRECTION('ref_axis',(0.,0.,-1.));
#25720=DIRECTION('',(-1.,0.,0.));
#25721=DIRECTION('center_axis',(1.,0.,0.));
#25722=DIRECTION('ref_axis',(0.,0.,-1.));
#25723=DIRECTION('',(-1.,0.,0.));
#25724=DIRECTION('center_axis',(1.,0.,0.));
#25725=DIRECTION('ref_axis',(0.,0.,-1.));
#25726=DIRECTION('',(-1.,0.,0.));
#25727=DIRECTION('center_axis',(1.,0.,0.));
#25728=DIRECTION('ref_axis',(0.,0.,-1.));
#25729=DIRECTION('',(-1.,0.,0.));
#25730=DIRECTION('center_axis',(1.,0.,0.));
#25731=DIRECTION('ref_axis',(0.,0.,-1.));
#25732=DIRECTION('',(-1.,0.,0.));
#25733=DIRECTION('center_axis',(1.,0.,0.));
#25734=DIRECTION('ref_axis',(0.,0.,-1.));
#25735=DIRECTION('',(-1.,0.,0.));
#25736=DIRECTION('center_axis',(1.,0.,0.));
#25737=DIRECTION('ref_axis',(0.,0.,-1.));
#25738=DIRECTION('',(-1.,0.,0.));
#25739=DIRECTION('center_axis',(1.,0.,0.));
#25740=DIRECTION('ref_axis',(0.,0.,-1.));
#25741=DIRECTION('',(-1.,0.,0.));
#25742=DIRECTION('center_axis',(1.,0.,0.));
#25743=DIRECTION('ref_axis',(0.,0.,-1.));
#25744=DIRECTION('',(-1.,0.,0.));
#25745=DIRECTION('center_axis',(1.,0.,0.));
#25746=DIRECTION('ref_axis',(0.,0.,-1.));
#25747=DIRECTION('',(-1.,0.,0.));
#25748=DIRECTION('center_axis',(1.,0.,0.));
#25749=DIRECTION('ref_axis',(0.,0.,-1.));
#25750=DIRECTION('',(-1.,0.,0.));
#25751=DIRECTION('center_axis',(1.,0.,0.));
#25752=DIRECTION('ref_axis',(0.,0.,-1.));
#25753=DIRECTION('',(-1.,0.,0.));
#25754=DIRECTION('center_axis',(1.,0.,0.));
#25755=DIRECTION('ref_axis',(0.,0.,-1.));
#25756=DIRECTION('',(-1.,0.,0.));
#25757=DIRECTION('center_axis',(1.,0.,0.));
#25758=DIRECTION('ref_axis',(0.,0.,-1.));
#25759=DIRECTION('',(-1.,0.,0.));
#25760=DIRECTION('center_axis',(1.,0.,0.));
#25761=DIRECTION('ref_axis',(0.,0.,-1.));
#25762=DIRECTION('',(-1.,0.,0.));
#25763=DIRECTION('center_axis',(1.,0.,0.));
#25764=DIRECTION('ref_axis',(0.,0.,-1.));
#25765=DIRECTION('',(-1.,0.,0.));
#25766=DIRECTION('center_axis',(1.,0.,0.));
#25767=DIRECTION('ref_axis',(0.,0.,-1.));
#25768=DIRECTION('',(-1.,0.,0.));
#25769=DIRECTION('center_axis',(1.,0.,0.));
#25770=DIRECTION('ref_axis',(0.,0.,-1.));
#25771=DIRECTION('',(-1.,0.,0.));
#25772=DIRECTION('center_axis',(1.,0.,0.));
#25773=DIRECTION('ref_axis',(0.,0.,-1.));
#25774=DIRECTION('',(-1.,0.,0.));
#25775=DIRECTION('center_axis',(1.,0.,0.));
#25776=DIRECTION('ref_axis',(0.,0.,-1.));
#25777=DIRECTION('',(-1.,0.,0.));
#25778=DIRECTION('center_axis',(1.,0.,0.));
#25779=DIRECTION('ref_axis',(0.,0.,-1.));
#25780=DIRECTION('',(-1.,0.,0.));
#25781=DIRECTION('center_axis',(1.,0.,0.));
#25782=DIRECTION('ref_axis',(0.,0.,-1.));
#25783=DIRECTION('',(-1.,0.,0.));
#25784=DIRECTION('center_axis',(1.,0.,0.));
#25785=DIRECTION('ref_axis',(0.,0.,-1.));
#25786=DIRECTION('',(-1.,0.,0.));
#25787=DIRECTION('center_axis',(1.,0.,0.));
#25788=DIRECTION('ref_axis',(0.,0.,-1.));
#25789=DIRECTION('',(-1.,0.,0.));
#25790=DIRECTION('center_axis',(1.,0.,0.));
#25791=DIRECTION('ref_axis',(0.,0.,-1.));
#25792=DIRECTION('',(-1.,0.,0.));
#25793=DIRECTION('center_axis',(1.,0.,0.));
#25794=DIRECTION('ref_axis',(0.,0.,-1.));
#25795=DIRECTION('',(-1.,0.,0.));
#25796=DIRECTION('center_axis',(1.,0.,0.));
#25797=DIRECTION('ref_axis',(0.,0.,-1.));
#25798=DIRECTION('',(-1.,0.,0.));
#25799=DIRECTION('center_axis',(1.,0.,0.));
#25800=DIRECTION('ref_axis',(0.,0.,-1.));
#25801=DIRECTION('',(-1.,0.,0.));
#25802=DIRECTION('center_axis',(1.,0.,0.));
#25803=DIRECTION('ref_axis',(0.,0.,-1.));
#25804=DIRECTION('',(-1.,0.,0.));
#25805=DIRECTION('center_axis',(1.,0.,0.));
#25806=DIRECTION('ref_axis',(0.,0.,-1.));
#25807=DIRECTION('',(-1.,0.,0.));
#25808=DIRECTION('center_axis',(1.,0.,0.));
#25809=DIRECTION('ref_axis',(0.,0.,-1.));
#25810=DIRECTION('',(-1.,0.,0.));
#25811=DIRECTION('center_axis',(1.,0.,0.));
#25812=DIRECTION('ref_axis',(0.,-1.17203152359781E-12,-1.));
#25813=DIRECTION('',(1.,0.,0.));
#25814=DIRECTION('center_axis',(1.,0.,0.));
#25815=DIRECTION('ref_axis',(0.,-1.17203152359781E-12,-1.));
#25816=DIRECTION('center_axis',(1.,0.,0.));
#25817=DIRECTION('ref_axis',(0.,-1.17203152359781E-12,-1.));
#25818=DIRECTION('',(1.,0.,0.));
#25819=DIRECTION('center_axis',(1.,0.,0.));
#25820=DIRECTION('ref_axis',(0.,-1.17203152359781E-12,-1.));
#25821=DIRECTION('center_axis',(1.,0.,0.));
#25822=DIRECTION('ref_axis',(0.,-1.17203152359781E-12,-1.));
#25823=DIRECTION('',(1.,0.,0.));
#25824=DIRECTION('center_axis',(1.,0.,0.));
#25825=DIRECTION('ref_axis',(0.,-1.17203152359781E-12,-1.));
#25826=DIRECTION('',(1.,0.,0.));
#25827=DIRECTION('center_axis',(1.,0.,0.));
#25828=DIRECTION('ref_axis',(0.,-1.17203152359781E-12,-1.));
#25829=DIRECTION('',(1.,0.,0.));
#25830=DIRECTION('center_axis',(1.,0.,0.));
#25831=DIRECTION('ref_axis',(0.,-1.17203152359781E-12,-1.));
#25832=DIRECTION('',(1.,0.,0.));
#25833=DIRECTION('center_axis',(1.,0.,0.));
#25834=DIRECTION('ref_axis',(0.,-1.17203152359781E-12,-1.));
#25835=DIRECTION('',(1.,0.,0.));
#25836=DIRECTION('center_axis',(1.,0.,0.));
#25837=DIRECTION('ref_axis',(0.,-1.17203152359781E-12,-1.));
#25838=DIRECTION('',(1.,0.,0.));
#25839=DIRECTION('center_axis',(1.,0.,0.));
#25840=DIRECTION('ref_axis',(0.,-1.17203152359781E-12,-1.));
#25841=DIRECTION('',(1.,0.,0.));
#25842=DIRECTION('center_axis',(1.,0.,0.));
#25843=DIRECTION('ref_axis',(0.,-1.17203152359781E-12,-1.));
#25844=DIRECTION('',(1.,0.,0.));
#25845=DIRECTION('center_axis',(1.,0.,0.));
#25846=DIRECTION('ref_axis',(0.,-1.17203152359781E-12,-1.));
#25847=DIRECTION('',(1.,0.,0.));
#25848=DIRECTION('center_axis',(1.,0.,0.));
#25849=DIRECTION('ref_axis',(0.,-1.17203152359781E-12,-1.));
#25850=DIRECTION('',(1.,0.,0.));
#25851=DIRECTION('center_axis',(1.,0.,0.));
#25852=DIRECTION('ref_axis',(0.,-1.17203152359781E-12,-1.));
#25853=DIRECTION('',(1.,0.,0.));
#25854=DIRECTION('center_axis',(1.,0.,0.));
#25855=DIRECTION('ref_axis',(0.,-1.17203152359781E-12,-1.));
#25856=DIRECTION('',(1.,0.,0.));
#25857=DIRECTION('center_axis',(1.,0.,0.));
#25858=DIRECTION('ref_axis',(0.,-1.17203152359781E-12,-1.));
#25859=DIRECTION('',(1.,0.,0.));
#25860=DIRECTION('center_axis',(1.,0.,0.));
#25861=DIRECTION('ref_axis',(0.,-1.17203152359781E-12,-1.));
#25862=DIRECTION('',(1.,0.,0.));
#25863=DIRECTION('center_axis',(1.,0.,0.));
#25864=DIRECTION('ref_axis',(0.,-1.17203152359781E-12,-1.));
#25865=DIRECTION('',(1.,0.,0.));
#25866=DIRECTION('center_axis',(1.,0.,0.));
#25867=DIRECTION('ref_axis',(0.,-1.17203152359781E-12,-1.));
#25868=DIRECTION('',(1.,0.,0.));
#25869=DIRECTION('center_axis',(1.,0.,0.));
#25870=DIRECTION('ref_axis',(0.,-1.17203152359781E-12,-1.));
#25871=DIRECTION('',(1.,0.,0.));
#25872=DIRECTION('center_axis',(1.,0.,0.));
#25873=DIRECTION('ref_axis',(0.,-1.17203152359781E-12,-1.));
#25874=DIRECTION('',(1.,0.,0.));
#25875=DIRECTION('center_axis',(1.,0.,0.));
#25876=DIRECTION('ref_axis',(0.,-1.17203152359781E-12,-1.));
#25877=DIRECTION('',(1.,0.,0.));
#25878=DIRECTION('center_axis',(1.,0.,0.));
#25879=DIRECTION('ref_axis',(0.,-1.17203152359781E-12,-1.));
#25880=DIRECTION('',(1.,0.,0.));
#25881=DIRECTION('center_axis',(1.,0.,0.));
#25882=DIRECTION('ref_axis',(0.,-1.17203152359781E-12,-1.));
#25883=DIRECTION('',(1.,0.,0.));
#25884=DIRECTION('center_axis',(1.,0.,0.));
#25885=DIRECTION('ref_axis',(0.,-1.17203152359781E-12,-1.));
#25886=DIRECTION('',(1.,0.,0.));
#25887=DIRECTION('center_axis',(1.,0.,0.));
#25888=DIRECTION('ref_axis',(0.,-1.17203152359781E-12,-1.));
#25889=DIRECTION('',(1.,0.,0.));
#25890=DIRECTION('center_axis',(1.,0.,0.));
#25891=DIRECTION('ref_axis',(0.,-1.17203152359781E-12,-1.));
#25892=DIRECTION('',(1.,0.,0.));
#25893=DIRECTION('center_axis',(1.,0.,0.));
#25894=DIRECTION('ref_axis',(0.,-1.17203152359781E-12,-1.));
#25895=DIRECTION('',(1.,0.,0.));
#25896=DIRECTION('center_axis',(1.,0.,0.));
#25897=DIRECTION('ref_axis',(0.,-1.17203152359781E-12,-1.));
#25898=DIRECTION('',(1.,0.,0.));
#25899=DIRECTION('center_axis',(1.,0.,0.));
#25900=DIRECTION('ref_axis',(0.,-1.17203152359781E-12,-1.));
#25901=DIRECTION('',(1.,0.,0.));
#25902=DIRECTION('center_axis',(1.,0.,0.));
#25903=DIRECTION('ref_axis',(0.,-1.17203152359781E-12,-1.));
#25904=DIRECTION('',(1.,0.,0.));
#25905=DIRECTION('center_axis',(1.,0.,0.));
#25906=DIRECTION('ref_axis',(0.,-1.17203152359781E-12,-1.));
#25907=DIRECTION('',(1.,0.,0.));
#25908=DIRECTION('center_axis',(1.,0.,0.));
#25909=DIRECTION('ref_axis',(0.,-1.17203152359781E-12,-1.));
#25910=DIRECTION('',(1.,0.,0.));
#25911=DIRECTION('center_axis',(1.,0.,0.));
#25912=DIRECTION('ref_axis',(0.,-1.17203152359781E-12,-1.));
#25913=DIRECTION('',(1.,0.,0.));
#25914=DIRECTION('center_axis',(1.,0.,0.));
#25915=DIRECTION('ref_axis',(0.,-1.17203152359781E-12,-1.));
#25916=DIRECTION('',(1.,0.,0.));
#25917=DIRECTION('center_axis',(1.,0.,0.));
#25918=DIRECTION('ref_axis',(0.,-1.17203152359781E-12,-1.));
#25919=DIRECTION('',(1.,0.,0.));
#25920=DIRECTION('center_axis',(1.,0.,0.));
#25921=DIRECTION('ref_axis',(0.,-1.17203152359781E-12,-1.));
#25922=DIRECTION('',(1.,0.,0.));
#25923=DIRECTION('center_axis',(1.,0.,0.));
#25924=DIRECTION('ref_axis',(0.,-1.17203152359781E-12,-1.));
#25925=DIRECTION('',(1.,0.,0.));
#25926=DIRECTION('center_axis',(1.,0.,0.));
#25927=DIRECTION('ref_axis',(0.,-1.17203152359781E-12,-1.));
#25928=DIRECTION('',(1.,0.,0.));
#25929=DIRECTION('center_axis',(1.,0.,0.));
#25930=DIRECTION('ref_axis',(0.,-1.17203152359781E-12,-1.));
#25931=DIRECTION('',(1.,0.,0.));
#25932=DIRECTION('center_axis',(1.,0.,0.));
#25933=DIRECTION('ref_axis',(0.,-1.17203152359781E-12,-1.));
#25934=DIRECTION('',(1.,0.,0.));
#25935=DIRECTION('center_axis',(1.,0.,0.));
#25936=DIRECTION('ref_axis',(0.,-1.17203152359781E-12,-1.));
#25937=DIRECTION('',(1.,0.,0.));
#25938=DIRECTION('center_axis',(1.,0.,0.));
#25939=DIRECTION('ref_axis',(0.,-1.17203152359781E-12,-1.));
#25940=DIRECTION('',(1.,0.,0.));
#25941=DIRECTION('center_axis',(1.,0.,0.));
#25942=DIRECTION('ref_axis',(0.,-1.17203152359781E-12,-1.));
#25943=DIRECTION('',(1.,0.,0.));
#25944=DIRECTION('center_axis',(1.,0.,0.));
#25945=DIRECTION('ref_axis',(0.,-1.17203152359781E-12,-1.));
#25946=DIRECTION('',(1.,0.,0.));
#25947=DIRECTION('center_axis',(1.,0.,0.));
#25948=DIRECTION('ref_axis',(0.,-1.17203152359781E-12,-1.));
#25949=DIRECTION('',(1.,0.,0.));
#25950=DIRECTION('center_axis',(1.,0.,0.));
#25951=DIRECTION('ref_axis',(0.,-1.17203152359781E-12,-1.));
#25952=DIRECTION('',(1.,0.,0.));
#25953=DIRECTION('center_axis',(1.,0.,0.));
#25954=DIRECTION('ref_axis',(0.,-1.17203152359781E-12,-1.));
#25955=DIRECTION('',(1.,0.,0.));
#25956=DIRECTION('center_axis',(1.,0.,0.));
#25957=DIRECTION('ref_axis',(0.,-1.17203152359781E-12,-1.));
#25958=DIRECTION('',(1.,0.,0.));
#25959=DIRECTION('center_axis',(1.,0.,0.));
#25960=DIRECTION('ref_axis',(0.,-1.17203152359781E-12,-1.));
#25961=DIRECTION('',(1.,0.,0.));
#25962=DIRECTION('center_axis',(1.,0.,0.));
#25963=DIRECTION('ref_axis',(0.,-1.17203152359781E-12,-1.));
#25964=DIRECTION('',(1.,0.,0.));
#25965=DIRECTION('center_axis',(1.,0.,0.));
#25966=DIRECTION('ref_axis',(0.,-1.17203152359781E-12,-1.));
#25967=DIRECTION('',(1.,0.,0.));
#25968=DIRECTION('center_axis',(1.,0.,0.));
#25969=DIRECTION('ref_axis',(0.,-1.17203152359781E-12,-1.));
#25970=DIRECTION('',(1.,0.,0.));
#25971=DIRECTION('center_axis',(1.,0.,0.));
#25972=DIRECTION('ref_axis',(0.,-1.17203152359781E-12,-1.));
#25973=DIRECTION('',(1.,0.,0.));
#25974=DIRECTION('center_axis',(1.,0.,0.));
#25975=DIRECTION('ref_axis',(0.,-1.17203152359781E-12,-1.));
#25976=DIRECTION('',(1.,0.,0.));
#25977=DIRECTION('center_axis',(1.,0.,0.));
#25978=DIRECTION('ref_axis',(0.,-1.17203152359781E-12,-1.));
#25979=DIRECTION('',(1.,0.,0.));
#25980=DIRECTION('center_axis',(1.,0.,0.));
#25981=DIRECTION('ref_axis',(0.,-1.17203152359781E-12,-1.));
#25982=DIRECTION('',(1.,0.,0.));
#25983=DIRECTION('center_axis',(1.,0.,0.));
#25984=DIRECTION('ref_axis',(0.,-1.17203152359781E-12,-1.));
#25985=DIRECTION('',(1.,0.,0.));
#25986=DIRECTION('center_axis',(1.,0.,0.));
#25987=DIRECTION('ref_axis',(0.,-1.17203152359781E-12,-1.));
#25988=DIRECTION('',(1.,0.,0.));
#25989=DIRECTION('center_axis',(1.,0.,0.));
#25990=DIRECTION('ref_axis',(0.,-1.17203152359781E-12,-1.));
#25991=DIRECTION('',(1.,0.,0.));
#25992=DIRECTION('center_axis',(1.,0.,0.));
#25993=DIRECTION('ref_axis',(0.,-1.17203152359781E-12,-1.));
#25994=DIRECTION('',(1.,0.,0.));
#25995=DIRECTION('center_axis',(1.,0.,0.));
#25996=DIRECTION('ref_axis',(0.,-1.17203152359781E-12,-1.));
#25997=DIRECTION('',(1.,0.,0.));
#25998=DIRECTION('center_axis',(1.,0.,0.));
#25999=DIRECTION('ref_axis',(0.,-1.17203152359781E-12,-1.));
#26000=DIRECTION('',(1.,0.,0.));
#26001=DIRECTION('center_axis',(1.,0.,0.));
#26002=DIRECTION('ref_axis',(0.,-1.17203152359781E-12,-1.));
#26003=DIRECTION('',(1.,0.,0.));
#26004=DIRECTION('center_axis',(1.,0.,0.));
#26005=DIRECTION('ref_axis',(0.,0.,-1.));
#26006=DIRECTION('center_axis',(1.,0.,0.));
#26007=DIRECTION('ref_axis',(0.,0.,-1.));
#26008=DIRECTION('center_axis',(-1.,0.,0.));
#26009=DIRECTION('ref_axis',(0.,-1.17203152359781E-12,-1.));
#26010=DIRECTION('center_axis',(1.,0.,0.));
#26011=DIRECTION('ref_axis',(0.,0.,-1.));
#26012=DIRECTION('',(-1.,0.,0.));
#26013=DIRECTION('center_axis',(1.,0.,0.));
#26014=DIRECTION('ref_axis',(0.,0.,-1.));
#26015=DIRECTION('center_axis',(1.,0.,0.));
#26016=DIRECTION('ref_axis',(0.,0.,-1.));
#26017=DIRECTION('center_axis',(1.,0.,0.));
#26018=DIRECTION('ref_axis',(0.,-1.17203152359781E-12,-1.));
#26019=DIRECTION('center_axis',(0.,1.,0.));
#26020=DIRECTION('ref_axis',(0.,0.,1.));
#26021=DIRECTION('',(-1.,0.,0.));
#26022=DIRECTION('',(0.,0.,1.));
#26023=DIRECTION('',(1.,0.,0.));
#26024=DIRECTION('',(0.,0.,1.));
#26025=DIRECTION('center_axis',(1.,0.,0.));
#26026=DIRECTION('ref_axis',(0.,0.,-1.));
#26027=DIRECTION('center_axis',(-1.,0.,0.));
#26028=DIRECTION('ref_axis',(0.,0.,-1.));
#26029=DIRECTION('',(0.,-1.,0.));
#26030=DIRECTION('',(0.,0.,-1.));
#26031=DIRECTION('center_axis',(0.,0.,1.));
#26032=DIRECTION('ref_axis',(0.,-1.,0.));
#26033=DIRECTION('',(0.,-1.,0.));
#26034=DIRECTION('',(1.,0.,0.));
#26035=DIRECTION('center_axis',(0.,-1.,0.));
#26036=DIRECTION('ref_axis',(0.,0.,-1.));
#26037=DIRECTION('',(1.,0.,0.));
#26038=DIRECTION('',(0.,0.,-1.));
#26039=DIRECTION('center_axis',(1.,0.,0.));
#26040=DIRECTION('ref_axis',(0.,0.,-1.));
#26041=DIRECTION('center_axis',(1.,0.,0.));
#26042=DIRECTION('ref_axis',(0.,0.,-1.));
#26043=DIRECTION('center_axis',(1.,0.,0.));
#26044=DIRECTION('ref_axis',(0.,0.,-1.));
#26045=DIRECTION('center_axis',(1.,0.,0.));
#26046=DIRECTION('ref_axis',(0.,0.,-1.));
#26047=DIRECTION('',(-1.,0.,0.));
#26048=DIRECTION('center_axis',(-1.,0.,0.));
#26049=DIRECTION('ref_axis',(0.,0.,-1.));
#26050=DIRECTION('center_axis',(1.,0.,0.));
#26051=DIRECTION('ref_axis',(0.,0.,-1.));
#26052=DIRECTION('center_axis',(1.,0.,0.));
#26053=DIRECTION('ref_axis',(0.,0.,-1.));
#26054=DIRECTION('center_axis',(1.,0.,0.));
#26055=DIRECTION('ref_axis',(0.,0.,-1.));
#26056=DIRECTION('center_axis',(-1.,0.,0.));
#26057=DIRECTION('ref_axis',(0.,0.,-1.));
#26058=DIRECTION('center_axis',(1.,0.,0.));
#26059=DIRECTION('ref_axis',(0.,0.,-1.));
#26060=DIRECTION('center_axis',(1.,0.,0.));
#26061=DIRECTION('ref_axis',(0.,0.,-1.));
#26062=DIRECTION('',(-1.,0.,0.));
#26063=DIRECTION('center_axis',(1.,0.,0.));
#26064=DIRECTION('ref_axis',(0.,0.,-1.));
#26065=DIRECTION('center_axis',(1.,0.,0.));
#26066=DIRECTION('ref_axis',(0.,0.,-1.));
#33258=CARTESIAN_POINT('',(0.,0.,0.));
#33259=CARTESIAN_POINT('Origin',(4.,0.,4.));
#33260=CARTESIAN_POINT('',(4.12884541125756,8.40637486662632E-6,4.59405635738975));
#33261=CARTESIAN_POINT('',(4.02115458874249,-9.26662433349265E-6,4.59413599269206));
#33262=CARTESIAN_POINT('',(4.,-7.27562663373442E-17,4.5941));
#33263=CARTESIAN_POINT('',(4.,0.254721014554615,3.46322028700965));
#33264=CARTESIAN_POINT('Ctrl Pts',(4.12884541125756,8.40637486662632E-6,
4.59405635738975));
#33265=CARTESIAN_POINT('Ctrl Pts',(4.12564700130467,0.0398130654959074,
4.59407663624518));
#33266=CARTESIAN_POINT('Ctrl Pts',(4.12244859135178,0.079613792300143,4.59013569217808));
#33267=CARTESIAN_POINT('Ctrl Pts',(4.11925018139889,0.118599576779877,4.58219388355888));
#33268=CARTESIAN_POINT('Ctrl Pts',(4.11129754205509,0.215535206692688,4.56244709042845));
#33269=CARTESIAN_POINT('Ctrl Pts',(4.10334490271129,0.30743256945264,4.51796551073728));
#33270=CARTESIAN_POINT('Ctrl Pts',(4.09539226336748,0.383054411795556,4.45418672179759));
#33271=CARTESIAN_POINT('Ctrl Pts',(4.08743962402367,0.458676254138472,4.3904079328579));
#33272=CARTESIAN_POINT('Ctrl Pts',(4.07948698467986,0.518022576064352,4.30733193466969));
#33273=CARTESIAN_POINT('Ctrl Pts',(4.07153434533606,0.553840407547632,4.21511760274296));
#33274=CARTESIAN_POINT('Ctrl Pts',(4.06358170599225,0.589658239030912,4.12290327081622));
#33275=CARTESIAN_POINT('Ctrl Pts',(4.05562906664845,0.601947580071592,4.02155060515096));
#33276=CARTESIAN_POINT('Ctrl Pts',(4.04767642730464,0.589200356533535,3.92344812692479));
#33277=CARTESIAN_POINT('Ctrl Pts',(4.03972378796084,0.576453132995478,3.82534564869861));
#33278=CARTESIAN_POINT('Ctrl Pts',(4.03177114861703,0.538669344878685,3.73049335791153));
#33279=CARTESIAN_POINT('Ctrl Pts',(4.02381850927322,0.480479105222089,3.65049437695417));
#33280=CARTESIAN_POINT('Ctrl Pts',(4.01587900618215,0.422384984811151,3.57062753914914));
#33281=CARTESIAN_POINT('Ctrl Pts',(4.00793950309107,0.343951772361455,3.50556498199611));
#33282=CARTESIAN_POINT('Ctrl Pts',(4.,0.254721014554615,3.46322028700965));
#33283=CARTESIAN_POINT('',(4.,0.254694598474614,4.53673594206822));
#33284=CARTESIAN_POINT('Origin',(4.,0.,4.));
#33285=CARTESIAN_POINT('Ctrl Pts',(3.99999999999998,0.254694598474614,4.53673594206822));
#33286=CARTESIAN_POINT('Ctrl Pts',(4.00705152958082,0.175425736340139,4.5743509952638));
#33287=CARTESIAN_POINT('Ctrl Pts',(4.01410305916165,0.0876996967667308,
4.59405101338575));
#33288=CARTESIAN_POINT('Ctrl Pts',(4.02115458874249,-9.26662433349265E-6,
4.59413599269206));
#33289=CARTESIAN_POINT('Origin',(4.,0.,4.));
#33290=CARTESIAN_POINT('',(4.42884541125756,-2.46302091461148E-6,4.59415045696459));
#33291=CARTESIAN_POINT('',(4.32115458874249,3.58587963140688E-6,4.59404994535016));
#33292=CARTESIAN_POINT('',(4.,-7.27562663373442E-17,4.5941));
#33293=CARTESIAN_POINT('Ctrl Pts',(4.42884541125756,-2.46302091461148E-6,
4.59415045696459));
#33294=CARTESIAN_POINT('Ctrl Pts',(4.42107867343035,0.0966117732708647,
4.59412799973471));
#33295=CARTESIAN_POINT('Ctrl Pts',(4.41331193560314,0.193236775309615,4.57009608476161));
#33296=CARTESIAN_POINT('Ctrl Pts',(4.40554519777592,0.278573173318151,4.52479781884576));
#33297=CARTESIAN_POINT('Ctrl Pts',(4.39759255843212,0.36595214906825,4.47841531183407));
#33298=CARTESIAN_POINT('Ctrl Pts',(4.38963991908831,0.441495654419193,4.40973622444741));
#33299=CARTESIAN_POINT('Ctrl Pts',(4.3816872797445,0.495967466205845,4.32715751007026));
#33300=CARTESIAN_POINT('Ctrl Pts',(4.3737346404007,0.550439277992498,4.24457879569311));
#33301=CARTESIAN_POINT('Ctrl Pts',(4.36578200105689,0.58383939621486,4.14810045432546));
#33302=CARTESIAN_POINT('Ctrl Pts',(4.35782936171309,0.59208420294366,4.04951827803692));
#33303=CARTESIAN_POINT('Ctrl Pts',(4.34987672236928,0.600329009672459,3.95093610174838));
#33304=CARTESIAN_POINT('Ctrl Pts',(4.34192408302547,0.583418504907695,3.85025009053894));
#33305=CARTESIAN_POINT('Ctrl Pts',(4.33397144368167,0.54342022548472,3.75977047903001));
#33306=CARTESIAN_POINT('Ctrl Pts',(4.32601880433786,0.503421946061746,3.66929086752108));
#33307=CARTESIAN_POINT('Ctrl Pts',(4.31806616499406,0.440335891980562,3.58901765571266));
#33308=CARTESIAN_POINT('Ctrl Pts',(4.31011352565025,0.361875197644003,3.52876534000234));
#33309=CARTESIAN_POINT('Ctrl Pts',(4.30216088630644,0.283414503307443,3.46851302429202));
#33310=CARTESIAN_POINT('Ctrl Pts',(4.29420824696263,0.189579168715509,3.4282816046798));
#33311=CARTESIAN_POINT('Ctrl Pts',(4.28625560761883,0.0918418319479975,
3.41298991457491));
#33312=CARTESIAN_POINT('Ctrl Pts',(4.27830296827502,-0.00589550481951406,
3.39769822447003));
#33313=CARTESIAN_POINT('Ctrl Pts',(4.27035032893122,-0.107534843762603,
3.4073462638725));
#33314=CARTESIAN_POINT('Ctrl Pts',(4.26239768958741,-0.200649373295791,
3.44075443909651));
#33315=CARTESIAN_POINT('Ctrl Pts',(4.25444505024361,-0.293763902828979,
3.47416261432052));
#33316=CARTESIAN_POINT('Ctrl Pts',(4.24649241089979,-0.378353622952266,
3.53133092536608));
#33317=CARTESIAN_POINT('Ctrl Pts',(4.23853977155599,-0.444076322467606,
3.60526974769923));
#33318=CARTESIAN_POINT('Ctrl Pts',(4.23058713221218,-0.509799021982947,
3.67920857003239));
#33319=CARTESIAN_POINT('Ctrl Pts',(4.22263449286838,-0.556654700890342,
3.76991790365313));
#33320=CARTESIAN_POINT('Ctrl Pts',(4.21468185352458,-0.578914549750806,
3.86630733464992));
#33321=CARTESIAN_POINT('Ctrl Pts',(4.20672921418077,-0.601174398611269,
3.96269676564671));
#33322=CARTESIAN_POINT('Ctrl Pts',(4.19877657483696,-0.598838417424802,
4.06476629401955));
#33323=CARTESIAN_POINT('Ctrl Pts',(4.19082393549315,-0.5721923335546,4.16003645884502));
#33324=CARTESIAN_POINT('Ctrl Pts',(4.18287129614934,-0.545546249684398,
4.25530662367048));
#33325=CARTESIAN_POINT('Ctrl Pts',(4.17491865680554,-0.494590063130461,
4.34377742494856));
#33326=CARTESIAN_POINT('Ctrl Pts',(4.16696601746173,-0.425553631634784,
4.41463223618795));
#33327=CARTESIAN_POINT('Ctrl Pts',(4.15901337811793,-0.356517200139107,
4.48548704742733));
#33328=CARTESIAN_POINT('Ctrl Pts',(4.15106073877413,-0.269400523701689,
4.53872586862801));
#33329=CARTESIAN_POINT('Ctrl Pts',(4.14310809943032,-0.174855236950146,
4.56783927594351));
#33330=CARTESIAN_POINT('Ctrl Pts',(4.1383538700394,-0.118334381217266,4.5852437891806));
#33331=CARTESIAN_POINT('Ctrl Pts',(4.13359964064848,-0.0591586432141876,
4.59402621418361));
#33332=CARTESIAN_POINT('Ctrl Pts',(4.12884541125756,8.40637486662632E-6,
4.59405635738975));
#33333=CARTESIAN_POINT('Ctrl Pts',(4.02115458874249,-9.26662433349265E-6,
4.59413599269206));
#33334=CARTESIAN_POINT('Ctrl Pts',(4.02205569850546,-0.0112175303500608,
4.59414685213492));
#33335=CARTESIAN_POINT('Ctrl Pts',(4.02295680826843,-0.0224255152200988,
4.5938373961197));
#33336=CARTESIAN_POINT('Ctrl Pts',(4.0238579180314,-0.0336155370699344,
4.59320407706013));
#33337=CARTESIAN_POINT('Ctrl Pts',(4.03181055737521,-0.132371772633995,
4.58761479340425));
#33338=CARTESIAN_POINT('Ctrl Pts',(4.03976319671902,-0.229728915328813,
4.55680066053817));
#33339=CARTESIAN_POINT('Ctrl Pts',(4.04771583606282,-0.31374319278985,4.50455967689729));
#33340=CARTESIAN_POINT('Ctrl Pts',(4.05566847540663,-0.397757470250888,
4.4523186932564));
#33341=CARTESIAN_POINT('Ctrl Pts',(4.06362111475043,-0.468428882478145,
4.37865085884071));
#33342=CARTESIAN_POINT('Ctrl Pts',(4.07157375409424,-0.517135915630147,
4.29254879227412));
#33343=CARTESIAN_POINT('Ctrl Pts',(4.07952639343804,-0.565842948782149,
4.20644672570752));
#33344=CARTESIAN_POINT('Ctrl Pts',(4.08747903278185,-0.592585602858896,
4.10791042699003));
#33345=CARTESIAN_POINT('Ctrl Pts',(4.09543167212566,-0.594084460855775,
4.00899459728238));
#33346=CARTESIAN_POINT('Ctrl Pts',(4.10338431146947,-0.595583318852653,
3.91007876757474));
#33347=CARTESIAN_POINT('Ctrl Pts',(4.11133695081327,-0.571838380769662,
3.81078340687695));
#33348=CARTESIAN_POINT('Ctrl Pts',(4.11928959015708,-0.525757920758293,
3.72324489380985));
#33349=CARTESIAN_POINT('Ctrl Pts',(4.12724222950088,-0.479677460746923,
3.63570638074275));
#33350=CARTESIAN_POINT('Ctrl Pts',(4.13519486884469,-0.411261478807175,
3.55992471530633));
#33351=CARTESIAN_POINT('Ctrl Pts',(4.1431475081885,-0.328872047298013,3.50516726345229));
#33352=CARTESIAN_POINT('Ctrl Pts',(4.1511001475323,-0.246482615788851,3.45040981159825));
#33353=CARTESIAN_POINT('Ctrl Pts',(4.15905278687611,-0.150119734710276,
3.41667657332659));
#33354=CARTESIAN_POINT('Ctrl Pts',(4.16700542621992,-0.0515665150750243,
3.40809082437526));
#33355=CARTESIAN_POINT('Ctrl Pts',(4.17495806556372,0.0469867045602276,
3.39950507542393));
#33356=CARTESIAN_POINT('Ctrl Pts',(4.18291070490753,0.147730262752155,3.41606681579293));
#33357=CARTESIAN_POINT('Ctrl Pts',(4.19086334425134,0.238347648045887,3.45575171487277));
#33358=CARTESIAN_POINT('Ctrl Pts',(4.19881598359514,0.32896503333962,3.49543661395261));
#33359=CARTESIAN_POINT('Ctrl Pts',(4.20676862293895,0.409456245735157,3.55824467174328));
#33360=CARTESIAN_POINT('Ctrl Pts',(4.21472126228276,0.469979735422806,3.63649644709345));
#33361=CARTESIAN_POINT('Ctrl Pts',(4.22267390162656,0.530503225110456,3.71474822244363));
#33362=CARTESIAN_POINT('Ctrl Pts',(4.23062654097037,0.571058992090217,3.80844371535332));
#33363=CARTESIAN_POINT('Ctrl Pts',(4.23857918031417,0.586688754827568,3.90612753493601));
#33364=CARTESIAN_POINT('Ctrl Pts',(4.24653181965798,0.602318517564919,4.0038113545187));
#33365=CARTESIAN_POINT('Ctrl Pts',(4.25448445900178,0.593022276059861,4.10548350077438));
#33366=CARTESIAN_POINT('Ctrl Pts',(4.26243709834559,0.559936509464549,4.19871308474845));
#33367=CARTESIAN_POINT('Ctrl Pts',(4.2703897376894,0.526850742869238,4.29194266872251));
#33368=CARTESIAN_POINT('Ctrl Pts',(4.27834237703321,0.469975451183674,4.37672969041494));
#33369=CARTESIAN_POINT('Ctrl Pts',(4.28629501637701,0.396264473279151,4.44270782630825));
#33370=CARTESIAN_POINT('Ctrl Pts',(4.29424765572082,0.322553495374627,4.50868596220156));
#33371=CARTESIAN_POINT('Ctrl Pts',(4.30220029506462,0.232006831251144,4.55585521229574));
#33372=CARTESIAN_POINT('Ctrl Pts',(4.31015293440843,0.135695012128791,4.57844846968215));
#33373=CARTESIAN_POINT('Ctrl Pts',(4.31382015251978,0.0912825306677821,
4.58886694826517));
#33374=CARTESIAN_POINT('Ctrl Pts',(4.31748737063114,0.0456441298716245,
4.59405951624442));
#33375=CARTESIAN_POINT('Ctrl Pts',(4.32115458874249,3.58587963140688E-6,
4.59404994535016));
#33376=CARTESIAN_POINT('Origin',(4.,0.,4.));
#33377=CARTESIAN_POINT('',(4.72884541125756,-4.67700812217808E-6,4.59405084457266));
#33378=CARTESIAN_POINT('',(4.62115458874249,3.7232086238465E-6,4.59414939806979));
#33379=CARTESIAN_POINT('',(4.,-7.27562663373442E-17,4.5941));
#33380=CARTESIAN_POINT('Ctrl Pts',(4.72884541125756,-4.67700812217808E-6,
4.59405084457266));
#33381=CARTESIAN_POINT('Ctrl Pts',(4.72446298489983,0.0545367878429411,
4.59403588702548));
#33382=CARTESIAN_POINT('Ctrl Pts',(4.7200805585421,0.10908225468116,4.58659074407712));
#33383=CARTESIAN_POINT('Ctrl Pts',(4.71569813218437,0.16154350694756,4.57176871113812));
#33384=CARTESIAN_POINT('Ctrl Pts',(4.70774549284056,0.256743148594298,4.54487167450041));
#33385=CARTESIAN_POINT('Ctrl Pts',(4.69979285349676,0.345079446524661,4.4936824501733));
#33386=CARTESIAN_POINT('Ctrl Pts',(4.69184021415295,0.415752085200636,4.42445961801412));
#33387=CARTESIAN_POINT('Ctrl Pts',(4.68388757480915,0.486424723876611,4.35523678585494));
#33388=CARTESIAN_POINT('Ctrl Pts',(4.67593493546534,0.539433703298198,4.26798034586369));
#33389=CARTESIAN_POINT('Ctrl Pts',(4.66798229612153,0.568297953762936,4.17335858623793));
#33390=CARTESIAN_POINT('Ctrl Pts',(4.66002965677773,0.597162204227674,4.07873682661218));
#33391=CARTESIAN_POINT('Ctrl Pts',(4.65207701743392,0.601881725735563,3.97674974735193));
#33392=CARTESIAN_POINT('Ctrl Pts',(4.64412437809011,0.581879492504365,3.87986665793328));
#33393=CARTESIAN_POINT('Ctrl Pts',(4.63617173874631,0.561877259273167,3.78298356851463));
#33394=CARTESIAN_POINT('Ctrl Pts',(4.6282190994025,0.517153271302883,3.69120446893757));
#33395=CARTESIAN_POINT('Ctrl Pts',(4.6202664600587,0.453175645250056,3.61575060413089));
#33396=CARTESIAN_POINT('Ctrl Pts',(4.61231382071489,0.389198019197228,3.5402967393242));
#33397=CARTESIAN_POINT('Ctrl Pts',(4.60436118137108,0.305966755061857,3.48116810928789));
#33398=CARTESIAN_POINT('Ctrl Pts',(4.59640854202727,0.213658008474022,3.4455939943611));
#33399=CARTESIAN_POINT('Ctrl Pts',(4.58845590268347,0.121349261886187,3.41001987943431));
#33400=CARTESIAN_POINT('Ctrl Pts',(4.58050326333966,0.0199630328458878,
3.39800027961704));
#33401=CARTESIAN_POINT('Ctrl Pts',(4.57255062399586,-0.0781048312986516,
3.41100475468789));
#33402=CARTESIAN_POINT('Ctrl Pts',(4.56459798465205,-0.17617269544319,3.42400922975875));
#33403=CARTESIAN_POINT('Ctrl Pts',(4.55664534530825,-0.270922194691968,
3.46203777971774));
#33404=CARTESIAN_POINT('Ctrl Pts',(4.54869270596444,-0.350768912290741,
3.52044089639904));
#33405=CARTESIAN_POINT('Ctrl Pts',(4.54074006662063,-0.430615629889515,
3.57884401308035));
#33406=CARTESIAN_POINT('Ctrl Pts',(4.53278742727683,-0.495559565838284,
3.65762169648397));
#33407=CARTESIAN_POINT('Ctrl Pts',(4.52483478793302,-0.537660439465301,
3.74714230187364));
#33408=CARTESIAN_POINT('Ctrl Pts',(4.51688214858921,-0.579761313092318,
3.8366629072633));
#33409=CARTESIAN_POINT('Ctrl Pts',(4.50892950924541,-0.599019124397585,
3.936926434639));
#33410=CARTESIAN_POINT('Ctrl Pts',(4.5009768699016,-0.593079343631488,4.03567430223551));
#33411=CARTESIAN_POINT('Ctrl Pts',(4.49302423055779,-0.587139562865391,
4.13442216983203));
#33412=CARTESIAN_POINT('Ctrl Pts',(4.48507159121399,-0.556002190027932,
4.23165437764937));
#33413=CARTESIAN_POINT('Ctrl Pts',(4.47711895187018,-0.503474193090318,
4.31548296397124));
#33414=CARTESIAN_POINT('Ctrl Pts',(4.46916631252638,-0.450946196152703,
4.39931155029312));
#33415=CARTESIAN_POINT('Ctrl Pts',(4.46121367318257,-0.377027575114933,
4.46973651511953));
#33416=CARTESIAN_POINT('Ctrl Pts',(4.45326103383876,-0.290755888038263,
4.51814744739689));
#33417=CARTESIAN_POINT('Ctrl Pts',(4.44530839449495,-0.204484200961595,
4.56655837967425));
#33418=CARTESIAN_POINT('Ctrl Pts',(4.43735575515115,-0.105859447846027,
4.59295527940255));
#33419=CARTESIAN_POINT('Ctrl Pts',(4.42940311580734,-0.00693984821361558,
4.59411076594835));
#33420=CARTESIAN_POINT('Ctrl Pts',(4.42921721429075,-0.0046274959494805,
4.59413777669183));
#33421=CARTESIAN_POINT('Ctrl Pts',(4.42903131277416,-0.00231498256911503,
4.59415099449182));
#33422=CARTESIAN_POINT('Ctrl Pts',(4.42884541125756,-2.46302091461148E-6,
4.59415045696459));
#33423=CARTESIAN_POINT('Ctrl Pts',(4.32115458874249,3.58587963140688E-6,
4.59404994535016));
#33424=CARTESIAN_POINT('Ctrl Pts',(4.32544000997495,-0.0533308355660028,
4.59403876103764));
#33425=CARTESIAN_POINT('Ctrl Pts',(4.3297254312074,-0.106668183692779,4.58692369872924));
#33426=CARTESIAN_POINT('Ctrl Pts',(4.33401085243985,-0.158055593105036,
4.57274269264177));
#33427=CARTESIAN_POINT('Ctrl Pts',(4.34196349178366,-0.253417405095285,
4.54642639353635));
#33428=CARTESIAN_POINT('Ctrl Pts',(4.34991613112746,-0.342064054954561,
4.49577653064689));
#33429=CARTESIAN_POINT('Ctrl Pts',(4.35786877047127,-0.413157291282808,
4.42698573291487));
#33430=CARTESIAN_POINT('Ctrl Pts',(4.36582140981507,-0.484250527611055,
4.35819493518285));
#33431=CARTESIAN_POINT('Ctrl Pts',(4.37377404915888,-0.537790350408272,
4.27126320260829));
#33432=CARTESIAN_POINT('Ctrl Pts',(4.38172668850269,-0.567230782432438,
4.17681912699824));
#33433=CARTESIAN_POINT('Ctrl Pts',(4.3896793278465,-0.596671214456604,4.0823750513882));
#33434=CARTESIAN_POINT('Ctrl Pts',(4.3976319671903,-0.602012255707717,3.98041863274268));
#33435=CARTESIAN_POINT('Ctrl Pts',(4.40558460653411,-0.582600893642323,
3.88341542999892));
#33436=CARTESIAN_POINT('Ctrl Pts',(4.41353724587791,-0.563189531576929,
3.78641222725516));
#33437=CARTESIAN_POINT('Ctrl Pts',(4.42148988522172,-0.519025766195027,
3.69436224041317));
#33438=CARTESIAN_POINT('Ctrl Pts',(4.42944252456553,-0.455509217992651,
3.61851983504546));
#33439=CARTESIAN_POINT('Ctrl Pts',(4.43739516390933,-0.391992669790276,
3.54267742967776));
#33440=CARTESIAN_POINT('Ctrl Pts',(4.44534780325314,-0.309123338767427,
3.48304260578434));
#33441=CARTESIAN_POINT('Ctrl Pts',(4.45330044259694,-0.217033129998519,
3.44690653227429));
#33442=CARTESIAN_POINT('Ctrl Pts',(4.46125308194075,-0.12494292122961,3.41077045876423));
#33443=CARTESIAN_POINT('Ctrl Pts',(4.46920572128456,-0.0236318347146405,
3.39813313563753));
#33444=CARTESIAN_POINT('Ctrl Pts',(4.47715836062837,0.074513469760962,3.41053964803971));
#33445=CARTESIAN_POINT('Ctrl Pts',(4.48511099997217,0.172658774236564,3.42294616044189));
#33446=CARTESIAN_POINT('Ctrl Pts',(4.49306363931598,0.2676382966728,3.46039650837296));
#33447=CARTESIAN_POINT('Ctrl Pts',(4.50101627865978,0.34783949666059,3.51831187658845));
#33448=CARTESIAN_POINT('Ctrl Pts',(4.50896891800359,0.428040696648381,3.57622724480394));
#33449=CARTESIAN_POINT('Ctrl Pts',(4.51692155734739,0.493463574187728,3.65460763330386));
#33450=CARTESIAN_POINT('Ctrl Pts',(4.5248741966912,0.536109291561612,3.74386997215216));
#33451=CARTESIAN_POINT('Ctrl Pts',(4.53282683603501,0.578755008935497,3.83313231100046));
#33452=CARTESIAN_POINT('Ctrl Pts',(4.54077947537881,0.598623566143919,3.93327660019715));
#33453=CARTESIAN_POINT('Ctrl Pts',(4.54873211472262,0.593285761408823,4.03205883640902));
#33454=CARTESIAN_POINT('Ctrl Pts',(4.55668475406643,0.587947956673727,4.1308410726209));
#33455=CARTESIAN_POINT('Ctrl Pts',(4.56463739341024,0.557403789995114,4.22826125584796));
#33456=CARTESIAN_POINT('Ctrl Pts',(4.57259003275404,0.505387701781775,4.31240844187621));
#33457=CARTESIAN_POINT('Ctrl Pts',(4.58054267209785,0.453371613568435,4.39655562790445));
#33458=CARTESIAN_POINT('Ctrl Pts',(4.58849531144165,0.37988360382037,4.46742981673387));
#33459=CARTESIAN_POINT('Ctrl Pts',(4.59644795078546,0.293908582600447,4.51636567348148));
#33460=CARTESIAN_POINT('Ctrl Pts',(4.60440059012926,0.207933561380525,4.56530153022909));
#33461=CARTESIAN_POINT('Ctrl Pts',(4.61235322947307,0.109471528688745,4.59229905489488));
#33462=CARTESIAN_POINT('Ctrl Pts',(4.62030586881688,0.01056080905581,4.59405743239568));
#33463=CARTESIAN_POINT('Ctrl Pts',(4.62058877545875,0.00704216595801619,
4.59411998479525));
#33464=CARTESIAN_POINT('Ctrl Pts',(4.62087168210062,0.00352295504485493,
4.59415059693914));
#33465=CARTESIAN_POINT('Ctrl Pts',(4.62115458874249,3.7232086238465E-6,
4.59414939806979));
#33466=CARTESIAN_POINT('Origin',(4.,0.,4.));
#33467=CARTESIAN_POINT('',(5.02884541125756,1.1583539301252E-5,4.59413174414479));
#33468=CARTESIAN_POINT('',(4.92115458874249,-9.52916733652962E-6,4.59405847898621));
#33469=CARTESIAN_POINT('',(4.,-7.27562663373442E-17,4.5941));
#33470=CARTESIAN_POINT('Ctrl Pts',(5.02884541125756,1.1583539301252E-5,
4.59413174414479));
#33471=CARTESIAN_POINT('Ctrl Pts',(5.02784729636931,0.0124287555737821,
4.59414271605904));
#33472=CARTESIAN_POINT('Ctrl Pts',(5.02684918148107,0.024845254523583,4.59376142828251));
#33473=CARTESIAN_POINT('Ctrl Pts',(5.02585106659282,0.0372368329321061,
4.59298328977014));
#33474=CARTESIAN_POINT('Ctrl Pts',(5.01789842724901,0.135968707532707,4.58678334723719));
#33475=CARTESIAN_POINT('Ctrl Pts',(5.00994578790521,0.233118536601742,4.55538989360237));
#33476=CARTESIAN_POINT('Ctrl Pts',(5.0019931485614,0.316808430381418,4.50264120614281));
#33477=CARTESIAN_POINT('Ctrl Pts',(4.9940405092176,0.400498324161095,4.44989251868324));
#33478=CARTESIAN_POINT('Ctrl Pts',(4.98608786987379,0.470728282651411,4.37578859739892));
#33479=CARTESIAN_POINT('Ctrl Pts',(4.97813523052998,0.518911736914097,4.289389655942));
#33480=CARTESIAN_POINT('Ctrl Pts',(4.97018259118617,0.567095191176782,4.20299071448508));
#33481=CARTESIAN_POINT('Ctrl Pts',(4.96222995184237,0.593232141211837,4.10429675285556));
#33482=CARTESIAN_POINT('Ctrl Pts',(4.95427731249856,0.594126988899363,4.00537445204741));
#33483=CARTESIAN_POINT('Ctrl Pts',(4.94632467315476,0.595021836586889,3.90645215123927));
#33484=CARTESIAN_POINT('Ctrl Pts',(4.93837203381095,0.570674581926886,3.80730151125251));
#33485=CARTESIAN_POINT('Ctrl Pts',(4.93041939446714,0.524062008404491,3.72004504823011));
#33486=CARTESIAN_POINT('Ctrl Pts',(4.92246675512334,0.477449434882097,3.6327885852077));
#33487=CARTESIAN_POINT('Ctrl Pts',(4.91451411577953,0.408571542497308,3.55742629914966));
#33488=CARTESIAN_POINT('Ctrl Pts',(4.90656147643572,0.325849591692228,3.50317225594031));
#33489=CARTESIAN_POINT('Ctrl Pts',(4.89860883709192,0.243127640887147,3.44891821273095));
#33490=CARTESIAN_POINT('Ctrl Pts',(4.89065619774811,0.146561631661773,3.41577241237029));
#33491=CARTESIAN_POINT('Ctrl Pts',(4.88270355840431,0.0479580738465473,
3.40778738038914));
#33492=CARTESIAN_POINT('Ctrl Pts',(4.8747509190605,-0.0506454839686783,
3.39980234840799));
#33493=CARTESIAN_POINT('Ctrl Pts',(4.86679827971669,-0.151286590373755,
3.41697808480634));
#33494=CARTESIAN_POINT('Ctrl Pts',(4.85884564037289,-0.241660499406316,
3.45721462188069));
#33495=CARTESIAN_POINT('Ctrl Pts',(4.85089300102908,-0.332034408438876,
3.49745115895503));
#33496=CARTESIAN_POINT('Ctrl Pts',(4.84294036168527,-0.41214112009892,3.56074849670536));
#33497=CARTESIAN_POINT('Ctrl Pts',(4.83498772234147,-0.472186497854497,
3.63936767349926));
#33498=CARTESIAN_POINT('Ctrl Pts',(4.82703508299766,-0.532231875610076,
3.71798685029316));
#33499=CARTESIAN_POINT('Ctrl Pts',(4.81908244365386,-0.572215919461187,
3.81192786613063));
#33500=CARTESIAN_POINT('Ctrl Pts',(4.81112980431005,-0.587250035475296,
3.9097051523746));
#33501=CARTESIAN_POINT('Ctrl Pts',(4.80317716496624,-0.602284151489406,
4.00748243861856));
#33502=CARTESIAN_POINT('Ctrl Pts',(4.79522452562244,-0.592368339666514,
4.10909599526903));
#33503=CARTESIAN_POINT('Ctrl Pts',(4.78727188627863,-0.558714943052599,
4.20212218107662));
#33504=CARTESIAN_POINT('Ctrl Pts',(4.77931924693482,-0.525061546438685,
4.2951483668842));
#33505=CARTESIAN_POINT('Ctrl Pts',(4.77136660759101,-0.467670565033749,
4.37958718184891));
#33506=CARTESIAN_POINT('Ctrl Pts',(4.76341396824721,-0.393558827964045,
4.44511483080773));
#33507=CARTESIAN_POINT('Ctrl Pts',(4.7554613289034,-0.319447090894342,4.51064247976655));
#33508=CARTESIAN_POINT('Ctrl Pts',(4.7475086895596,-0.228614598159871,4.55725896271948));
#33509=CARTESIAN_POINT('Ctrl Pts',(4.73955605021579,-0.13216685911108,4.5792647797218));
#33510=CARTESIAN_POINT('Ctrl Pts',(4.73598583722972,-0.0888681559330128,
4.58914394690572));
#33511=CARTESIAN_POINT('Ctrl Pts',(4.73241562424364,-0.0444377444908,4.59406302997518));
#33512=CARTESIAN_POINT('Ctrl Pts',(4.72884541125756,-4.67700812217808E-6,
4.59405084457266));
#33513=CARTESIAN_POINT('Ctrl Pts',(4.62115458874249,3.7232086238465E-6,
4.59414939806979));
#33514=CARTESIAN_POINT('Ctrl Pts',(4.62882432144443,-0.0954043143036648,
4.59411689615543));
#33515=CARTESIAN_POINT('Ctrl Pts',(4.63649405414636,-0.190827729806029,
4.57070400848325));
#33516=CARTESIAN_POINT('Ctrl Pts',(4.6441637868483,-0.275369369969159,4.52648596729292));
#33517=CARTESIAN_POINT('Ctrl Pts',(4.65211642619211,-0.363029422787103,
4.48063689435358));
#33518=CARTESIAN_POINT('Ctrl Pts',(4.66006906553591,-0.438990121848901,
4.4124195181391));
#33519=CARTESIAN_POINT('Ctrl Pts',(4.66802170487971,-0.493964237128006,
4.33017434199545));
#33520=CARTESIAN_POINT('Ctrl Pts',(4.67597434422352,-0.548938352407109,
4.24792916585179));
#33521=CARTESIAN_POINT('Ctrl Pts',(4.68392698356733,-0.582925883903521,
4.15165618977896));
#33522=CARTESIAN_POINT('Ctrl Pts',(4.69187962291114,-0.591771392992132,
4.05312609631255));
#33523=CARTESIAN_POINT('Ctrl Pts',(4.69983226225494,-0.600616902080743,
3.95459600284613));
#33524=CARTESIAN_POINT('Ctrl Pts',(4.70778490159875,-0.584320388761555,
3.85380879198612));
#33525=CARTESIAN_POINT('Ctrl Pts',(4.71573754094256,-0.544874323741249,
3.76308707295491));
#33526=CARTESIAN_POINT('Ctrl Pts',(4.72369018028636,-0.505428258720944,
3.6723653539237));
#33527=CARTESIAN_POINT('Ctrl Pts',(4.73164281963017,-0.442832641999522,
3.59170912672127));
#33528=CARTESIAN_POINT('Ctrl Pts',(4.73959545897397,-0.364740640256699,
3.53097971363863));
#33529=CARTESIAN_POINT('Ctrl Pts',(4.74754809831778,-0.286648638513876,
3.47025030055599));
#33530=CARTESIAN_POINT('Ctrl Pts',(4.75550073766158,-0.193060251749651,
3.42944770159313));
#33531=CARTESIAN_POINT('Ctrl Pts',(4.76345337700539,-0.095417934894009,
3.41356059019365));
#33532=CARTESIAN_POINT('Ctrl Pts',(4.7714060163492,0.00222438196163176,
3.39767347879416));
#33533=CARTESIAN_POINT('Ctrl Pts',(4.77935865569301,0.10392062890869,3.40670185495805));
#33534=CARTESIAN_POINT('Ctrl Pts',(4.78731129503681,0.19723705468272,3.43954187673519));
#33535=CARTESIAN_POINT('Ctrl Pts',(4.79526393438062,0.290553480456751,3.47238189851233));
#33536=CARTESIAN_POINT('Ctrl Pts',(4.80321657372443,0.375490085057754,3.52903356590271));
#33537=CARTESIAN_POINT('Ctrl Pts',(4.81116921306823,0.441662211759978,3.60257044098769));
#33538=CARTESIAN_POINT('Ctrl Pts',(4.81912185241204,0.507834338462201,3.67610731607267));
#33539=CARTESIAN_POINT('Ctrl Pts',(4.82707449175584,0.555241987265645,3.76652939885225));
#33540=CARTESIAN_POINT('Ctrl Pts',(4.83502713109965,0.57808892742485,3.86278135818256));
#33541=CARTESIAN_POINT('Ctrl Pts',(4.84297977044346,0.600935867584054,3.95903331751286));
#33542=CARTESIAN_POINT('Ctrl Pts',(4.85093240978726,0.599222099099018,4.0611151533939));
#33543=CARTESIAN_POINT('Ctrl Pts',(4.85888504913107,0.573157153508111,4.15654597106253));
#33544=CARTESIAN_POINT('Ctrl Pts',(4.86683768847488,0.547092207917203,4.25197678873116));
#33545=CARTESIAN_POINT('Ctrl Pts',(4.87479032781868,0.496676085220424,4.34075658818739));
#33546=CARTESIAN_POINT('Ctrl Pts',(4.88274296716249,0.428072843071251,4.41203082979109));
#33547=CARTESIAN_POINT('Ctrl Pts',(4.89069560650629,0.359469600922078,4.48330507139479));
#33548=CARTESIAN_POINT('Ctrl Pts',(4.8986482458501,0.272679239320511,4.53707375514596));
#33549=CARTESIAN_POINT('Ctrl Pts',(4.90660088519391,0.178313062033339,4.56676292714126));
#33550=CARTESIAN_POINT('Ctrl Pts',(4.9114521197101,0.120748216373203,4.58487378690922));
#33551=CARTESIAN_POINT('Ctrl Pts',(4.9163033542263,0.0603642649825261,4.59402420038378));
#33552=CARTESIAN_POINT('Ctrl Pts',(4.92115458874249,-9.52916733652962E-6,
4.59405847898621));
#33553=CARTESIAN_POINT('Origin',(4.,0.,4.));
#33554=CARTESIAN_POINT('',(5.32884541125756,-1.45357002139801E-5,4.59407911932661));
#33555=CARTESIAN_POINT('',(5.22115458874249,1.46139895546772E-5,4.59411444380891));
#33556=CARTESIAN_POINT('',(4.,-7.27562663373442E-17,4.5941));
#33557=CARTESIAN_POINT('Ctrl Pts',(5.32884541125756,-1.45357002139801E-5,
4.59407911932661));
#33558=CARTESIAN_POINT('Ctrl Pts',(5.32327896849499,0.0692531541268509,
4.59401614001471));
#33559=CARTESIAN_POINT('Ctrl Pts',(5.31771252573242,0.138542285837495,4.5819075943171));
#33560=CARTESIAN_POINT('Ctrl Pts',(5.31214608296985,0.203593590158122,4.55818044906639));
#33561=CARTESIAN_POINT('Ctrl Pts',(5.30419344362604,0.296530782575621,4.5242820624512));
#33562=CARTESIAN_POINT('Ctrl Pts',(5.29624080428224,0.380818089806801,4.46666879957728));
#33563=CARTESIAN_POINT('Ctrl Pts',(5.28828816493843,0.446150240572578,4.39238466650784));
#33564=CARTESIAN_POINT('Ctrl Pts',(5.28033552559462,0.511482391338355,4.3181005334384));
#33565=CARTESIAN_POINT('Ctrl Pts',(5.27238288625081,0.557859385638729,4.22714553017344));
#33566=CARTESIAN_POINT('Ctrl Pts',(5.26443024690701,0.579611004278495,4.13064014464439));
#33567=CARTESIAN_POINT('Ctrl Pts',(5.2564776075632,0.601362622918262,4.03413475911534));
#33568=CARTESIAN_POINT('Ctrl Pts',(5.2485249682194,0.598488865897423,3.93207899132219));
#33569=CARTESIAN_POINT('Ctrl Pts',(5.24057232887559,0.571341089151559,3.8369505488493));
#33570=CARTESIAN_POINT('Ctrl Pts',(5.23261968953179,0.544193312405696,3.74182210637642));
#33571=CARTESIAN_POINT('Ctrl Pts',(5.22466705018798,0.492771515934809,3.65362098922379));
#33572=CARTESIAN_POINT('Ctrl Pts',(5.21671441084417,0.423362714708271,3.58313098523844));
#33573=CARTESIAN_POINT('Ctrl Pts',(5.20876177150037,0.353953913481732,3.51264098125308));
#33574=CARTESIAN_POINT('Ctrl Pts',(5.20080913215656,0.266558107499543,3.45986209043499));
#33575=CARTESIAN_POINT('Ctrl Pts',(5.19285649281275,0.171860624350003,3.43124725102074));
#33576=CARTESIAN_POINT('Ctrl Pts',(5.18490385346895,0.0771631412004631,
3.40263241160649));
#33577=CARTESIAN_POINT('Ctrl Pts',(5.17695121412514,-0.0248360191164267,
3.39818162359609));
#33578=CARTESIAN_POINT('Ctrl Pts',(5.16899857478133,-0.121666070051256,
3.41843905644231));
#33579=CARTESIAN_POINT('Ctrl Pts',(5.16104593543753,-0.218496120986084,
3.43869648928852));
#33580=CARTESIAN_POINT('Ctrl Pts',(5.15309329609372,-0.310157062538852,
3.48366214299137));
#33581=CARTESIAN_POINT('Ctrl Pts',(5.14514065674991,-0.385442096207774,
3.54783835396576));
#33582=CARTESIAN_POINT('Ctrl Pts',(5.13718801740611,-0.460727129876697,
3.61201456494015));
#33583=CARTESIAN_POINT('Ctrl Pts',(5.1292353780623,-0.519636255661773,3.6954013331861));
#33584=CARTESIAN_POINT('Ctrl Pts',(5.1212827387185,-0.554967030609594,3.78780349058054));
#33585=CARTESIAN_POINT('Ctrl Pts',(5.11333009937469,-0.590297805557415,
3.88020564797498));
#33586=CARTESIAN_POINT('Ctrl Pts',(5.10537746003088,-0.60205022966798,3.98162319451792));
#33587=CARTESIAN_POINT('Ctrl Pts',(5.09742482068708,-0.588787409028971,
4.07965645386523));
#33588=CARTESIAN_POINT('Ctrl Pts',(5.08947218134327,-0.575524588389962,
4.17768971321255));
#33589=CARTESIAN_POINT('Ctrl Pts',(5.08151954199946,-0.537246523001379,
4.27233868536424));
#33590=CARTESIAN_POINT('Ctrl Pts',(5.07356690265566,-0.47863322769376,4.35203124438164));
#33591=CARTESIAN_POINT('Ctrl Pts',(5.06561426331185,-0.42001993238614,4.43172380339905));
#33592=CARTESIAN_POINT('Ctrl Pts',(5.05766162396805,-0.341071407159484,
4.49645994928216));
#33593=CARTESIAN_POINT('Ctrl Pts',(5.04970898462424,-0.251440184480074,
4.53832480650817));
#33594=CARTESIAN_POINT('Ctrl Pts',(5.04275446016868,-0.1730583412759,4.5749353153996));
#33595=CARTESIAN_POINT('Ctrl Pts',(5.03579993571312,-0.0865070403179845,
4.59405529558476));
#33596=CARTESIAN_POINT('Ctrl Pts',(5.02884541125756,1.1583539301252E-5,
4.59413174414479));
#33597=CARTESIAN_POINT('Ctrl Pts',(4.92115458874249,-9.52916733652962E-6,
4.59405847898621));
#33598=CARTESIAN_POINT('Ctrl Pts',(4.9242559935701,-0.0386066277022544,
4.59408039337166));
#33599=CARTESIAN_POINT('Ctrl Pts',(4.92735739839772,-0.0771995748988638,
4.59037647703175));
#33600=CARTESIAN_POINT('Ctrl Pts',(4.93045880322533,-0.115049119822012,
4.58290605049323));
#33601=CARTESIAN_POINT('Ctrl Pts',(4.93841144256913,-0.212103131417409,
4.56375034161047));
#33602=CARTESIAN_POINT('Ctrl Pts',(4.94636408191294,-0.304269161635426,
4.51982926360553));
#33603=CARTESIAN_POINT('Ctrl Pts',(4.95431672125675,-0.380278658005779,
4.45651276645759));
#33604=CARTESIAN_POINT('Ctrl Pts',(4.96226936060055,-0.456288154376132,
4.39319626930964));
#33605=CARTESIAN_POINT('Ctrl Pts',(4.97022199994436,-0.516141116898821,
4.31048435301868));
#33606=CARTESIAN_POINT('Ctrl Pts',(4.97817463928816,-0.552519705724467,
4.21848967586497));
#33607=CARTESIAN_POINT('Ctrl Pts',(4.98612727863197,-0.588898294550112,
4.12649499871126));
#33608=CARTESIAN_POINT('Ctrl Pts',(4.99407991797578,-0.601802509678713,
4.0252175606948));
#33609=CARTESIAN_POINT('Ctrl Pts',(5.00203255731958,-0.589654635058918,
3.92703990798411));
#33610=CARTESIAN_POINT('Ctrl Pts',(5.00998519666339,-0.577506760439122,
3.82886225527341));
#33611=CARTESIAN_POINT('Ctrl Pts',(5.0179378360072,-0.540306796070929,3.73378438786847));
#33612=CARTESIAN_POINT('Ctrl Pts',(5.025890475351,-0.482602944251693,3.65343086999412));
#33613=CARTESIAN_POINT('Ctrl Pts',(5.03384311469481,-0.424899092432456,
3.57307735211977));
#33614=CARTESIAN_POINT('Ctrl Pts',(5.04179575403862,-0.346691353162178,
3.50744818377599));
#33615=CARTESIAN_POINT('Ctrl Pts',(5.04974839338242,-0.257541687734669,
3.46456742464414));
#33616=CARTESIAN_POINT('Ctrl Pts',(5.05770103272623,-0.16839202230716,3.42168666551229));
#33617=CARTESIAN_POINT('Ctrl Pts',(5.06565367207003,-0.0683004307224215,
3.40155431559236));
#33618=CARTESIAN_POINT('Ctrl Pts',(5.07360631141384,0.0304955267282049,
3.40663182885918));
#33619=CARTESIAN_POINT('Ctrl Pts',(5.08155895075765,0.129291484178831,3.41170934212599));
#33620=CARTESIAN_POINT('Ctrl Pts',(5.08951159010146,0.226791807495345,3.44199671857955));
#33621=CARTESIAN_POINT('Ctrl Pts',(5.09746422944526,0.311075754224562,3.49379091394262));
#33622=CARTESIAN_POINT('Ctrl Pts',(5.10541686878907,0.395359700953779,3.54558510930568));
#33623=CARTESIAN_POINT('Ctrl Pts',(5.11336950813287,0.466427271095698,3.61888612357825));
#33624=CARTESIAN_POINT('Ctrl Pts',(5.12132214747668,0.515589486279599,3.70473190942573));
#33625=CARTESIAN_POINT('Ctrl Pts',(5.12927478682048,0.564751701463499,3.79057769527322));
#33626=CARTESIAN_POINT('Ctrl Pts',(5.13722742616429,0.592008561689381,3.88896825269562));
#33627=CARTESIAN_POINT('Ctrl Pts',(5.1451800655081,0.594027544563649,3.98787399599556));
#33628=CARTESIAN_POINT('Ctrl Pts',(5.1531327048519,0.596046527437917,4.0867797392955));
#33629=CARTESIAN_POINT('Ctrl Pts',(5.16108534419571,0.572827632960568,4.18620066847299));
#33630=CARTESIAN_POINT('Ctrl Pts',(5.16903798353952,0.527209687216453,4.2739812208502));
#33631=CARTESIAN_POINT('Ctrl Pts',(5.17699062288332,0.481591741472338,4.3617617732274));
#33632=CARTESIAN_POINT('Ctrl Pts',(5.18494326222713,0.413574744461461,4.43790194880433));
#33633=CARTESIAN_POINT('Ctrl Pts',(5.19289590157094,0.331474700441294,4.49309257410834));
#33634=CARTESIAN_POINT('Ctrl Pts',(5.20084854091474,0.24937465642113,4.54828319941234));
#33635=CARTESIAN_POINT('Ctrl Pts',(5.20880118025855,0.153191565391677,4.58252427444343));
#33636=CARTESIAN_POINT('Ctrl Pts',(5.21675381960235,0.0546851202186884,
4.59162936142496));
#33637=CARTESIAN_POINT('Ctrl Pts',(5.21822074264906,0.0365148790664279,
4.59330886194775));
#33638=CARTESIAN_POINT('Ctrl Pts',(5.21968766569578,0.018265586889787,4.59413312238171));
#33639=CARTESIAN_POINT('Ctrl Pts',(5.22115458874249,1.46139895546772E-5,
4.59411444380891));
#33640=CARTESIAN_POINT('Origin',(4.,0.,4.));
#33641=CARTESIAN_POINT('',(5.62884541125756,1.52328526200479E-5,4.59408648697874));
#33642=CARTESIAN_POINT('',(5.52115458874249,-1.55733839743342E-5,4.59409663347568));
#33643=CARTESIAN_POINT('',(4.,-7.27562663373442E-17,4.5941));
#33644=CARTESIAN_POINT('Ctrl Pts',(5.62884541125756,1.52328526200479E-5,
4.59408648697874));
#33645=CARTESIAN_POINT('Ctrl Pts',(5.62666327996447,0.0271682673899915,
4.59411287463303));
#33646=CARTESIAN_POINT('Ctrl Pts',(5.62448114867138,0.054317778225707,4.59228554395034));
#33647=CARTESIAN_POINT('Ctrl Pts',(5.62229901737829,0.0812075234320336,
4.58857548522516));
#33648=CARTESIAN_POINT('Ctrl Pts',(5.61434637803449,0.179205497408217,4.57505441109036));
#33649=CARTESIAN_POINT('Ctrl Pts',(5.60639373869068,0.273753285393806,4.53652709601604));
#33650=CARTESIAN_POINT('Ctrl Pts',(5.59844109934688,0.353291132582354,4.47770402899113));
#33651=CARTESIAN_POINT('Ctrl Pts',(5.59048846000307,0.432828979770902,4.41888096196622));
#33652=CARTESIAN_POINT('Ctrl Pts',(5.58253582065927,0.497356886162411,4.33976214299073));
#33653=CARTESIAN_POINT('Ctrl Pts',(5.57458318131546,0.538985436353474,4.25002092526659));
#33654=CARTESIAN_POINT('Ctrl Pts',(5.56663054197165,0.580613986544537,4.16027970754245));
#33655=CARTESIAN_POINT('Ctrl Pts',(5.55867790262784,0.599343180535155,4.05991609106967));
#33656=CARTESIAN_POINT('Ctrl Pts',(5.55072526328404,0.592883119270616,3.96120089488413));
#33657=CARTESIAN_POINT('Ctrl Pts',(5.54277262394023,0.586423058006077,3.86248569869858));
#33658=CARTESIAN_POINT('Ctrl Pts',(5.53481998459642,0.554773741486382,3.76541892280029));
#33659=CARTESIAN_POINT('Ctrl Pts',(5.52686734525262,0.501804729712613,3.68186830256729));
#33660=CARTESIAN_POINT('Ctrl Pts',(5.51891470590881,0.448835717938844,3.5983176823343));
#33661=CARTESIAN_POINT('Ctrl Pts',(5.51096206656501,0.374547010911001,3.52828321776661));
#33662=CARTESIAN_POINT('Ctrl Pts',(5.5030094272212,0.288021414854312,3.48032757600706));
#33663=CARTESIAN_POINT('Ctrl Pts',(5.4950567878774,0.201495818797622,3.4323719342475));
#33664=CARTESIAN_POINT('Ctrl Pts',(5.48710414853359,0.102733333712086,3.40649511529609));
#33665=CARTESIAN_POINT('Ctrl Pts',(5.47915150918978,0.00380901851787326,
3.40586091270526));
#33666=CARTESIAN_POINT('Ctrl Pts',(5.47119886984597,-0.0951152966763399,
3.40522671011442));
#33667=CARTESIAN_POINT('Ctrl Pts',(5.46324623050217,-0.194201441979227,
3.42983512388417));
#33668=CARTESIAN_POINT('Ctrl Pts',(5.45529359115836,-0.281334786601535,
3.47667744027106));
#33669=CARTESIAN_POINT('Ctrl Pts',(5.44734095181456,-0.368468131223842,
3.52351975665794));
#33670=CARTESIAN_POINT('Ctrl Pts',(5.43938831247075,-0.443648675165568,
3.59259597566196));
#33671=CARTESIAN_POINT('Ctrl Pts',(5.43143567312694,-0.497684572991269,
3.67546058871077));
#33672=CARTESIAN_POINT('Ctrl Pts',(5.42348303378314,-0.551720470816969,
3.75832520175959));
#33673=CARTESIAN_POINT('Ctrl Pts',(5.41553039443933,-0.584611722526643,
3.85497820885321));
#33674=CARTESIAN_POINT('Ctrl Pts',(5.40757775509553,-0.592336924628993,
3.95360246348684));
#33675=CARTESIAN_POINT('Ctrl Pts',(5.39962511575172,-0.600062126731343,
4.05222671812048));
#33676=CARTESIAN_POINT('Ctrl Pts',(5.39167247640791,-0.582621279226368,
4.15282222029412));
#33677=CARTESIAN_POINT('Ctrl Pts',(5.3837198370641,-0.542146763261091,4.24308979978386));
#33678=CARTESIAN_POINT('Ctrl Pts',(5.3757671977203,-0.501672247295815,4.3333573792736));
#33679=CARTESIAN_POINT('Ctrl Pts',(5.36781455837649,-0.438164062870237,
4.41329703607943));
#33680=CARTESIAN_POINT('Ctrl Pts',(5.35986191903269,-0.359386950494509,
4.47313505840055));
#33681=CARTESIAN_POINT('Ctrl Pts',(5.35190927968888,-0.28060983811878,4.53297308072167));
#33682=CARTESIAN_POINT('Ctrl Pts',(5.34395664034507,-0.1865637977929,4.57270946855809));
#33683=CARTESIAN_POINT('Ctrl Pts',(5.33600400100126,-0.0887472388280498,
4.58748590729807));
#33684=CARTESIAN_POINT('Ctrl Pts',(5.33361780442003,-0.0593972924141157,
4.59191959101989));
#33685=CARTESIAN_POINT('Ctrl Pts',(5.3312316078388,-0.0297078841644672,
4.59410611700271));
#33686=CARTESIAN_POINT('Ctrl Pts',(5.32884541125756,-1.45357002139801E-5,
4.59407911932661));
#33687=CARTESIAN_POINT('Ctrl Pts',(5.22115458874249,1.46139895546772E-5,
4.59411444380891));
#33688=CARTESIAN_POINT('Ctrl Pts',(5.22764030503958,-0.0806785298274998,
4.59403186011492));
#33689=CARTESIAN_POINT('Ctrl Pts',(5.23412602133668,-0.161404528346198,
4.57747154641029));
#33690=CARTESIAN_POINT('Ctrl Pts',(5.24061173763377,-0.235476461490165,
4.54549665421293));
#33691=CARTESIAN_POINT('Ctrl Pts',(5.24856437697758,-0.32630179870949,4.50628976108741));
#33692=CARTESIAN_POINT('Ctrl Pts',(5.25651701632139,-0.407122673831612,
4.44390687590439));
#33693=CARTESIAN_POINT('Ctrl Pts',(5.26446965566519,-0.468057634114636,
4.36597515601533));
#33694=CARTESIAN_POINT('Ctrl Pts',(5.272422295009,-0.52899259439766,4.28804343612627));
#33695=CARTESIAN_POINT('Ctrl Pts',(5.28037493435281,-0.570041639841584,
4.19456288153117));
#33696=CARTESIAN_POINT('Ctrl Pts',(5.28832757369661,-0.586185965564114,
4.09696276320888));
#33697=CARTESIAN_POINT('Ctrl Pts',(5.29628021304042,-0.602330291286644,
3.99936264488659));
#33698=CARTESIAN_POINT('Ctrl Pts',(5.30423285238423,-0.59356989728778,3.89764296283709));
#33699=CARTESIAN_POINT('Ctrl Pts',(5.31218549172803,-0.560975861048054,
3.80424033358521));
#33700=CARTESIAN_POINT('Ctrl Pts',(5.32013813107184,-0.528381824808328,
3.71083770433334));
#33701=CARTESIAN_POINT('Ctrl Pts',(5.32809077041564,-0.471954146327742,
3.62575212787907));
#33702=CARTESIAN_POINT('Ctrl Pts',(5.33604340975945,-0.398591877830097,
3.55938647478623));
#33703=CARTESIAN_POINT('Ctrl Pts',(5.34399604910326,-0.325229609332449,
3.49302082169338));
#33704=CARTESIAN_POINT('Ctrl Pts',(5.35194868844707,-0.234932750817741,
3.44537509196196));
#33705=CARTESIAN_POINT('Ctrl Pts',(5.35990132779087,-0.138741323057917,
3.42227462497344));
#33706=CARTESIAN_POINT('Ctrl Pts',(5.36785396713468,-0.042549895298095,
3.39917415798493));
#33707=CARTESIAN_POINT('Ctrl Pts',(5.37580660647848,0.059536101706843,3.40061895373932));
#33708=CARTESIAN_POINT('Ctrl Pts',(5.38375924582229,0.155035264439678,3.42643236627792));
#33709=CARTESIAN_POINT('Ctrl Pts',(5.39171188516609,0.250534427172515,3.45224577881651));
#33710=CARTESIAN_POINT('Ctrl Pts',(5.3996645245099,0.339446755633248,3.5024278081393));
#33711=CARTESIAN_POINT('Ctrl Pts',(5.40761716385371,0.41090150670596,3.57084301769608));
#33712=CARTESIAN_POINT('Ctrl Pts',(5.41556980319751,0.482356257778672,3.63925822725286));
#33713=CARTESIAN_POINT('Ctrl Pts',(5.42352244254132,0.536353431463363,3.72590661704362));
#33714=CARTESIAN_POINT('Ctrl Pts',(5.43147508188513,0.566291137850326,3.82019424128906));
#33715=CARTESIAN_POINT('Ctrl Pts',(5.43942772122893,0.596228844237288,3.91448186553449));
#33716=CARTESIAN_POINT('Ctrl Pts',(5.44738036057274,0.602107083326521,4.01640872423458));
#33717=CARTESIAN_POINT('Ctrl Pts',(5.45533299991655,0.583207160329387,4.11351287069736));
#33718=CARTESIAN_POINT('Ctrl Pts',(5.46328563926035,0.564307237332252,4.21061701716013));
#33719=CARTESIAN_POINT('Ctrl Pts',(5.47123827860416,0.520629152248751,4.30289845138559));
#33720=CARTESIAN_POINT('Ctrl Pts',(5.47919091794796,0.457513145863858,4.37907451119169));
#33721=CARTESIAN_POINT('Ctrl Pts',(5.48714355729177,0.394397139478966,4.45525057099779));
#33722=CARTESIAN_POINT('Ctrl Pts',(5.49509619663558,0.311843211792683,4.51532125638452));
#33723=CARTESIAN_POINT('Ctrl Pts',(5.50304883597938,0.219944704826683,4.5519421079172));
#33724=CARTESIAN_POINT('Ctrl Pts',(5.50908408690042,0.150203009669811,4.5797336395568));
#33725=CARTESIAN_POINT('Ctrl Pts',(5.51511933782146,0.0750795109720808,
4.59401975858331));
#33726=CARTESIAN_POINT('Ctrl Pts',(5.52115458874249,-1.55733839743342E-5,
4.59409663347568));
#33727=CARTESIAN_POINT('Origin',(4.,0.,4.));
#33728=CARTESIAN_POINT('',(5.92884541125757,-1.3134308860685E-5,4.59412454375027));
#33729=CARTESIAN_POINT('',(5.82115458874249,1.31105368646138E-5,4.59407040741879));
#33730=CARTESIAN_POINT('',(4.,-7.27562663373442E-17,4.5941));
#33731=CARTESIAN_POINT('Ctrl Pts',(5.92884541125757,-1.3134308860685E-5,
4.59412454375027));
#33732=CARTESIAN_POINT('Ctrl Pts',(5.92209495209015,0.0839697382976411,
4.5940436242297));
#33733=CARTESIAN_POINT('Ctrl Pts',(5.91534449292274,0.16798613900316,4.57606223573506));
#33734=CARTESIAN_POINT('Ctrl Pts',(5.90859403375532,0.244517407380453,4.54150437939301));
#33735=CARTESIAN_POINT('Ctrl Pts',(5.90064139441152,0.334678026211646,4.50079216098422));
#33736=CARTESIAN_POINT('Ctrl Pts',(5.89268875506771,0.41445008323119,4.43707358099086));
#33737=CARTESIAN_POINT('Ctrl Pts',(5.8847361157239,0.474080337065587,4.35813908232779));
#33738=CARTESIAN_POINT('Ctrl Pts',(5.8767834763801,0.533710590899983,4.27920458366471));
#33739=CARTESIAN_POINT('Ctrl Pts',(5.86883083703629,0.573199041549232,4.18505416633191));
#33740=CARTESIAN_POINT('Ctrl Pts',(5.86087819769249,0.587717699183782,4.08719901244189));
#33741=CARTESIAN_POINT('Ctrl Pts',(5.85292555834868,0.602236356818331,3.98934385855186));
#33742=CARTESIAN_POINT('Ctrl Pts',(5.84497291900487,0.591785221438181,3.88778396810461));
#33743=CARTESIAN_POINT('Ctrl Pts',(5.83702027966107,0.557642080814915,3.79493641494568));
#33744=CARTESIAN_POINT('Ctrl Pts',(5.82906764031726,0.523498940191649,3.70208886178675));
#33745=CARTESIAN_POINT('Ctrl Pts',(5.82111500097346,0.465663794325265,3.61795364591614));
#33746=CARTESIAN_POINT('Ctrl Pts',(5.81316236162965,0.391207780605707,3.55281744653948));
#33747=CARTESIAN_POINT('Ctrl Pts',(5.80520972228584,0.31675176688615,3.48768124716281));
#33748=CARTESIAN_POINT('Ctrl Pts',(5.79725708294203,0.225674885313418,3.44154406428009));
#33749=CARTESIAN_POINT('Ctrl Pts',(5.78930444359823,0.129112523455512,3.42004679519738));
#33750=CARTESIAN_POINT('Ctrl Pts',(5.78135180425442,0.0325501615976049,
3.39854952611466));
#33751=CARTESIAN_POINT('Ctrl Pts',(5.77339916491062,-0.0694976805454773,
3.40169217083197));
#33752=CARTESIAN_POINT('Ctrl Pts',(5.76544652556681,-0.164554263536051,
3.42909049911887));
#33753=CARTESIAN_POINT('Ctrl Pts',(5.75749388622301,-0.259610846526622,
3.45648882740576));
#33754=CARTESIAN_POINT('Ctrl Pts',(5.7495412468792,-0.347676170364685,3.50814283926225));
#33755=CARTESIAN_POINT('Ctrl Pts',(5.74158860753539,-0.417983050247216,
3.57773712775495));
#33756=CARTESIAN_POINT('Ctrl Pts',(5.73363596819158,-0.488289930129746,
3.64733141624764));
#33757=CARTESIAN_POINT('Ctrl Pts',(5.72568332884778,-0.540838366056745,
3.73486598137654));
#33758=CARTESIAN_POINT('Ctrl Pts',(5.71773068950397,-0.569203595796233,
3.82963853060694));
#33759=CARTESIAN_POINT('Ctrl Pts',(5.70977805016017,-0.597568825535722,
3.92441107983734));
#33760=CARTESIAN_POINT('Ctrl Pts',(5.70182541081636,-0.6017508490877,4.02642161316923));
#33761=CARTESIAN_POINT('Ctrl Pts',(5.69387277147255,-0.581238357244447,
4.12319795341528));
#33762=CARTESIAN_POINT('Ctrl Pts',(5.68592013212875,-0.560725865401195,
4.21997429366132));
#33763=CARTESIAN_POINT('Ctrl Pts',(5.67796749278494,-0.515518858162713,
4.31151644082153));
#33764=CARTESIAN_POINT('Ctrl Pts',(5.67001485344113,-0.451144507802385,
4.38663212069642));
#33765=CARTESIAN_POINT('Ctrl Pts',(5.66206221409732,-0.386770157442057,
4.46174780057131));
#33766=CARTESIAN_POINT('Ctrl Pts',(5.65410957475352,-0.303228463959881,
4.52043701316089));
#33767=CARTESIAN_POINT('Ctrl Pts',(5.64615693540972,-0.210733537235404,
4.55552420285805));
#33768=CARTESIAN_POINT('Ctrl Pts',(5.640386427359,-0.143618370026196,4.5809837895275));
#33769=CARTESIAN_POINT('Ctrl Pts',(5.63461591930828,-0.07178924788396,4.59401670649762));
#33770=CARTESIAN_POINT('Ctrl Pts',(5.62884541125756,1.52328526200479E-5,
4.59408648697874));
#33771=CARTESIAN_POINT('Ctrl Pts',(5.52115458874249,-1.55733839743342E-5,
4.59409663347568));
#33772=CARTESIAN_POINT('Ctrl Pts',(5.52307197716526,-0.0238731473664388,
4.59412105649149));
#33773=CARTESIAN_POINT('Ctrl Pts',(5.52498936558803,-0.0477278534282068,
4.59271130989713));
#33774=CARTESIAN_POINT('Ctrl Pts',(5.5269067540108,-0.0714062077139717,
4.58984482465595));
#33775=CARTESIAN_POINT('Ctrl Pts',(5.53485939335461,-0.169615527042917,
4.57795567218339));
#33776=CARTESIAN_POINT('Ctrl Pts',(5.54281203269841,-0.264791079455087,
4.54100634955965));
#33777=CARTESIAN_POINT('Ctrl Pts',(5.55076467204222,-0.345296357402727,
4.48351441471562));
#33778=CARTESIAN_POINT('Ctrl Pts',(5.55871731138603,-0.425801635350366,
4.4260224798716));
#33779=CARTESIAN_POINT('Ctrl Pts',(5.56666995072984,-0.491636638833473,
4.34798793280729));
#33780=CARTESIAN_POINT('Ctrl Pts',(5.57462259007364,-0.534752142022197,
4.2589515597096));
#33781=CARTESIAN_POINT('Ctrl Pts',(5.58257522941745,-0.577867645210921,
4.16991518661191));
#33782=CARTESIAN_POINT('Ctrl Pts',(5.59052786876125,-0.598263648105263,
4.06987698748084));
#33783=CARTESIAN_POINT('Ctrl Pts',(5.59848050810506,-0.59344646156208,3.97106799465478));
#33784=CARTESIAN_POINT('Ctrl Pts',(5.60643314744886,-0.588629275018896,
3.87225900182873));
#33785=CARTESIAN_POINT('Ctrl Pts',(5.61438578679267,-0.558598899038186,
3.77467921530768));
#33786=CARTESIAN_POINT('Ctrl Pts',(5.62233842613648,-0.50702695609161,3.69025909300064));
#33787=CARTESIAN_POINT('Ctrl Pts',(5.63029106548029,-0.455455013145033,
3.6058389706936));
#33788=CARTESIAN_POINT('Ctrl Pts',(5.63824370482409,-0.382341503232591,
3.53457851260056));
#33789=CARTESIAN_POINT('Ctrl Pts',(5.6461963441679,-0.296625548722353,3.48519028027742));
#33790=CARTESIAN_POINT('Ctrl Pts',(5.6541489835117,-0.210909594212113,3.43580204795428));
#33791=CARTESIAN_POINT('Ctrl Pts',(5.66210162285551,-0.112591195104077,
3.40828604140104));
#33792=CARTESIAN_POINT('Ctrl Pts',(5.67005426219932,-0.0136911147678568,
3.40600646716786));
#33793=CARTESIAN_POINT('Ctrl Pts',(5.67800690154312,0.0852089655683624,
3.40372689293467));
#33794=CARTESIAN_POINT('Ctrl Pts',(5.68595954088693,0.184690727132768,3.42668375102154));
#33795=CARTESIAN_POINT('Ctrl Pts',(5.69391218023074,0.272591169676606,3.47207025288287));
#33796=CARTESIAN_POINT('Ctrl Pts',(5.70186481957454,0.360491612220445,3.51745675474419));
#33797=CARTESIAN_POINT('Ctrl Pts',(5.70981745891835,0.436810735743714,3.58527290037998));
#33798=CARTESIAN_POINT('Ctrl Pts',(5.71777009826216,0.492217487918224,3.667227242308));
#33799=CARTESIAN_POINT('Ctrl Pts',(5.72572273760596,0.547624240092733,3.74918158423602));
#33800=CARTESIAN_POINT('Ctrl Pts',(5.73367537694977,0.582118620918482,3.84527412245626));
#33801=CARTESIAN_POINT('Ctrl Pts',(5.74162801629357,0.591483222595687,3.94375623549444));
#33802=CARTESIAN_POINT('Ctrl Pts',(5.74958065563738,0.600847824272892,4.04223834853263));
#33803=CARTESIAN_POINT('Ctrl Pts',(5.75753329498119,0.585082646801554,4.14311003638875));
#33804=CARTESIAN_POINT('Ctrl Pts',(5.76548593432499,0.546115197731279,4.23403836123177));
#33805=CARTESIAN_POINT('Ctrl Pts',(5.7734385736688,0.507147748661005,4.32496668607478));
#33806=CARTESIAN_POINT('Ctrl Pts',(5.78139121301261,0.444978027991796,4.4059516479047));
#33807=CARTESIAN_POINT('Ctrl Pts',(5.78934385235641,0.367207131024688,4.46709173242012));
#33808=CARTESIAN_POINT('Ctrl Pts',(5.79729649170022,0.28943623405758,4.52823181693554));
#33809=CARTESIAN_POINT('Ctrl Pts',(5.80524913104403,0.196064160792572,4.56952702413646));
#33810=CARTESIAN_POINT('Ctrl Pts',(5.81320177038783,0.0985069184831505,
4.58592845199323));
#33811=CARTESIAN_POINT('Ctrl Pts',(5.81585270983939,0.0659871057213339,
4.59139571767544));
#33812=CARTESIAN_POINT('Ctrl Pts',(5.81850364929094,0.0330022532417819,
4.59409688335147));
#33813=CARTESIAN_POINT('Ctrl Pts',(5.82115458874249,1.31105368646138E-5,
4.59407040741879));
#33814=CARTESIAN_POINT('Origin',(4.,0.,4.));
#33815=CARTESIAN_POINT('',(6.22884541125756,-1.27841859475647E-5,4.5940334609955));
#33816=CARTESIAN_POINT('',(6.12115458874249,-9.50793186244619E-6,4.59413936148612));
#33817=CARTESIAN_POINT('',(4.,-7.27562663373442E-17,4.5941));
#33818=CARTESIAN_POINT('Ctrl Pts',(6.22884541125756,-1.27841859475647E-5,
4.5940334609955));
#33819=CARTESIAN_POINT('Ctrl Pts',(6.22547926355963,0.0418951881409122,
4.59406590912705));
#33820=CARTESIAN_POINT('Ctrl Pts',(6.2221131158617,0.0838018877146867,4.58971510200585));
#33821=CARTESIAN_POINT('Ctrl Pts',(6.21874696816377,0.124749109322564,4.58093223526196));
#33822=CARTESIAN_POINT('Ctrl Pts',(6.21079432881996,0.22148832423537,4.56018241146135));
#33823=CARTESIAN_POINT('Ctrl Pts',(6.20284168947616,0.31287214740051,4.51469474440412));
#33824=CARTESIAN_POINT('Ctrl Pts',(6.19488905013236,0.387808805213989,4.4501133836823));
#33825=CARTESIAN_POINT('Ctrl Pts',(6.18693641078855,0.462745463027469,4.38553202296047));
#33826=CARTESIAN_POINT('Ctrl Pts',(6.17898377144474,0.521234955489287,4.30185696857405));
#33827=CARTESIAN_POINT('Ctrl Pts',(6.17103113210093,0.556083161424236,4.20927485003939));
#33828=CARTESIAN_POINT('Ctrl Pts',(6.16307849275713,0.590931367359184,4.11669273150472));
#33829=CARTESIAN_POINT('Ctrl Pts',(6.15512585341332,0.602138286767263,4.0152035488218));
#33830=CARTESIAN_POINT('Ctrl Pts',(6.14717321406952,0.588356486924291,3.9172389266648));
#33831=CARTESIAN_POINT('Ctrl Pts',(6.13922057472571,0.574574687081318,3.81927430450779));
#33832=CARTESIAN_POINT('Ctrl Pts',(6.1312679353819,0.535804167987293,3.7248342428767));
#33833=CARTESIAN_POINT('Ctrl Pts',(6.12331529603809,0.476773096629474,3.64545304401991));
#33834=CARTESIAN_POINT('Ctrl Pts',(6.11536265669429,0.417742025271657,3.56607184516312));
#33835=CARTESIAN_POINT('Ctrl Pts',(6.10741001735048,0.338450401650047,3.50174950908064));
#33836=CARTESIAN_POINT('Ctrl Pts',(6.09945737800668,0.248599092144812,3.46035682177302));
#33837=CARTESIAN_POINT('Ctrl Pts',(6.09150473866287,0.158747782639575,3.41896413446539));
#33838=CARTESIAN_POINT('Ctrl Pts',(6.08355209931906,0.0583367872507115,
3.40050109593262));
#33839=CARTESIAN_POINT('Ctrl Pts',(6.07559945997526,-0.0403606640336046,
3.40722161935946));
#33840=CARTESIAN_POINT('Ctrl Pts',(6.06764682063145,-0.139058115317921,
3.4139421427863));
#33841=CARTESIAN_POINT('Ctrl Pts',(6.05969418128764,-0.23604202249769,3.44584622817275));
#33842=CARTESIAN_POINT('Ctrl Pts',(6.05174154194384,-0.319452991027635,
3.49903499090221));
#33843=CARTESIAN_POINT('Ctrl Pts',(6.04378890260003,-0.40286395955758,3.55222375363166));
#33844=CARTESIAN_POINT('Ctrl Pts',(6.03583626325623,-0.472701989437702,
3.62669719370411));
#33845=CARTESIAN_POINT('Ctrl Pts',(6.02788362391242,-0.520429378860104,
3.71334895258148));
#33846=CARTESIAN_POINT('Ctrl Pts',(6.01993098456861,-0.568156768282506,
3.80000071145885));
#33847=CARTESIAN_POINT('Ctrl Pts',(6.0119783452248,-0.593773517247188,3.89883078914114));
#33848=CARTESIAN_POINT('Ctrl Pts',(6.004025705881,-0.594147126960238,3.99775637428654));
#33849=CARTESIAN_POINT('Ctrl Pts',(5.99607306653719,-0.594520736673288,
4.09668195943193));
#33850=CARTESIAN_POINT('Ctrl Pts',(5.98812042719339,-0.569651207134705,
4.19570305204043));
#33851=CARTESIAN_POINT('Ctrl Pts',(5.98016778784958,-0.52257944308796,4.28271270390554));
#33852=CARTESIAN_POINT('Ctrl Pts',(5.97221514850578,-0.475507679041215,
4.36972235577065));
#33853=CARTESIAN_POINT('Ctrl Pts',(5.96426250916196,-0.406233680486307,
4.44472056689237));
#33854=CARTESIAN_POINT('Ctrl Pts',(5.95630986981816,-0.323226996343023,
4.49853792802592));
#33855=CARTESIAN_POINT('Ctrl Pts',(5.94835723047435,-0.240220312199739,
4.55235528915947));
#33856=CARTESIAN_POINT('Ctrl Pts',(5.94040459113055,-0.143480942468078,
4.58499180030486));
#33857=CARTESIAN_POINT('Ctrl Pts',(5.93245195178675,-0.0448366672808267,
4.59245712746544));
#33858=CARTESIAN_POINT('Ctrl Pts',(5.93124977161035,-0.0299248641651563,
4.59358564190382));
#33859=CARTESIAN_POINT('Ctrl Pts',(5.93004759143396,-0.0149695309183627,
4.59413895459864));
#33860=CARTESIAN_POINT('Ctrl Pts',(5.92884541125757,-1.3134308860685E-5,
4.59412454375027));
#33861=CARTESIAN_POINT('Ctrl Pts',(5.82115458874249,1.31105368646138E-5,
4.59407040741879));
#33862=CARTESIAN_POINT('Ctrl Pts',(5.82645628863475,-0.0659629472043463,
4.59401745734129));
#33863=CARTESIAN_POINT('Ctrl Pts',(5.831757988527,-0.131956164688202,4.58305467757793));
#33864=CARTESIAN_POINT('Ctrl Pts',(5.83705968841925,-0.194280919321303,
4.56148970414564));
#33865=CARTESIAN_POINT('Ctrl Pts',(5.84501232776306,-0.287769103462499,
4.52914187992864));
#33866=CARTESIAN_POINT('Ctrl Pts',(5.85296496710686,-0.373003060391055,
4.47293858298203));
#33867=CARTESIAN_POINT('Ctrl Pts',(5.86091760645067,-0.439561779454174,
4.39975142997742));
#33868=CARTESIAN_POINT('Ctrl Pts',(5.86887024579447,-0.506120498517293,
4.32656427697281));
#33869=CARTESIAN_POINT('Ctrl Pts',(5.87682288513828,-0.554003979714975,
4.2363932679102));
#33870=CARTESIAN_POINT('Ctrl Pts',(5.88477552448209,-0.577357812582609,
4.14026304025204));
#33871=CARTESIAN_POINT('Ctrl Pts',(5.8927281638259,-0.600711645450243,4.04413281259387));
#33872=CARTESIAN_POINT('Ctrl Pts',(5.9006808031697,-0.59953582998783,3.94204336634015));
#33873=CARTESIAN_POINT('Ctrl Pts',(5.90863344251351,-0.573974130801472,
3.84647652011691));
#33874=CARTESIAN_POINT('Ctrl Pts',(5.91658608185731,-0.548412431615114,
3.75090967389367));
#33875=CARTESIAN_POINT('Ctrl Pts',(5.92453872120112,-0.498464848704808,
3.66186542770092));
#33876=CARTESIAN_POINT('Ctrl Pts',(5.93249136054493,-0.430238144626613,
3.59023066587279));
#33877=CARTESIAN_POINT('Ctrl Pts',(5.94044399988873,-0.362011440548417,
3.51859590404466));
#33878=CARTESIAN_POINT('Ctrl Pts',(5.94839663923254,-0.275505615302329,
3.46437062658116));
#33879=CARTESIAN_POINT('Ctrl Pts',(5.95634927857635,-0.181297202577209,
3.43418458862315));
#33880=CARTESIAN_POINT('Ctrl Pts',(5.96430191792015,-0.087088789852092,
3.40399855066514));
#33881=CARTESIAN_POINT('Ctrl Pts',(5.97225455726396,0.0148222103520573,
3.39785175221263));
#33882=CARTESIAN_POINT('Ctrl Pts',(5.98020719660777,0.111975824940657,3.41649576758492));
#33883=CARTESIAN_POINT('Ctrl Pts',(5.98815983595157,0.209129439529257,3.43513978295721));
#33884=CARTESIAN_POINT('Ctrl Pts',(5.99611247529537,0.301525668502307,3.47857461215431));
#33885=CARTESIAN_POINT('Ctrl Pts',(6.00406511463918,0.377867748972965,3.54148967172874));
#33886=CARTESIAN_POINT('Ctrl Pts',(6.01201775398299,0.454209829443624,3.60440473130317));
#33887=CARTESIAN_POINT('Ctrl Pts',(6.0199703933268,0.514497761411887,3.68680002125492));
#33888=CARTESIAN_POINT('Ctrl Pts',(6.02792303267061,0.551360647735685,3.77860175380959));
#33889=CARTESIAN_POINT('Ctrl Pts',(6.03587567201441,0.588223534059482,3.87040348636426));
#33890=CARTESIAN_POINT('Ctrl Pts',(6.04382831135821,0.601661374738811,3.97161166152184));
#33891=CARTESIAN_POINT('Ctrl Pts',(6.05178095070202,0.590030977261751,4.06985190192822));
#33892=CARTESIAN_POINT('Ctrl Pts',(6.05973359004583,0.578400579784692,4.16809214233459));
#33893=CARTESIAN_POINT('Ctrl Pts',(6.06768622938964,0.541701944151245,4.26336444798975));
#33894=CARTESIAN_POINT('Ctrl Pts',(6.07563886873345,0.484422419230229,4.3440210474869));
#33895=CARTESIAN_POINT('Ctrl Pts',(6.08359150807725,0.427142894309213,4.42467764698404));
#33896=CARTESIAN_POINT('Ctrl Pts',(6.09154414742105,0.349282480100627,4.49071854032316));
#33897=CARTESIAN_POINT('Ctrl Pts',(6.09949678676486,0.26035984028865,4.53406826097581));
#33898=CARTESIAN_POINT('Ctrl Pts',(6.10671605409073,0.179637418414302,4.5734203814938));
#33899=CARTESIAN_POINT('Ctrl Pts',(6.11393532141662,0.0897989573399868,
4.59407340590587));
#33900=CARTESIAN_POINT('Ctrl Pts',(6.12115458874249,-9.50793186244619E-6,
4.59413936148612));
#33901=CARTESIAN_POINT('Origin',(4.,0.,4.));
#33902=CARTESIAN_POINT('',(6.52884541125757,2.61457539729726E-5,4.59508370962656));
#33903=CARTESIAN_POINT('',(6.42115458874249,-0.000630941829811112,4.59394485456974));
#33904=CARTESIAN_POINT('',(4.,-7.27562663373442E-17,4.5941));
#33905=CARTESIAN_POINT('Ctrl Pts',(6.52884541125757,2.61457539729726E-5,
4.59508370962656));
#33906=CARTESIAN_POINT('Ctrl Pts',(6.5129582963415,0.196771080344787,4.59506033873941));
#33907=CARTESIAN_POINT('Ctrl Pts',(6.49707118142544,0.393450480974957,4.48779253427891));
#33908=CARTESIAN_POINT('Ctrl Pts',(6.48118406650938,0.500111739713094,4.32240987211318));
#33909=CARTESIAN_POINT('Ctrl Pts',(6.46527878782176,0.606894944490356,4.15683812760557));
#33910=CARTESIAN_POINT('Ctrl Pts',(6.44937350913416,0.623454053851315,3.93301856375293));
#33911=CARTESIAN_POINT('Ctrl Pts',(6.43346823044654,0.541809843535619,3.75368369989414));
#33912=CARTESIAN_POINT('Ctrl Pts',(6.41756295175893,0.460165633219924,3.57434883603535));
#33913=CARTESIAN_POINT('Ctrl Pts',(6.40165767307132,0.280318103227576,3.43949867217041));
#33914=CARTESIAN_POINT('Ctrl Pts',(6.3857523943837,0.085604811340831,3.41110814665827));
#33915=CARTESIAN_POINT('Ctrl Pts',(6.36984711569609,-0.109108480545914,
3.38271762114613));
#33916=CARTESIAN_POINT('Ctrl Pts',(6.35394183700848,-0.318687534327053,
3.46078673398678));
#33917=CARTESIAN_POINT('Ctrl Pts',(6.33803655832087,-0.448733343985475,
3.60951691634857));
#33918=CARTESIAN_POINT('Ctrl Pts',(6.33008391897706,-0.513756248814686,
3.68388200752946));
#33919=CARTESIAN_POINT('Ctrl Pts',(6.32213127963325,-0.558895842613217,
3.77591236609064));
#33920=CARTESIAN_POINT('Ctrl Pts',(6.31417864028945,-0.579995970841135,
3.87270290659392));
#33921=CARTESIAN_POINT('Ctrl Pts',(6.30622600094564,-0.601096099069052,
3.9694934470972));
#33922=CARTESIAN_POINT('Ctrl Pts',(6.29827336160184,-0.598156761726356,
4.07104416954258));
#33923=CARTESIAN_POINT('Ctrl Pts',(6.29032072225803,-0.570614590620327,
4.16591643177432));
#33924=CARTESIAN_POINT('Ctrl Pts',(6.28236808291422,-0.543072419514299,
4.26078869400605));
#33925=CARTESIAN_POINT('Ctrl Pts',(6.27441544357042,-0.490927414644939,
4.34898249602413));
#33926=CARTESIAN_POINT('Ctrl Pts',(6.26646280422661,-0.421087730399527,
4.41916768405122));
#33927=CARTESIAN_POINT('Ctrl Pts',(6.2585101648828,-0.351248046154114,4.48935287207832));
#33928=CARTESIAN_POINT('Ctrl Pts',(6.250557525539,-0.263713682532649,4.54152944611444));
#33929=CARTESIAN_POINT('Ctrl Pts',(6.24260488619519,-0.168899197391682,
4.5696117428605));
#33930=CARTESIAN_POINT('Ctrl Pts',(6.23801839454932,-0.114217245248871,
4.58580752565092));
#33931=CARTESIAN_POINT('Ctrl Pts',(6.23343190290344,-0.0571138332845632,
4.59398924930378));
#33932=CARTESIAN_POINT('Ctrl Pts',(6.22884541125756,-1.27841859475647E-5,
4.5940334609955));
#33933=CARTESIAN_POINT('Ctrl Pts',(6.12115458874249,-9.50793186244619E-6,
4.59413936148612));
#33934=CARTESIAN_POINT('Ctrl Pts',(6.12188796076042,-0.00913273504488762,
4.59414606160884));
#33935=CARTESIAN_POINT('Ctrl Pts',(6.12262133277835,-0.0182556526135436,
4.59394031163173));
#33936=CARTESIAN_POINT('Ctrl Pts',(6.12335470479628,-0.0273686726716501,
4.59352013235631));
#33937=CARTESIAN_POINT('Ctrl Pts',(6.13130734414009,-0.126189680404606,
4.58896373511797));
#33938=CARTESIAN_POINT('Ctrl Pts',(6.13925998348389,-0.223846830455152,
4.55919239267511));
#33939=CARTESIAN_POINT('Ctrl Pts',(6.14721262282769,-0.308403173896691,
4.50784224986958));
#33940=CARTESIAN_POINT('Ctrl Pts',(6.1551652621715,-0.392959517338232,4.45649210706404));
#33941=CARTESIAN_POINT('Ctrl Pts',(6.16311790151532,-0.464415054170765,
4.38356316389581));
#33942=CARTESIAN_POINT('Ctrl Pts',(6.17107054085912,-0.514027768136376,
4.29797916579711));
#33943=CARTESIAN_POINT('Ctrl Pts',(6.17902318020293,-0.563640482101988,
4.2123951676984));
#33944=CARTESIAN_POINT('Ctrl Pts',(6.18697581954673,-0.591410373200678,
4.11415611466921));
#33945=CARTESIAN_POINT('Ctrl Pts',(6.19492845889053,-0.593952774873424,
4.0152594949342));
#33946=CARTESIAN_POINT('Ctrl Pts',(6.20288109823434,-0.59649517654617,3.9163628751992));
#33947=CARTESIAN_POINT('Ctrl Pts',(6.21083373757815,-0.573810088792972,
3.81680868875837));
#33948=CARTESIAN_POINT('Ctrl Pts',(6.21878637692196,-0.528651094032059,
3.72879442104321));
#33949=CARTESIAN_POINT('Ctrl Pts',(6.22673901626577,-0.483492099271145,
3.64078015332805));
#33950=CARTESIAN_POINT('Ctrl Pts',(6.23469165560957,-0.415859197502516,
3.56430580433857));
#33951=CARTESIAN_POINT('Ctrl Pts',(6.24264429495337,-0.334059153459168,
3.50867301156809));
#33952=CARTESIAN_POINT('Ctrl Pts',(6.25059693429718,-0.252259109415819,
3.45304021879761));
#33953=CARTESIAN_POINT('Ctrl Pts',(6.25854957364099,-0.156291923097747,
3.41824898224614));
#33954=CARTESIAN_POINT('Ctrl Pts',(6.2665022129848,-0.057819682214149,3.40864436538418));
#33955=CARTESIAN_POINT('Ctrl Pts',(6.2744548523286,0.0406525586694487,3.39903974852221));
#33956=CARTESIAN_POINT('Ctrl Pts',(6.28240749167241,0.141629854118573,3.41462175134974));
#33957=CARTESIAN_POINT('Ctrl Pts',(6.29036013101621,0.232632044389671,3.453312878872));
#33958=CARTESIAN_POINT('Ctrl Pts',(6.29831277036002,0.323634234660771,3.49200400639426));
#33959=CARTESIAN_POINT('Ctrl Pts',(6.30626540970382,0.404661319753841,3.55380425861124));
#33960=CARTESIAN_POINT('Ctrl Pts',(6.31421804904763,0.466059055789261,3.63148218419904));
#33961=CARTESIAN_POINT('Ctrl Pts',(6.32217068839144,0.527456791824679,3.70916010978684));
#33962=CARTESIAN_POINT('Ctrl Pts',(6.33012332773525,0.569225178802449,3.80271570874544));
#33963=CARTESIAN_POINT('Ctrl Pts',(6.33807596707905,0.585790493249255,3.90010619949006));
#33964=CARTESIAN_POINT('Ctrl Pts',(6.34602860642286,0.602355807696062,3.99749669023468));
#33965=CARTESIAN_POINT('Ctrl Pts',(6.35398124576666,0.593718049611903,4.09872207276531));
#33966=CARTESIAN_POINT('Ctrl Pts',(6.36193388511047,0.56173881546021,4.19248215342453));
#33967=CARTESIAN_POINT('Ctrl Pts',(6.36988652445427,0.529759581308516,4.28624223408375));
#33968=CARTESIAN_POINT('Ctrl Pts',(6.37783916379808,0.474438871089287,4.37253701287156));
#33969=CARTESIAN_POINT('Ctrl Pts',(6.38579180314189,0.401374624788453,4.4390182948332));
#33970=CARTESIAN_POINT('Ctrl Pts',(6.39757939834209,0.293077024234899,4.53755846574697));
#33971=CARTESIAN_POINT('Ctrl Pts',(6.40936699354229,0.145797072855576,4.59256860517148));
#33972=CARTESIAN_POINT('Ctrl Pts',(6.42115458874249,-0.000630941829811112,
4.59394485456974));
#33973=CARTESIAN_POINT('Origin',(4.,0.,4.));
#33974=CARTESIAN_POINT('',(6.82884541125756,0.000528213615369061,4.5937871332276));
#33975=CARTESIAN_POINT('',(6.72115458874249,0.000109070110168276,4.59505938903171));
#33976=CARTESIAN_POINT('',(4.,-7.27562663373442E-17,4.5941));
#33977=CARTESIAN_POINT('Ctrl Pts',(6.82884541125756,0.000528213615369061,
4.5937871332276));
#33978=CARTESIAN_POINT('Ctrl Pts',(6.82429524715479,0.0572034606387535,
4.59426930340541));
#33979=CARTESIAN_POINT('Ctrl Pts',(6.81974508305202,0.113754426020979,4.58681959872387));
#33980=CARTESIAN_POINT('Ctrl Pts',(6.81519491894924,0.167823213394864,4.57092612439125));
#33981=CARTESIAN_POINT('Ctrl Pts',(6.79928964026163,0.356822799356826,4.51536985589957));
#33982=CARTESIAN_POINT('Ctrl Pts',(6.78338436157403,0.515493156338912,4.35664088088147));
#33983=CARTESIAN_POINT('Ctrl Pts',(6.76747908288642,0.570983871223461,4.16762126762428));
#33984=CARTESIAN_POINT('Ctrl Pts',(6.7515738041988,0.626474586108011,3.97860165436708));
#33985=CARTESIAN_POINT('Ctrl Pts',(6.73566852551118,0.578785658895023,3.75929140287077));
#33986=CARTESIAN_POINT('Ctrl Pts',(6.71976324682357,0.449805704301045,3.61038767491097));
#33987=CARTESIAN_POINT('Ctrl Pts',(6.70385796813595,0.320825749707067,3.46148394695116));
#33988=CARTESIAN_POINT('Ctrl Pts',(6.68795268944834,0.110554767732096,3.38298674252784));
#33989=CARTESIAN_POINT('Ctrl Pts',(6.67204741076073,-0.0844443642884844,
3.4109402193496));
#33990=CARTESIAN_POINT('Ctrl Pts',(6.65614213207312,-0.279443496309066,
3.43889369617135));
#33991=CARTESIAN_POINT('Ctrl Pts',(6.64023685338551,-0.459170778375258,
3.57329785423817));
#33992=CARTESIAN_POINT('Ctrl Pts',(6.6243315746979,-0.541132009270427,3.75243704050979));
#33993=CARTESIAN_POINT('Ctrl Pts',(6.60842629601029,-0.623093240165596,
3.9315762267814));
#33994=CARTESIAN_POINT('Ctrl Pts',(6.59252101732267,-0.60728841988974,4.15545044125781));
#33995=CARTESIAN_POINT('Ctrl Pts',(6.57661573863506,-0.500919754058047,
4.32127168369798));
#33996=CARTESIAN_POINT('Ctrl Pts',(6.56069229617589,-0.394429615589227,
4.48728229340579));
#33997=CARTESIAN_POINT('Ctrl Pts',(6.54476885371673,-0.197168666623305,
4.59510713395368));
#33998=CARTESIAN_POINT('Ctrl Pts',(6.52884541125757,2.61457539729726E-5,
4.59508370962656));
#33999=CARTESIAN_POINT('Ctrl Pts',(6.42115458874249,-0.000630941829811112,
4.59394485456974));
#34000=CARTESIAN_POINT('Ctrl Pts',(6.4252722722299,-0.0517816819022344,
4.59442561076518));
#34001=CARTESIAN_POINT('Ctrl Pts',(6.42938995571731,-0.102828462800867,
4.58836159088269));
#34002=CARTESIAN_POINT('Ctrl Pts',(6.43350763920472,-0.152073274319339,
4.5753220992581));
#34003=CARTESIAN_POINT('Ctrl Pts',(6.44941291789233,-0.342290043897387,
4.52495476314113));
#34004=CARTESIAN_POINT('Ctrl Pts',(6.46531819657995,-0.5056209461254,4.37051151428857));
#34005=CARTESIAN_POINT('Ctrl Pts',(6.48122347526756,-0.56632363157735,4.18304963962536));
#34006=CARTESIAN_POINT('Ctrl Pts',(6.49712875395518,-0.627026317029301,
3.99558776496215));
#34007=CARTESIAN_POINT('Ctrl Pts',(6.51303403264279,-0.58510078570519,3.77510726448829));
#34008=CARTESIAN_POINT('Ctrl Pts',(6.5289393113304,-0.460166914262479,3.62276494217392));
#34009=CARTESIAN_POINT('Ctrl Pts',(6.54484459001801,-0.335233042819767,
3.47042261985956));
#34010=CARTESIAN_POINT('Ctrl Pts',(6.56074986870563,-0.127290831258456,
3.38621847570468));
#34011=CARTESIAN_POINT('Ctrl Pts',(6.57665514739324,0.068373869747762,3.4088573345089));
#34012=CARTESIAN_POINT('Ctrl Pts',(6.59256042608085,0.26403857075398,3.43149619331313));
#34013=CARTESIAN_POINT('Ctrl Pts',(6.60846570476847,0.447425761205104,3.56097805507645));
#34014=CARTESIAN_POINT('Ctrl Pts',(6.62437098345608,0.534230294511761,3.73782813427527));
#34015=CARTESIAN_POINT('Ctrl Pts',(6.64027626214369,0.621034827818418,3.91467821347409));
#34016=CARTESIAN_POINT('Ctrl Pts',(6.65618154083131,0.611256703980608,4.1388965101084));
#34017=CARTESIAN_POINT('Ctrl Pts',(6.67208681951892,0.509439333868548,4.30754322537844));
#34018=CARTESIAN_POINT('Ctrl Pts',(6.68799209820653,0.40762196375649,4.47618994064847));
#34019=CARTESIAN_POINT('Ctrl Pts',(6.70389737689414,0.213765347370184,4.58926507455422));
#34020=CARTESIAN_POINT('Ctrl Pts',(6.71980265558175,0.016851802420978,4.59484308232941));
#34021=CARTESIAN_POINT('Ctrl Pts',(6.72025329996867,0.0112726493937942,
4.59500112406784));
#34022=CARTESIAN_POINT('Ctrl Pts',(6.72070394435558,0.00569104238866241,
4.59507287148453));
#34023=CARTESIAN_POINT('Ctrl Pts',(6.72115458874249,0.000109070110168276,
4.59505938903171));
#34024=CARTESIAN_POINT('Origin',(4.,0.,4.));
#34025=CARTESIAN_POINT('',(7.12884541125757,-0.000233413975479213,4.59320261234329));
#34026=CARTESIAN_POINT('',(7.02115458874249,0.000491936389841303,4.5936290357477));
#34027=CARTESIAN_POINT('',(4.,-7.27562663373442E-17,4.5941));
#34028=CARTESIAN_POINT('Ctrl Pts',(7.12884541125757,-0.000233413975479213,
4.59320261234329));
#34029=CARTESIAN_POINT('Ctrl Pts',(7.11972691928047,0.113624805666132,4.59280158872514));
#34030=CARTESIAN_POINT('Ctrl Pts',(7.11060842730338,0.227688545642871,4.56127879346404));
#34031=CARTESIAN_POINT('Ctrl Pts',(7.10148993532628,0.322592019514134,4.50005536307953));
#34032=CARTESIAN_POINT('Ctrl Pts',(7.08558465663867,0.488131036726243,4.39326405099382));
#34033=CARTESIAN_POINT('Ctrl Pts',(7.06967937795105,0.595374147168556,4.19610732087965));
#34034=CARTESIAN_POINT('Ctrl Pts',(7.05377409926343,0.595079946532544,3.99911121186167));
#34035=CARTESIAN_POINT('Ctrl Pts',(7.03786882057582,0.594785745896532,3.80211510284369));
#34036=CARTESIAN_POINT('Ctrl Pts',(7.02196354188821,0.486954234182196,3.60527961492189));
#34037=CARTESIAN_POINT('Ctrl Pts',(7.0060582632006,0.321096900356496,3.49898325846904));
#34038=CARTESIAN_POINT('Ctrl Pts',(6.99015298451299,0.155239566530797,3.3926869020162));
#34039=CARTESIAN_POINT('Ctrl Pts',(6.97424770582538,-0.0686435894062663,
3.37692967703231));
#34040=CARTESIAN_POINT('Ctrl Pts',(6.95834242713776,-0.247754555527299,
3.45894666907189));
#34041=CARTESIAN_POINT('Ctrl Pts',(6.94243714845015,-0.426865521648332,
3.54096366111146));
#34042=CARTESIAN_POINT('Ctrl Pts',(6.92653186976253,-0.561204297953336,
3.72075487017451));
#34043=CARTESIAN_POINT('Ctrl Pts',(6.91062659107492,-0.589088840804576,
3.91576771430201));
#34044=CARTESIAN_POINT('Ctrl Pts',(6.89472131238731,-0.616973383655816,
4.11078055842951));
#34045=CARTESIAN_POINT('Ctrl Pts',(6.8788160336997,-0.538403693053295,4.32101503762147));
#34046=CARTESIAN_POINT('Ctrl Pts',(6.86291075501209,-0.389454440281117,
4.44994049623482));
#34047=CARTESIAN_POINT('Ctrl Pts',(6.85155564042725,-0.283116420949728,
4.54198310574898));
#34048=CARTESIAN_POINT('Ctrl Pts',(6.8402005258424,-0.140907108175025,4.59258385846765));
#34049=CARTESIAN_POINT('Ctrl Pts',(6.82884541125756,0.000528213615369061,
4.5937871332276));
#34050=CARTESIAN_POINT('Ctrl Pts',(6.72115458874249,0.000109070110168276,
4.59505938903171));
#34051=CARTESIAN_POINT('Ctrl Pts',(6.73660922304319,-0.191322006690816,
4.59459701474307));
#34052=CARTESIAN_POINT('Ctrl Pts',(6.75206385734389,-0.38318268672033,4.49389457135631));
#34053=CARTESIAN_POINT('Ctrl Pts',(6.76751849164459,-0.49122657597837,4.33588597251985));
#34054=CARTESIAN_POINT('Ctrl Pts',(6.78342377033221,-0.60242093591639,4.17326997329048));
#34055=CARTESIAN_POINT('Ctrl Pts',(6.79932904901982,-0.624839182280325,
3.94995709318712));
#34056=CARTESIAN_POINT('Ctrl Pts',(6.81523432770743,-0.548195780923551,
3.76848141254984));
#34057=CARTESIAN_POINT('Ctrl Pts',(6.83113960639504,-0.471552379566775,
3.58700573191256));
#34058=CARTESIAN_POINT('Ctrl Pts',(6.84704488508266,-0.295847330489284,
3.44736725074137));
#34059=CARTESIAN_POINT('Ctrl Pts',(6.86295016377027,-0.101752734572189,
3.41368297698799));
#34060=CARTESIAN_POINT('Ctrl Pts',(6.87885544245788,0.0923418613449005,
3.37999870323461));
#34061=CARTESIAN_POINT('Ctrl Pts',(6.8947607211455,0.304826004101594,3.45226863689903));
#34062=CARTESIAN_POINT('Ctrl Pts',(6.91066599983311,0.438133727661537,3.59730899203965));
#34063=CARTESIAN_POINT('Ctrl Pts',(6.92657127852072,0.571441451221483,3.74234934718029));
#34064=CARTESIAN_POINT('Ctrl Pts',(6.94247655720833,0.625572755584675,3.96016012379713));
#34065=CARTESIAN_POINT('Ctrl Pts',(6.95838183589594,0.57567402069499,4.15073208753033));
#34066=CARTESIAN_POINT('Ctrl Pts',(6.97428711458356,0.525775285805305,4.34130405126353));
#34067=CARTESIAN_POINT('Ctrl Pts',(6.99019239327118,0.371846511662747,4.5046372021131));
#34068=CARTESIAN_POINT('Ctrl Pts',(7.00609767195879,0.184564651688987,4.56573572985967));
#34069=CARTESIAN_POINT('Ctrl Pts',(7.01111664422002,0.125467135782336,4.58501560681028));
#34070=CARTESIAN_POINT('Ctrl Pts',(7.01613561648126,0.0630485115161635,
4.59411554829291));
#34071=CARTESIAN_POINT('Ctrl Pts',(7.02115458874249,0.000491936389841303,
4.5936290357477));
#34072=CARTESIAN_POINT('Origin',(4.,0.,4.));
#34073=CARTESIAN_POINT('',(7.42884541125756,-0.000438237927964824,4.59464495791636));
#34074=CARTESIAN_POINT('',(7.32115458874249,-0.000317338366111653,4.59328419319629));
#34075=CARTESIAN_POINT('',(4.,-7.27562663373442E-17,4.5941));
#34076=CARTESIAN_POINT('Ctrl Pts',(7.42884541125756,-0.000438237927964824,
4.59464495791636));
#34077=CARTESIAN_POINT('Ctrl Pts',(7.41515859140615,0.169409178821721,4.5932420274804));
#34078=CARTESIAN_POINT('Ctrl Pts',(7.40147177155473,0.340360224580004,4.51673272682389));
#34079=CARTESIAN_POINT('Ctrl Pts',(7.38778495170331,0.450965110664874,4.38826722161738));
#34080=CARTESIAN_POINT('Ctrl Pts',(7.37187967301569,0.579497637321094,4.23897909740477));
#34081=CARTESIAN_POINT('Ctrl Pts',(7.35597439432808,0.626535888751401,4.01952688559808));
#34082=CARTESIAN_POINT('Ctrl Pts',(7.34006911564046,0.570481892017836,3.83067375781486));
#34083=CARTESIAN_POINT('Ctrl Pts',(7.32416383695285,0.51442789528427,3.64182063003164));
#34084=CARTESIAN_POINT('Ctrl Pts',(7.30825855826524,0.355281650386831,3.48356658627189));
#34085=CARTESIAN_POINT('Ctrl Pts',(7.29235327957763,0.166116376105148,3.42857518785077));
#34086=CARTESIAN_POINT('Ctrl Pts',(7.27644800089002,-0.023048898176535,
3.37358378942964));
#34087=CARTESIAN_POINT('Ctrl Pts',(7.2605427222024,-0.242233201842457,3.42185503634715));
#34088=CARTESIAN_POINT('Ctrl Pts',(7.24463744351479,-0.390796368104757,
3.5512248149675));
#34089=CARTESIAN_POINT('Ctrl Pts',(7.22873216482718,-0.539359534367058,
3.68059459358785));
#34090=CARTESIAN_POINT('Ctrl Pts',(7.21282688613957,-0.617301563225728,
3.89106290391106));
#34091=CARTESIAN_POINT('Ctrl Pts',(7.19692160745195,-0.588834786584626,
4.08599160058025));
#34092=CARTESIAN_POINT('Ctrl Pts',(7.18101632876434,-0.560368009943526,
4.28092029724944));
#34093=CARTESIAN_POINT('Ctrl Pts',(7.16511105007672,-0.425492427802657,
4.46030938026461));
#34094=CARTESIAN_POINT('Ctrl Pts',(7.14920577138911,-0.24613717474127,4.54179097474357));
#34095=CARTESIAN_POINT('Ctrl Pts',(7.1424189846786,-0.169606239833077,4.57655919310821));
#34096=CARTESIAN_POINT('Ctrl Pts',(7.13563219796808,-0.0849767524450092,
4.59350108952231));
#34097=CARTESIAN_POINT('Ctrl Pts',(7.12884541125757,-0.000233413975479213,
4.59320261234329));
#34098=CARTESIAN_POINT('Ctrl Pts',(7.02115458874249,0.000491936389841303,
4.5936290357477));
#34099=CARTESIAN_POINT('Ctrl Pts',(7.03204089516887,-0.135195214358064,
4.59257377495492));
#34100=CARTESIAN_POINT('Ctrl Pts',(7.04292720159524,-0.271531381894462,
4.54641716720817));
#34101=CARTESIAN_POINT('Ctrl Pts',(7.05381350802162,-0.376033620593693,
4.46121547122365));
#34102=CARTESIAN_POINT('Ctrl Pts',(7.06971878670923,-0.528715087097646,
4.33673278019746));
#34103=CARTESIAN_POINT('Ctrl Pts',(7.08562406539685,-0.613443074300594,
4.1289034935015));
#34104=CARTESIAN_POINT('Ctrl Pts',(7.10152934408446,-0.591314251018945,
3.93315398851514));
#34105=CARTESIAN_POINT('Ctrl Pts',(7.11743462277207,-0.569185427737295,
3.73740448352876));
#34106=CARTESIAN_POINT('Ctrl Pts',(7.13333990145968,-0.440199793971044,
3.55373476025198));
#34107=CARTESIAN_POINT('Ctrl Pts',(7.14924518014729,-0.263582002606135,
3.46647820559892));
#34108=CARTESIAN_POINT('Ctrl Pts',(7.16515045883491,-0.0869642112412332,
3.37922165094586));
#34109=CARTESIAN_POINT('Ctrl Pts',(7.18105573752253,0.137285737722324,3.38837826491652));
#34110=CARTESIAN_POINT('Ctrl Pts',(7.19696101621014,0.306201705590428,3.48974370695041));
#34111=CARTESIAN_POINT('Ctrl Pts',(7.21286629489775,0.47511767345854,3.59110914898431));
#34112=CARTESIAN_POINT('Ctrl Pts',(7.22877157358536,0.588699660231196,3.78468341908144));
#34113=CARTESIAN_POINT('Ctrl Pts',(7.24467685227297,0.594795648982816,3.98158540759));
#34114=CARTESIAN_POINT('Ctrl Pts',(7.26058213096058,0.600891637734436,4.17848739609855));
#34115=CARTESIAN_POINT('Ctrl Pts',(7.2764874096482,0.499501628465021,4.37871710301853));
#34116=CARTESIAN_POINT('Ctrl Pts',(7.29239268833581,0.337179610128186,4.49033751492072));
#34117=CARTESIAN_POINT('Ctrl Pts',(7.30197998847137,0.239335998647354,4.5576194790522));
#34118=CARTESIAN_POINT('Ctrl Pts',(7.31156728860693,0.119353510611835,4.59270637405629));
#34119=CARTESIAN_POINT('Ctrl Pts',(7.32115458874249,-0.000317338366111653,
4.59328419319629));
#34120=CARTESIAN_POINT('Origin',(4.,0.,4.));
#34121=CARTESIAN_POINT('',(7.72884541125757,0.000455182276646732,4.59460030787683));
#34122=CARTESIAN_POINT('',(7.62115458874249,-0.000367422317862595,4.59479267874092));
#34123=CARTESIAN_POINT('',(4.,-7.27562663373442E-17,4.5941));
#34124=CARTESIAN_POINT('Ctrl Pts',(7.72884541125757,0.000455182276646732,
4.59460030787683));
#34125=CARTESIAN_POINT('Ctrl Pts',(7.72649554221944,0.0296217258780686,
4.59484761241511));
#34126=CARTESIAN_POINT('Ctrl Pts',(7.72414567318131,0.0587549042441869,
4.59288776399295));
#34127=CARTESIAN_POINT('Ctrl Pts',(7.72179580414318,0.0875427725731367,
4.58860617484604));
#34128=CARTESIAN_POINT('Ctrl Pts',(7.70589052545556,0.282395788279217,4.55962589232715));
#34129=CARTESIAN_POINT('Ctrl Pts',(7.68998524676794,0.461428877889185,4.42427810603975));
#34130=CARTESIAN_POINT('Ctrl Pts',(7.67407996808033,0.542437620895056,4.24470879335187));
#34131=CARTESIAN_POINT('Ctrl Pts',(7.65817468939272,0.623446363900926,4.065139480664));
#34132=CARTESIAN_POINT('Ctrl Pts',(7.64226941070511,0.606430760302702,3.84134864157567));
#34133=CARTESIAN_POINT('Ctrl Pts',(7.6263641320175,0.499203655448083,3.67609156159133));
#34134=CARTESIAN_POINT('Ctrl Pts',(7.61045885332988,0.391976550593464,3.51083448160699));
#34135=CARTESIAN_POINT('Ctrl Pts',(7.59455357464227,0.19453794448245,3.40411116072664));
#34136=CARTESIAN_POINT('Ctrl Pts',(7.57864829595466,-0.00245670798462758,
3.40492443279829));
#34137=CARTESIAN_POINT('Ctrl Pts',(7.56274301726704,-0.199451360451705,
3.40573770486994));
#34138=CARTESIAN_POINT('Ctrl Pts',(7.54683773857943,-0.396002059274846,
3.5140875698936));
#34139=CARTESIAN_POINT('Ctrl Pts',(7.53093245989182,-0.50186103876401,3.68022435377194));
#34140=CARTESIAN_POINT('Ctrl Pts',(7.51502718120421,-0.607720018253171,
3.84636113765028));
#34141=CARTESIAN_POINT('Ctrl Pts',(7.4991219025166,-0.622887278408357,4.07028484038331));
#34142=CARTESIAN_POINT('Ctrl Pts',(7.48321662382898,-0.540398655351294,
4.24917917107494));
#34143=CARTESIAN_POINT('Ctrl Pts',(7.46731134514137,-0.45791003229423,4.42807350176658));
#34144=CARTESIAN_POINT('Ctrl Pts',(7.45140606645375,-0.277765526024924,
4.56193846041682));
#34145=CARTESIAN_POINT('Ctrl Pts',(7.43550078776614,-0.0826798719492015,
4.58930892143267));
#34146=CARTESIAN_POINT('Ctrl Pts',(7.43328232892995,-0.0554694406452989,
4.59312653709876));
#34147=CARTESIAN_POINT('Ctrl Pts',(7.43106387009376,-0.0279683367079049,
4.5948723550368));
#34148=CARTESIAN_POINT('Ctrl Pts',(7.42884541125756,-0.000438237927964824,
4.59464495791636));
#34149=CARTESIAN_POINT('Ctrl Pts',(7.32115458874249,-0.000317338366111653,
4.59328419319629));
#34150=CARTESIAN_POINT('Ctrl Pts',(7.32747256729455,-0.0791797758050172,
4.59366497286126));
#34151=CARTESIAN_POINT('Ctrl Pts',(7.3337905458466,-0.157906876560309,4.57905936436794));
#34152=CARTESIAN_POINT('Ctrl Pts',(7.34010852439865,-0.230073660466993,
4.54880513582638));
#34153=CARTESIAN_POINT('Ctrl Pts',(7.35601380308626,-0.411750885321067,
4.47264122794544));
#34154=CARTESIAN_POINT('Ctrl Pts',(7.37191908177388,-0.551851307624962,
4.29730229529918));
#34155=CARTESIAN_POINT('Ctrl Pts',(7.38782436046149,-0.586046744500155,
4.10329655692985));
#34156=CARTESIAN_POINT('Ctrl Pts',(7.4037296391491,-0.620242181375348,3.90929081856053));
#34157=CARTESIAN_POINT('Ctrl Pts',(7.41963491783671,-0.548532632821828,
3.69661827446815));
#34158=CARTESIAN_POINT('Ctrl Pts',(7.43554019652432,-0.403844087697925,
3.56292915991696));
#34159=CARTESIAN_POINT('Ctrl Pts',(7.45144547521194,-0.259155542574025,
3.42924004536577));
#34160=CARTESIAN_POINT('Ctrl Pts',(7.46735075389955,-0.0414880008797467,
3.37453436035576));
#34161=CARTESIAN_POINT('Ctrl Pts',(7.48325603258717,0.149214809903968,3.42393064079835));
#34162=CARTESIAN_POINT('Ctrl Pts',(7.49916131127478,0.339917620687686,3.47332692124094));
#34163=CARTESIAN_POINT('Ctrl Pts',(7.51506658996239,0.50365570056084,3.62682516713614));
#34164=CARTESIAN_POINT('Ctrl Pts',(7.53097186865001,0.56524745100941,3.81394547807041));
#34165=CARTESIAN_POINT('Ctrl Pts',(7.54687714733762,0.626839201457978,4.00106578900469));
#34166=CARTESIAN_POINT('Ctrl Pts',(7.56278242602523,0.58628462248197,4.22180816497804));
#34167=CARTESIAN_POINT('Ctrl Pts',(7.57868770471284,0.462204660718925,4.3748170457164));
#34168=CARTESIAN_POINT('Ctrl Pts',(7.59284333272272,0.351774041004839,4.51099427596058));
#34169=CARTESIAN_POINT('Ctrl Pts',(7.60699896073261,0.175183620117616,4.59352033541115));
#34170=CARTESIAN_POINT('Ctrl Pts',(7.62115458874249,-0.000367422317862596,
4.59479267874092));
#34171=CARTESIAN_POINT('Origin',(4.,0.,4.));
#34172=CARTESIAN_POINT('',(8.02884541125756,0.000208508845897126,4.59318438507865));
#34173=CARTESIAN_POINT('',(7.92115458874249,0.000504499356536197,4.59443266285439));
#34174=CARTESIAN_POINT('',(4.,-7.27562663373442E-17,4.5941));
#34175=CARTESIAN_POINT('Ctrl Pts',(8.02884541125756,0.000208508845897126,
4.59318438507865));
#34176=CARTESIAN_POINT('Ctrl Pts',(8.02192721434511,0.0865993248636432,
4.5934556945658));
#34177=CARTESIAN_POINT('Ctrl Pts',(8.01500901743265,0.17288466952141,4.57582457789876));
#34178=CARTESIAN_POINT('Ctrl Pts',(8.0080908205202,0.250602156771344,4.53974023855861));
#34179=CARTESIAN_POINT('Ctrl Pts',(7.99218554183259,0.42927852421987,4.4567805482338));
#34180=CARTESIAN_POINT('Ctrl Pts',(7.97628026314498,0.562668370741438,4.27628395749428));
#34181=CARTESIAN_POINT('Ctrl Pts',(7.96037498445736,0.589524722071826,4.08112686462655));
#34182=CARTESIAN_POINT('Ctrl Pts',(7.94446970576975,0.616381073402214,3.88596977175883));
#34183=CARTESIAN_POINT('Ctrl Pts',(7.92856442708213,0.536703929541425,3.67615217676291));
#34184=CARTESIAN_POINT('Ctrl Pts',(7.91265914839452,0.387077664089382,3.54801344261061));
#34185=CARTESIAN_POINT('Ctrl Pts',(7.89675386970691,0.237451398637336,3.41987470845831));
#34186=CARTESIAN_POINT('Ctrl Pts',(7.88084859101929,0.0178760115940344,
3.37341483514963));
#34187=CARTESIAN_POINT('Ctrl Pts',(7.86494331233168,-0.170828768780714,
3.42996623095257));
#34188=CARTESIAN_POINT('Ctrl Pts',(7.84903803364407,-0.359533549155462,
3.48651762675552));
#34189=CARTESIAN_POINT('Ctrl Pts',(7.83313275495647,-0.517367722861657,
3.64608029167009));
#34190=CARTESIAN_POINT('Ctrl Pts',(7.81722747626885,-0.571860514742998,
3.83538980050754));
#34191=CARTESIAN_POINT('Ctrl Pts',(7.80132219758124,-0.626353306624339,
4.02469930934499));
#34192=CARTESIAN_POINT('Ctrl Pts',(7.78541691889362,-0.577504716680827,
4.24375566210532));
#34193=CARTESIAN_POINT('Ctrl Pts',(7.769511640206,-0.447743950807975,4.3919774491103));
#34194=CARTESIAN_POINT('Ctrl Pts',(7.75595623055652,-0.337154229471824,
4.51830073342946));
#34195=CARTESIAN_POINT('Ctrl Pts',(7.74240082090705,-0.16779438404434,4.593173711641));
#34196=CARTESIAN_POINT('Ctrl Pts',(7.72884541125757,0.000455182276646732,
4.59460030787683));
#34197=CARTESIAN_POINT('Ctrl Pts',(7.62115458874249,-0.000367422317862596,
4.59479267874092));
#34198=CARTESIAN_POINT('Ctrl Pts',(7.62290423942022,-0.022065717876263,
4.59494994172972));
#34199=CARTESIAN_POINT('Ctrl Pts',(7.62465389009795,-0.043748134618359,
4.59386587358433));
#34200=CARTESIAN_POINT('Ctrl Pts',(7.62640354077568,-0.0652877816099521,
4.59148835294282));
#34201=CARTESIAN_POINT('Ctrl Pts',(7.64230881946329,-0.261094917625702,
4.56987539392751));
#34202=CARTESIAN_POINT('Ctrl Pts',(7.6582140981509,-0.445103845107109,4.44137409039354));
#34203=CARTESIAN_POINT('Ctrl Pts',(7.67411937683852,-0.532825449416136,
4.2649868044631));
#34204=CARTESIAN_POINT('Ctrl Pts',(7.69002465552613,-0.620547053725161,
4.08859951853267));
#34205=CARTESIAN_POINT('Ctrl Pts',(7.70592993421374,-0.611981334861803,
3.86432625020577));
#34206=CARTESIAN_POINT('Ctrl Pts',(7.72183521290136,-0.511061308497056,
3.69514379608856));
#34207=CARTESIAN_POINT('Ctrl Pts',(7.73774049158897,-0.410141282132307,
3.52596134197134));
#34208=CARTESIAN_POINT('Ctrl Pts',(7.75364577027658,-0.216866948266163,
3.4118697020638));
#34209=CARTESIAN_POINT('Ctrl Pts',(7.76955104896419,-0.0199817042712483,
3.40525493058698));
#34210=CARTESIAN_POINT('Ctrl Pts',(7.78545632765181,0.176903539723664,3.39864015911017));
#34211=CARTESIAN_POINT('Ctrl Pts',(7.80136160633942,0.377399693847348,3.49950225606407));
#34212=CARTESIAN_POINT('Ctrl Pts',(7.81726688502703,0.489447406431712,3.66152961365368));
#34213=CARTESIAN_POINT('Ctrl Pts',(7.83317216371464,0.601495119016078,3.82355697124329));
#34214=CARTESIAN_POINT('Ctrl Pts',(7.84907744240226,0.625094390061116,4.04674958946861));
#34215=CARTESIAN_POINT('Ctrl Pts',(7.86498272108987,0.549409432699027,4.22862686054007));
#34216=CARTESIAN_POINT('Ctrl Pts',(7.88088799977748,0.473724475336938,4.41050413161152));
#34217=CARTESIAN_POINT('Ctrl Pts',(7.89679327846509,0.298755289567731,4.55106605552911));
#34218=CARTESIAN_POINT('Ctrl Pts',(7.91269855715271,0.104840323164387,4.58577254351526));
#34219=CARTESIAN_POINT('Ctrl Pts',(7.9155172343493,0.0704753991278659,4.59192310448195));
#34220=CARTESIAN_POINT('Ctrl Pts',(7.91833591154589,0.0355154700816755,
4.59474920414003));
#34221=CARTESIAN_POINT('Ctrl Pts',(7.92115458874249,0.000504499356536197,
4.59443266285439));
#34222=CARTESIAN_POINT('Origin',(4.,0.,4.));
#34223=CARTESIAN_POINT('',(8.32884541125757,-0.000534402448739424,4.5938336238991));
#34224=CARTESIAN_POINT('',(8.2211545887425,0.000116005647334215,4.59313666129657));
#34225=CARTESIAN_POINT('',(4.,-7.27562663373442E-17,4.5941));
#34226=CARTESIAN_POINT('Ctrl Pts',(8.32884541125757,-0.000534402448739424,
4.5938336238991));
#34227=CARTESIAN_POINT('Ctrl Pts',(8.31735888647079,0.142509087977489,4.59259298046846));
#34228=CARTESIAN_POINT('Ctrl Pts',(8.30587236168401,0.286359812054371,4.54070236535691));
#34229=CARTESIAN_POINT('Ctrl Pts',(8.29438583689723,0.393155811111917,4.44670960845581));
#34230=CARTESIAN_POINT('Ctrl Pts',(8.27848055820962,0.541035187969857,4.31655875596735));
#34231=CARTESIAN_POINT('Ctrl Pts',(8.262575279522,0.617867056310918,4.10568264439756));
#34232=CARTESIAN_POINT('Ctrl Pts',(8.24667000083439,0.588373472681163,3.91090666274675));
#34233=CARTESIAN_POINT('Ctrl Pts',(8.23076472214677,0.558879889051408,3.71613068109593));
#34234=CARTESIAN_POINT('Ctrl Pts',(8.21485944345917,0.423060853450833,3.53745482936408));
#34235=CARTESIAN_POINT('Ctrl Pts',(8.19895416477155,0.243278720997716,3.45691949951456));
#34236=CARTESIAN_POINT('Ctrl Pts',(8.18304888608394,0.0634965885445972,
3.37638416966503));
#34237=CARTESIAN_POINT('Ctrl Pts',(8.16714360739632,-0.160248640761069,
3.39398936169784));
#34238=CARTESIAN_POINT('Ctrl Pts',(8.15123832870871,-0.325222623502191,
3.50165151624576));
#34239=CARTESIAN_POINT('Ctrl Pts',(8.1353330500211,-0.490196606243315,3.60931367079368));
#34240=CARTESIAN_POINT('Ctrl Pts',(8.11942777133349,-0.59639934241989,3.80703278785672));
#34241=CARTESIAN_POINT('Ctrl Pts',(8.10352249264588,-0.595067028646789,
4.00402461368555));
#34242=CARTESIAN_POINT('Ctrl Pts',(8.08761721395827,-0.593734714873688,
4.20101643951437));
#34243=CARTESIAN_POINT('Ctrl Pts',(8.07171193527065,-0.484867351150922,
4.39728097410898));
#34244=CARTESIAN_POINT('Ctrl Pts',(8.05580665658303,-0.3184522251018,4.50270184645125));
#34245=CARTESIAN_POINT('Ctrl Pts',(8.04681957480788,-0.224421408301879,
4.56226861162124));
#34246=CARTESIAN_POINT('Ctrl Pts',(8.03783249303272,-0.112017456676448,
4.59283194056482));
#34247=CARTESIAN_POINT('Ctrl Pts',(8.02884541125756,0.000208508845897126,
4.59318438507865));
#34248=CARTESIAN_POINT('Ctrl Pts',(7.92115458874249,0.000504499356536197,
4.59443266285439));
#34249=CARTESIAN_POINT('Ctrl Pts',(7.93424119023351,-0.162045019349314,
4.59296301969496));
#34250=CARTESIAN_POINT('Ctrl Pts',(7.94732779172453,-0.325694779556815,
4.52375140444135));
#34251=CARTESIAN_POINT('Ctrl Pts',(7.96041439321555,-0.436005268305889,
4.40499428651169));
#34252=CARTESIAN_POINT('Ctrl Pts',(7.97631967190316,-0.570075146335334,
4.26065848946726));
#34253=CARTESIAN_POINT('Ctrl Pts',(7.99222495059077,-0.625354155356748,
4.04313584332371));
#34254=CARTESIAN_POINT('Ctrl Pts',(8.00813022927838,-0.576460513088508,
3.85230354456612));
#34255=CARTESIAN_POINT('Ctrl Pts',(8.024035507966,-0.527566870820267,3.66147124580852));
#34256=CARTESIAN_POINT('Ctrl Pts',(8.03994078665361,-0.374500577262366,
3.49732929443689));
#34257=CARTESIAN_POINT('Ctrl Pts',(8.05584606534123,-0.187543198716277,
3.43524473024767));
#34258=CARTESIAN_POINT('Ctrl Pts',(8.07175134402884,-0.000585820170193818,
3.37316016605846));
#34259=CARTESIAN_POINT('Ctrl Pts',(8.08765662271645,0.220262643364076,3.41313298905166));
#34260=CARTESIAN_POINT('Ctrl Pts',(8.10356190140406,0.37359792075985,3.53680937001953));
#34261=CARTESIAN_POINT('Ctrl Pts',(8.11946718009167,0.526933198155627,3.66048575098741));
#34262=CARTESIAN_POINT('Ctrl Pts',(8.13537245877928,0.612755289412907,3.86786568992997));
#34263=CARTESIAN_POINT('Ctrl Pts',(8.1512777374669,0.591658321059451,4.06372909240644));
#34264=CARTESIAN_POINT('Ctrl Pts',(8.16718301615451,0.570561352705995,4.2595924948829));
#34265=CARTESIAN_POINT('Ctrl Pts',(8.18308829484212,0.44254532474181,4.44393936089328));
#34266=CARTESIAN_POINT('Ctrl Pts',(8.19899357352974,0.266389781296621,4.53212540863836));
#34267=CARTESIAN_POINT('Ctrl Pts',(8.20638057860065,0.184576572093718,4.57308230066594));
#34268=CARTESIAN_POINT('Ctrl Pts',(8.21376758367158,0.0923795717789203,
4.59329710918813));
#34269=CARTESIAN_POINT('Ctrl Pts',(8.2211545887425,0.000116005647334215,
4.59313666129657));
#34270=CARTESIAN_POINT('Origin',(4.,0.,4.));
#34271=CARTESIAN_POINT('',(8.62884541125757,3.48566139269993E-5,4.59507810043999));
#34272=CARTESIAN_POINT('',(8.5211545887425,-0.000547905086566465,4.594005652201));
#34273=CARTESIAN_POINT('',(4.,-7.27562663373442E-17,4.5941));
#34274=CARTESIAN_POINT('Ctrl Pts',(8.62884541125757,3.48566139269993E-5,
4.59507810043999));
#34275=CARTESIAN_POINT('Ctrl Pts',(8.62869583728408,0.00188744051982823,
4.59507966949126));
#34276=CARTESIAN_POINT('Ctrl Pts',(8.62854626331059,0.00374001065808006,
4.59507176912216));
#34277=CARTESIAN_POINT('Ctrl Pts',(8.6283966893371,0.00559249142073073,
4.59505435897699));
#34278=CARTESIAN_POINT('Ctrl Pts',(8.61249141064948,0.202580123064263,4.59320301275402));
#34279=CARTESIAN_POINT('Ctrl Pts',(8.59658613196187,0.398557131004382,4.48381890612783));
#34280=CARTESIAN_POINT('Ctrl Pts',(8.58068085327426,0.503539164298441,4.31712659320126));
#34281=CARTESIAN_POINT('Ctrl Pts',(8.56477557458664,0.608521197592498,4.15043428027469));
#34282=CARTESIAN_POINT('Ctrl Pts',(8.54887029589904,0.622508256240502,3.92643376104774));
#34283=CARTESIAN_POINT('Ctrl Pts',(8.53296501721142,0.539078074654942,3.74797659726896));
#34284=CARTESIAN_POINT('Ctrl Pts',(8.51705973852381,0.455647893069379,3.56951943349019));
#34285=CARTESIAN_POINT('Ctrl Pts',(8.50115445983619,0.274800471250253,3.43660562515959));
#34286=CARTESIAN_POINT('Ctrl Pts',(8.48524918114857,0.0795732942734406,
3.41026356994308));
#34287=CARTESIAN_POINT('Ctrl Pts',(8.46934390246096,-0.115653882703369,
3.38392151472657));
#34288=CARTESIAN_POINT('Ctrl Pts',(8.45343862377335,-0.32526081483786,3.46415121262414));
#34289=CARTESIAN_POINT('Ctrl Pts',(8.43753334508574,-0.453004866631874,
3.61411458059983));
#34290=CARTESIAN_POINT('Ctrl Pts',(8.42162806639813,-0.580748918425883,
3.76407794857552));
#34291=CARTESIAN_POINT('Ctrl Pts',(8.40572278771052,-0.626630089879422,
3.98377498662932));
#34292=CARTESIAN_POINT('Ctrl Pts',(8.3898175090229,-0.569581688133314,4.17233010950212));
#34293=CARTESIAN_POINT('Ctrl Pts',(8.37391223033529,-0.512533286387202,
4.36088523237493));
#34294=CARTESIAN_POINT('Ctrl Pts',(8.35800695164768,-0.352555311441432,
4.51829844006673));
#34295=CARTESIAN_POINT('Ctrl Pts',(8.34210167296007,-0.163102881281137,
4.57229224720906));
#34296=CARTESIAN_POINT('Ctrl Pts',(8.33768291905923,-0.110469810133188,
4.58729263485501));
#34297=CARTESIAN_POINT('Ctrl Pts',(8.3332641651584,-0.0555618361628184,
4.59431088730997));
#34298=CARTESIAN_POINT('Ctrl Pts',(8.32884541125757,-0.000534402448739424,
4.5938336238991));
#34299=CARTESIAN_POINT('Ctrl Pts',(8.2211545887425,0.000116005647334215,
4.59313666129657));
#34300=CARTESIAN_POINT('Ctrl Pts',(8.22967286235919,-0.106277085140544,
4.59295164192424));
#34301=CARTESIAN_POINT('Ctrl Pts',(8.23819113597589,-0.212758691085218,
4.56567285125378));
#34302=CARTESIAN_POINT('Ctrl Pts',(8.24670940959258,-0.303508593564514,
4.51186277431583));
#34303=CARTESIAN_POINT('Ctrl Pts',(8.26261468828019,-0.472956366054245,
4.41138886276846));
#34304=CARTESIAN_POINT('Ctrl Pts',(8.2785199669678,-0.587556852107514,4.21841581019395));
#34305=CARTESIAN_POINT('Ctrl Pts',(8.29442524565541,-0.594690356875377,
4.02154867831793));
#34306=CARTESIAN_POINT('Ctrl Pts',(8.31033052434302,-0.60182386164324,3.82468154644191));
#34307=CARTESIAN_POINT('Ctrl Pts',(8.32623580303064,-0.501490385125681,
3.62392033526436));
#34308=CARTESIAN_POINT('Ctrl Pts',(8.34214108171825,-0.339758814980244,
3.51144609945163));
#34309=CARTESIAN_POINT('Ctrl Pts',(8.35804636040587,-0.178027244834812,
3.3989718636389));
#34310=CARTESIAN_POINT('Ctrl Pts',(8.37395163909348,0.0451024189384938,
3.37478460319097));
#34311=CARTESIAN_POINT('Ctrl Pts',(8.38985691778109,0.227178474572579,3.44999008482693));
#34312=CARTESIAN_POINT('Ctrl Pts',(8.4057621964687,0.40925453020667,3.5251955664629));
#34313=CARTESIAN_POINT('Ctrl Pts',(8.42166747515631,0.550276977701535,3.69979379018275));
#34314=CARTESIAN_POINT('Ctrl Pts',(8.43757275384392,0.585494275335268,3.89361663829603));
#34315=CARTESIAN_POINT('Ctrl Pts',(8.45347803253154,0.620711572969,4.0874394864093));
#34316=CARTESIAN_POINT('Ctrl Pts',(8.46938331121915,0.550123720741606,4.30048695891599));
#34317=CARTESIAN_POINT('Ctrl Pts',(8.48528858990677,0.406141674070155,4.4349366697363));
#34318=CARTESIAN_POINT('Ctrl Pts',(8.49724392285201,0.297916389879728,4.53599689564107));
#34319=CARTESIAN_POINT('Ctrl Pts',(8.50919925579725,0.148224117540273,4.59265016978245));
#34320=CARTESIAN_POINT('Ctrl Pts',(8.5211545887425,-0.000547905086566465,
4.594005652201));
#34321=CARTESIAN_POINT('Origin',(4.,0.,4.));
#34322=CARTESIAN_POINT('',(8.92884541125757,0.000516595407308196,4.59372894893997));
#34323=CARTESIAN_POINT('',(8.82115458874249,0.000142235148737217,4.59503945166131));
#34324=CARTESIAN_POINT('',(4.,-7.27562663373442E-17,4.5941));
#34325=CARTESIAN_POINT('Ctrl Pts',(8.92884541125757,0.000516595407308196,
4.59372894893997));
#34326=CARTESIAN_POINT('Ctrl Pts',(8.92412750940976,0.0592956068199462,
4.59421507565108));
#34327=CARTESIAN_POINT('Ctrl Pts',(8.91940960756194,0.117944888069788,4.58619493689145));
#34328=CARTESIAN_POINT('Ctrl Pts',(8.91469170571413,0.17383025386194,4.56912565303288));
#34329=CARTESIAN_POINT('Ctrl Pts',(8.89878642702651,0.362234410233906,4.51158064138869));
#34330=CARTESIAN_POINT('Ctrl Pts',(8.8828811483389,0.519225559109383,4.35118846702123));
#34331=CARTESIAN_POINT('Ctrl Pts',(8.86697586965128,0.572720006672535,4.16159443076672));
#34332=CARTESIAN_POINT('Ctrl Pts',(8.85107059096367,0.626214454235688,3.97200039451221));
#34333=CARTESIAN_POINT('Ctrl Pts',(8.83516531227606,0.576212200486512,3.75320449637065));
#34334=CARTESIAN_POINT('Ctrl Pts',(8.81926003358845,0.445672164925724,3.60566855627755));
#34335=CARTESIAN_POINT('Ctrl Pts',(8.80335475490084,0.315132129364936,3.45813261618446));
#34336=CARTESIAN_POINT('Ctrl Pts',(8.78744947621322,0.104054311992536,3.38185663413984));
#34337=CARTESIAN_POINT('Ctrl Pts',(8.77154419752561,-0.0906432834200916,
3.41186331412789));
#34338=CARTESIAN_POINT('Ctrl Pts',(8.755638918838,-0.285340878832719,3.44186999411594));
#34339=CARTESIAN_POINT('Ctrl Pts',(8.73973364015038,-0.463658252285575,
3.57815933613666));
#34340=CARTESIAN_POINT('Ctrl Pts',(8.72382836146277,-0.543719609875046,
3.75815304026071));
#34341=CARTESIAN_POINT('Ctrl Pts',(8.70792308277515,-0.623780967464517,
3.93814674438476));
#34342=CARTESIAN_POINT('Ctrl Pts',(8.69201780408754,-0.605586309190603,
4.16184481061213));
#34343=CARTESIAN_POINT('Ctrl Pts',(8.67611252539993,-0.497489852380174,
4.32653455081593));
#34344=CARTESIAN_POINT('Ctrl Pts',(8.66035682068581,-0.390409939629295,
4.48967554111606));
#34345=CARTESIAN_POINT('Ctrl Pts',(8.64460111597169,-0.195111159088962,
4.59491282095998));
#34346=CARTESIAN_POINT('Ctrl Pts',(8.62884541125757,3.48566139269993E-5,
4.59507810043999));
#34347=CARTESIAN_POINT('Ctrl Pts',(8.5211545887425,-0.000547905086566465,
4.594005652201));
#34348=CARTESIAN_POINT('Ctrl Pts',(8.52510453448487,-0.0497009834700827,
4.59445349267793));
#34349=CARTESIAN_POINT('Ctrl Pts',(8.52905448022724,-0.0987536084630192,
4.58886509038946));
#34350=CARTESIAN_POINT('Ctrl Pts',(8.53300442596961,-0.146177075786514,
4.57684766499685));
#34351=CARTESIAN_POINT('Ctrl Pts',(8.54890970465722,-0.337137537856201,
4.52845700030318));
#34352=CARTESIAN_POINT('Ctrl Pts',(8.56481498334483,-0.501682220880061,
4.37582372178193));
#34353=CARTESIAN_POINT('Ctrl Pts',(8.58072026203244,-0.564259167724997,
4.18903057354857));
#34354=CARTESIAN_POINT('Ctrl Pts',(8.59662554072005,-0.626836114569933,
4.00223742531521));
#34355=CARTESIAN_POINT('Ctrl Pts',(8.61253081940767,-0.587445325235947,
3.78128440736974));
#34356=CARTESIAN_POINT('Ctrl Pts',(8.62843609809528,-0.464173383698336,
3.62762379780141));
#34357=CARTESIAN_POINT('Ctrl Pts',(8.6443413767829,-0.340901442160722,3.47396318823307));
#34358=CARTESIAN_POINT('Ctrl Pts',(8.66024665547051,-0.133748348419481,
3.38759498704188));
#34359=CARTESIAN_POINT('Ctrl Pts',(8.67615193415812,0.0621699608040676,
3.40817581827756));
#34360=CARTESIAN_POINT('Ctrl Pts',(8.69205721284573,0.25808827002761,3.42875664951325));
#34361=CARTESIAN_POINT('Ctrl Pts',(8.70796249153334,0.44277179473346,3.55628651317581));
#34362=CARTESIAN_POINT('Ctrl Pts',(8.72386777022095,0.531421673692279,3.73220909121499));
#34363=CARTESIAN_POINT('Ctrl Pts',(8.73977304890857,0.620071552651101,3.90813166925417));
#34364=CARTESIAN_POINT('Ctrl Pts',(8.75567832759618,0.612687785862888,4.13244696166997));
#34365=CARTESIAN_POINT('Ctrl Pts',(8.7715836062838,0.512660686655375,4.30215887618246));
#34366=CARTESIAN_POINT('Ctrl Pts',(8.78748888497141,0.412633587447865,4.47187079069495));
#34367=CARTESIAN_POINT('Ctrl Pts',(8.80339416365902,0.21996315582106,4.58697932730413));
#34368=CARTESIAN_POINT('Ctrl Pts',(8.81929944234663,0.0231155027642346,
4.59463151583965));
#34369=CARTESIAN_POINT('Ctrl Pts',(8.81991782447859,0.0154622529370322,
4.59492902566351));
#34370=CARTESIAN_POINT('Ctrl Pts',(8.82053620661054,0.00780268890311657,
4.59506410656044));
#34371=CARTESIAN_POINT('Ctrl Pts',(8.82115458874249,0.000142235148737217,
4.59503945166131));
#34372=CARTESIAN_POINT('Origin',(4.,0.,4.));
#34373=CARTESIAN_POINT('',(9.22884541125756,-0.000264402795292107,4.59322887297718));
#34374=CARTESIAN_POINT('',(9.12115458874249,0.000475196148639644,4.59357609051269));
#34375=CARTESIAN_POINT('',(4.,-7.27562663373442E-17,4.5941));
#34376=CARTESIAN_POINT('Ctrl Pts',(9.22884541125756,-0.000264402795292107,
4.59322887297718));
#34377=CARTESIAN_POINT('Ctrl Pts',(9.21955918153543,0.115675446261185,4.59276508993807));
#34378=CARTESIAN_POINT('Ctrl Pts',(9.21027295181329,0.231857423975292,4.55999255403315));
#34379=CARTESIAN_POINT('Ctrl Pts',(9.20098672209116,0.327844211240712,4.49662776730038));
#34380=CARTESIAN_POINT('Ctrl Pts',(9.18508144340355,0.492248565587605,4.38809775866155));
#34381=CARTESIAN_POINT('Ctrl Pts',(9.16917616471593,0.597407924103304,4.18982173958679));
#34382=CARTESIAN_POINT('Ctrl Pts',(9.15327088602831,0.595037558282966,3.99283966966863));
#34383=CARTESIAN_POINT('Ctrl Pts',(9.1373656073407,0.592667192462628,3.79585759975047));
#34384=CARTESIAN_POINT('Ctrl Pts',(9.12146032865309,0.482767102306254,3.60016947898891));
#34385=CARTESIAN_POINT('Ctrl Pts',(9.10555504996548,0.315798759724268,3.49562701355602));
#34386=CARTESIAN_POINT('Ctrl Pts',(9.08964977127787,0.148830417142278,3.39108454812312));
#34387=CARTESIAN_POINT('Ctrl Pts',(9.07374449259025,-0.0752061778653251,
3.37768773801888));
#34388=CARTESIAN_POINT('Ctrl Pts',(9.05783921390264,-0.253442899077741,
3.46158783167087));
#34389=CARTESIAN_POINT('Ctrl Pts',(9.04193393521502,-0.431679620290152,
3.54548792532286));
#34390=CARTESIAN_POINT('Ctrl Pts',(9.02602865652741,-0.56411646770738,3.72668492273107));
#34391=CARTESIAN_POINT('Ctrl Pts',(9.0101233778398,-0.589944043936388,3.92198082849844));
#34392=CARTESIAN_POINT('Ctrl Pts',(8.99421809915219,-0.615771620165397,
4.11727673426582));
#34393=CARTESIAN_POINT('Ctrl Pts',(8.97831282046457,-0.534989925206181,
4.32667154839236));
#34394=CARTESIAN_POINT('Ctrl Pts',(8.96240754177696,-0.384690495792338,
4.45402003099517));
#34395=CARTESIAN_POINT('Ctrl Pts',(8.95122016493716,-0.278973620993485,
4.54359378149875));
#34396=CARTESIAN_POINT('Ctrl Pts',(8.94003278809737,-0.138863784294423,
4.59257621560968));
#34397=CARTESIAN_POINT('Ctrl Pts',(8.92884541125757,0.000516595407308196,
4.59372894893997));
#34398=CARTESIAN_POINT('Ctrl Pts',(8.82115458874249,0.000142235148737217,
4.59503945166131));
#34399=CARTESIAN_POINT('Ctrl Pts',(8.83644148529816,-0.189230254871984,
4.59442996300828));
#34400=CARTESIAN_POINT('Ctrl Pts',(8.85172838185382,-0.379146468724227,
4.49620311855542));
#34401=CARTESIAN_POINT('Ctrl Pts',(8.86701527840948,-0.487657002993039,
4.34104488491935));
#34402=CARTESIAN_POINT('Ctrl Pts',(8.88292055709709,-0.600556981206626,
4.17961022500168));
#34403=CARTESIAN_POINT('Ctrl Pts',(8.89882583578469,-0.62533206314696,3.95654506470448));
#34404=CARTESIAN_POINT('Ctrl Pts',(8.91473111447231,-0.550606579334316,
3.77427148852754));
#34405=CARTESIAN_POINT('Ctrl Pts',(8.93063639315992,-0.47588109552167,3.5919979123506));
#34406=CARTESIAN_POINT('Ctrl Pts',(8.94654167184753,-0.301655045956043,
3.45051592029392));
#34407=CARTESIAN_POINT('Ctrl Pts',(8.96244695053515,-0.107925661701669,
3.41478805750048));
#34408=CARTESIAN_POINT('Ctrl Pts',(8.97835222922276,0.0858037225526985,
3.37906019470703));
#34409=CARTESIAN_POINT('Ctrl Pts',(8.99425750791037,0.299036441495806,3.4490864611768));
#34410=CARTESIAN_POINT('Ctrl Pts',(9.01016278659798,0.433865051721373,3.5927137579139));
#34411=CARTESIAN_POINT('Ctrl Pts',(9.0260680652856,0.568693661946943,3.736341054651));
#34412=CARTESIAN_POINT('Ctrl Pts',(9.04197334397321,0.625118163454969,3.95356938165542));
#34413=CARTESIAN_POINT('Ctrl Pts',(9.05787862266082,0.577230812276762,4.14465668133936));
#34414=CARTESIAN_POINT('Ctrl Pts',(9.07378390134844,0.529343461098555,4.3357439810233));
#34415=CARTESIAN_POINT('Ctrl Pts',(9.08968918003605,0.377144257234124,4.50069025338676));
#34416=CARTESIAN_POINT('Ctrl Pts',(9.10559445872366,0.190516636080703,4.56375914846174));
#34417=CARTESIAN_POINT('Ctrl Pts',(9.11078116872994,0.129657384941762,4.58432590969837));
#34418=CARTESIAN_POINT('Ctrl Pts',(9.11596787873622,0.0651369761893139,
4.59405891310139));
#34419=CARTESIAN_POINT('Ctrl Pts',(9.12115458874249,0.000475196148639644,
4.59357609051269));
#34420=CARTESIAN_POINT('Origin',(4.,0.,4.));
#34421=CARTESIAN_POINT('',(9.52884541125756,-0.000414715089906426,4.59470005288553));
#34422=CARTESIAN_POINT('',(9.4211545887425,-0.000345133784900094,4.59331940772745));
#34423=CARTESIAN_POINT('',(4.,-7.27562663373442E-17,4.5941));
#34424=CARTESIAN_POINT('Ctrl Pts',(9.52884541125756,-0.000414715089906426,
4.59470005288553));
#34425=CARTESIAN_POINT('Ctrl Pts',(9.5149908536611,0.17147269131647,4.59333531965569));
#34426=CARTESIAN_POINT('Ctrl Pts',(9.50113629606464,0.344448366351018,4.51470554290992));
#34427=CARTESIAN_POINT('Ctrl Pts',(9.48728173846818,0.455032043431697,4.38349290156166));
#34428=CARTESIAN_POINT('Ctrl Pts',(9.47137645978057,0.581984072756561,4.23285845412795));
#34429=CARTESIAN_POINT('Ctrl Pts',(9.45547118109296,0.626706888961734,4.01292269047354));
#34430=CARTESIAN_POINT('Ctrl Pts',(9.43956590240535,0.56866566691212,3.82467080855373));
#34431=CARTESIAN_POINT('Ctrl Pts',(9.42366062371773,0.510624444862503,3.63641892663391));
#34432=CARTESIAN_POINT('Ctrl Pts',(9.40775534503012,0.349819184558098,3.47985092644869));
#34433=CARTESIAN_POINT('Ctrl Pts',(9.39185006634251,0.160084858421151,3.42685620983728));
#34434=CARTESIAN_POINT('Ctrl Pts',(9.37594478765489,-0.0296494677157886,
3.37386149322587));
#34435=CARTESIAN_POINT('Ctrl Pts',(9.36003950896728,-0.248312859685263,
3.42444006018826));
#34436=CARTESIAN_POINT('Ctrl Pts',(9.34413423027966,-0.395504338780113,
3.55536837257802));
#34437=CARTESIAN_POINT('Ctrl Pts',(9.32822895159205,-0.542695817874971,
3.6862966849678));
#34438=CARTESIAN_POINT('Ctrl Pts',(9.31232367290444,-0.618415384095196,
3.89757474278496));
#34439=CARTESIAN_POINT('Ctrl Pts',(9.29641839421683,-0.587895816063128,
4.09219260031737));
#34440=CARTESIAN_POINT('Ctrl Pts',(9.28051311552922,-0.55737624803106,4.28681045784976));
#34441=CARTESIAN_POINT('Ctrl Pts',(9.26460783684159,-0.42061754574671,4.4647681150974));
#34442=CARTESIAN_POINT('Ctrl Pts',(9.24870255815398,-0.240413519515492,
4.54435494461976));
#34443=CARTESIAN_POINT('Ctrl Pts',(9.24208350918851,-0.165420852186184,
4.57747534017911));
#34444=CARTESIAN_POINT('Ctrl Pts',(9.23546446022304,-0.0829041350566004,
4.59355944875842));
#34445=CARTESIAN_POINT('Ctrl Pts',(9.22884541125756,-0.000264402795292107,
4.59322887297718));
#34446=CARTESIAN_POINT('Ctrl Pts',(9.12115458874249,0.000475196148639644,
4.59357609051269));
#34447=CARTESIAN_POINT('Ctrl Pts',(9.13187315742383,-0.133151270259641,
4.59257831599443));
#34448=CARTESIAN_POINT('Ctrl Pts',(9.14259172610516,-0.267381477949042,
4.54795275857003));
#34449=CARTESIAN_POINT('Ctrl Pts',(9.1533102947865,-0.371151898503526,4.46515291500219));
#34450=CARTESIAN_POINT('Ctrl Pts',(9.16921557347411,-0.525136773491911,
4.34228626868117));
#34451=CARTESIAN_POINT('Ctrl Pts',(9.18512085216173,-0.612050485026272,
4.13536145825263));
#34452=CARTESIAN_POINT('Ctrl Pts',(9.20102613084934,-0.591985933785934,
3.93938960239856));
#34453=CARTESIAN_POINT('Ctrl Pts',(9.21693140953695,-0.571921382545595,
3.74341774654449));
#34454=CARTESIAN_POINT('Ctrl Pts',(9.23283668822456,-0.444878568530549,
3.55839884526489));
#34455=CARTESIAN_POINT('Ctrl Pts',(9.24874196691217,-0.269190177198291,
3.46928575052316));
#34456=CARTESIAN_POINT('Ctrl Pts',(9.26464724559978,-0.0935017858660342,
3.38017265578144));
#34457=CARTESIAN_POINT('Ctrl Pts',(9.28055252428739,0.130832182783434,3.38696536757758));
#34458=CARTESIAN_POINT('Ctrl Pts',(9.29645780297501,0.300807061133818,3.48654496003073));
#34459=CARTESIAN_POINT('Ctrl Pts',(9.31236308166262,0.470781939484206,3.58612455248389));
#34460=CARTESIAN_POINT('Ctrl Pts',(9.32826836035024,0.586397727535503,3.77849102559406));
#34461=CARTESIAN_POINT('Ctrl Pts',(9.34417363903785,0.594568546715174,3.97531783326339));
#34462=CARTESIAN_POINT('Ctrl Pts',(9.36007891772546,0.602739365894845,4.17214464093271));
#34463=CARTESIAN_POINT('Ctrl Pts',(9.37598419641307,0.503465216202894,4.37343178316119));
#34464=CARTESIAN_POINT('Ctrl Pts',(9.39188947510069,0.342328587234952,4.48675671999422));
#34465=CARTESIAN_POINT('Ctrl Pts',(9.40164451298129,0.243500144778355,4.55626125828842));
#34466=CARTESIAN_POINT('Ctrl Pts',(9.41139955086189,0.121401365174849,4.59267772446372));
#34467=CARTESIAN_POINT('Ctrl Pts',(9.4211545887425,-0.000345133784900094,
4.59331940772745));
#34468=CARTESIAN_POINT('Origin',(4.,0.,4.));
#34469=CARTESIAN_POINT('',(9.82884541125756,0.000474857175501747,4.59454166667424));
#34470=CARTESIAN_POINT('',(9.7211545887425,-0.000338423355870402,4.59484023865297));
#34471=CARTESIAN_POINT('',(4.,-7.27562663373442E-17,4.5941));
#34472=CARTESIAN_POINT('Ctrl Pts',(9.82884541125756,0.000474857175501747,
4.59454166667424));
#34473=CARTESIAN_POINT('Ctrl Pts',(9.82632780447438,0.0317313679687054,
4.59481419231428));
#34474=CARTESIAN_POINT('Ctrl Pts',(9.82381019769121,0.0629485386443197,
4.59256288124703));
#34475=CARTESIAN_POINT('Ctrl Pts',(9.82129259090804,0.093741277189286,4.58765086492638));
#34476=CARTESIAN_POINT('Ctrl Pts',(9.80538731222043,0.288278045752977,4.55661862072519));
#34477=CARTESIAN_POINT('Ctrl Pts',(9.78948203353282,0.465874751366426,4.41939150759219));
#34478=CARTESIAN_POINT('Ctrl Pts',(9.77357675484521,0.54498650030893,4.23897841027765));
#34479=CARTESIAN_POINT('Ctrl Pts',(9.7576714761576,0.624098249251433,4.05856531296313));
#34480=CARTESIAN_POINT('Ctrl Pts',(9.74176619746998,0.604725041522997,3.83496623146707));
#34481=CARTESIAN_POINT('Ctrl Pts',(9.72586091878237,0.495762234499694,3.67084840431546));
#34482=CARTESIAN_POINT('Ctrl Pts',(9.70995564009475,0.386799427476386,3.50673057716384));
#34483=CARTESIAN_POINT('Ctrl Pts',(9.69405036140714,0.188247021158209,3.40209400435668));
#34484=CARTESIAN_POINT('Ctrl Pts',(9.67814508271953,-0.00872811953311764,
3.40498337331868));
#34485=CARTESIAN_POINT('Ctrl Pts',(9.66223980403192,-0.205703260224436,
3.40787274228067));
#34486=CARTESIAN_POINT('Ctrl Pts',(9.6463345253443,-0.4011011352889,3.51828805301183));
#34487=CARTESIAN_POINT('Ctrl Pts',(9.63042924665669,-0.505203307099277,
3.68553126611098));
#34488=CARTESIAN_POINT('Ctrl Pts',(9.61452396796908,-0.609305478909656,
3.85277447921013));
#34489=CARTESIAN_POINT('Ctrl Pts',(9.59861868928147,-0.622111947465945,
4.07684559467727));
#34490=CARTESIAN_POINT('Ctrl Pts',(9.58271341059386,-0.537742524204099,
4.25486063595701));
#34491=CARTESIAN_POINT('Ctrl Pts',(9.56680813190624,-0.453373100942255,
4.43287567723675));
#34492=CARTESIAN_POINT('Ctrl Pts',(9.55090285321863,-0.271827785862281,
4.5648346443291));
#34493=CARTESIAN_POINT('Ctrl Pts',(9.53499757453102,-0.0764645071000137,
4.59014756226876));
#34494=CARTESIAN_POINT('Ctrl Pts',(9.53294685343987,-0.0512756623106346,
4.5934112419387));
#34495=CARTESIAN_POINT('Ctrl Pts',(9.53089613234871,-0.025857110284879,
4.59490205769144));
#34496=CARTESIAN_POINT('Ctrl Pts',(9.52884541125756,-0.000414715089906426,
4.59470005288553));
#34497=CARTESIAN_POINT('Ctrl Pts',(9.4211545887425,-0.000345133784900094,
4.59331940772745));
#34498=CARTESIAN_POINT('Ctrl Pts',(9.42730482954951,-0.0771024252662454,
4.59372396859559));
#34499=CARTESIAN_POINT('Ctrl Pts',(9.43345507035652,-0.153719688677923,
4.57990840728947));
#34500=CARTESIAN_POINT('Ctrl Pts',(9.43960531116353,-0.224276981305518,
4.55119942103951));
#34501=CARTESIAN_POINT('Ctrl Pts',(9.45551058985114,-0.406746812634079,
4.47695445381419));
#34502=CARTESIAN_POINT('Ctrl Pts',(9.47141586853875,-0.548687367047265,
4.30310178792596));
#34503=CARTESIAN_POINT('Ctrl Pts',(9.48732114722636,-0.58492554696818,4.10946721245096));
#34504=CARTESIAN_POINT('Ctrl Pts',(9.50322642591398,-0.621163726889096,
3.91583263697596));
#34505=CARTESIAN_POINT('Ctrl Pts',(9.5191317046016,-0.55169953231774,3.70241615191419));
#34506=CARTESIAN_POINT('Ctrl Pts',(9.53503698328921,-0.408427982613559,
3.56720957829912));
#34507=CARTESIAN_POINT('Ctrl Pts',(9.55094226197682,-0.265156432909381,
3.43200300468405));
#34508=CARTESIAN_POINT('Ctrl Pts',(9.56684754066442,-0.0480775280723801,
3.37500634251568));
#34509=CARTESIAN_POINT('Ctrl Pts',(9.58275281935204,0.14313528264739,3.42239004773181));
#34510=CARTESIAN_POINT('Ctrl Pts',(9.59865809803965,0.334348093367161,3.46977375294793));
#34511=CARTESIAN_POINT('Ctrl Pts',(9.61456337672728,0.499694809969701,3.62153782554855));
#34512=CARTESIAN_POINT('Ctrl Pts',(9.63046865541489,0.563255215433827,3.80799862400389));
#34513=CARTESIAN_POINT('Ctrl Pts',(9.6463739341025,0.626815620897955,3.99445942245922));
#34514=CARTESIAN_POINT('Ctrl Pts',(9.6622792127901,0.588589715223662,4.21561694676927));
#34515=CARTESIAN_POINT('Ctrl Pts',(9.67818449147771,0.466129217091882,4.36992501817411));
#34516=CARTESIAN_POINT('Ctrl Pts',(9.69250785723264,0.355848439261942,4.50888586187125));
#34517=CARTESIAN_POINT('Ctrl Pts',(9.70683122298757,0.177255492135987,4.59363345408847));
#34518=CARTESIAN_POINT('Ctrl Pts',(9.7211545887425,-0.000338423355870402,
4.59484023865297));
#34519=CARTESIAN_POINT('Origin',(4.,0.,4.));
#34520=CARTESIAN_POINT('',(10.1288454112576,0.000175993811045716,4.59316417414361));
#34521=CARTESIAN_POINT('',(10.0211545887425,0.000517772199431355,4.59437035498519));
#34522=CARTESIAN_POINT('',(4.,-7.27562663373442E-17,4.5941));
#34523=CARTESIAN_POINT('Ctrl Pts',(10.1288454112576,0.000175993811045716,
4.59316417414361));
#34524=CARTESIAN_POINT('Ctrl Pts',(10.1217594766001,0.0886689559287146,
4.59339827721605));
#34525=CARTESIAN_POINT('Ctrl Pts',(10.1146735419426,0.177068724884878,4.57486525982572));
#34526=CARTESIAN_POINT('Ctrl Pts',(10.1075876072851,0.256276603526552,4.53706914692868));
#34527=CARTESIAN_POINT('Ctrl Pts',(10.0916823285975,0.434068729046268,4.45223097977176));
#34528=CARTESIAN_POINT('Ctrl Pts',(10.0757770499098,0.565548899719798,4.27033860735548));
#34529=CARTESIAN_POINT('Ctrl Pts',(10.0598717712222,0.590346983641159,4.0749093118617));
#34530=CARTESIAN_POINT('Ctrl Pts',(10.0439664925346,0.61514506756252,3.87948001636793));
#34531=CARTESIAN_POINT('Ctrl Pts',(10.028061213847,0.533261064731712,3.67051379779667));
#34532=CARTESIAN_POINT('Ctrl Pts',(10.0121559351594,0.382292645022166,3.5439591030842));
#34533=CARTESIAN_POINT('Ctrl Pts',(9.99625065647179,0.231324225312614,3.41740440837173));
#34534=CARTESIAN_POINT('Ctrl Pts',(9.98034537778417,0.011271388724311,3.37326123751805));
#34535=CARTESIAN_POINT('Ctrl Pts',(9.96444009909655,-0.17682691184915,3.43179826703564));
#34536=CARTESIAN_POINT('Ctrl Pts',(9.94853482040894,-0.364925212422603,
3.49033529655323));
#34537=CARTESIAN_POINT('Ctrl Pts',(9.93262954172133,-0.521068976981223,
3.65155252644206));
#34538=CARTESIAN_POINT('Ctrl Pts',(9.91672426303372,-0.573563594737602,
3.84142582527571));
#34539=CARTESIAN_POINT('Ctrl Pts',(9.90081898434611,-0.626058212493981,
4.03129912410937));
#34540=CARTESIAN_POINT('Ctrl Pts',(9.8849137056585,-0.574903683448118,4.24982849188785));
#34541=CARTESIAN_POINT('Ctrl Pts',(9.86900842697089,-0.443588003168223,
4.39667448814241));
#34542=CARTESIAN_POINT('Ctrl Pts',(9.85562075506645,-0.333057953489513,
4.52027659892262));
#34543=CARTESIAN_POINT('Ctrl Pts',(9.842233083162,-0.165735336637852,4.59309247934331));
#34544=CARTESIAN_POINT('Ctrl Pts',(9.82884541125756,0.000474857175501747,
4.59454166667424));
#34545=CARTESIAN_POINT('Ctrl Pts',(9.7211545887425,-0.000338423355870402,
4.59484023865297));
#34546=CARTESIAN_POINT('Ctrl Pts',(9.72273650167518,-0.0199523965301825,
4.59497351934566));
#34547=CARTESIAN_POINT('Ctrl Pts',(9.72431841460787,-0.0395541838993478,
4.59408780127083));
#34548=CARTESIAN_POINT('Ctrl Pts',(9.72590032754056,-0.0590504136254521,
4.592143576127));
#34549=CARTESIAN_POINT('Ctrl Pts',(9.74180560622817,-0.255074455621757,
4.57259544417541));
#34550=CARTESIAN_POINT('Ctrl Pts',(9.75771088491579,-0.4404274490251,4.4460405617726));
#34551=CARTESIAN_POINT('Ctrl Pts',(9.7736161636034,-0.530003140903138,4.2705875768224));
#34552=CARTESIAN_POINT('Ctrl Pts',(9.78952144229101,-0.619578832781174,
4.0951345918722));
#34553=CARTESIAN_POINT('Ctrl Pts',(9.80542672097862,-0.61337722313391,3.87078350437461));
#34554=CARTESIAN_POINT('Ctrl Pts',(9.82133199966623,-0.514245828742901,
3.70054684219675));
#34555=CARTESIAN_POINT('Ctrl Pts',(9.83723727835384,-0.41511443435189,3.53031018001889));
#34556=CARTESIAN_POINT('Ctrl Pts',(9.85314255704146,-0.223053255217129,
3.41418794316076));
#34557=CARTESIAN_POINT('Ctrl Pts',(9.86904783572907,-0.0262486593588972,
3.40549855006092));
#34558=CARTESIAN_POINT('Ctrl Pts',(9.88495311441669,0.170555936499329,3.39680915696108));
#34559=CARTESIAN_POINT('Ctrl Pts',(9.9008583931043,0.372103949081026,3.49555260761951));
#34560=CARTESIAN_POINT('Ctrl Pts',(9.91676367179191,0.485853057801912,3.65639008698476));
#34561=CARTESIAN_POINT('Ctrl Pts',(9.93266895047952,0.5996021665228,3.81722756635002));
#34562=CARTESIAN_POINT('Ctrl Pts',(9.94857422916713,0.625552371382872,4.04015907442209));
#34563=CARTESIAN_POINT('Ctrl Pts',(9.96447950785475,0.551788436173011,4.22282389414861));
#34564=CARTESIAN_POINT('Ctrl Pts',(9.98038478654236,0.478024500963153,4.40548871387512));
#34565=CARTESIAN_POINT('Ctrl Pts',(9.99629006522997,0.304546425683368,4.54788684525607));
#34566=CARTESIAN_POINT('Ctrl Pts',(10.0121953439176,0.111008003250015,4.58463509072946));
#34567=CARTESIAN_POINT('Ctrl Pts',(10.0151817588592,0.0746687445744621,
4.59153503329043));
#34568=CARTESIAN_POINT('Ctrl Pts',(10.0181681738009,0.0376222632219309,
4.59471031472953));
#34569=CARTESIAN_POINT('Ctrl Pts',(10.0211545887425,0.000517772199431355,
4.59437035498519));
#34570=CARTESIAN_POINT('Origin',(4.,0.,4.));
#34571=CARTESIAN_POINT('',(10.4288454112576,-0.000541293539476018,4.59389423388278));
#34572=CARTESIAN_POINT('',(10.3211545887425,8.19078234495683E-5,4.59312629593825));
#34573=CARTESIAN_POINT('',(4.,-7.27562663373442E-17,4.5941));
#34574=CARTESIAN_POINT('Ctrl Pts',(10.4288454112576,-0.000541293539476018,
4.59389423388278));
#34575=CARTESIAN_POINT('Ctrl Pts',(10.4171911487257,0.144553461780974,4.59260897165526));
#34576=CARTESIAN_POINT('Ctrl Pts',(10.4055368861939,0.290497422953868,4.53904330389552));
#34577=CARTESIAN_POINT('Ctrl Pts',(10.3938826236621,0.397841883685798,4.4425412994096));
#34578=CARTESIAN_POINT('Ctrl Pts',(10.3779773449745,0.544341377656434,4.31083916286766));
#34579=CARTESIAN_POINT('Ctrl Pts',(10.3620720662869,0.618946539098701,4.09916502578488));
#34580=CARTESIAN_POINT('Ctrl Pts',(10.3461667875993,0.587401834162399,3.90471069671543));
#34581=CARTESIAN_POINT('Ctrl Pts',(10.3302615089117,0.555857129226098,3.710256367646));
#34582=CARTESIAN_POINT('Ctrl Pts',(10.314356230224,0.418162557911234,3.5330218465899));
#34583=CARTESIAN_POINT('Ctrl Pts',(10.2984509515364,0.237541641988682,3.45438572744188));
#34584=CARTESIAN_POINT('Ctrl Pts',(10.2825456728488,0.0569207260661262,
3.37574960829385));
#34585=CARTESIAN_POINT('Ctrl Pts',(10.2666403941612,-0.16662653446412,3.3957118910539));
#34586=CARTESIAN_POINT('Ctrl Pts',(10.2507351154736,-0.330456695071223,
3.50510674001315));
#34587=CARTESIAN_POINT('Ctrl Pts',(10.234829836786,-0.494286855678321,3.61450158897239));
#34588=CARTESIAN_POINT('Ctrl Pts',(10.2189245580984,-0.59839991636228,3.81332900413083));
#34589=CARTESIAN_POINT('Ctrl Pts',(10.2030192794108,-0.594991564317383,
4.01029584814195));
#34590=CARTESIAN_POINT('Ctrl Pts',(10.1871140007231,-0.591583212272486,
4.20726269215308));
#34591=CARTESIAN_POINT('Ctrl Pts',(10.1712087220355,-0.480653447498727,
4.40236896501689));
#34592=CARTESIAN_POINT('Ctrl Pts',(10.1553034433479,-0.313136524928893,
4.50603012050002));
#34593=CARTESIAN_POINT('Ctrl Pts',(10.1464840993178,-0.220249792163878,
4.56350936438632));
#34594=CARTESIAN_POINT('Ctrl Pts',(10.1376647552877,-0.109964716607974,
4.59287280319057));
#34595=CARTESIAN_POINT('Ctrl Pts',(10.1288454112576,0.000175993811045716,
4.59316417414361));
#34596=CARTESIAN_POINT('Ctrl Pts',(10.0211545887425,0.000517772199431355,
4.59437035498519));
#34597=CARTESIAN_POINT('Ctrl Pts',(10.0340734524885,-0.159991692577292,
4.59289973094197));
#34598=CARTESIAN_POINT('Ctrl Pts',(10.0469923162344,-0.321586704601994,
4.52564765365589));
#34599=CARTESIAN_POINT('Ctrl Pts',(10.0599111799804,-0.431712787135162,
4.40956688772629));
#34600=CARTESIAN_POINT('Ctrl Pts',(10.075816458668,-0.567296385500051,4.2666520796839));
#34601=CARTESIAN_POINT('Ctrl Pts',(10.0917217373556,-0.624864812642908,
4.04972410403331));
#34602=CARTESIAN_POINT('Ctrl Pts',(10.1076270160433,-0.577985082339038,
3.85838710972745));
#34603=CARTESIAN_POINT('Ctrl Pts',(10.1235322947309,-0.531105352035168,
3.6670501154216));
#34604=CARTESIAN_POINT('Ctrl Pts',(10.1394375734185,-0.379777464284567,
3.50130410246047));
#34605=CARTESIAN_POINT('Ctrl Pts',(10.1553428521061,-0.193484782987353,
3.43725262786029));
#34606=CARTESIAN_POINT('Ctrl Pts',(10.1712481307937,-0.00719210169012799,
3.37320115326011));
#34607=CARTESIAN_POINT('Ctrl Pts',(10.1871534094813,0.214065373153706,3.41084421702088));
#34608=CARTESIAN_POINT('Ctrl Pts',(10.2030586881689,0.368695569727689,3.53289771681035));
#34609=CARTESIAN_POINT('Ctrl Pts',(10.2189639668565,0.523325766301663,3.65495121659981));
#34610=CARTESIAN_POINT('Ctrl Pts',(10.2348692455442,0.611328684605784,3.86141515241798));
#34611=CARTESIAN_POINT('Ctrl Pts',(10.2507745242318,0.592297107651237,4.05749001970593));
#34612=CARTESIAN_POINT('Ctrl Pts',(10.2666798029194,0.573265530696689,4.25356488699388));
#34613=CARTESIAN_POINT('Ctrl Pts',(10.282585081607,0.447199458483466,4.43925068575162));
#34614=CARTESIAN_POINT('Ctrl Pts',(10.2984903602946,0.271983097956201,4.5292883529079));
#34615=CARTESIAN_POINT('Ctrl Pts',(10.3060451031106,0.188758241169316,4.57205474716445));
#34616=CARTESIAN_POINT('Ctrl Pts',(10.3135998459265,0.0944446272328244,
4.59324204311815));
#34617=CARTESIAN_POINT('Ctrl Pts',(10.3211545887425,8.19078234495684E-5,
4.59312629593825));
#34618=CARTESIAN_POINT('Origin',(4.,0.,4.));
#34619=CARTESIAN_POINT('',(10.7288454112576,7.37317986114466E-5,4.59506942345298));
#34620=CARTESIAN_POINT('',(10.6211545887425,-0.000548317120500629,4.59406879148573));
#34621=CARTESIAN_POINT('',(4.,-7.27562663373442E-17,4.5941));
#34622=CARTESIAN_POINT('Ctrl Pts',(10.7288454112576,7.37317986114466E-5,
4.59506942345298));
#34623=CARTESIAN_POINT('Ctrl Pts',(10.728528099539,0.00400402563557926,
4.59507627971693));
#34624=CARTESIAN_POINT('Ctrl Pts',(10.7282107878205,0.00793419209028873,
4.59504072157671));
#34625=CARTESIAN_POINT('Ctrl Pts',(10.727893476102,0.0118635052742893,4.59496237136513));
#34626=CARTESIAN_POINT('Ctrl Pts',(10.7119881974144,0.208820685209451,4.59103505989901));
#34627=CARTESIAN_POINT('Ctrl Pts',(10.6960829187267,0.403634001393415,4.47959161118634));
#34628=CARTESIAN_POINT('Ctrl Pts',(10.6801776400391,0.506853420906232,4.31180214209248));
#34629=CARTESIAN_POINT('Ctrl Pts',(10.6642723613515,0.610072840419052,4.14401267299861));
#34630=CARTESIAN_POINT('Ctrl Pts',(10.6483670826639,0.621698363260717,3.91987718352354));
#34631=CARTESIAN_POINT('Ctrl Pts',(10.6324618039763,0.536392041177647,3.74230920804366));
#34632=CARTESIAN_POINT('Ctrl Pts',(10.6165565252887,0.451085719094577,3.56474123256377));
#34633=CARTESIAN_POINT('Ctrl Pts',(10.6006512466011,0.26884755208677,3.43374077107907));
#34634=CARTESIAN_POINT('Ctrl Pts',(10.5847459679135,0.0733535965831807,
3.40945769333085));
#34635=CARTESIAN_POINT('Ctrl Pts',(10.5688406892258,-0.122140358920403,
3.38517461558263));
#34636=CARTESIAN_POINT('Ctrl Pts',(10.5529354105382,-0.33089010291977,3.46760892157089));
#34637=CARTESIAN_POINT('Ctrl Pts',(10.5370301318506,-0.457046584443773,
3.61891026549369));
#34638=CARTESIAN_POINT('Ctrl Pts',(10.521124853163,-0.583203065967777,3.7702116094165));
#34639=CARTESIAN_POINT('Ctrl Pts',(10.5052195744754,-0.626766285016417,
3.99037999127385));
#34640=CARTESIAN_POINT('Ctrl Pts',(10.4893142957878,-0.567733854410369,
4.17832340467295));
#34641=CARTESIAN_POINT('Ctrl Pts',(10.4734090171002,-0.508701423804317,
4.36626681807206));
#34642=CARTESIAN_POINT('Ctrl Pts',(10.4575037384126,-0.347073343543565,
4.52198526301292));
#34643=CARTESIAN_POINT('Ctrl Pts',(10.4415984597249,-0.157062390163684,
4.57397941748279));
#34644=CARTESIAN_POINT('Ctrl Pts',(10.4373474435692,-0.106278015462724,
4.58787593542499));
#34645=CARTESIAN_POINT('Ctrl Pts',(10.4330964274134,-0.0534661480554494,
4.59436304694399));
#34646=CARTESIAN_POINT('Ctrl Pts',(10.4288454112576,-0.000541293539476018,
4.59389423388278));
#34647=CARTESIAN_POINT('Ctrl Pts',(10.3211545887425,8.19078234495684E-5,
4.59312629593825));
#34648=CARTESIAN_POINT('Ctrl Pts',(10.3295051246142,-0.104220686264852,
4.59299835631127));
#34649=CARTESIAN_POINT('Ctrl Pts',(10.3378556604858,-0.208583275928277,
4.56684300569277));
#34650=CARTESIAN_POINT('Ctrl Pts',(10.3462061963575,-0.298097175589899,
4.5150330474864));
#34651=CARTESIAN_POINT('Ctrl Pts',(10.3621114750451,-0.468594439767441,
4.41635053935381));
#34652=CARTESIAN_POINT('Ctrl Pts',(10.3780167537327,-0.585222319281217,
4.22459598753381));
#34653=CARTESIAN_POINT('Ctrl Pts',(10.3939220324203,-0.594430225977177,
4.02781496975607));
#34654=CARTESIAN_POINT('Ctrl Pts',(10.4098273111079,-0.603638132673137,
3.83103395197833));
#34655=CARTESIAN_POINT('Ctrl Pts',(10.4257325897955,-0.505426066551287,
3.62922646824286));
#34656=CARTESIAN_POINT('Ctrl Pts',(10.4416378684831,-0.344888853364916,
3.51505397731042));
#34657=CARTESIAN_POINT('Ctrl Pts',(10.4575431471707,-0.184351640178541,
3.40088148637798));
#34658=CARTESIAN_POINT('Ctrl Pts',(10.4734484258584,0.0385107200723601,
3.37434398824859));
#34659=CARTESIAN_POINT('Ctrl Pts',(10.489353704546,0.221369260089487,3.4476263793543));
#34660=CARTESIAN_POINT('Ctrl Pts',(10.5052589832336,0.40422780010661,3.52090877046001));
#34661=CARTESIAN_POINT('Ctrl Pts',(10.5211642619212,0.54708251988996,3.69401105080081));
#34662=CARTESIAN_POINT('Ctrl Pts',(10.5370695406088,0.584340575799814,3.88745197659776));
#34663=CARTESIAN_POINT('Ctrl Pts',(10.5529748192964,0.621598631709669,4.08089290239472));
#34664=CARTESIAN_POINT('Ctrl Pts',(10.568880097984,0.55326002374602,4.29467247364782));
#34665=CARTESIAN_POINT('Ctrl Pts',(10.5847853766716,0.4107029495177,4.43063215550545));
#34666=CARTESIAN_POINT('Ctrl Pts',(10.5969084473619,0.302045344566967,4.53426120008624));
#34667=CARTESIAN_POINT('Ctrl Pts',(10.6090315180522,0.150270129189204,4.59268036842864));
#34668=CARTESIAN_POINT('Ctrl Pts',(10.6211545887425,-0.000548317120500629,
4.59406879148573));
#34669=CARTESIAN_POINT('Origin',(4.,0.,4.));
#34670=CARTESIAN_POINT('',(11.0288454112576,0.000503618959454472,4.59367252935801));
#34671=CARTESIAN_POINT('',(10.9211545887425,0.000179316795020235,4.59501533910171));
#34672=CARTESIAN_POINT('',(4.,-7.27562663373442E-17,4.5941));
#34673=CARTESIAN_POINT('Ctrl Pts',(11.0288454112576,0.000503618959454472,
4.59367252935801));
#34674=CARTESIAN_POINT('Ctrl Pts',(11.0239597716647,0.0613870506829751,
4.59415995979602));
#34675=CARTESIAN_POINT('Ctrl Pts',(11.0190741320719,0.122135879976345,4.58554712933309));
#34676=CARTESIAN_POINT('Ctrl Pts',(11.014188492479,0.179818659528701,4.56726203449827));
#34677=CARTESIAN_POINT('Ctrl Pts',(10.9982832137914,0.36760588100072,4.50773461262244));
#34678=CARTESIAN_POINT('Ctrl Pts',(10.9823779351038,0.52289792528528,4.34569680405454));
#34679=CARTESIAN_POINT('Ctrl Pts',(10.9664726564162,0.574391255511512,4.15554951523459));
#34680=CARTESIAN_POINT('Ctrl Pts',(10.9505673777285,0.625884585737745,3.96540222641464));
#34681=CARTESIAN_POINT('Ctrl Pts',(10.9346620990409,0.573579201905647,3.74714545734266));
#34682=CARTESIAN_POINT('Ctrl Pts',(10.9187568203533,0.441491523412615,3.60099348269406));
#34683=CARTESIAN_POINT('Ctrl Pts',(10.9028515416657,0.309403844919578,3.45484150804546));
#34684=CARTESIAN_POINT('Ctrl Pts',(10.8869462629781,0.0975338717655902,
3.38079432782024));
#34685=CARTESIAN_POINT('Ctrl Pts',(10.8710409842905,-0.0968366678563846,
3.41285127449999));
#34686=CARTESIAN_POINT('Ctrl Pts',(10.8551357056029,-0.291207207478354,
3.44490822117975));
#34687=CARTESIAN_POINT('Ctrl Pts',(10.8392304269153,-0.468078313568319,
3.58306929476445));
#34688=CARTESIAN_POINT('Ctrl Pts',(10.8233251482276,-0.546238257009186,
3.76389677537701));
#34689=CARTESIAN_POINT('Ctrl Pts',(10.80741986954,-0.624398200450053,3.94472425598957));
#34690=CARTESIAN_POINT('Ctrl Pts',(10.7915145908524,-0.603846981241821,
4.16821814362997));
#34691=CARTESIAN_POINT('Ctrl Pts',(10.7756093121648,-0.494020849794526,
4.33175950034039));
#34692=CARTESIAN_POINT('Ctrl Pts',(10.7600213451957,-0.386385759396791,
4.49203819249975));
#34693=CARTESIAN_POINT('Ctrl Pts',(10.7444333782267,-0.193002309618558,
4.59473260886404));
#34694=CARTESIAN_POINT('Ctrl Pts',(10.7288454112576,7.37317986114466E-5,
4.59506942345298));
#34695=CARTESIAN_POINT('Ctrl Pts',(10.6211545887425,-0.000548317120500629,
4.59406879148573));
#34696=CARTESIAN_POINT('Ctrl Pts',(10.6249367967398,-0.0476013079303647,
4.5945019577127));
#34697=CARTESIAN_POINT('Ctrl Pts',(10.6287190047372,-0.0945611723716044,
4.58938408097059));
#34698=CARTESIAN_POINT('Ctrl Pts',(10.6325012127345,-0.140089514783682,
4.57835619988505));
#34699=CARTESIAN_POINT('Ctrl Pts',(10.6484064914221,-0.331549364363767,
4.53198076994489));
#34700=CARTESIAN_POINT('Ctrl Pts',(10.6643117701097,-0.497693523030948,
4.38109011760241));
#34701=CARTESIAN_POINT('Ctrl Pts',(10.6802170487973,-0.562235622104956,
4.19496684675621));
#34702=CARTESIAN_POINT('Ctrl Pts',(10.6961223274849,-0.626777721178965,
4.00884357591002));
#34703=CARTESIAN_POINT('Ctrl Pts',(10.7120276061725,-0.589717760659791,
3.78748768656011));
#34704=CARTESIAN_POINT('Ctrl Pts',(10.7279328848602,-0.468072106540212,
3.63253643830059));
#34705=CARTESIAN_POINT('Ctrl Pts',(10.7438381635478,-0.346426452420629,
3.47758519004106));
#34706=CARTESIAN_POINT('Ctrl Pts',(10.7597434422354,-0.140195104700642,
3.38903858287192));
#34707=CARTESIAN_POINT('Ctrl Pts',(10.775648720923,0.0559292266755373,3.40755347270721));
#34708=CARTESIAN_POINT('Ctrl Pts',(10.7915539996106,0.252053558051711,3.4260683625425));
#34709=CARTESIAN_POINT('Ctrl Pts',(10.8074592782982,0.438070873084069,3.55164474938222));
#34710=CARTESIAN_POINT('Ctrl Pts',(10.8233645569858,0.528569890453362,3.72662326908837));
#34711=CARTESIAN_POINT('Ctrl Pts',(10.8392698356734,0.619068907822657,3.90160178879453));
#34712=CARTESIAN_POINT('Ctrl Pts',(10.8551751143611,0.614049627528876,4.12598244136713));
#34713=CARTESIAN_POINT('Ctrl Pts',(10.8710803930487,0.515816690734684,4.29673912390739));
#34714=CARTESIAN_POINT('Ctrl Pts',(10.8869856717363,0.417583753940498,4.46749580644764));
#34715=CARTESIAN_POINT('Ctrl Pts',(10.9028909504239,0.226137160645921,4.58462851895556));
#34716=CARTESIAN_POINT('Ctrl Pts',(10.9187962291115,0.0293810870543861,
4.59435487532392));
#34717=CARTESIAN_POINT('Ctrl Pts',(10.9195823489885,0.0196563998352688,
4.59483560139116));
#34718=CARTESIAN_POINT('Ctrl Pts',(10.9203684688655,0.00991874240631306,
4.5950539509358));
#34719=CARTESIAN_POINT('Ctrl Pts',(10.9211545887425,0.000179316795020235,
4.59501533910171));
#34720=CARTESIAN_POINT('Origin',(4.,0.,4.));
#34721=CARTESIAN_POINT('',(11.3288454112576,-0.000294350894641693,4.59325842069974));
#34722=CARTESIAN_POINT('',(11.2211545887425,0.000456638431143918,4.59352536526061));
#34723=CARTESIAN_POINT('',(4.,-7.27562663373442E-17,4.5941));
#34724=CARTESIAN_POINT('Ctrl Pts',(11.3288454112576,-0.000294350894641693,
4.59325842069974));
#34725=CARTESIAN_POINT('Ctrl Pts',(11.3193914437904,0.117725031793324,4.59273125875086));
#34726=CARTESIAN_POINT('Ctrl Pts',(11.3099374763232,0.236024696118704,4.55868066117597));
#34727=CARTESIAN_POINT('Ctrl Pts',(11.300483508856,0.333060002447629,4.49314500997921));
#34728=CARTESIAN_POINT('Ctrl Pts',(11.2845782301684,0.496311419914153,4.38288835848583));
#34729=CARTESIAN_POINT('Ctrl Pts',(11.2686729514808,0.599375291650127,4.18351506848348));
#34730=CARTESIAN_POINT('Ctrl Pts',(11.2527676727932,0.594929048027223,3.98656891995295));
#34731=CARTESIAN_POINT('Ctrl Pts',(11.2368623941056,0.59048280440432,3.78962277142242));
#34732=CARTESIAN_POINT('Ctrl Pts',(11.220957115418,0.478526445422532,3.5951037643637));
#34733=CARTESIAN_POINT('Ctrl Pts',(11.2050518367303,0.310465594643358,3.49232679739763));
#34734=CARTESIAN_POINT('Ctrl Pts',(11.1891465580427,0.142404743864184,3.38954983043155));
#34735=CARTESIAN_POINT('Ctrl Pts',(11.1732412793551,-0.0817605987123653,
3.37851490355812));
#34736=CARTESIAN_POINT('Ctrl Pts',(11.1573360006675,-0.259103191428711,
3.46428878834836));
#34737=CARTESIAN_POINT('Ctrl Pts',(11.1414307219799,-0.436445784145052,
3.5500626731386));
#34738=CARTESIAN_POINT('Ctrl Pts',(11.1255254432923,-0.566965627001181,
3.73264536959251));
#34739=CARTESIAN_POINT('Ctrl Pts',(11.1096201646047,-0.590733529996744,
3.92820262793532));
#34740=CARTESIAN_POINT('Ctrl Pts',(11.0937148859171,-0.614501432992307,
4.12375988627813));
#34741=CARTESIAN_POINT('Ctrl Pts',(11.0778096072294,-0.531517396127296,
4.33229170650985));
#34742=CARTESIAN_POINT('Ctrl Pts',(11.0619043285418,-0.379884178365051,
4.45804909903384));
#34743=CARTESIAN_POINT('Ctrl Pts',(11.0508846894471,-0.274828280424841,
4.54517747360242));
#34744=CARTESIAN_POINT('Ctrl Pts',(11.0398650503523,-0.136819945681758,
4.59257312212411));
#34745=CARTESIAN_POINT('Ctrl Pts',(11.0288454112576,0.000503618959454472,
4.59367252935801));
#34746=CARTESIAN_POINT('Ctrl Pts',(10.9211545887425,0.000179316795020235,
4.59501533910171));
#34747=CARTESIAN_POINT('Ctrl Pts',(10.9362737475531,-0.187135527734918,
4.59427273168419));
#34748=CARTESIAN_POINT('Ctrl Pts',(10.9513929063637,-0.375104412928531,
4.49848156101044));
#34749=CARTESIAN_POINT('Ctrl Pts',(10.9665120651743,-0.484035620954107,
4.34616539940523));
#34750=CARTESIAN_POINT('Ctrl Pts',(10.982417343862,-0.598630701482551,4.1859295668894));
#34751=CARTESIAN_POINT('Ctrl Pts',(10.9983226225496,-0.625755308650954,
3.96313790162893));
#34752=CARTESIAN_POINT('Ctrl Pts',(11.0142279012372,-0.55295497039508,3.7800869107734));
#34753=CARTESIAN_POINT('Ctrl Pts',(11.0301331799248,-0.480154632139201,
3.59703591991786));
#34754=CARTESIAN_POINT('Ctrl Pts',(11.0460384586124,-0.307429348459053,
3.45372560346725));
#34755=CARTESIAN_POINT('Ctrl Pts',(11.0619437373,-0.114087262216405,3.41595799577618));
#34756=CARTESIAN_POINT('Ctrl Pts',(11.0778490159876,0.0792548240262376,
3.37819038808511));
#34757=CARTESIAN_POINT('Ctrl Pts',(11.0937542946752,0.293213712831377,3.4459654891536));
#34758=CARTESIAN_POINT('Ctrl Pts',(11.1096595733629,0.429548534313776,3.58816383989905));
#34759=CARTESIAN_POINT('Ctrl Pts',(11.1255648520505,0.565883355796175,3.7303621906445));
#34760=CARTESIAN_POINT('Ctrl Pts',(11.1414701307381,0.624594109955846,3.94698379106692));
#34761=CARTESIAN_POINT('Ctrl Pts',(11.1573754094257,0.578723302329844,4.13856516675647));
#34762=CARTESIAN_POINT('Ctrl Pts',(11.1732806881133,0.53285249470384,4.33014654244603));
#34763=CARTESIAN_POINT('Ctrl Pts',(11.1891859668009,0.382400125292158,4.49668769340272));
#34764=CARTESIAN_POINT('Ctrl Pts',(11.2050912454885,0.196447557013804,4.56171996888228));
#34765=CARTESIAN_POINT('Ctrl Pts',(11.2104456932399,0.133847376870746,4.58361282144047));
#34766=CARTESIAN_POINT('Ctrl Pts',(11.2158001409912,0.0672239414478651,
4.5940016224088));
#34767=CARTESIAN_POINT('Ctrl Pts',(11.2211545887425,0.000456638431143918,
4.59352536526061));
#34768=CARTESIAN_POINT('Origin',(4.,0.,4.));
#34769=CARTESIAN_POINT('',(11.6288454112576,-0.000389145320547679,4.59475273347735));
#34770=CARTESIAN_POINT('',(11.5211545887425,-0.0003715675665865,4.59335763259963));
#34771=CARTESIAN_POINT('',(4.,-7.27562663373442E-17,4.5941));
#34772=CARTESIAN_POINT('Ctrl Pts',(11.6288454112576,-0.000389145320547679,
4.59475273347735));
#34773=CARTESIAN_POINT('Ctrl Pts',(11.6148231159161,0.173538999407471,4.59343557735163));
#34774=CARTESIAN_POINT('Ctrl Pts',(11.6008008205746,0.348531733704351,4.51264940831536));
#34775=CARTESIAN_POINT('Ctrl Pts',(11.586778525233,0.459048433726307,4.37867598496766));
#34776=CARTESIAN_POINT('Ctrl Pts',(11.5708732465454,0.584405864209301,4.22671194604376));
#34777=CARTESIAN_POINT('Ctrl Pts',(11.5549679678578,0.626808276394098,4.00631705984067));
#34778=CARTESIAN_POINT('Ctrl Pts',(11.5390626891702,0.566786276503563,3.81868733396413));
#34779=CARTESIAN_POINT('Ctrl Pts',(11.5231574104826,0.506764276613028,3.6310576080876));
#34780=CARTESIAN_POINT('Ctrl Pts',(11.507252131795,0.344317864647159,3.47619304253762));
#34781=CARTESIAN_POINT('Ctrl Pts',(11.4913468531074,0.154035560439752,3.4252008940353));
#34782=CARTESIAN_POINT('Ctrl Pts',(11.4754415744198,-0.0362467437676612,
3.37420874553297));
#34783=CARTESIAN_POINT('Ctrl Pts',(11.4595362957322,-0.254364940216614,
3.4270890140783));
#34784=CARTESIAN_POINT('Ctrl Pts',(11.4436310170445,-0.400168380917644,
3.55956131753494));
#34785=CARTESIAN_POINT('Ctrl Pts',(11.4277257383569,-0.545971821618673,
3.69203362099157));
#34786=CARTESIAN_POINT('Ctrl Pts',(11.4118204596693,-0.619460506571779,
3.90409795935952));
#34787=CARTESIAN_POINT('Ctrl Pts',(11.3959151809817,-0.586891540696359,
4.09838336016249));
#34788=CARTESIAN_POINT('Ctrl Pts',(11.3800099022941,-0.554322574820941,
4.29266876096545));
#34789=CARTESIAN_POINT('Ctrl Pts',(11.3641046236065,-0.415695958117004,
4.46917522420345));
#34790=CARTESIAN_POINT('Ctrl Pts',(11.3481993449189,-0.234663168166497,
4.54685844933023));
#34791=CARTESIAN_POINT('Ctrl Pts',(11.3417480336984,-0.161234786808821,
4.57836740127901));
#34792=CARTESIAN_POINT('Ctrl Pts',(11.335296722478,-0.080829826651965,4.59361815176584));
#34793=CARTESIAN_POINT('Ctrl Pts',(11.3288454112576,-0.000294350894641693,
4.59325842069974));
#34794=CARTESIAN_POINT('Ctrl Pts',(11.2211545887425,0.000456638431143918,
4.59352536526061));
#34795=CARTESIAN_POINT('Ctrl Pts',(11.2317054196788,-0.131106980996848,
4.59258691018808));
#34796=CARTESIAN_POINT('Ctrl Pts',(11.2422562506151,-0.263229208150973,
4.54946171071576));
#34797=CARTESIAN_POINT('Ctrl Pts',(11.2528070815514,-0.366229002642205,
4.4690386804108));
#34798=CARTESIAN_POINT('Ctrl Pts',(11.268712360239,-0.521500226874852,4.34780171645731));
#34799=CARTESIAN_POINT('Ctrl Pts',(11.2846176389266,-0.610589908195122,
4.1418043885479));
#34800=CARTESIAN_POINT('Ctrl Pts',(11.3005229176142,-0.592591834014348,
3.94563195463032));
#34801=CARTESIAN_POINT('Ctrl Pts',(11.3164281963018,-0.574593759833574,
3.74945952071274));
#34802=CARTESIAN_POINT('Ctrl Pts',(11.3323334749894,-0.449507930151742,
3.56311198078699));
#34803=CARTESIAN_POINT('Ctrl Pts',(11.3482387536771,-0.274768466013715,
3.47215224147272));
#34804=CARTESIAN_POINT('Ctrl Pts',(11.3641440323647,-0.100029001875688,
3.38119250215845));
#34805=CARTESIAN_POINT('Ctrl Pts',(11.3800493110523,0.12436409671854,3.38562056345565));
#34806=CARTESIAN_POINT('Ctrl Pts',(11.3959545897399,0.295379012183608,3.48340324695247));
#34807=CARTESIAN_POINT('Ctrl Pts',(11.4118598684275,0.466393927648671,3.5811859304493));
#34808=CARTESIAN_POINT('Ctrl Pts',(11.4277651471151,0.584030659984583,3.77232323614575));
#34809=CARTESIAN_POINT('Ctrl Pts',(11.4436704258027,0.594275398502411,3.96905299961855));
#34810=CARTESIAN_POINT('Ctrl Pts',(11.4595757044903,0.60452013702024,4.16578276309136));
#34811=CARTESIAN_POINT('Ctrl Pts',(11.475480983178,0.507372881719984,4.36810498434052));
#34812=CARTESIAN_POINT('Ctrl Pts',(11.4913862618656,0.34743954227408,4.48312185891572));
#34813=CARTESIAN_POINT('Ctrl Pts',(11.5013090374912,0.247662438486696,4.55487707062799));
#34814=CARTESIAN_POINT('Ctrl Pts',(11.5112318131169,0.123448374926332,4.59265218509947));
#34815=CARTESIAN_POINT('Ctrl Pts',(11.5211545887425,-0.0003715675665865,
4.59335763259963));
#34816=CARTESIAN_POINT('Origin',(4.,0.,4.));
#34817=CARTESIAN_POINT('',(11.9288454112576,0.000492284285450728,4.5944814532616));
#34818=CARTESIAN_POINT('',(11.8211545887425,-0.000307672146732893,4.59488449882539));
#34819=CARTESIAN_POINT('',(4.,-7.27562663373442E-17,4.5941));
#34820=CARTESIAN_POINT('Ctrl Pts',(11.9288454112576,0.000492284285450728,
4.5944814532616));
#34821=CARTESIAN_POINT('Ctrl Pts',(11.9261600667293,0.0338400408399785,
4.59477876231094));
#34822=CARTESIAN_POINT('Ctrl Pts',(11.9234747222011,0.0671420792079604,
4.59221542322669));
#34823=CARTESIAN_POINT('Ctrl Pts',(11.9207893776729,0.0999293694653808,
4.5866302815369));
#34824=CARTESIAN_POINT('Ctrl Pts',(11.9048840989853,0.294128282668868,4.55354952256816));
#34825=CARTESIAN_POINT('Ctrl Pts',(11.8889788202977,0.470268877700486,4.41445832512751));
#34826=CARTESIAN_POINT('Ctrl Pts',(11.8730735416101,0.547474845215755,4.2332214826164));
#34827=CARTESIAN_POINT('Ctrl Pts',(11.8571682629225,0.624680812731027,4.05198464010529));
#34828=CARTESIAN_POINT('Ctrl Pts',(11.8412629842349,0.602952152729945,3.82860215252373));
#34829=CARTESIAN_POINT('Ctrl Pts',(11.8253577055472,0.492265746621211,3.66564180763548));
#34830=CARTESIAN_POINT('Ctrl Pts',(11.8094524268596,0.38157934051248,3.50268146274723));
#34831=CARTESIAN_POINT('Ctrl Pts',(11.793547148172,0.181935188296101,3.40014326055229));
#34832=CARTESIAN_POINT('Ctrl Pts',(11.7776418694844,-0.0149985615777061,
3.40510840546499));
#34833=CARTESIAN_POINT('Ctrl Pts',(11.7617365907968,-0.211932311451519,
3.41007355037768));
#34834=CARTESIAN_POINT('Ctrl Pts',(11.7458313121092,-0.406155658982761,
3.52254204239802));
#34835=CARTESIAN_POINT('Ctrl Pts',(11.7299260334216,-0.508489459897291,
3.69087310813977));
#34836=CARTESIAN_POINT('Ctrl Pts',(11.714020754734,-0.610823260811815,3.8592041738815));
#34837=CARTESIAN_POINT('Ctrl Pts',(11.6981154760463,-0.621267515109637,
4.08339781334463));
#34838=CARTESIAN_POINT('Ctrl Pts',(11.6822101973587,-0.53502666307716,4.26051379213839));
#34839=CARTESIAN_POINT('Ctrl Pts',(11.6663049186711,-0.448785811044678,
4.43762977093217));
#34840=CARTESIAN_POINT('Ctrl Pts',(11.6503996399835,-0.265859852681883,
4.56766808905658));
#34841=CARTESIAN_POINT('Ctrl Pts',(11.6344943612959,-0.070240649109886,
4.59092065229643));
#34842=CARTESIAN_POINT('Ctrl Pts',(11.6326113779498,-0.0470818155087989,
4.59367346098309));
#34843=CARTESIAN_POINT('Ctrl Pts',(11.6307283946037,-0.0237450789937817,
4.59492960773286));
#34844=CARTESIAN_POINT('Ctrl Pts',(11.6288454112576,-0.000389145320547679,
4.59475273347735));
#34845=CARTESIAN_POINT('Ctrl Pts',(11.5211545887425,-0.0003715675665865,
4.59335763259963));
#34846=CARTESIAN_POINT('Ctrl Pts',(11.5271370918045,-0.0750233800274846,
4.5937829512795));
#34847=CARTESIAN_POINT('Ctrl Pts',(11.5331195948664,-0.149531931096223,
4.58073359799715));
#34848=CARTESIAN_POINT('Ctrl Pts',(11.5391020979284,-0.218455391669058,
4.55353248138526));
#34849=CARTESIAN_POINT('Ctrl Pts',(11.555007376616,-0.40169756257477,4.48121470137836));
#34850=CARTESIAN_POINT('Ctrl Pts',(11.5709126553036,-0.545462480794654,
4.3088676134633));
#34851=CARTESIAN_POINT('Ctrl Pts',(11.5868179339912,-0.583739378074245,
4.1156257090067));
#34852=CARTESIAN_POINT('Ctrl Pts',(11.6027232126789,-0.622016275353834,
3.92238380455011));
#34853=CARTESIAN_POINT('Ctrl Pts',(11.6186284913665,-0.554805151693135,
3.70824708355197));
#34854=CARTESIAN_POINT('Ctrl Pts',(11.6345337700541,-0.412966511608993,
3.57153806891708));
#34855=CARTESIAN_POINT('Ctrl Pts',(11.6504390487417,-0.271127871524847,
3.43482905428217));
#34856=CARTESIAN_POINT('Ctrl Pts',(11.6663443274293,-0.0546617150172531,
3.37554774601052));
#34857=CARTESIAN_POINT('Ctrl Pts',(11.6822496061169,0.137039856773353,3.42091361287512));
#34858=CARTESIAN_POINT('Ctrl Pts',(11.6981548848045,0.328741428563947,3.46627947973972));
#34859=CARTESIAN_POINT('Ctrl Pts',(11.7140601634921,0.495678415637556,3.61629252174057));
#34860=CARTESIAN_POINT('Ctrl Pts',(11.7299654421798,0.56120041605148,3.80207309651931));
#34861=CARTESIAN_POINT('Ctrl Pts',(11.7458707208674,0.626722416465409,3.98785367129807));
#34862=CARTESIAN_POINT('Ctrl Pts',(11.761775999555,0.590829430219633,4.20940177885472));
#34863=CARTESIAN_POINT('Ctrl Pts',(11.7776812782426,0.470001998091193,4.36499190112672));
#34864=CARTESIAN_POINT('Ctrl Pts',(11.7921723817426,0.359917612963646,4.5067481450567));
#34865=CARTESIAN_POINT('Ctrl Pts',(11.8066634852425,0.179330777996457,4.59375393408315));
#34866=CARTESIAN_POINT('Ctrl Pts',(11.8211545887425,-0.000307672146732893,
4.59488449882539));
#34867=CARTESIAN_POINT('Origin',(4.,0.,4.));
#34868=CARTESIAN_POINT('',(12.2288454112576,0.000142795628640946,4.59314744373127));
#34869=CARTESIAN_POINT('',(12.1211545887425,0.00052868291625318,4.59430727435519));
#34870=CARTESIAN_POINT('',(4.,-7.27562663373442E-17,4.5941));
#34871=CARTESIAN_POINT('Ctrl Pts',(12.2288454112576,0.000142795628640946,
4.59314744373127));
#34872=CARTESIAN_POINT('Ctrl Pts',(12.221591738855,0.0907369315914116,4.59334157666405));
#34873=CARTESIAN_POINT('Ctrl Pts',(12.2143380664525,0.181251971066953,4.57388161006077));
#34874=CARTESIAN_POINT('Ctrl Pts',(12.2070843940499,0.261922584292681,4.53433840020651));
#34875=CARTESIAN_POINT('Ctrl Pts',(12.1911791153623,0.438810719578057,4.44763117963851));
#34876=CARTESIAN_POINT('Ctrl Pts',(12.1752738366747,0.56836661021043,4.26436322928705));
#34877=CARTESIAN_POINT('Ctrl Pts',(12.1593685579871,0.591103672269137,4.06868343852597));
#34878=CARTESIAN_POINT('Ctrl Pts',(12.1434632792995,0.613840734327844,3.87300364776488));
#34879=CARTESIAN_POINT('Ctrl Pts',(12.1275580006119,0.529758967812885,3.66491201659415));
#34880=CARTESIAN_POINT('Ctrl Pts',(12.1116527219243,0.377465162701742,3.53995541841648));
#34881=CARTESIAN_POINT('Ctrl Pts',(12.0957474432367,0.225171357590603,3.41499882023882));
#34882=CARTESIAN_POINT('Ctrl Pts',(12.0798421645491,0.00466551388328543,
3.37317725505421));
#34883=CARTESIAN_POINT('Ctrl Pts',(12.0639368858614,-0.182805413822737,
3.43369341627091));
#34884=CARTESIAN_POINT('Ctrl Pts',(12.0480316071738,-0.37027634152876,3.49420957748762));
#34885=CARTESIAN_POINT('Ctrl Pts',(12.0321263284862,-0.524712353233489,
3.65706346510565));
#34886=CARTESIAN_POINT('Ctrl Pts',(12.0162210497986,-0.575202966010955,
3.84747946371059));
#34887=CARTESIAN_POINT('Ctrl Pts',(12.000315771111,-0.625693578788423,4.03789546231555));
#34888=CARTESIAN_POINT('Ctrl Pts',(11.9844104924234,-0.572238792638624,
4.25587357190742));
#34889=CARTESIAN_POINT('Ctrl Pts',(11.9685052137358,-0.439382783876041,
4.40132746645495));
#34890=CARTESIAN_POINT('Ctrl Pts',(11.9552852795764,-0.328957325572706,
4.52222386487166));
#34891=CARTESIAN_POINT('Ctrl Pts',(11.942065345417,-0.163678510702966,4.59301780268865));
#34892=CARTESIAN_POINT('Ctrl Pts',(11.9288454112576,0.000492284285450728,
4.5944814532616));
#34893=CARTESIAN_POINT('Ctrl Pts',(11.8211545887425,-0.000307672146732893,
4.59488449882539));
#34894=CARTESIAN_POINT('Ctrl Pts',(11.8225687639301,-0.0178384446610953,
4.59499482973335));
#34895=CARTESIAN_POINT('Ctrl Pts',(11.8239829391178,-0.035360185088601,
4.59428731490513));
#34896=CARTESIAN_POINT('Ctrl Pts',(11.8253971143054,-0.0528064866265509,
4.59273302680715));
#34897=CARTESIAN_POINT('Ctrl Pts',(11.8413023929931,-0.249025661204777,
4.57525189322826));
#34898=CARTESIAN_POINT('Ctrl Pts',(11.8572076716807,-0.435702132350142,
4.45065748908313));
#34899=CARTESIAN_POINT('Ctrl Pts',(11.8731129503683,-0.527121962142897,
4.27615829360067));
#34900=CARTESIAN_POINT('Ctrl Pts',(11.8890182290559,-0.618541791935657,
4.10165909811819));
#34901=CARTESIAN_POINT('Ctrl Pts',(11.9049235077435,-0.614704980375792,
3.87725511129838));
#34902=CARTESIAN_POINT('Ctrl Pts',(11.9208287864311,-0.517373229009482,
3.70598315013913));
#34903=CARTESIAN_POINT('Ctrl Pts',(11.9367340651187,-0.420041477643178,
3.53471118897989));
#34904=CARTESIAN_POINT('Ctrl Pts',(11.9526393438063,-0.229214786470442,
3.41657125348121));
#34905=CARTESIAN_POINT('Ctrl Pts',(11.9685446224939,-0.0325126988662629,
3.4058082039356));
#34906=CARTESIAN_POINT('Ctrl Pts',(11.9844499011816,0.164189388737916,3.39504515438998));
#34907=CARTESIAN_POINT('Ctrl Pts',(12.0003551798692,0.366766872773537,3.49165899079743));
#34908=CARTESIAN_POINT('Ctrl Pts',(12.0162604585568,0.482204742918021,3.65128872687397));
#34909=CARTESIAN_POINT('Ctrl Pts',(12.0321657372444,0.597642613062508,3.81091846295053));
#34910=CARTESIAN_POINT('Ctrl Pts',(12.048071015932,0.625940869315854,4.03356409869619));
#34911=CARTESIAN_POINT('Ctrl Pts',(12.0639762946196,0.554106149607013,4.21699617753661));
#34912=CARTESIAN_POINT('Ctrl Pts',(12.0798815733072,0.482271429898174,4.40042825637702));
#34913=CARTESIAN_POINT('Ctrl Pts',(12.0957868519948,0.310303734227154,4.5446467783122));
#34914=CARTESIAN_POINT('Ctrl Pts',(12.1116921306825,0.117163353092859,4.583432699452));
#34915=CARTESIAN_POINT('Ctrl Pts',(12.1148462833691,0.0788619649798074,
4.59112427906975));
#34916=CARTESIAN_POINT('Ctrl Pts',(12.1180004360558,0.0397279339241207,
4.59466958677844));
#34917=CARTESIAN_POINT('Ctrl Pts',(12.1211545887425,0.00052868291625318,
4.59430727435519));
#34918=CARTESIAN_POINT('Origin',(4.,0.,4.));
#34919=CARTESIAN_POINT('',(12.5288454112576,-0.000545899910317726,4.59395595168017));
#34920=CARTESIAN_POINT('',(12.4211545887425,4.74932194801069E-5,4.59311952367199));
#34921=CARTESIAN_POINT('',(4.,-7.27562663373442E-17,4.5941));
#34922=CARTESIAN_POINT('Ctrl Pts',(12.5288454112576,-0.000545899910317726,
4.59395595168017));
#34923=CARTESIAN_POINT('Ctrl Pts',(12.5170234109807,0.14659828900878,4.5926299020853));
#34924=CARTESIAN_POINT('Ctrl Pts',(12.5052014107038,0.29463204299547,4.53735693360054));
#34925=CARTESIAN_POINT('Ctrl Pts',(12.493379410427,0.402483765871145,4.43832383497591));
#34926=CARTESIAN_POINT('Ctrl Pts',(12.4774741317394,0.547587104485886,4.30508504322883));
#34927=CARTESIAN_POINT('Ctrl Pts',(12.4615688530518,0.619957272242066,4.09263639239171));
#34928=CARTESIAN_POINT('Ctrl Pts',(12.4456635743641,0.586364949835353,3.89852531496775));
#34929=CARTESIAN_POINT('Ctrl Pts',(12.4297582956765,0.55277262742864,3.7044142375438));
#34930=CARTESIAN_POINT('Ctrl Pts',(12.4138530169889,0.41321781485904,3.52864073353302));
#34931=CARTESIAN_POINT('Ctrl Pts',(12.3979477383013,0.231778177981285,3.45191255961345));
#34932=CARTESIAN_POINT('Ctrl Pts',(12.3820424596137,0.0503385411035255,
3.37518438569388));
#34933=CARTESIAN_POINT('Ctrl Pts',(12.3661371809261,-0.172985920082391,
3.39750154186552));
#34934=CARTESIAN_POINT('Ctrl Pts',(12.3502319022385,-0.335654061078685,
3.50861693417539));
#34935=CARTESIAN_POINT('Ctrl Pts',(12.3343266235509,-0.498322202074975,
3.61973232648525));
#34936=CARTESIAN_POINT('Ctrl Pts',(12.3184213448632,-0.600334022881645,
3.81964595493332));
#34937=CARTESIAN_POINT('Ctrl Pts',(12.3025160661756,-0.594850011148503,
4.0165659389844));
#34938=CARTESIAN_POINT('Ctrl Pts',(12.286610787488,-0.58936599941536,4.21348592303547));
#34939=CARTESIAN_POINT('Ctrl Pts',(12.2707055088004,-0.476386155142398,
4.40741226268955));
#34940=CARTESIAN_POINT('Ctrl Pts',(12.2548002301128,-0.307786043036728,
4.50930218712431));
#34941=CARTESIAN_POINT('Ctrl Pts',(12.2461486238277,-0.216076754679914,
4.564724762732));
#34942=CARTESIAN_POINT('Ctrl Pts',(12.2374970175426,-0.107910718865932,
4.59291589733543));
#34943=CARTESIAN_POINT('Ctrl Pts',(12.2288454112576,0.000142795628640946,
4.59314744373127));
#34944=CARTESIAN_POINT('Ctrl Pts',(12.1211545887425,0.00052868291625318,
4.59430727435519));
#34945=CARTESIAN_POINT('Ctrl Pts',(12.1339057147434,-0.157940052872902,
4.59284257311225));
#34946=CARTESIAN_POINT('Ctrl Pts',(12.1466568407444,-0.317474678016714,
4.52751565545538));
#34947=CARTESIAN_POINT('Ctrl Pts',(12.1594079667453,-0.427372353356377,
4.41409399619463));
#34948=CARTESIAN_POINT('Ctrl Pts',(12.1753132454329,-0.564454612073754,
4.27261605145303));
#34949=CARTESIAN_POINT('Ctrl Pts',(12.1912185241205,-0.62430606291093,4.0563068416254));
#34950=CARTESIAN_POINT('Ctrl Pts',(12.2071238028081,-0.579445451749542,
3.8644864045766));
#34951=CARTESIAN_POINT('Ctrl Pts',(12.2230290814957,-0.534584840588155,
3.6726659675278));
#34952=CARTESIAN_POINT('Ctrl Pts',(12.2389343601834,-0.38501216742821,3.50533430325784));
#34953=CARTESIAN_POINT('Ctrl Pts',(12.254839638871,-0.199404875886796,3.43932303278057));
#34954=CARTESIAN_POINT('Ctrl Pts',(12.2707449175586,-0.0137975843453769,
3.37331176230329));
#34955=CARTESIAN_POINT('Ctrl Pts',(12.2866501962462,0.207844325577514,3.40862088561871));
#34956=CARTESIAN_POINT('Ctrl Pts',(12.3025554749338,0.363752265741203,3.52903794710619));
#34957=CARTESIAN_POINT('Ctrl Pts',(12.3184607536214,0.519660205904889,3.64945500859368));
#34958=CARTESIAN_POINT('Ctrl Pts',(12.334366032309,0.609834176309377,3.85498000825323));
#34959=CARTESIAN_POINT('Ctrl Pts',(12.3502713109967,0.592870104691008,4.05124456128685));
#34960=CARTESIAN_POINT('Ctrl Pts',(12.3661765896843,0.575906033072638,4.24750911432049));
#34961=CARTESIAN_POINT('Ctrl Pts',(12.3820818683719,0.451803919431404,4.4345132207282));
#34962=CARTESIAN_POINT('Ctrl Pts',(12.3979871470595,0.277546204023914,4.52639250633888));
#34963=CARTESIAN_POINT('Ctrl Pts',(12.4057096276205,0.192938958450368,4.57100260157974));
#34964=CARTESIAN_POINT('Ctrl Pts',(12.4134321081815,0.0965080911524262,
4.59318808505049));
#34965=CARTESIAN_POINT('Ctrl Pts',(12.4211545887425,4.74932194801069E-5,
4.59311952367199));
#34966=CARTESIAN_POINT('Origin',(4.,0.,4.));
#34967=CARTESIAN_POINT('',(12.8288454112576,0.000112157221815526,4.59505491513413));
#34968=CARTESIAN_POINT('',(12.7211545887425,-0.000546355209092884,4.59413239245978));
#34969=CARTESIAN_POINT('',(4.,-7.27562663373442E-17,4.5941));
#34970=CARTESIAN_POINT('Ctrl Pts',(12.8288454112576,0.000112157221815526,
4.59505491513413));
#34971=CARTESIAN_POINT('Ctrl Pts',(12.828360361794,0.00612048155630211,
4.59507046002904));
#34972=CARTESIAN_POINT('Ctrl Pts',(12.8278753123304,0.0121283652366354,
4.59498736156652));
#34973=CARTESIAN_POINT('Ctrl Pts',(12.8273902628668,0.0181332013859869,
4.59480429815638));
#34974=CARTESIAN_POINT('Ctrl Pts',(12.8114849841792,0.215038052543873,4.58880145767424));
#34975=CARTESIAN_POINT('Ctrl Pts',(12.7955797054916,0.408666038032992,4.47531104548453));
#34976=CARTESIAN_POINT('Ctrl Pts',(12.779674426804,0.510111378641258,4.30644305748136));
#34977=CARTESIAN_POINT('Ctrl Pts',(12.7637691481164,0.611556719249521,4.1375750694782));
#34978=CARTESIAN_POINT('Ctrl Pts',(12.7478638694288,0.620819414976937,3.9133295056616));
#34979=CARTESIAN_POINT('Ctrl Pts',(12.7319585907412,0.533646427817818,3.7366704418887));
#34980=CARTESIAN_POINT('Ctrl Pts',(12.7160533120536,0.446473440658691,3.56001137811579));
#34981=CARTESIAN_POINT('Ctrl Pts',(12.700148033366,0.26286477061301,3.43093881438659));
#34982=CARTESIAN_POINT('Ctrl Pts',(12.6842427546783,0.0671257511235207,
3.4087174113557));
#34983=CARTESIAN_POINT('Ctrl Pts',(12.6683374759907,-0.128613268365957,
3.38649600832481));
#34984=CARTESIAN_POINT('Ctrl Pts',(12.6524321973031,-0.336482637299241,
3.47112576599221));
#34985=CARTESIAN_POINT('Ctrl Pts',(12.6365269186155,-0.461037535689932,
3.62374828002683));
#34986=CARTESIAN_POINT('Ctrl Pts',(12.6206216399279,-0.585592434080627,
3.77637079406146));
#34987=CARTESIAN_POINT('Ctrl Pts',(12.6047163612403,-0.626832861928724,
3.9969860644633));
#34988=CARTESIAN_POINT('Ctrl Pts',(12.5888110825527,-0.565822959504995,
4.18429689252621));
#34989=CARTESIAN_POINT('Ctrl Pts',(12.5729058038651,-0.504813057081268,
4.37160772058911));
#34990=CARTESIAN_POINT('Ctrl Pts',(12.5570005251774,-0.341552824385721,
4.52561410631309));
#34991=CARTESIAN_POINT('Ctrl Pts',(12.5410952464898,-0.151004453301302,
4.57560283284656));
#34992=CARTESIAN_POINT('Ctrl Pts',(12.5370119680791,-0.102085973774189,
4.58843617527608));
#34993=CARTESIAN_POINT('Ctrl Pts',(12.5329286896683,-0.0513689988622793,
4.59441396466913));
#34994=CARTESIAN_POINT('Ctrl Pts',(12.5288454112576,-0.000545899910317726,
4.59395595168017));
#34995=CARTESIAN_POINT('Ctrl Pts',(12.4211545887425,4.74932194801069E-5,
4.59311952367199));
#34996=CARTESIAN_POINT('Ctrl Pts',(12.4293373868691,-0.102162877376194,
4.59304687552285));
#34997=CARTESIAN_POINT('Ctrl Pts',(12.4375201849957,-0.204406628577491,
4.5679880979308));
#34998=CARTESIAN_POINT('Ctrl Pts',(12.4457029831223,-0.292652646395614,
4.51814611323009));
#34999=CARTESIAN_POINT('Ctrl Pts',(12.4616082618099,-0.46418046423393,4.42126596969699));
#35000=CARTESIAN_POINT('Ctrl Pts',(12.4775135404976,-0.582822782736806,
4.23075121781716));
#35001=CARTESIAN_POINT('Ctrl Pts',(12.4934188191852,-0.594104068590283,
4.03407817163935));
#35002=CARTESIAN_POINT('Ctrl Pts',(12.5093240978728,-0.605385354443759,
3.83740512546155));
#35003=CARTESIAN_POINT('Ctrl Pts',(12.5252293765604,-0.509305607647849,
3.63457378498577));
#35004=CARTESIAN_POINT('Ctrl Pts',(12.541134655248,-0.34998058313236,3.51871572067214));
#35005=CARTESIAN_POINT('Ctrl Pts',(12.5570399339356,-0.19065555861687,3.4028576563585));
#35006=CARTESIAN_POINT('Ctrl Pts',(12.5729452126232,0.031914743618199,3.37397286820701));
#35007=CARTESIAN_POINT('Ctrl Pts',(12.5888504913108,0.215535456959467,3.44532402892222));
#35008=CARTESIAN_POINT('Ctrl Pts',(12.6047557699985,0.399156170300736,3.51667518963742));
#35009=CARTESIAN_POINT('Ctrl Pts',(12.6206610486861,0.543827294748204,3.68826229921932));
#35010=CARTESIAN_POINT('Ctrl Pts',(12.6365663273737,0.583121970486127,3.88129981619987));
#35011=CARTESIAN_POINT('Ctrl Pts',(12.6524716060613,0.622416646224052,4.07433733318042));
#35012=CARTESIAN_POINT('Ctrl Pts',(12.6683768847489,0.556334873252426,4.28882525755962));
#35013=CARTESIAN_POINT('Ctrl Pts',(12.6842821634365,0.415218606030559,4.42627980869829));
#35014=CARTESIAN_POINT('Ctrl Pts',(12.6965729718718,0.306170972122536,4.53249785050629));
#35015=CARTESIAN_POINT('Ctrl Pts',(12.7088637803072,0.152317016475741,4.59271595401221));
#35016=CARTESIAN_POINT('Ctrl Pts',(12.7211545887425,-0.000546355209092884,
4.59413239245978));
#35017=CARTESIAN_POINT('Origin',(4.,0.,4.));
#35018=CARTESIAN_POINT('',(13.1288454112576,0.000488576923893258,4.59361798633976));
#35019=CARTESIAN_POINT('',(13.0211545887425,0.000215375668158819,4.59498635240753));
#35020=CARTESIAN_POINT('',(4.,-7.27562663373442E-17,4.5941));
#35021=CARTESIAN_POINT('Ctrl Pts',(13.1288454112576,0.000488576923893258,
4.59361798633976));
#35022=CARTESIAN_POINT('Ctrl Pts',(13.1237920339197,0.0634769139372694,
4.59410397103046));
#35023=CARTESIAN_POINT('Ctrl Pts',(13.1187386565818,0.126326538027094,4.58487602541266));
#35024=CARTESIAN_POINT('Ctrl Pts',(13.1136852792439,0.185787091792062,4.56533540718874));
#35025=CARTESIAN_POINT('Ctrl Pts',(13.0977800005563,0.372936519850693,4.50383218710482));
#35026=CARTESIAN_POINT('Ctrl Pts',(13.0818747218686,0.526512210440984,4.34016674272733));
#35027=CARTESIAN_POINT('Ctrl Pts',(13.065969443181,0.575998703695535,4.14948732200047));
#35028=CARTESIAN_POINT('Ctrl Pts',(13.0500641644934,0.625485196950086,3.9588079012736));
#35029=CARTESIAN_POINT('Ctrl Pts',(13.0341588858058,0.570882492868891,3.74111450419737));
#35030=CARTESIAN_POINT('Ctrl Pts',(13.0182536071182,0.437261843116128,3.59636272886105));
#35031=CARTESIAN_POINT('Ctrl Pts',(13.0023483284306,0.303641193363369,3.45161095352474));
#35032=CARTESIAN_POINT('Ctrl Pts',(12.986443049743,0.0910025979390456,3.37980079992835));
#35033=CARTESIAN_POINT('Ctrl Pts',(12.9705377710554,-0.10301929613509,3.41390445256627));
#35034=CARTESIAN_POINT('Ctrl Pts',(12.9546324923678,-0.297041190209231,
3.4480081052042));
#35035=CARTESIAN_POINT('Ctrl Pts',(12.9387272136801,-0.472446382933184,
3.58802556407645));
#35036=CARTESIAN_POINT('Ctrl Pts',(12.9228219349925,-0.54869623058984,3.76966673571907));
#35037=CARTESIAN_POINT('Ctrl Pts',(12.9069166563049,-0.624946078246494,
3.95130790736168));
#35038=CARTESIAN_POINT('Ctrl Pts',(12.8910113776173,-0.602040580835857,
4.17457279177466));
#35039=CARTESIAN_POINT('Ctrl Pts',(12.8751060989297,-0.490496973717212,
4.33694759959386));
#35040=CARTESIAN_POINT('Ctrl Pts',(12.8596858697056,-0.382355015061345,
4.49437060399126));
#35041=CARTESIAN_POINT('Ctrl Pts',(12.8442656404816,-0.190898750836606,
4.59456072668396));
#35042=CARTESIAN_POINT('Ctrl Pts',(12.8288454112576,0.000112157221815526,
4.59505491513413));
#35043=CARTESIAN_POINT('Ctrl Pts',(12.7211545887425,-0.000546355209092884,
4.59413239245978));
#35044=CARTESIAN_POINT('Ctrl Pts',(12.7247690589948,-0.0455002825709059,
4.59454893744622));
#35045=CARTESIAN_POINT('Ctrl Pts',(12.7283835292471,-0.0903685417208244,
4.58988016539195));
#35046=CARTESIAN_POINT('Ctrl Pts',(12.7319979994994,-0.13398639330236,4.5798004937111));
#35047=CARTESIAN_POINT('Ctrl Pts',(12.747903278187,-0.325924363941296,4.53544544968711));
#35048=CARTESIAN_POINT('Ctrl Pts',(12.7638085568746,-0.493649543747071,
4.38631418374101));
#35049=CARTESIAN_POINT('Ctrl Pts',(12.7797138355622,-0.560149626020051,
4.20088146397168));
#35050=CARTESIAN_POINT('Ctrl Pts',(12.7956191142498,-0.626649708293032,
4.01544874420235));
#35051=CARTESIAN_POINT('Ctrl Pts',(12.8115243929374,-0.591924693033219,
3.79371457060979));
#35052=CARTESIAN_POINT('Ctrl Pts',(12.827429671625,-0.471918838153678,3.63748989490844));
#35053=CARTESIAN_POINT('Ctrl Pts',(12.8433349503126,-0.351912983274129,
3.48126521920708));
#35054=CARTESIAN_POINT('Ctrl Pts',(12.8592402290002,-0.146626288774854,
3.39055004139693));
#35055=CARTESIAN_POINT('Ctrl Pts',(12.8751455076879,0.0496822801939141,
3.40699693328572));
#35056=CARTESIAN_POINT('Ctrl Pts',(12.8910507863755,0.245990849162665,3.42344382517451));
#35057=CARTESIAN_POINT('Ctrl Pts',(12.9069560650631,0.433321292600904,3.54705278676224));
#35058=CARTESIAN_POINT('Ctrl Pts',(12.9228613437507,0.525659396179275,3.72106781235173));
#35059=CARTESIAN_POINT('Ctrl Pts',(12.9387666224383,0.617997499757654,3.89508283794124));
#35060=CARTESIAN_POINT('Ctrl Pts',(12.9546719011259,0.615343263476151,4.11950392753251));
#35061=CARTESIAN_POINT('Ctrl Pts',(12.9705771798135,0.518915400343756,4.29128641125856));
#35062=CARTESIAN_POINT('Ctrl Pts',(12.9864824585012,0.422487537211366,4.46306889498459));
#35063=CARTESIAN_POINT('Ctrl Pts',(13.0023877371888,0.232286047228094,4.58221277284539));
#35064=CARTESIAN_POINT('Ctrl Pts',(13.0182930158764,0.0356434078328121,
4.59401221668908));
#35065=CARTESIAN_POINT('Ctrl Pts',(13.0192468734984,0.0238505254767134,
4.59471984273368));
#35066=CARTESIAN_POINT('Ctrl Pts',(13.0202007311205,0.0120344772878951,
4.59504140054066));
#35067=CARTESIAN_POINT('Ctrl Pts',(13.0211545887425,0.000215375668158819,
4.59498635240753));
#35068=CARTESIAN_POINT('Origin',(4.,0.,4.));
#35069=CARTESIAN_POINT('',(13.4288454112576,-0.000323145728561625,4.59329116515504));
#35070=CARTESIAN_POINT('',(13.3211545887425,0.000436239896754628,4.59347700091179));
#35071=CARTESIAN_POINT('',(4.,-7.27562663373442E-17,4.5941));
#35072=CARTESIAN_POINT('Ctrl Pts',(13.4288454112576,-0.000323145728561625,
4.59329116515504));
#35073=CARTESIAN_POINT('Ctrl Pts',(13.4192237060453,0.11977362227264,4.59270025156928));
#35074=CARTESIAN_POINT('Ctrl Pts',(13.4096020008331,0.240190260834984,4.55734300206483));
#35075=CARTESIAN_POINT('Ctrl Pts',(13.3999802956209,0.338238798929947,4.48960747645051));
#35076=CARTESIAN_POINT('Ctrl Pts',(13.3840750169333,0.500319146323361,4.37763642888821));
#35077=CARTESIAN_POINT('Ctrl Pts',(13.3681697382457,0.601276083433826,4.17718801339723));
#35078=CARTESIAN_POINT('Ctrl Pts',(13.3522644595581,0.594754455875995,3.9802996620979));
#35079=CARTESIAN_POINT('Ctrl Pts',(13.3363591808704,0.588232828318166,3.78341131079859));
#35080=CARTESIAN_POINT('Ctrl Pts',(13.3204539021828,0.474232636092054,3.59008302369095));
#35081=CARTESIAN_POINT('Ctrl Pts',(13.3045486234952,0.305097944517489,3.48908297116948));
#35082=CARTESIAN_POINT('Ctrl Pts',(13.2886433448076,0.135963252942929,3.388082918648));
#35083=CARTESIAN_POINT('Ctrl Pts',(13.27273806612,-0.0883059379800925,3.3794111007127));
#35084=CARTESIAN_POINT('Ctrl Pts',(13.2568327874324,-0.264734703826722,
3.46704924928509));
#35085=CARTESIAN_POINT('Ctrl Pts',(13.2409275087448,-0.441163469673367,
3.55468739785749));
#35086=CARTESIAN_POINT('Ctrl Pts',(13.2250222300572,-0.569751810443623,
3.7386355129376));
#35087=CARTESIAN_POINT('Ctrl Pts',(13.2091169513696,-0.591457400179852,
3.9344324022836));
#35088=CARTESIAN_POINT('Ctrl Pts',(13.1932116726819,-0.613162989916079,
4.1302292916296));
#35089=CARTESIAN_POINT('Ctrl Pts',(13.1773063939943,-0.527985828618295,
4.33787495524147));
#35090=CARTESIAN_POINT('Ctrl Pts',(13.1614011153067,-0.375035665205916,
4.46202728915223));
#35091=CARTESIAN_POINT('Ctrl Pts',(13.150549213957,-0.270680367988337,4.54673431669939));
#35092=CARTESIAN_POINT('Ctrl Pts',(13.1396973126073,-0.134776053786733,
4.59257435599745));
#35093=CARTESIAN_POINT('Ctrl Pts',(13.1288454112576,0.000488576923893258,
4.59361798633976));
#35094=CARTESIAN_POINT('Ctrl Pts',(13.0211545887425,0.000215375668158819,
4.59498635240753));
#35095=CARTESIAN_POINT('Ctrl Pts',(13.0361060098081,-0.185045360160338,
4.59412349007018));
#35096=CARTESIAN_POINT('Ctrl Pts',(13.0510574308736,-0.371056311319581,
4.5007301079696));
#35097=CARTESIAN_POINT('Ctrl Pts',(13.0660088519392,-0.480360474535337,
4.35124746348123));
#35098=CARTESIAN_POINT('Ctrl Pts',(13.0819141306268,-0.596637928700896,
4.19222825660313));
#35099=CARTESIAN_POINT('Ctrl Pts',(13.0978194093145,-0.626109048224722,
3.96973483302036));
#35100=CARTESIAN_POINT('Ctrl Pts',(13.1137246880021,-0.555241941841719,
3.78592675992164));
#35101=CARTESIAN_POINT('Ctrl Pts',(13.1296299666897,-0.484374835458714,
3.60211868682292));
#35102=CARTESIAN_POINT('Ctrl Pts',(13.1455352453773,-0.313169503168878,
3.45699596420825));
#35103=CARTESIAN_POINT('Ctrl Pts',(13.1614405240649,-0.120236190459409,
3.4171928066662));
#35104=CARTESIAN_POINT('Ctrl Pts',(13.1773458027525,0.0726971222500488,
3.37738964912416));
#35105=CARTESIAN_POINT('Ctrl Pts',(13.1932510814401,0.287358415379145,3.44290605665475));
#35106=CARTESIAN_POINT('Ctrl Pts',(13.2091563601277,0.425184304693362,3.58365966669054));
#35107=CARTESIAN_POINT('Ctrl Pts',(13.2250616388154,0.563010194007583,3.72441327672633));
#35108=CARTESIAN_POINT('Ctrl Pts',(13.240966917503,0.624000679506934,3.94040408926733));
#35109=CARTESIAN_POINT('Ctrl Pts',(13.2568721961906,0.580151510544767,4.13245826101242));
#35110=CARTESIAN_POINT('Ctrl Pts',(13.2727774748782,0.536302341582597,4.32451243275751));
#35111=CARTESIAN_POINT('Ctrl Pts',(13.2886827535658,0.387613518158899,4.49262996370669));
#35112=CARTESIAN_POINT('Ctrl Pts',(13.3045880322534,0.202356657484476,4.55961839611428));
#35113=CARTESIAN_POINT('Ctrl Pts',(13.3101102177498,0.13803695776657,4.58287624384712));
#35114=CARTESIAN_POINT('Ctrl Pts',(13.3156324032461,0.0693092633201986,
4.59394375907155));
#35115=CARTESIAN_POINT('Ctrl Pts',(13.3211545887425,0.000436239896754628,
4.59347700091179));
#35116=CARTESIAN_POINT('Origin',(4.,0.,4.));
#35117=CARTESIAN_POINT('',(13.7288454112576,-0.000361622974213827,4.59480268714608));
#35118=CARTESIAN_POINT('',(13.6211545887425,-0.000396530615921017,4.59339874939382));
#35119=CARTESIAN_POINT('',(4.,-7.27562663373442E-17,4.5941));
#35120=CARTESIAN_POINT('Ctrl Pts',(13.7288454112576,-0.000361622974213827,
4.59480268714608));
#35121=CARTESIAN_POINT('Ctrl Pts',(13.714655378171,0.175608319374377,4.59354294412002));
#35122=CARTESIAN_POINT('Ctrl Pts',(13.7004653450845,0.352610168065205,4.51056419690263));
#35123=CARTESIAN_POINT('Ctrl Pts',(13.6862753119979,0.463013835099274,4.37381700684221));
#35124=CARTESIAN_POINT('Ctrl Pts',(13.6703700333103,0.586762742631886,4.22054025587244));
#35125=CARTESIAN_POINT('Ctrl Pts',(13.6544647546227,0.626840040937572,3.99971072753873));
#35126=CARTESIAN_POINT('Ctrl Pts',(13.6385594759351,0.564843930165024,3.81272399872504));
#35127=CARTESIAN_POINT('Ctrl Pts',(13.6226541972475,0.502847819392478,3.62573726991136));
#35128=CARTESIAN_POINT('Ctrl Pts',(13.6067489185599,0.338778299541704,3.4725933406177));
#35129=CARTESIAN_POINT('Ctrl Pts',(13.5908436398723,0.147969152919217,3.42360942419035));
#35130=CARTESIAN_POINT('Ctrl Pts',(13.5749383611846,-0.0428399937032757,
3.37462550776301));
#35131=CARTESIAN_POINT('Ctrl Pts',(13.559033082497,-0.260388767097474,3.42980160420198));
#35132=CARTESIAN_POINT('Ctrl Pts',(13.5431278038094,-0.404787974250376,
3.56380318433064));
#35133=CARTESIAN_POINT('Ctrl Pts',(13.5272225251218,-0.549187181403275,
3.6978047644593));
#35134=CARTESIAN_POINT('Ctrl Pts',(13.5113172464342,-0.620436822314871,
3.91063182827765));
#35135=CARTESIAN_POINT('Ctrl Pts',(13.4954119677466,-0.585822076202281,
4.10456319205082));
#35136=CARTESIAN_POINT('Ctrl Pts',(13.479506689059,-0.551207330089691,4.298494555824));
#35137=CARTESIAN_POINT('Ctrl Pts',(13.4636014103714,-0.410728196952908,
4.47353021955202));
#35138=CARTESIAN_POINT('Ctrl Pts',(13.4476961316837,-0.228886751546343,
4.54930121159921));
#35139=CARTESIAN_POINT('Ctrl Pts',(13.4414125582084,-0.15704808052867,4.57923546205676));
#35140=CARTESIAN_POINT('Ctrl Pts',(13.435128984733,-0.0787538239969463,
4.5936770685736));
#35141=CARTESIAN_POINT('Ctrl Pts',(13.4288454112576,-0.000323145728561625,
4.59329116515504));
#35142=CARTESIAN_POINT('Ctrl Pts',(13.3211545887425,0.000436239896754628,
4.59347700091179));
#35143=CARTESIAN_POINT('Ctrl Pts',(13.3315376819337,-0.129062311182503,
4.59259937855127));
#35144=CARTESIAN_POINT('Ctrl Pts',(13.341920775125,-0.259074650003773,4.55094414667863));
#35145=CARTESIAN_POINT('Ctrl Pts',(13.3523038683163,-0.361265427801182,
4.47287234722855));
#35146=CARTESIAN_POINT('Ctrl Pts',(13.3682091470039,-0.517805754487323,
4.35327853206923));
#35147=CARTESIAN_POINT('Ctrl Pts',(13.3841144256915,-0.609061509934468,
4.14823156788458));
#35148=CARTESIAN_POINT('Ctrl Pts',(13.4000197043791,-0.593131911953917,
3.95188034580653));
#35149=CARTESIAN_POINT('Ctrl Pts',(13.4159249830667,-0.577202313973367,
3.75552912372848));
#35150=CARTESIAN_POINT('Ctrl Pts',(13.4318302617543,-0.454087362565127,
3.56787364375704));
#35151=CARTESIAN_POINT('Ctrl Pts',(13.4477355404419,-0.280316234851803,
3.47507736324643));
#35152=CARTESIAN_POINT('Ctrl Pts',(13.4636408191295,-0.106545107138479,
3.38228108273583));
#35153=CARTESIAN_POINT('Ctrl Pts',(13.4795460978172,0.117882196879929,3.38434400168606));
#35154=CARTESIAN_POINT('Ctrl Pts',(13.4954513765048,0.2899181539344,3.48031891499009));
#35155=CARTESIAN_POINT('Ctrl Pts',(13.5113566551924,0.461954110988876,3.57629382829412));
#35156=CARTESIAN_POINT('Ctrl Pts',(13.52726193388,0.581598721079409,3.76618073595195));
#35157=CARTESIAN_POINT('Ctrl Pts',(13.5431672125676,0.593916240998451,3.96279160341967));
#35158=CARTESIAN_POINT('Ctrl Pts',(13.5590724912552,0.606233760917493,4.15940247088739));
#35159=CARTESIAN_POINT('Ctrl Pts',(13.5749777699428,0.511224190665043,4.362737298165));
#35160=CARTESIAN_POINT('Ctrl Pts',(13.5908830486304,0.352511905377589,4.47943333495374));
#35161=CARTESIAN_POINT('Ctrl Pts',(13.6009735620011,0.251822790258117,4.55346680161908));
#35162=CARTESIAN_POINT('Ctrl Pts',(13.6110640753718,0.125494626822297,4.59262991567553));
#35163=CARTESIAN_POINT('Ctrl Pts',(13.6211545887425,-0.000396530615921017,
4.59339874939382));
#35164=CARTESIAN_POINT('Origin',(4.,0.,4.));
#35165=CARTESIAN_POINT('',(14.0288454112576,0.000507412974116619,4.59441995931617));
#35166=CARTESIAN_POINT('',(13.9211545887425,-0.000275297881949146,4.59492513410986));
#35167=CARTESIAN_POINT('',(4.,-7.27562663373442E-17,4.5941));
#35168=CARTESIAN_POINT('Ctrl Pts',(14.0288454112576,0.000507412974116619,
4.59441995931617));
#35169=CARTESIAN_POINT('Ctrl Pts',(14.0259923289843,0.0359476882196221,
4.59474138052009));
#35170=CARTESIAN_POINT('Ctrl Pts',(14.0231392467111,0.0713355155074759,
4.59184535342408));
#35171=CARTESIAN_POINT('Ctrl Pts',(14.0202861644378,0.106106362061302,4.58554453803953));
#35172=CARTESIAN_POINT('Ctrl Pts',(14.0043808857502,0.299945849210873,4.55041893875697));
#35173=CARTESIAN_POINT('Ctrl Pts',(13.9884756070626,0.474610768799237,4.40947910659883));
#35174=CARTESIAN_POINT('Ctrl Pts',(13.972570328375,0.549902379214768,4.22743864981956));
#35175=CARTESIAN_POINT('Ctrl Pts',(13.9566650496873,0.625193989630293,4.04539819304031));
#35176=CARTESIAN_POINT('Ctrl Pts',(13.9407597709997,0.601112290873006,3.82225711163994));
#35177=CARTESIAN_POINT('Ctrl Pts',(13.9248544923121,0.488714580199595,3.66047234987686));
#35178=CARTESIAN_POINT('Ctrl Pts',(13.9089492136245,0.376316869526181,3.49868758811377));
#35179=CARTESIAN_POINT('Ctrl Pts',(13.8930439349369,0.175603146936639,3.39825914598798));
#35180=CARTESIAN_POINT('Ctrl Pts',(13.8771386562493,-0.0212673376532481,
3.40529951534663));
#35181=CARTESIAN_POINT('Ctrl Pts',(13.8612333775617,-0.218137822243141,
3.41233988470529));
#35182=CARTESIAN_POINT('Ctrl Pts',(13.8453280988741,-0.411165068833379,
3.52684906554841));
#35183=CARTESIAN_POINT('Ctrl Pts',(13.8294228201864,-0.511719132099071,
3.69624928651676));
#35184=CARTESIAN_POINT('Ctrl Pts',(13.8135175414988,-0.612273195364761,
3.8656495074851));
#35185=CARTESIAN_POINT('Ctrl Pts',(13.7976122628112,-0.62035407530591,4.08994076857866));
#35186=CARTESIAN_POINT('Ctrl Pts',(13.7817069841236,-0.532251373727382,
4.26613801168402));
#35187=CARTESIAN_POINT('Ctrl Pts',(13.765801705436,-0.44414867214885,4.44233525478938));
#35188=CARTESIAN_POINT('Ctrl Pts',(13.7498964267484,-0.259862389050636,
4.57043847990653));
#35189=CARTESIAN_POINT('Ctrl Pts',(13.7339911480608,-0.0640089891217576,
4.59162810566218));
#35190=CARTESIAN_POINT('Ctrl Pts',(13.7322759024597,-0.0428879079209441,
4.59391322201126));
#35191=CARTESIAN_POINT('Ctrl Pts',(13.7305606568586,-0.0216323041412813,
4.594954960835));
#35192=CARTESIAN_POINT('Ctrl Pts',(13.7288454112576,-0.000361622974213827,
4.59480268714608));
#35193=CARTESIAN_POINT('Ctrl Pts',(13.6211545887425,-0.000396530615921017,
4.59339874939382));
#35194=CARTESIAN_POINT('Ctrl Pts',(13.6269693540594,-0.0729426448807452,
4.59384179797573));
#35195=CARTESIAN_POINT('Ctrl Pts',(13.6327841193764,-0.145343639818557,
4.58153501668255));
#35196=CARTESIAN_POINT('Ctrl Pts',(13.6385988846933,-0.212609537044371,
4.5558040579697));
#35197=CARTESIAN_POINT('Ctrl Pts',(13.6545041633809,-0.396603693856438,
4.48542149789704));
#35198=CARTESIAN_POINT('Ctrl Pts',(13.6704094420685,-0.542177007158105,
4.31459913145184));
#35199=CARTESIAN_POINT('Ctrl Pts',(13.6863147207561,-0.582488370180261,
4.12177136240739));
#35200=CARTESIAN_POINT('Ctrl Pts',(13.7022199994437,-0.622799733202417,
3.92894359336294));
#35201=CARTESIAN_POINT('Ctrl Pts',(13.7181252781313,-0.557849145945042,
3.71411042171923));
#35202=CARTESIAN_POINT('Ctrl Pts',(13.734030556819,-0.417459170243993,3.57591415105311));
#35203=CARTESIAN_POINT('Ctrl Pts',(13.7499358355066,-0.277069194542941,
3.43771788038699));
#35204=CARTESIAN_POINT('Ctrl Pts',(13.7658411141942,-0.0612398303982075,
3.37615851069845));
#35205=CARTESIAN_POINT('Ctrl Pts',(13.7817463928818,0.130929209162332,3.41950150018632));
#35206=CARTESIAN_POINT('Ctrl Pts',(13.7976516715694,0.323098248722867,3.46284448967418));
#35207=CARTESIAN_POINT('Ctrl Pts',(13.813556950257,0.491606963699209,3.61108983833845));
#35208=CARTESIAN_POINT('Ctrl Pts',(13.8294622289446,0.559083281190044,3.79616955381596));
#35209=CARTESIAN_POINT('Ctrl Pts',(13.8453675076322,0.62655959868088,3.98124926929349));
#35210=CARTESIAN_POINT('Ctrl Pts',(13.8612727863198,0.593003518686204,4.20316335158427));
#35211=CARTESIAN_POINT('Ctrl Pts',(13.8771780650075,0.4738225734989,4.36001824251097));
#35212=CARTESIAN_POINT('Ctrl Pts',(13.8918369062525,0.363981395029584,4.50458099992985));
#35213=CARTESIAN_POINT('Ctrl Pts',(13.9064957474975,0.181409709145346,4.59388191268165));
#35214=CARTESIAN_POINT('Ctrl Pts',(13.9211545887425,-0.000275297881949146,
4.59492513410986));
#35215=CARTESIAN_POINT('Origin',(4.,0.,4.));
#35216=CARTESIAN_POINT('',(14.3288454112576,0.000109044058801022,4.5931342436645));
#35217=CARTESIAN_POINT('',(14.2211545887425,0.000537210645871958,4.59424369460725));
#35218=CARTESIAN_POINT('',(4.,-7.27562663373442E-17,4.5941));
#35219=CARTESIAN_POINT('Ctrl Pts',(14.3288454112576,0.000109044058801022,
4.5931342436645));
#35220=CARTESIAN_POINT('Ctrl Pts',(14.32142400111,0.0928032711674493,4.59328573107644));
#35221=CARTESIAN_POINT('Ctrl Pts',(14.3140025909624,0.185434358886594,4.57287353691408));
#35222=CARTESIAN_POINT('Ctrl Pts',(14.3065811808148,0.267539471941071,4.53154830171049));
#35223=CARTESIAN_POINT('Ctrl Pts',(14.2906759021272,0.443503969097433,4.44298165875801));
#35224=CARTESIAN_POINT('Ctrl Pts',(14.2747706234396,0.571121189235106,4.25835848700565));
#35225=CARTESIAN_POINT('Ctrl Pts',(14.258865344752,0.591794703906212,4.06244993615984));
#35226=CARTESIAN_POINT('Ctrl Pts',(14.2429600660644,0.612468218577319,3.86654138531401));
#35227=CARTESIAN_POINT('Ctrl Pts',(14.2270547873768,0.526198027781844,3.65934745537473));
#35228=CARTESIAN_POINT('Ctrl Pts',(14.2111495086891,0.372595753342289,3.53600283331781));
#35229=CARTESIAN_POINT('Ctrl Pts',(14.1952442300015,0.218993478902743,3.4126582112609));
#35230=CARTESIAN_POINT('Ctrl Pts',(14.1793389513139,-0.00194087918087354,
3.37316289708635));
#35231=CARTESIAN_POINT('Ctrl Pts',(14.1634336726263,-0.18876361063844,3.43565146815417));
#35232=CARTESIAN_POINT('Ctrl Pts',(14.1475283939387,-0.375586342096006,
3.49814003922198));
#35233=CARTESIAN_POINT('Ctrl Pts',(14.1316231152511,-0.528297446927522,
3.66261249553216));
#35234=CARTESIAN_POINT('Ctrl Pts',(14.1157178365635,-0.576778446468407,
3.85355004340287));
#35235=CARTESIAN_POINT('Ctrl Pts',(14.0998125578759,-0.625259446009293,
4.04448759127359));
#35236=CARTESIAN_POINT('Ctrl Pts',(14.0839072791882,-0.569510340259543,
4.26189023070484));
#35237=CARTESIAN_POINT('Ctrl Pts',(14.0680020005006,-0.435128760029281,
4.40593586721696));
#35238=CARTESIAN_POINT('Ctrl Pts',(14.0549498040863,-0.324852491748397,
4.52414265738481));
#35239=CARTESIAN_POINT('Ctrl Pts',(14.0418976076719,-0.161623710204441,
4.5929495310973));
#35240=CARTESIAN_POINT('Ctrl Pts',(14.0288454112576,0.000507412974116619,
4.59441995931617));
#35241=CARTESIAN_POINT('Ctrl Pts',(13.9211545887425,-0.000275297881949146,
4.59492513410986));
#35242=CARTESIAN_POINT('Ctrl Pts',(13.9224010261851,-0.015723926578741,
4.59501383895544));
#35243=CARTESIAN_POINT('Ctrl Pts',(13.9236474636277,-0.0311661445373128,
4.59446443570748));
#35244=CARTESIAN_POINT('Ctrl Pts',(13.9248939010703,-0.0465566941337027,
4.59325663951544));
#35245=CARTESIAN_POINT('Ctrl Pts',(13.9407991797579,-0.242949206199084,
4.5778444460306));
#35246=CARTESIAN_POINT('Ctrl Pts',(13.9567044584455,-0.430928419949921,
4.4552243594983));
#35247=CARTESIAN_POINT('Ctrl Pts',(13.9726097371331,-0.524182233176515,
4.28169833602613));
#35248=CARTESIAN_POINT('Ctrl Pts',(13.9885150158207,-0.617436046403107,
4.10817231255396));
#35249=CARTESIAN_POINT('Ctrl Pts',(14.0044202945084,-0.615964459105464,
3.88374035214192));
#35250=CARTESIAN_POINT('Ctrl Pts',(14.020325573196,-0.52044316191294,3.71145211607799));
#35251=CARTESIAN_POINT('Ctrl Pts',(14.0362308518836,-0.424921864720413,
3.53916388001405));
#35252=CARTESIAN_POINT('Ctrl Pts',(14.0521361305712,-0.235350857633014,
3.41901936829824));
#35253=CARTESIAN_POINT('Ctrl Pts',(14.0680414092588,-0.0387731270173405,
3.40618385781531));
#35254=CARTESIAN_POINT('Ctrl Pts',(14.0839466879464,0.157804603598333,3.39334834733239));
#35255=CARTESIAN_POINT('Ctrl Pts',(14.0998519666341,0.361389057742269,3.48782183808236));
#35256=CARTESIAN_POINT('Ctrl Pts',(14.1157572453217,0.478502867019537,3.64622609995664));
#35257=CARTESIAN_POINT('Ctrl Pts',(14.1316625240093,0.595616676296804,3.80463036183091));
#35258=CARTESIAN_POINT('Ctrl Pts',(14.1475678026969,0.626259840707404,4.02696539482948));
#35259=CARTESIAN_POINT('Ctrl Pts',(14.1634730813845,0.556362315559365,4.21114435801894));
#35260=CARTESIAN_POINT('Ctrl Pts',(14.1793783600721,0.486464790411328,4.3953233212084));
#35261=CARTESIAN_POINT('Ctrl Pts',(14.1952836387597,0.316026575704654,4.54134621458875));
#35262=CARTESIAN_POINT('Ctrl Pts',(14.2111889174473,0.123305688986428,4.58216550323889));
#35263=CARTESIAN_POINT('Ctrl Pts',(14.2145108078791,0.0830550475387342,
4.59069079896363));
#35264=CARTESIAN_POINT('Ctrl Pts',(14.2178326983108,0.0418324306113591,
4.59462708830176));
#35265=CARTESIAN_POINT('Ctrl Pts',(14.2211545887425,0.000537210645871958,
4.59424369460725));
#35266=CARTESIAN_POINT('Origin',(4.,0.,4.));
#35267=CARTESIAN_POINT('',(14.6288454112575,-0.000548182068839831,4.59401855345973));
#35268=CARTESIAN_POINT('',(14.5211545887425,1.28950532977596E-5,4.59311636453746));
#35269=CARTESIAN_POINT('',(4.,-7.27562663373442E-17,4.5941));
#35270=CARTESIAN_POINT('Ctrl Pts',(14.6288454112575,-0.000548182068839831,
4.59401855345973));
#35271=CARTESIAN_POINT('Ctrl Pts',(14.6168556732357,0.148643716013534,4.59265593252186));
#35272=CARTESIAN_POINT('Ctrl Pts',(14.6048659352138,0.29876355451001,4.53564313143304));
#35273=CARTESIAN_POINT('Ctrl Pts',(14.5928761971919,0.407080942069735,4.43405768361063));
#35274=CARTESIAN_POINT('Ctrl Pts',(14.5769709185042,0.55077200793829,4.29929703619113));
#35275=CARTESIAN_POINT('Ctrl Pts',(14.5610656398166,0.620899143473568,4.08609746938767));
#35276=CARTESIAN_POINT('Ctrl Pts',(14.545160361129,0.585262934872208,3.89235120454656));
#35277=CARTESIAN_POINT('Ctrl Pts',(14.5292550824414,0.549626726270847,3.69860493970543));
#35278=CARTESIAN_POINT('Ctrl Pts',(14.5133498037538,0.408227173532835,3.52431197682665));
#35279=CARTESIAN_POINT('Ctrl Pts',(14.4974445250662,0.225988969153725,3.44950027073699));
#35280=CARTESIAN_POINT('Ctrl Pts',(14.4815392463786,0.04375076477463,3.37468856464734));
#35281=CARTESIAN_POINT('Ctrl Pts',(14.465633967691,-0.179326091245555,3.39935811534679));
#35282=CARTESIAN_POINT('Ctrl Pts',(14.4497286890033,-0.340814144225853,
3.51218170883678));
#35283=CARTESIAN_POINT('Ctrl Pts',(14.4338234103157,-0.50230219720616,3.62500530232677));
#35284=CARTESIAN_POINT('Ctrl Pts',(14.4179181316281,-0.602201447146573,
3.82598293860731));
#35285=CARTESIAN_POINT('Ctrl Pts',(14.4020128529405,-0.594642384863179,
4.02283418976097));
#35286=CARTESIAN_POINT('Ctrl Pts',(14.3861075742529,-0.587083322579785,
4.21968544091462));
#35287=CARTESIAN_POINT('Ctrl Pts',(14.3702022955653,-0.47206594807259,4.4124103069414));
#35288=CARTESIAN_POINT('Ctrl Pts',(14.3542970168777,-0.302401373731467,
4.51251768287848));
#35289=CARTESIAN_POINT('Ctrl Pts',(14.3458131483376,-0.211902365642262,
4.565914912441));
#35290=CARTESIAN_POINT('Ctrl Pts',(14.3373292797976,-0.10585540495725,4.59296106912451));
#35291=CARTESIAN_POINT('Ctrl Pts',(14.3288454112576,0.000109044058801022,
4.5931342436645));
#35292=CARTESIAN_POINT('Ctrl Pts',(14.2211545887425,0.000537210645871958,
4.59424369460725));
#35293=CARTESIAN_POINT('Ctrl Pts',(14.2337379769984,-0.155889919212927,
4.59279139152499));
#35294=CARTESIAN_POINT('Ctrl Pts',(14.2463213652543,-0.313358837143528,
4.52935553548989));
#35295=CARTESIAN_POINT('Ctrl Pts',(14.2589047535102,-0.422984449084643,
4.4185751090669));
#35296=CARTESIAN_POINT('Ctrl Pts',(14.2748100321978,-0.561550141707708,
4.27854974232482));
#35297=CARTESIAN_POINT('Ctrl Pts',(14.2907153108854,-0.623677968224056,
4.06288332492072));
#35298=CARTESIAN_POINT('Ctrl Pts',(14.306620589573,-0.580841459108965,3.87060075163287));
#35299=CARTESIAN_POINT('Ctrl Pts',(14.3225258682606,-0.538004949993874,
3.67831817834502));
#35300=CARTESIAN_POINT('Ctrl Pts',(14.3384311469482,-0.390204105247342,
3.50941944917344));
#35301=CARTESIAN_POINT('Ctrl Pts',(14.3543364256359,-0.205302819838896,
3.44145571503774));
#35302=CARTESIAN_POINT('Ctrl Pts',(14.3702417043235,-0.0204015344304391,
3.37349198090203));
#35303=CARTESIAN_POINT('Ctrl Pts',(14.3861469830111,0.201600191639931,3.40646324180223));
#35304=CARTESIAN_POINT('Ctrl Pts',(14.4020522616987,0.358768557879186,3.52523048963197));
#35305=CARTESIAN_POINT('Ctrl Pts',(14.4179575403863,0.515936924118427,3.6439977374617));
#35306=CARTESIAN_POINT('Ctrl Pts',(14.4338628190739,0.608271930526566,3.84856097222098));
#35307=CARTESIAN_POINT('Ctrl Pts',(14.4497680977615,0.59337724853295,4.04499341086509));
#35308=CARTESIAN_POINT('Ctrl Pts',(14.4656733764491,0.578482566539332,4.2414258495092));
#35309=CARTESIAN_POINT('Ctrl Pts',(14.4815786551367,0.456358196143958,4.42972749203816));
#35310=CARTESIAN_POINT('Ctrl Pts',(14.4974839338244,0.283078481576349,4.52343819058819));
#35311=CARTESIAN_POINT('Ctrl Pts',(14.5053741521304,0.197118668938093,4.56992576768087));
#35312=CARTESIAN_POINT('Ctrl Pts',(14.5132643704364,0.0985699939877532,
4.59313537862966));
#35313=CARTESIAN_POINT('Ctrl Pts',(14.5211545887425,1.28950532977596E-5,
4.59311636453746));
#35314=CARTESIAN_POINT('Origin',(4.,0.,4.));
#35315=CARTESIAN_POINT('',(14.9288454112575,0.000149915246051877,4.59503491979621));
#35316=CARTESIAN_POINT('',(14.8211545887425,-0.000542004001680995,4.59419620878869));
#35317=CARTESIAN_POINT('',(4.,-7.27562663373442E-17,4.5941));
#35318=CARTESIAN_POINT('Ctrl Pts',(14.9288454112575,0.000149915246051877,
4.59503491979621));
#35319=CARTESIAN_POINT('Ctrl Pts',(14.9281926240489,0.00823674021970066,
4.59506221957623));
#35320=CARTESIAN_POINT('Ctrl Pts',(14.9275398368403,0.0163225255999611,
4.59491168338633));
#35321=CARTESIAN_POINT('Ctrl Pts',(14.9268870496317,0.0244008833477238,
4.59458015690877));
#35322=CARTESIAN_POINT('Ctrl Pts',(14.9109817709441,0.221231534471853,4.58650245417764));
#35323=CARTESIAN_POINT('Ctrl Pts',(14.8950764922565,0.413652681988333,4.47097768448731));
#35324=CARTESIAN_POINT('Ctrl Pts',(14.8791712135689,0.513312675625014,4.30104993462962));
#35325=CARTESIAN_POINT('Ctrl Pts',(14.8632659348813,0.612972669261697,4.13112218477192));
#35326=CARTESIAN_POINT('Ctrl Pts',(14.8473606561937,0.619871509018575,3.90679145474687));
#35327=CARTESIAN_POINT('Ctrl Pts',(14.831455377506,0.530841539545133,3.73106092513143));
#35328=CARTESIAN_POINT('Ctrl Pts',(14.8155500988184,0.441811570071688,3.55533039551599));
#35329=CARTESIAN_POINT('Ctrl Pts',(14.7996448201308,0.256852791367914,3.42820006631018));
#35330=CARTESIAN_POINT('Ctrl Pts',(14.7837395414432,0.0608904496539635,
3.40804280624462));
#35331=CARTESIAN_POINT('Ctrl Pts',(14.7678342627556,-0.135071892059981,
3.38788554617906));
#35332=CARTESIAN_POINT('Ctrl Pts',(14.751928984068,-0.342037796784102,3.47470135525375));
#35333=CARTESIAN_POINT('Ctrl Pts',(14.7360237053804,-0.464977277074429,
3.62862808681558));
#35334=CARTESIAN_POINT('Ctrl Pts',(14.7201184266927,-0.587916757364756,
3.78255481837741));
#35335=CARTESIAN_POINT('Ctrl Pts',(14.7042131480052,-0.62682981322129,4.00359247242638));
#35336=CARTESIAN_POINT('Ctrl Pts',(14.6883078693175,-0.56384921567034,4.19024990955517));
#35337=CARTESIAN_POINT('Ctrl Pts',(14.6724025906299,-0.500868618119389,
4.37690734668397));
#35338=CARTESIAN_POINT('Ctrl Pts',(14.6564973119423,-0.335994367160947,
4.52918456689258));
#35339=CARTESIAN_POINT('Ctrl Pts',(14.6405920332547,-0.144929743580805,
4.57716231297912));
#35340=CARTESIAN_POINT('Ctrl Pts',(14.636676492589,-0.097893704910838,4.5889734116427));
#35341=CARTESIAN_POINT('Ctrl Pts',(14.6327609519233,-0.0492704262804658,
4.59446355048005));
#35342=CARTESIAN_POINT('Ctrl Pts',(14.6288454112575,-0.000548182068839831,
4.59401855345973));
#35343=CARTESIAN_POINT('Ctrl Pts',(14.5211545887425,1.28950532977596E-5,
4.59311636453746));
#35344=CARTESIAN_POINT('Ctrl Pts',(14.5291696491241,-0.100103612291989,
4.59309704959697));
#35345=CARTESIAN_POINT('Ctrl Pts',(14.5371847095056,-0.200228812305367,
4.56910822985942));
#35346=CARTESIAN_POINT('Ctrl Pts',(14.5451997698872,-0.287175610734119,
4.52120162576233));
#35347=CARTESIAN_POINT('Ctrl Pts',(14.5611050485748,-0.459714929737158,
4.42613460781534));
#35348=CARTESIAN_POINT('Ctrl Pts',(14.5770103272624,-0.580358509003398,
4.23688081735026));
#35349=CARTESIAN_POINT('Ctrl Pts',(14.59291560595,-0.593711920942704,4.04033758828107));
#35350=CARTESIAN_POINT('Ctrl Pts',(14.6088208846377,-0.607065332882009,
3.84379435921188));
#35351=CARTESIAN_POINT('Ctrl Pts',(14.6247261633253,-0.513128577494387,
3.63996169153858));
#35352=CARTESIAN_POINT('Ctrl Pts',(14.6406314420129,-0.35503343871745,3.52243092280774));
#35353=CARTESIAN_POINT('Ctrl Pts',(14.6565367207005,-0.196938299940509,
3.40490015407689));
#35354=CARTESIAN_POINT('Ctrl Pts',(14.6724419993881,0.025315222225754,3.37367128428849));
#35355=CARTESIAN_POINT('Ctrl Pts',(14.6883472780757,0.209677713173688,3.44308328926485));
#35356=CARTESIAN_POINT('Ctrl Pts',(14.7042525567633,0.394040204121622,3.51249529424121));
#35357=CARTESIAN_POINT('Ctrl Pts',(14.720157835451,0.540511663851219,3.68254817398232));
#35358=CARTESIAN_POINT('Ctrl Pts',(14.7360631141386,0.581838594751101,3.87516084045512));
#35359=CARTESIAN_POINT('Ctrl Pts',(14.7519683928262,0.623165525650983,4.06777350692792));
#35360=CARTESIAN_POINT('Ctrl Pts',(14.7678736715138,0.559347927721136,4.2829459601324));
#35361=CARTESIAN_POINT('Ctrl Pts',(14.7837789502014,0.419688142031033,4.42188011275284));
#35362=CARTESIAN_POINT('Ctrl Pts',(14.7962374963817,0.310293146587505,4.53070672248707));
#35363=CARTESIAN_POINT('Ctrl Pts',(14.8086960425621,0.154364940471616,4.59275708529138));
#35364=CARTESIAN_POINT('Ctrl Pts',(14.8211545887425,-0.000542004001680995,
4.59419620878869));
#35365=CARTESIAN_POINT('Origin',(4.,0.,4.));
#35366=CARTESIAN_POINT('',(15.2288454112576,0.000471544078774977,4.59356550157774));
#35367=CARTESIAN_POINT('',(15.1211545887425,0.000250233060073018,4.59495282954609));
#35368=CARTESIAN_POINT('',(4.,-7.27562663373442E-17,4.5941));
#35369=CARTESIAN_POINT('Ctrl Pts',(15.2288454112576,0.000471544078774977,
4.59356550157774));
#35370=CARTESIAN_POINT('Ctrl Pts',(15.2236242961746,0.0655651715058866,
4.59404721416646));
#35371=CARTESIAN_POINT('Ctrl Pts',(15.2184031810917,0.130516835945995,4.58418155789741));
#35372=CARTESIAN_POINT('Ctrl Pts',(15.2131820660088,0.191734887706884,4.56334598510492));
#35373=CARTESIAN_POINT('Ctrl Pts',(15.1972767873211,0.378225734681762,4.49987379829874));
#35374=CARTESIAN_POINT('Ctrl Pts',(15.1813715086335,0.530068013118856,4.33459889729257));
#35375=CARTESIAN_POINT('Ctrl Pts',(15.1654662299459,0.577542172676889,4.143408524424));
#35376=CARTESIAN_POINT('Ctrl Pts',(15.1495609512583,0.625016332234921,3.95221815155542));
#35377=CARTESIAN_POINT('Ctrl Pts',(15.1336556725707,0.568122372913892,3.73511230682445));
#35378=CARTESIAN_POINT('Ctrl Pts',(15.1177503938831,0.432983593849097,3.59177680914072));
#35379=CARTESIAN_POINT('Ctrl Pts',(15.1018451151955,0.297844814784303,3.44844131145699));
#35380=CARTESIAN_POINT('Ctrl Pts',(15.0859398365078,0.0844612159757424,
3.37887616082051));
#35381=CARTESIAN_POINT('Ctrl Pts',(15.0700345578202,-0.109190481519281,
3.41502273134472));
#35382=CARTESIAN_POINT('Ctrl Pts',(15.0541292791326,-0.302842179014298,
3.45116930186893));
#35383=CARTESIAN_POINT('Ctrl Pts',(15.038224000445,-0.47676197519578,3.59302759355383));
#35384=CARTESIAN_POINT('Ctrl Pts',(15.0223187217574,-0.551093257596978,
3.77546228038711));
#35385=CARTESIAN_POINT('Ctrl Pts',(15.0064134430698,-0.625424539998176,
3.95789696722038));
#35386=CARTESIAN_POINT('Ctrl Pts',(14.9905081643822,-0.600167308619091,
4.18090804920204));
#35387=CARTESIAN_POINT('Ctrl Pts',(14.9746028856946,-0.486918615563658,
4.34209827230691));
#35388=CARTESIAN_POINT('Ctrl Pts',(14.9593503942156,-0.378317895025423,
4.49667289829699));
#35389=CARTESIAN_POINT('Ctrl Pts',(14.9440979027365,-0.188800216398263,
4.59439705548643));
#35390=CARTESIAN_POINT('Ctrl Pts',(14.9288454112575,0.000149915246051877,
4.59503491979621));
#35391=CARTESIAN_POINT('Ctrl Pts',(14.8211545887425,-0.000542004001680995,
4.59419620878869));
#35392=CARTESIAN_POINT('Ctrl Pts',(14.8246013212497,-0.0433979515083632,
4.5945943510493));
#35393=CARTESIAN_POINT('Ctrl Pts',(14.828048053757,-0.0861757330942537,
4.59035339483295));
#35394=CARTESIAN_POINT('Ctrl Pts',(14.8314947862642,-0.127868389248254,
4.58118038604969));
#35395=CARTESIAN_POINT('Ctrl Pts',(14.8474000649518,-0.320263161387096,
4.5388506546897));
#35396=CARTESIAN_POINT('Ctrl Pts',(14.8633053436395,-0.489550732214419,
4.39149533993331));
#35397=CARTESIAN_POINT('Ctrl Pts',(14.8792106223271,-0.558001411172811,
4.20677376822741));
#35398=CARTESIAN_POINT('Ctrl Pts',(14.8951159010147,-0.6264520901312,4.0220521965215));
#35399=CARTESIAN_POINT('Ctrl Pts',(14.9110211797023,-0.594065877220663,
3.79996436786608));
#35400=CARTESIAN_POINT('Ctrl Pts',(14.9269264583899,-0.475713151262041,
3.64248361741852));
#35401=CARTESIAN_POINT('Ctrl Pts',(14.9428317370775,-0.357360425303418,
3.48500286697096));
#35402=CARTESIAN_POINT('Ctrl Pts',(14.9587370157651,-0.153041186296697,
3.39212919473125));
#35403=CARTESIAN_POINT('Ctrl Pts',(14.9746422944528,0.0434298152403689,
3.40650626183085));
#35404=CARTESIAN_POINT('Ctrl Pts',(14.9905475731404,0.239900816777435,3.42088332893044));
#35405=CARTESIAN_POINT('Ctrl Pts',(15.006452851828,0.428523580844854,3.54251113536931));
#35406=CARTESIAN_POINT('Ctrl Pts',(15.0223581305156,0.522690514153935,3.71554333807889));
#35407=CARTESIAN_POINT('Ctrl Pts',(15.0382634092032,0.616857447463019,3.88857554078846));
#35408=CARTESIAN_POINT('Ctrl Pts',(15.0541686878908,0.616568550013756,4.11301213976874));
#35409=CARTESIAN_POINT('Ctrl Pts',(15.0700739665784,0.521956471292605,4.28580134389743));
#35410=CARTESIAN_POINT('Ctrl Pts',(15.085979245266,0.427344392571456,4.45859054802613));
#35411=CARTESIAN_POINT('Ctrl Pts',(15.1018845239536,0.238409132578427,4.57973235730324));
#35412=CARTESIAN_POINT('Ctrl Pts',(15.1177898026413,0.0419017695106382,
4.59360357799603));
#35413=CARTESIAN_POINT('Ctrl Pts',(15.1189113980083,0.0280446248267054,
4.59458173733358));
#35414=CARTESIAN_POINT('Ctrl Pts',(15.1200329933754,0.0141498265549413,
4.59502647517791));
#35415=CARTESIAN_POINT('Ctrl Pts',(15.1211545887425,0.000250233060073018,
4.59495282954609));
#35416=CARTESIAN_POINT('Origin',(4.,0.,4.));
#35417=CARTESIAN_POINT('',(15.5288454112575,-0.000350670266729247,4.59332700645389));
#35418=CARTESIAN_POINT('',(15.4211545887425,0.000414092275955974,4.59343115273787));
#35419=CARTESIAN_POINT('',(4.,-7.27562663373442E-17,4.5941));
#35420=CARTESIAN_POINT('Ctrl Pts',(15.5288454112575,-0.000350670266729247,
4.59332700645389));
#35421=CARTESIAN_POINT('Ctrl Pts',(15.5190559683003,0.121821298278883,4.59267222728074));
#35422=CARTESIAN_POINT('Ctrl Pts',(15.509266525343,0.244354036528086,4.55597946496206));
#35423=CARTESIAN_POINT('Ctrl Pts',(15.4994770823858,0.343380025451582,4.48601555964668));
#35424=CARTESIAN_POINT('Ctrl Pts',(15.4835718036982,0.504271299656008,4.37234255322809));
#35425=CARTESIAN_POINT('Ctrl Pts',(15.4676665250105,0.603110088323456,4.17084127710728));
#35426=CARTESIAN_POINT('Ctrl Pts',(15.4517612463229,0.594513801222153,3.97403259246294));
#35427=CARTESIAN_POINT('Ctrl Pts',(15.4358559676353,0.58591751412085,3.7772239078186));
#35428=CARTESIAN_POINT('Ctrl Pts',(15.4199506889477,0.469886151250777,3.58510781465072));
#35429=CARTESIAN_POINT('Ctrl Pts',(15.4040454102601,0.299696405559752,3.48589589518039));
#35430=CARTESIAN_POINT('Ctrl Pts',(15.3881401315725,0.129506659868722,3.38668397571006));
#35431=CARTESIAN_POINT('Ctrl Pts',(15.3722348528849,-0.0948414686432761,
3.38037622993726));
#35432=CARTESIAN_POINT('Ctrl Pts',(15.3563295741973,-0.270336810750117,
3.46986890786216));
#35433=CARTESIAN_POINT('Ctrl Pts',(15.3404242955096,-0.445832152856957,
3.55936158578705));
#35434=CARTESIAN_POINT('Ctrl Pts',(15.324519016822,-0.572474708558633,3.74465468740961));
#35435=CARTESIAN_POINT('Ctrl Pts',(15.3086137381344,-0.592115574081638,
3.94066945956945));
#35436=CARTESIAN_POINT('Ctrl Pts',(15.2927084594468,-0.611756439604643,
4.13668423172929));
#35437=CARTESIAN_POINT('Ctrl Pts',(15.2768031807592,-0.524395614948954,
4.3434206744264));
#35438=CARTESIAN_POINT('Ctrl Pts',(15.2608979020716,-0.370145494864779,
4.46595415947185));
#35439=CARTESIAN_POINT('Ctrl Pts',(15.2502137384669,-0.266529987624151,
4.54826443060822));
#35440=CARTESIAN_POINT('Ctrl Pts',(15.2395295748622,-0.13273198696893,4.59257975504152));
#35441=CARTESIAN_POINT('Ctrl Pts',(15.2288454112576,0.000471544078774977,
4.59356550157774));
#35442=CARTESIAN_POINT('Ctrl Pts',(15.1211545887425,0.000250233060073018,
4.59495282954609));
#35443=CARTESIAN_POINT('Ctrl Pts',(15.135938272063,-0.18295950063263,4.59398211075496));
#35444=CARTESIAN_POINT('Ctrl Pts',(15.1507219553836,-0.367002343096231,
4.50294888365168));
#35445=CARTESIAN_POINT('Ctrl Pts',(15.1655056387041,-0.476631971954554,
4.35629051265579));
#35446=CARTESIAN_POINT('Ctrl Pts',(15.1814109173917,-0.594578884209397,
4.19850559451431));
#35447=CARTESIAN_POINT('Ctrl Pts',(15.1973161960793,-0.626393242576541,
3.97633512612291));
#35448=CARTESIAN_POINT('Ctrl Pts',(15.2132214747669,-0.557467239648298,
3.79179038730953));
#35449=CARTESIAN_POINT('Ctrl Pts',(15.2291267534545,-0.488541236720055,
3.60724564849615));
#35450=CARTESIAN_POINT('Ctrl Pts',(15.2450320321422,-0.318874872496425,
3.46032663926078));
#35451=CARTESIAN_POINT('Ctrl Pts',(15.2609373108298,-0.126371763436977,
3.41849235301362));
#35452=CARTESIAN_POINT('Ctrl Pts',(15.2768425895174,0.0661313456224706,
3.37665806676646));
#35453=CARTESIAN_POINT('Ctrl Pts',(15.292747868205,0.281471199517752,3.4399085035075));
#35454=CARTESIAN_POINT('Ctrl Pts',(15.3086531468926,0.420772847618048,3.57920173859056));
#35455=CARTESIAN_POINT('Ctrl Pts',(15.3245584255802,0.560074495718348,3.71849497367363));
#35456=CARTESIAN_POINT('Ctrl Pts',(15.3404637042678,0.623337938023671,3.9338310070987));
#35457=CARTESIAN_POINT('Ctrl Pts',(15.3563689829554,0.581515278282945,4.12633664243329));
#35458=CARTESIAN_POINT('Ctrl Pts',(15.3722742616431,0.53969261854222,4.31884227776789));
#35459=CARTESIAN_POINT('Ctrl Pts',(15.3881795403307,0.392783856755445,4.48851751501199));
#35460=CARTESIAN_POINT('Ctrl Pts',(15.4040848190183,0.208243281137944,4.55745466359042));
#35461=CARTESIAN_POINT('Ctrl Pts',(15.4097747422597,0.142226097106806,4.58211610408423));
#35462=CARTESIAN_POINT('Ctrl Pts',(15.4154646655011,0.0713929250243718,
4.593885435962));
#35463=CARTESIAN_POINT('Ctrl Pts',(15.4211545887425,0.000414092275955974,
4.59343115273787));
#35464=CARTESIAN_POINT('Origin',(4.,0.,4.));
#35465=CARTESIAN_POINT('',(15.8288454112575,-0.000332254705457391,4.59484959654372));
#35466=CARTESIAN_POINT('',(15.7211545887425,-0.000419917270904514,4.59344262983929));
#35467=CARTESIAN_POINT('',(4.,-7.27562663373442E-17,4.5941));
#35468=CARTESIAN_POINT('Ctrl Pts',(15.8288454112575,-0.000332254705457391,
4.59484959654372));
#35469=CARTESIAN_POINT('Ctrl Pts',(15.814487640426,0.177680873019276,4.5936575613883));
#35470=CARTESIAN_POINT('Ctrl Pts',(15.8001298695944,0.356683508224643,4.50844978272675));
#35471=CARTESIAN_POINT('Ctrl Pts',(15.7857720987628,0.466927807092597,4.36891650689757));
#35472=CARTESIAN_POINT('Ctrl Pts',(15.7698668200752,0.589054446233417,4.21434406913608));
#35473=CARTESIAN_POINT('Ctrl Pts',(15.7539615413876,0.626802179063893,3.99310442736787));
#35474=CARTESIAN_POINT('Ctrl Pts',(15.7380562627,0.562838843643149,3.80678146521555));
#35475=CARTESIAN_POINT('Ctrl Pts',(15.7221509840123,0.498875508222402,3.62045850306322));
#35476=CARTESIAN_POINT('Ctrl Pts',(15.7062457053247,0.333201104550436,3.46905222052678));
#35477=CARTESIAN_POINT('Ctrl Pts',(15.6903404266371,0.141886309687413,3.42208197707538));
#35478=CARTESIAN_POINT('Ctrl Pts',(15.6744351479495,-0.0494284851756215,
3.37511173362399));
#35479=CARTESIAN_POINT('Ctrl Pts',(15.6585298692619,-0.266383671229707,
3.43257752925765));
#35480=CARTESIAN_POINT('Ctrl Pts',(15.6426245905743,-0.409362605655794,
3.5680935017987));
#35481=CARTESIAN_POINT('Ctrl Pts',(15.6267193118867,-0.552341540081869,
3.70360947433975));
#35482=CARTESIAN_POINT('Ctrl Pts',(15.6108140331991,-0.621344222879956,
3.9171756237882));
#35483=CARTESIAN_POINT('Ctrl Pts',(15.5949087545115,-0.584687541371933,
4.11073140955597));
#35484=CARTESIAN_POINT('Ctrl Pts',(15.5790034758238,-0.548030859863907,
4.30428719532377));
#35485=CARTESIAN_POINT('Ctrl Pts',(15.5630981971362,-0.405714814049763,
4.47783261741089));
#35486=CARTESIAN_POINT('Ctrl Pts',(15.5471929184486,-0.223084911271984,
4.55168296009627));
#35487=CARTESIAN_POINT('Ctrl Pts',(15.5410770827183,-0.152860773312716,
4.58007960584922));
#35488=CARTESIAN_POINT('Ctrl Pts',(15.5349612469879,-0.0766761255292402,
4.5937360717991));
#35489=CARTESIAN_POINT('Ctrl Pts',(15.5288454112575,-0.000350670266729247,
4.59332700645389));
#35490=CARTESIAN_POINT('Ctrl Pts',(15.4211545887425,0.000414092275955974,
4.59343115273787));
#35491=CARTESIAN_POINT('Ctrl Pts',(15.4313699441887,-0.12701715326484,4.59261555920332));
#35492=CARTESIAN_POINT('Ctrl Pts',(15.4415852996349,-0.254917899718674,
4.55240018390688));
#35493=CARTESIAN_POINT('Ctrl Pts',(15.4518006550811,-0.356261725310785,
4.47665348962993));
#35494=CARTESIAN_POINT('Ctrl Pts',(15.4677059337687,-0.514053766693778,
4.35871610717824));
#35495=CARTESIAN_POINT('Ctrl Pts',(15.4836112124564,-0.607465460011524,
4.15464228236211));
#35496=CARTESIAN_POINT('Ctrl Pts',(15.499516491144,-0.593606107615349,3.95813408188558));
#35497=CARTESIAN_POINT('Ctrl Pts',(15.5154217698316,-0.579746755219174,
3.76162588140906));
#35498=CARTESIAN_POINT('Ctrl Pts',(15.5313270485192,-0.458616357109098,
3.57268330527213));
#35499=CARTESIAN_POINT('Ctrl Pts',(15.5472323272068,-0.285832867492734,
3.47806079093568));
#35500=CARTESIAN_POINT('Ctrl Pts',(15.5631376058944,-0.113049377876356,
3.38343827659922));
#35501=CARTESIAN_POINT('Ctrl Pts',(15.579042884582,0.111387203246309,3.38313582406324));
#35502=CARTESIAN_POINT('Ctrl Pts',(15.5949481632696,0.284425092952457,3.47729230673655));
#35503=CARTESIAN_POINT('Ctrl Pts',(15.6108534419572,0.457462982658595,3.57144878940986));
#35504=CARTESIAN_POINT('Ctrl Pts',(15.6267587206449,0.579102180948212,3.76006420729246));
#35505=CARTESIAN_POINT('Ctrl Pts',(15.6426639993325,0.593491114096805,3.95653434015292));
#35506=CARTESIAN_POINT('Ctrl Pts',(15.6585692780201,0.607880047245398,4.15300447301339));
#35507=CARTESIAN_POINT('Ctrl Pts',(15.6744745567077,0.515018715252963,4.35732932085173));
#35508=CARTESIAN_POINT('Ctrl Pts',(15.6903798353953,0.357545113131455,4.47569155781202));
#35509=CARTESIAN_POINT('Ctrl Pts',(15.700638086511,0.255981111243369,4.55203033647815));
#35510=CARTESIAN_POINT('Ctrl Pts',(15.7108963376268,0.127540214881222,4.59261107697802));
#35511=CARTESIAN_POINT('Ctrl Pts',(15.7211545887425,-0.000419917270904514,
4.59344262983929));
#35512=CARTESIAN_POINT('Origin',(4.,0.,4.));
#35513=CARTESIAN_POINT('',(16.1288454112575,0.000520203518568921,4.59435747030618));
#35514=CARTESIAN_POINT('',(16.0211545887425,-0.00024144267326323,4.59496181546483));
#35515=CARTESIAN_POINT('',(4.,-7.27562663373442E-17,4.5941));
#35516=CARTESIAN_POINT('Ctrl Pts',(16.1288454112575,0.000520203518568921,
4.59435747030618));
#35517=CARTESIAN_POINT('Ctrl Pts',(16.1258245912393,0.0380542554257849,
4.59470210862833));
#35518=CARTESIAN_POINT('Ctrl Pts',(16.122803771221,0.0755288363057283,4.59145263304759));
#35519=CARTESIAN_POINT('Ctrl Pts',(16.1197829512027,0.112271568866026,4.58439375503351));
#35520=CARTESIAN_POINT('Ctrl Pts',(16.1038776725151,0.305730099191281,4.54722721702202));
#35521=CARTESIAN_POINT('Ctrl Pts',(16.0879723938275,0.478899942385972,4.40445440507416));
#35522=CARTESIAN_POINT('Ctrl Pts',(16.0720671151398,0.55226883266698,4.22163055421683));
#35523=CARTESIAN_POINT('Ctrl Pts',(16.0561618364522,0.625637722947984,4.03880670335952));
#35524=CARTESIAN_POINT('Ctrl Pts',(16.0402565577646,0.599205660315318,3.81593181359275));
#35525=CARTESIAN_POINT('Ctrl Pts',(16.024351279077,0.485109129681553,3.65534060523843));
#35526=CARTESIAN_POINT('Ctrl Pts',(16.0084460003894,0.371012599047788,3.4947493968841));
#35527=CARTESIAN_POINT('Ctrl Pts',(15.9925407217018,0.169251600412921,3.39644186994223));
#35528=CARTESIAN_POINT('Ctrl Pts',(15.9766354430142,-0.0275337514538456,
3.40555668173602));
#35529=CARTESIAN_POINT('Ctrl Pts',(15.9607301643265,-0.224319103320618,
3.41467149352982));
#35530=CARTESIAN_POINT('Ctrl Pts',(15.9448248856389,-0.416128808419276,
3.53120864405929));
#35531=CARTESIAN_POINT('Ctrl Pts',(15.9289196069513,-0.514891964967956,
3.70165920408156));
#35532=CARTESIAN_POINT('Ctrl Pts',(15.9130143282637,-0.613655121516638,
3.87210976410384));
#35533=CARTESIAN_POINT('Ctrl Pts',(15.8971090495761,-0.619371729515322,
4.09647373361892));
#35534=CARTESIAN_POINT('Ctrl Pts',(15.8812037708885,-0.52941696442075,4.27173266988224));
#35535=CARTESIAN_POINT('Ctrl Pts',(15.8652984922009,-0.439462199326184,
4.44699160614554));
#35536=CARTESIAN_POINT('Ctrl Pts',(15.8493932135132,-0.25383606113837,4.57314550915708));
#35537=CARTESIAN_POINT('Ctrl Pts',(15.8334879348256,-0.0577702193188812,
4.59226984378546));
#35538=CARTESIAN_POINT('Ctrl Pts',(15.8319404269696,-0.0386939468137543,
4.59413055045147));
#35539=CARTESIAN_POINT('Ctrl Pts',(15.8303929191136,-0.0195188482833839,
4.59497807636063));
#35540=CARTESIAN_POINT('Ctrl Pts',(15.8288454112575,-0.000332254705457391,
4.59484959654372));
#35541=CARTESIAN_POINT('Ctrl Pts',(15.7211545887425,-0.000419917270904514,
4.59344262983929));
#35542=CARTESIAN_POINT('Ctrl Pts',(15.7268016163144,-0.0708602278282204,
4.59390038836772));
#35543=CARTESIAN_POINT('Ctrl Pts',(15.7324486438863,-0.141154849878182,
4.58231274148771));
#35544=CARTESIAN_POINT('Ctrl Pts',(15.7380956714582,-0.206740066761224,
4.55801389847688));
#35545=CARTESIAN_POINT('Ctrl Pts',(15.7540009501458,-0.391465772281827,
4.48957437609924));
#35546=CARTESIAN_POINT('Ctrl Pts',(15.7699062288334,-0.538831311072463,
4.32029570526172));
#35547=CARTESIAN_POINT('Ctrl Pts',(15.785811507521,-0.58117266224226,4.12790349002296));
#35548=CARTESIAN_POINT('Ctrl Pts',(15.8017167862086,-0.62351401341206,3.93551127478418));
#35549=CARTESIAN_POINT('Ctrl Pts',(15.8176220648962,-0.560831176961022,
3.72000551514415));
#35550=CARTESIAN_POINT('Ctrl Pts',(15.8335273435838,-0.421905459495345,
3.58033733863277));
#35551=CARTESIAN_POINT('Ctrl Pts',(15.8494326222715,-0.282979742029676,
3.44066916212139));
#35552=CARTESIAN_POINT('Ctrl Pts',(15.8653379009591,-0.0678111435493865,
3.37683856873865));
#35553=CARTESIAN_POINT('Ctrl Pts',(15.8812431796467,0.124804018556085,3.41815386651619));
#35554=CARTESIAN_POINT('Ctrl Pts',(15.8971484583343,0.317419180661557,3.45946916429373));
#35555=CARTESIAN_POINT('Ctrl Pts',(15.9130537370219,0.487480906392202,3.60593035323155));
#35556=CARTESIAN_POINT('Ctrl Pts',(15.9289590157095,0.556904046010802,3.79028865163133));
#35557=CARTESIAN_POINT('Ctrl Pts',(15.9448642943971,0.6263271856294,3.9746469500311));
#35558=CARTESIAN_POINT('Ctrl Pts',(15.9607695730847,0.595111739135951,4.19690235789283));
#35559=CARTESIAN_POINT('Ctrl Pts',(15.9766748517723,0.477590518943614,4.35500459477727));
#35560=CARTESIAN_POINT('Ctrl Pts',(15.9915014307624,0.368039615220995,4.50238430120742));
#35561=CARTESIAN_POINT('Ctrl Pts',(16.0063280097524,0.18349252241573,4.59401752470064));
#35562=CARTESIAN_POINT('Ctrl Pts',(16.0211545887425,-0.00024144267326323,
4.59496181546483));
#35563=CARTESIAN_POINT('Origin',(4.,0.,4.));
#35564=CARTESIAN_POINT('',(16.4288454112575,7.48704377684928E-5,4.59312461313858));
#35565=CARTESIAN_POINT('',(16.3211545887425,0.000543344619121817,4.59417988242975));
#35566=CARTESIAN_POINT('',(4.,-7.27562663373442E-17,4.5941));
#35567=CARTESIAN_POINT('Ctrl Pts',(16.4288454112575,7.48704377684928E-5,
4.59312461313858));
#35568=CARTESIAN_POINT('Ctrl Pts',(16.4212562633649,0.0948679978941589,
4.5932308806522));
#35569=CARTESIAN_POINT('Ctrl Pts',(16.4136671154723,0.189615837117123,4.57184094704105));
#35570=CARTESIAN_POINT('Ctrl Pts',(16.4060779675797,0.273126642574496,4.52869916135151));
#35571=CARTESIAN_POINT('Ctrl Pts',(16.3901726888921,0.448147956300534,4.43828293357696));
#35572=CARTESIAN_POINT('Ctrl Pts',(16.3742674102045,0.573812330828296,4.25232504748949));
#35573=CARTESIAN_POINT('Ctrl Pts',(16.3583621315169,0.592420001795879,4.05620949715111));
#35574=CARTESIAN_POINT('Ctrl Pts',(16.3424568528292,0.611027672763462,3.86009394681272));
#35575=CARTESIAN_POINT('Ctrl Pts',(16.3265515741416,0.522578640170867,3.6538207322234));
#35576=CARTESIAN_POINT('Ctrl Pts',(16.310646295454,0.367684957814641,3.53210178682255));
#35577=CARTESIAN_POINT('Ctrl Pts',(16.2947410167664,0.212791275458425,3.4103828414217));
#35578=CARTESIAN_POINT('Ctrl Pts',(16.2788357380788,-0.00854705666138705,
3.3732181652093));
#35579=CARTESIAN_POINT('Ctrl Pts',(16.2629304593912,-0.19470084048803,3.43767220519428));
#35580=CARTESIAN_POINT('Ctrl Pts',(16.2470251807036,-0.380854624314662,
3.50212624517926));
#35581=CARTESIAN_POINT('Ctrl Pts',(16.231119902016,-0.531823859848111,3.66819900136163));
#35582=CARTESIAN_POINT('Ctrl Pts',(16.2152146233283,-0.578289861113055,
3.85963689006134));
#35583=CARTESIAN_POINT('Ctrl Pts',(16.1993093446407,-0.624755862378002,
4.05107477876107));
#35584=CARTESIAN_POINT('Ctrl Pts',(16.1834040659531,-0.566718629374431,
4.26787779997815));
#35585=CARTESIAN_POINT('Ctrl Pts',(16.1674987872655,-0.430826404144746,
4.41049917854914));
#35586=CARTESIAN_POINT('Ctrl Pts',(16.1546143285962,-0.320743594918802,
4.52603310245269));
#35587=CARTESIAN_POINT('Ctrl Pts',(16.1417298699269,-0.159570744489656,
4.592887512417));
#35588=CARTESIAN_POINT('Ctrl Pts',(16.1288454112575,0.000520203518568921,
4.59435747030618));
#35589=CARTESIAN_POINT('Ctrl Pts',(16.0211545887425,-0.00024144267326323,
4.59496181546483));
#35590=CARTESIAN_POINT('Ctrl Pts',(16.0222332884401,-0.0136089074611732,
4.59503051682625));
#35591=CARTESIAN_POINT('Ctrl Pts',(16.0233119881376,-0.0269720681925484,
4.59461918253551));
#35592=CARTESIAN_POINT('Ctrl Pts',(16.0243906878352,-0.0403017303441999,
4.59371435609144));
#35593=CARTESIAN_POINT('Ctrl Pts',(16.0402959665228,-0.236845765548457,
4.58037281461397));
#35594=CARTESIAN_POINT('Ctrl Pts',(16.0562012452104,-0.426106842065734,
4.45974066575184));
#35595=CARTESIAN_POINT('Ctrl Pts',(16.072106523898,-0.521184280535122,4.2872070887372));
#35596=CARTESIAN_POINT('Ctrl Pts',(16.0880118025856,-0.616261719004504,
4.11467351172257));
#35597=CARTESIAN_POINT('Ctrl Pts',(16.1039170812732,-0.61715551942601,3.89023850655542));
#35598=CARTESIAN_POINT('Ctrl Pts',(16.1198223599609,-0.523455286459661,
3.71695313254649));
#35599=CARTESIAN_POINT('Ctrl Pts',(16.1357276386485,-0.429755053493313,
3.54366775853756));
#35600=CARTESIAN_POINT('Ctrl Pts',(16.1516329173361,-0.241460787139106,
3.42153201568684));
#35601=CARTESIAN_POINT('Ctrl Pts',(16.1675381960237,-0.045029248433429,
3.40662546997421));
#35602=CARTESIAN_POINT('Ctrl Pts',(16.1834434747113,0.151402290272254,3.39171892426158));
#35603=CARTESIAN_POINT('Ctrl Pts',(16.1993487533989,0.355971101329402,3.48404157568705));
#35604=CARTESIAN_POINT('Ctrl Pts',(16.2152540320865,0.474747841293266,3.64120276856532));
#35605=CARTESIAN_POINT('Ctrl Pts',(16.2311593107741,0.593524581257127,3.79836396144359));
#35606=CARTESIAN_POINT('Ctrl Pts',(16.2470645894618,0.626509250127697,4.02036369577466));
#35607=CARTESIAN_POINT('Ctrl Pts',(16.2629698681494,0.558556683425868,4.20526908558792));
#35608=CARTESIAN_POINT('Ctrl Pts',(16.278875146837,0.490604116724039,4.39017447540119));
#35609=CARTESIAN_POINT('Ctrl Pts',(16.2947804255246,0.32171431444981,4.53798552069667));
#35610=CARTESIAN_POINT('Ctrl Pts',(16.3106857042122,0.129434328669215,4.58083364284428));
#35611=CARTESIAN_POINT('Ctrl Pts',(16.314175332389,0.0872479785030607,4.5902345478711));
#35612=CARTESIAN_POINT('Ctrl Pts',(16.3176649605657,0.0439357035691123,
4.5945828907904));
#35613=CARTESIAN_POINT('Ctrl Pts',(16.3211545887425,0.000543344619121817,
4.59417988242975));
#35614=CARTESIAN_POINT('Origin',(4.,0.,4.));
#35615=CARTESIAN_POINT('',(16.7288454112575,-0.000548108868865471,4.59408180714414));
#35616=CARTESIAN_POINT('',(16.6211545887425,-2.1752937549985E-5,4.5931168278739));
#35617=CARTESIAN_POINT('',(4.,-7.27562663373442E-17,4.5941));
#35618=CARTESIAN_POINT('Ctrl Pts',(16.7288454112575,-0.000548108868865471,
4.59408180714414));
#35619=CARTESIAN_POINT('Ctrl Pts',(16.7166879354906,0.15068989439403,4.59268722311157));
#35620=CARTESIAN_POINT('Ctrl Pts',(16.7045304597237,0.302891836883802,4.53390177381835));
#35621=CARTESIAN_POINT('Ctrl Pts',(16.6923729839567,0.411632901649024,4.42974331917764));
#35622=CARTESIAN_POINT('Ctrl Pts',(16.6764677052691,0.553895734249677,4.29347578465895));
#35623=CARTESIAN_POINT('Ctrl Pts',(16.6605624265815,0.621772048174623,4.07954898308531));
#35624=CARTESIAN_POINT('Ctrl Pts',(16.6446571478939,0.58409591167956,3.88618905124272));
#35625=CARTESIAN_POINT('Ctrl Pts',(16.6287518692063,0.546419775184499,3.69282911940014));
#35626=CARTESIAN_POINT('Ctrl Pts',(16.6128465905187,0.403191188269443,3.52003605728863));
#35627=CARTESIAN_POINT('Ctrl Pts',(16.596941311831,0.220174658543969,3.44714912875817));
#35628=CARTESIAN_POINT('Ctrl Pts',(16.5810360331434,0.0371581288184754,
3.37426220022769));
#35629=CARTESIAN_POINT('Ctrl Pts',(16.5651307544558,-0.185646343717467,
3.40128140527831));
#35630=CARTESIAN_POINT('Ctrl Pts',(16.5492254757682,-0.34593637135519,3.51580066803907));
#35631=CARTESIAN_POINT('Ctrl Pts',(16.5333201970806,-0.506226398992903,
3.63031993079982));
#35632=CARTESIAN_POINT('Ctrl Pts',(16.517414918393,-0.604001981732426,3.83233925127069));
#35633=CARTESIAN_POINT('Ctrl Pts',(16.5015096397054,-0.594368708523554,
4.02909990422408));
#35634=CARTESIAN_POINT('Ctrl Pts',(16.4856043610178,-0.584735435314682,
4.22586055717748));
#35635=CARTESIAN_POINT('Ctrl Pts',(16.4696990823301,-0.467693306157413,
4.4173625426134));
#35636=CARTESIAN_POINT('Ctrl Pts',(16.4537938036425,-0.296983115116624,
4.51567625060054));
#35637=CARTESIAN_POINT('Ctrl Pts',(16.4454776728475,-0.20772669247752,4.56707991793767));
#35638=CARTESIAN_POINT('Ctrl Pts',(16.4371615420525,-0.103798720846626,
4.59300816600183));
#35639=CARTESIAN_POINT('Ctrl Pts',(16.4288454112575,7.48704377684928E-5,
4.59312461313858));
#35640=CARTESIAN_POINT('Ctrl Pts',(16.3211545887425,0.000543344619121817,
4.59417988242975));
#35641=CARTESIAN_POINT('Ctrl Pts',(16.3335702392533,-0.153841115924154,
4.59274603025257));
#35642=CARTESIAN_POINT('Ctrl Pts',(16.3459858897642,-0.309239316255332,
4.53116741914846));
#35643=CARTESIAN_POINT('Ctrl Pts',(16.3584015402751,-0.418549561707542,
4.42300972860235));
#35644=CARTESIAN_POINT('Ctrl Pts',(16.3743068189627,-0.558583297016706,
4.28445249321304));
#35645=CARTESIAN_POINT('Ctrl Pts',(16.3902120976503,-0.622980598348072,
4.06945282343469));
#35646=CARTESIAN_POINT('Ctrl Pts',(16.4061173763379,-0.582172949355422,
3.87672947174358));
#35647=CARTESIAN_POINT('Ctrl Pts',(16.4220226550255,-0.541365300362771,
3.68400612005246));
#35648=CARTESIAN_POINT('Ctrl Pts',(16.4379279337131,-0.395352701046104,
3.5135590864486));
#35649=CARTESIAN_POINT('Ctrl Pts',(16.4538332124007,-0.211177959727979,
3.44365043774355));
#35650=CARTESIAN_POINT('Ctrl Pts',(16.4697384910883,-0.0270032184098532,
3.37374178903851));
#35651=CARTESIAN_POINT('Ctrl Pts',(16.485643769776,0.195333664909731,3.40437152523229));
#35652=CARTESIAN_POINT('Ctrl Pts',(16.5015490484636,0.353744999708243,3.52147576730199));
#35653=CARTESIAN_POINT('Ctrl Pts',(16.5174543271512,0.512156334506764,3.63858000937169));
#35654=CARTESIAN_POINT('Ctrl Pts',(16.5333596058388,0.606642120784206,3.84215875731731));
#35655=CARTESIAN_POINT('Ctrl Pts',(16.5492648845264,0.59381848284593,4.03873726278877));
#35656=CARTESIAN_POINT('Ctrl Pts',(16.565170163214,0.580994844907655,4.23531576826023));
#35657=CARTESIAN_POINT('Ctrl Pts',(16.5810754419016,0.460861782753675,4.42489403125753));
#35658=CARTESIAN_POINT('Ctrl Pts',(16.5969807205892,0.288579316114369,4.52042573380721));
#35659=CARTESIAN_POINT('Ctrl Pts',(16.6050386766403,0.201297315476928,4.56882414767653));
#35660=CARTESIAN_POINT('Ctrl Pts',(16.6130966326914,0.100630370301649,4.59308406930439));
#35661=CARTESIAN_POINT('Ctrl Pts',(16.6211545887425,-2.1752937549985E-5,
4.5931168278739));
#35662=CARTESIAN_POINT('Origin',(4.,0.,4.));
#35663=CARTESIAN_POINT('',(17.0288454112575,0.000186802344652959,4.59500977980842));
#35664=CARTESIAN_POINT('',(16.9211545887425,-0.000535257393875686,4.59425998651214));
#35665=CARTESIAN_POINT('',(4.,-7.27562663373442E-17,4.5941));
#35666=CARTESIAN_POINT('Ctrl Pts',(17.0288454112575,0.000186802344652959,
4.59500977980842));
#35667=CARTESIAN_POINT('Ctrl Pts',(17.0280248863039,0.0103527338555297,
4.59505157132578));
#35668=CARTESIAN_POINT('Ctrl Pts',(17.0272043613502,0.0205166685362397,
4.5948136789481));
#35669=CARTESIAN_POINT('Ctrl Pts',(17.0263838363966,0.0306658549750798,
4.59428997251885));
#35670=CARTESIAN_POINT('Ctrl Pts',(17.010478557709,0.227400443050786,4.58413830477164));
#35671=CARTESIAN_POINT('Ctrl Pts',(16.9945732790214,0.418593379366704,4.46659200952389));
#35672=CARTESIAN_POINT('Ctrl Pts',(16.9786680003338,0.516456956272638,4.29562337257973));
#35673=CARTESIAN_POINT('Ctrl Pts',(16.9627627216462,0.614320533178566,4.12465473563558));
#35674=CARTESIAN_POINT('Ctrl Pts',(16.9468574429585,0.618854750674521,3.90026375699502));
#35675=CARTESIAN_POINT('Ctrl Pts',(16.9309521642709,0.527977687913284,3.72548128085037));
#35676=CARTESIAN_POINT('Ctrl Pts',(16.9150468855833,0.437100625152047,3.55069880470573));
#35677=CARTESIAN_POINT('Ctrl Pts',(16.8991416068957,0.25081228213362,3.42552483105699));
#35678=CARTESIAN_POINT('Ctrl Pts',(16.8832363282081,0.054648384762208,3.40743395292956));
#35679=CARTESIAN_POINT('Ctrl Pts',(16.8673310495205,-0.141515512609204,
3.38934307480212));
#35680=CARTESIAN_POINT('Ctrl Pts',(16.8514257708328,-0.347554964333599,
3.47833529219599));
#35681=CARTESIAN_POINT('Ctrl Pts',(16.8355204921452,-0.468865370989487,
3.63354914383413));
#35682=CARTESIAN_POINT('Ctrl Pts',(16.8196152134576,-0.590175777645383,
3.78876299547228));
#35683=CARTESIAN_POINT('Ctrl Pts',(16.80370993477,-0.62675713923276,4.01019848135471));
#35684=CARTESIAN_POINT('Ctrl Pts',(16.7878046560824,-0.561812842140477,
4.19618179452704));
#35685=CARTESIAN_POINT('Ctrl Pts',(16.7718993773948,-0.496868545048197,
4.38216510769936));
#35686=CARTESIAN_POINT('Ctrl Pts',(16.7559940987072,-0.330398589276266,
4.53269624816158));
#35687=CARTESIAN_POINT('Ctrl Pts',(16.7400888200196,-0.138838935752124,
4.57865768466082));
#35688=CARTESIAN_POINT('Ctrl Pts',(16.7363410170989,-0.0937012275068688,
4.58948769960953));
#35689=CARTESIAN_POINT('Ctrl Pts',(16.7325932141782,-0.0471704703862807,
4.59451171761327));
#35690=CARTESIAN_POINT('Ctrl Pts',(16.7288454112575,-0.000548108868865471,
4.59408180714414));
#35691=CARTESIAN_POINT('Ctrl Pts',(16.6211545887425,-2.1752937549985E-5,
4.5931168278739));
#35692=CARTESIAN_POINT('Ctrl Pts',(16.629001911379,-0.0980428491191961,
4.59314873014073));
#35693=CARTESIAN_POINT('Ctrl Pts',(16.6368492340155,-0.196049888122182,
4.57020350190738));
#35694=CARTESIAN_POINT('Ctrl Pts',(16.6446965566521,-0.281666676968544,
4.52419924569128));
#35695=CARTESIAN_POINT('Ctrl Pts',(16.6606018353397,-0.455198332287519,
4.43095591292362));
#35696=CARTESIAN_POINT('Ctrl Pts',(16.6765071140273,-0.577829771800838,
4.24298410528626));
#35697=CARTESIAN_POINT('Ctrl Pts',(16.6924123927149,-0.593253826592341,
4.0465925244149));
#35698=CARTESIAN_POINT('Ctrl Pts',(16.7083176714025,-0.608677881383846,
3.85020094354353));
#35699=CARTESIAN_POINT('Ctrl Pts',(16.7242229500901,-0.516894551453523,
3.64538958943816));
#35700=CARTESIAN_POINT('Ctrl Pts',(16.7401282287778,-0.360046858872914,
3.52619917105016));
#35701=CARTESIAN_POINT('Ctrl Pts',(16.7560335074654,-0.203199166292313,
3.40700875266216));
#35702=CARTESIAN_POINT('Ctrl Pts',(16.771938786153,0.0187128889385656,3.37343926999153));
#35703=CARTESIAN_POINT('Ctrl Pts',(16.7878440648406,0.203796679382533,3.44090440927292));
#35704=CARTESIAN_POINT('Ctrl Pts',(16.8037493435282,0.388880469826499,3.50836954855431));
#35705=CARTESIAN_POINT('Ctrl Pts',(16.8196546222158,0.537135995483554,3.67686930978772));
#35706=CARTESIAN_POINT('Ctrl Pts',(16.8355599009034,0.58049059114602,3.86903573125179));
#35707=CARTESIAN_POINT('Ctrl Pts',(16.851465179591,0.623845186808487,4.06120215271587));
#35708=CARTESIAN_POINT('Ctrl Pts',(16.8673704582787,0.562298852476364,4.2770352344106));
#35709=CARTESIAN_POINT('Ctrl Pts',(16.8832757369663,0.424111061064287,4.41743355636644));
#35710=CARTESIAN_POINT('Ctrl Pts',(16.8959020208917,0.314411738992559,4.5288876912157));
#35711=CARTESIAN_POINT('Ctrl Pts',(16.9085283048171,0.156414067554279,4.59280392009262));
#35712=CARTESIAN_POINT('Ctrl Pts',(16.9211545887425,-0.000535257393875686,
4.59425998651214));
#35713=CARTESIAN_POINT('Origin',(4.,0.,4.));
#35714=CARTESIAN_POINT('',(17.3288454112575,0.000452601584348983,4.59351524744837));
#35715=CARTESIAN_POINT('',(17.2211545887425,0.000283723793354941,4.5949151055343));
#35716=CARTESIAN_POINT('',(4.,-7.27562663373442E-17,4.5941));
#35717=CARTESIAN_POINT('Ctrl Pts',(17.3288454112575,0.000452601584348983,
4.59351524744837));
#35718=CARTESIAN_POINT('Ctrl Pts',(17.3234565584296,0.0676518012035294,
4.59398979695312));
#35719=CARTESIAN_POINT('Ctrl Pts',(17.3180677056016,0.134706745978521,4.58346365752876));
#35720=CARTESIAN_POINT('Ctrl Pts',(17.3126788527736,0.197661386620268,4.56129398922237));
#35721=CARTESIAN_POINT('Ctrl Pts',(17.296773574086,0.383472937993069,4.49585988588324));
#35722=CARTESIAN_POINT('Ctrl Pts',(17.2808682953984,0.533564938357213,4.32899388620009));
#35723=CARTESIAN_POINT('Ctrl Pts',(17.2649630167108,0.579021491014364,4.13731379770915));
#35724=CARTESIAN_POINT('Ctrl Pts',(17.2490577380232,0.624478043671518,3.94563370921821));
#35725=CARTESIAN_POINT('Ctrl Pts',(17.2331524593355,0.565299148621668,3.72913953191949));
#35726=CARTESIAN_POINT('Ctrl Pts',(17.2172471806479,0.428657250819126,3.58723623291525));
#35727=CARTESIAN_POINT('Ctrl Pts',(17.2013419019603,0.292015353016592,3.44533293391101));
#35728=CARTESIAN_POINT('Ctrl Pts',(17.1854366232727,0.0779104524613767,
3.37802051320125));
#35729=CARTESIAN_POINT('Ctrl Pts',(17.1695313445851,-0.115349538542919,
3.41620598662221));
#35730=CARTESIAN_POINT('Ctrl Pts',(17.1536260658975,-0.308609529547215,
3.45439146004317));
#35731=CARTESIAN_POINT('Ctrl Pts',(17.1377207872099,-0.48102461100059,3.59807482759486));
#35732=CARTESIAN_POINT('Ctrl Pts',(17.1218155085223,-0.553429071780215,
3.78128276563952));
#35733=CARTESIAN_POINT('Ctrl Pts',(17.1059102298347,-0.625833532559839,
3.96449070368418));
#35734=CARTESIAN_POINT('Ctrl Pts',(17.090004951147,-0.598227372665711,4.18722321222181));
#35735=CARTESIAN_POINT('Ctrl Pts',(17.0740996724594,-0.483286172800906,
4.34721094636728));
#35736=CARTESIAN_POINT('Ctrl Pts',(17.0590149187255,-0.374274584390508,
4.4989451987145));
#35737=CARTESIAN_POINT('Ctrl Pts',(17.0439301649915,-0.186706445247169,
4.59424147319602));
#35738=CARTESIAN_POINT('Ctrl Pts',(17.0288454112575,0.000186802344652959,
4.59500977980842));
#35739=CARTESIAN_POINT('Ctrl Pts',(16.9211545887425,-0.000535257393875686,
4.59425998651214));
#35740=CARTESIAN_POINT('Ctrl Pts',(16.9244335835047,-0.0412943609811605,
4.59463812105998));
#35741=CARTESIAN_POINT('Ctrl Pts',(16.9277125782669,-0.0819827620002526,
4.59080381827239));
#35742=CARTESIAN_POINT('Ctrl Pts',(16.9309915730291,-0.121736182180322,
4.58249572362891));
#35743=CARTESIAN_POINT('Ctrl Pts',(16.9468968517167,-0.31456638552074,4.54219600671859));
#35744=CARTESIAN_POINT('Ctrl Pts',(16.9628021304043,-0.485397543709551,
4.39663301068103));
#35745=CARTESIAN_POINT('Ctrl Pts',(16.978707409092,-0.555791216176751,4.21264310503418));
#35746=CARTESIAN_POINT('Ctrl Pts',(16.9946126877796,-0.626184888643955,
4.02865319938731));
#35747=CARTESIAN_POINT('Ctrl Pts',(17.0105179664672,-0.596141075389537,
3.80623638413113));
#35748=CARTESIAN_POINT('Ctrl Pts',(17.0264232451548,-0.479454624411006,
3.64751705115182));
#35749=CARTESIAN_POINT('Ctrl Pts',(17.0423285238424,-0.362768173432475,
3.48879771817251));
#35750=CARTESIAN_POINT('Ctrl Pts',(17.05823380253,-0.159439084729831,3.39377586747005));
#35751=CARTESIAN_POINT('Ctrl Pts',(17.0741390812176,0.0371725263090214,
3.40608151284405));
#35752=CARTESIAN_POINT('Ctrl Pts',(17.0900443599052,0.233784137347885,3.41838715821804));
#35753=CARTESIAN_POINT('Ctrl Pts',(17.1059496385929,0.423678270722955,3.5380202996685));
#35754=CARTESIAN_POINT('Ctrl Pts',(17.1218549172805,0.519663574146654,3.71005045990219));
#35755=CARTESIAN_POINT('Ctrl Pts',(17.1377601959681,0.615648877570348,3.88208062013586));
#35756=CARTESIAN_POINT('Ctrl Pts',(17.1536654746557,0.617725351042682,4.10650779915277));
#35757=CARTESIAN_POINT('Ctrl Pts',(17.1695707533433,0.524939565793509,4.28028453107927));
#35758=CARTESIAN_POINT('Ctrl Pts',(17.1854760320309,0.432153780544336,4.45406126300578));
#35759=CARTESIAN_POINT('Ctrl Pts',(17.2013813107185,0.244505736573655,4.5771875478419));
#35760=CARTESIAN_POINT('Ctrl Pts',(17.2172865894061,0.0481554769387473,
4.59312900463441));
#35761=CARTESIAN_POINT('Ctrl Pts',(17.2185759225182,0.0322386925622284,
4.59442127046022));
#35762=CARTESIAN_POINT('Ctrl Pts',(17.2198652556304,0.0162647237884017,
4.5950091984451));
#35763=CARTESIAN_POINT('Ctrl Pts',(17.2211545887425,0.000283723793354941,
4.5949151055343));
#35764=CARTESIAN_POINT('Origin',(4.,0.,4.));
#35765=CARTESIAN_POINT('',(17.6288454112575,-0.000376811216598938,4.5933658344624));
#35766=CARTESIAN_POINT('',(17.5211545887425,0.000390292690419375,4.59338796628294));
#35767=CARTESIAN_POINT('',(4.,-7.27562663373442E-17,4.5941));
#35768=CARTESIAN_POINT('Ctrl Pts',(17.6288454112575,-0.000376811216598938,
4.5933658344624));
#35769=CARTESIAN_POINT('Ctrl Pts',(17.6188882305552,0.123868145157646,4.5926473455414));
#35770=CARTESIAN_POINT('Ctrl Pts',(17.608931049853,0.248515939035854,4.55458993700248));
#35771=CARTESIAN_POINT('Ctrl Pts',(17.5989738691507,0.348483110949462,4.48236965854082));
#35772=CARTESIAN_POINT('Ctrl Pts',(17.5830685904631,0.508167440925656,4.36700731952407));
#35773=CARTESIAN_POINT('Ctrl Pts',(17.5671633117754,0.604877102606476,4.16447556457896));
#35774=CARTESIAN_POINT('Ctrl Pts',(17.5512580330878,0.594207110796467,3.96776840716434));
#35775=CARTESIAN_POINT('Ctrl Pts',(17.5353527544002,0.583537118986457,3.77106124974973));
#35776=CARTESIAN_POINT('Ctrl Pts',(17.5194474757126,0.465487473685617,3.58017868986561));
#35777=CARTESIAN_POINT('Ctrl Pts',(17.503542197025,0.294261577747463,3.48276592343564));
#35778=CARTESIAN_POINT('Ctrl Pts',(17.4876369183374,0.123035681809298,3.38535315700567));
#35779=CARTESIAN_POINT('Ctrl Pts',(17.4717316396498,-0.101366464766187,
3.38141018402985));
#35780=CARTESIAN_POINT('Ctrl Pts',(17.4558263609621,-0.275908889943427,
3.47274745088526));
#35781=CARTESIAN_POINT('Ctrl Pts',(17.4399210822745,-0.450451315120656,
3.56408471774066));
#35782=CARTESIAN_POINT('Ctrl Pts',(17.4240158035869,-0.575134018899647,
3.75070222442727));
#35783=CARTESIAN_POINT('Ctrl Pts',(17.4081105248993,-0.592707978595278,
3.94691310701022));
#35784=CARTESIAN_POINT('Ctrl Pts',(17.3922052462117,-0.610281938290908,
4.14312398959316));
#35785=CARTESIAN_POINT('Ctrl Pts',(17.3762999675241,-0.520747153903178,
4.34892824807245));
#35786=CARTESIAN_POINT('Ctrl Pts',(17.3603946888365,-0.365214210518585,
4.46982927381454));
#35787=CARTESIAN_POINT('Ctrl Pts',(17.3498782629768,-0.262377240481122,
4.54976793433994));
#35788=CARTESIAN_POINT('Ctrl Pts',(17.3393618371172,-0.130687628661636,
4.59258915708319));
#35789=CARTESIAN_POINT('Ctrl Pts',(17.3288454112575,0.000452601584348983,
4.59351524744837));
#35790=CARTESIAN_POINT('Ctrl Pts',(17.2211545887425,0.000283723793354941,
4.5949151055343));
#35791=CARTESIAN_POINT('Ctrl Pts',(17.235770534318,-0.18087770297476,4.59384846352355));
#35792=CARTESIAN_POINT('Ctrl Pts',(17.2503864798935,-0.362942684182573,
4.50513801271133));
#35793=CARTESIAN_POINT('Ctrl Pts',(17.265002425469,-0.47285052735612,4.36129398677095));
#35794=CARTESIAN_POINT('Ctrl Pts',(17.2809077041566,-0.592453796716944,
4.20476088336606));
#35795=CARTESIAN_POINT('Ctrl Pts',(17.2968129828442,-0.626607860139456,
3.98293804780737));
#35796=CARTESIAN_POINT('Ctrl Pts',(17.3127182615318,-0.559630616639302,
3.79767714163318));
#35797=CARTESIAN_POINT('Ctrl Pts',(17.3286235402194,-0.492653373139145,
3.61241623545897));
#35798=CARTESIAN_POINT('Ctrl Pts',(17.3445288189071,-0.324544822716309,
3.46371725866926));
#35799=CARTESIAN_POINT('Ctrl Pts',(17.3604340975947,-0.132493299638714,
3.41985649047097));
#35800=CARTESIAN_POINT('Ctrl Pts',(17.3763393762823,0.0595582234388708,
3.37599572227269));
#35801=CARTESIAN_POINT('Ctrl Pts',(17.3922446549699,0.275552719171213,3.43697316266583));
#35802=CARTESIAN_POINT('Ctrl Pts',(17.4081499336575,0.416314653091553,3.5747905507646));
#35803=CARTESIAN_POINT('Ctrl Pts',(17.4240552123451,0.557076587011893,3.71260793886338));
#35804=CARTESIAN_POINT('Ctrl Pts',(17.4399604910327,0.622605959120231,3.92726527466781));
#35805=CARTESIAN_POINT('Ctrl Pts',(17.4558657697203,0.582814454063527,4.12020099097945));
#35806=CARTESIAN_POINT('Ctrl Pts',(17.4717710484079,0.543022949006823,4.31313670729109));
#35807=CARTESIAN_POINT('Ctrl Pts',(17.4876763270955,0.397910566785078,4.48435080410994));
#35808=CARTESIAN_POINT('Ctrl Pts',(17.5035816057832,0.214106774115907,4.55522901164789));
#35809=CARTESIAN_POINT('Ctrl Pts',(17.5094392667696,0.146414762764002,4.58133232736073));
#35810=CARTESIAN_POINT('Ctrl Pts',(17.515296927756,0.073474912906076,4.59382676872096));
#35811=CARTESIAN_POINT('Ctrl Pts',(17.5211545887425,0.000390292690419375,
4.59338796628294));
#35812=CARTESIAN_POINT('Origin',(4.,0.,4.));
#35813=CARTESIAN_POINT('',(17.9288454112575,-0.000301159635511528,4.59489313984584));
#35814=CARTESIAN_POINT('',(17.8211545887425,-0.000441626631060947,4.59348913571676));
#35815=CARTESIAN_POINT('',(4.,-7.27562663373442E-17,4.5941));
#35816=CARTESIAN_POINT('Ctrl Pts',(17.9288454112575,-0.000301159635511528,
4.59489313984584));
#35817=CARTESIAN_POINT('Ctrl Pts',(17.9143199026809,0.179756887528332,4.59377956832623));
#35818=CARTESIAN_POINT('Ctrl Pts',(17.8997943941043,0.360751589755073,4.50630604003092));
#35819=CARTESIAN_POINT('Ctrl Pts',(17.8852688855277,0.470789914960854,4.36397502945801));
#35820=CARTESIAN_POINT('Ctrl Pts',(17.8693636068401,0.591280720462369,4.20812407407766));
#35821=CARTESIAN_POINT('Ctrl Pts',(17.8534583281524,0.626694694978596,3.98649889312445));
#35822=CARTESIAN_POINT('Ctrl Pts',(17.8375530494648,0.560771239653389,3.80086039350393));
#35823=CARTESIAN_POINT('Ctrl Pts',(17.8216477707772,0.494847784328189,3.61522189388343));
#35824=CARTESIAN_POINT('Ctrl Pts',(17.8057424920896,0.327586899161578,3.46557007559562));
#35825=CARTESIAN_POINT('Ctrl Pts',(17.789837213402,0.135787706397568,3.42061872235194));
#35826=CARTESIAN_POINT('Ctrl Pts',(17.7739319347144,-0.0560114863664412,
3.37566736910827));
#35827=CARTESIAN_POINT('Ctrl Pts',(17.7580266560268,-0.272348986727849,
3.43541648090873));
#35828=CARTESIAN_POINT('Ctrl Pts',(17.7421213773392,-0.41389176700556,3.57243179339102));
#35829=CARTESIAN_POINT('Ctrl Pts',(17.7262160986515,-0.555434547283271,
3.7094471058733));
#35830=CARTESIAN_POINT('Ctrl Pts',(17.710310819964,-0.622182607477285,3.92372861903742));
#35831=CARTESIAN_POINT('Ctrl Pts',(17.6944055412763,-0.583488062224059,
4.11688732754162));
#35832=CARTESIAN_POINT('Ctrl Pts',(17.6785002625887,-0.544793516970831,
4.31004603604583));
#35833=CARTESIAN_POINT('Ctrl Pts',(17.6625949839011,-0.400656366270352,
4.48208193989012));
#35834=CARTESIAN_POINT('Ctrl Pts',(17.6466897052135,-0.217258291784321,
4.55400343026805));
#35835=CARTESIAN_POINT('Ctrl Pts',(17.6407416072282,-0.148672903323923,
4.58089991415997));
#35836=CARTESIAN_POINT('Ctrl Pts',(17.6347935092429,-0.0745967331795002,
4.59379503652584));
#35837=CARTESIAN_POINT('Ctrl Pts',(17.6288454112575,-0.000376811216598938,
4.5933658344624));
#35838=CARTESIAN_POINT('Ctrl Pts',(17.5211545887425,0.000390292690419375,
4.59338796628294));
#35839=CARTESIAN_POINT('Ctrl Pts',(17.5312022064437,-0.12497140465997,4.59263529057266));
#35840=CARTESIAN_POINT('Ctrl Pts',(17.5412498241448,-0.250759050797478,
4.55382993891589));
#35841=CARTESIAN_POINT('Ctrl Pts',(17.551297441846,-0.351218450958555,4.48038168762358));
#35842=CARTESIAN_POINT('Ctrl Pts',(17.5672027205336,-0.510244680247213,
4.36411383780432));
#35843=CARTESIAN_POINT('Ctrl Pts',(17.5831079992212,-0.605801935707933,
4.16103581990878));
#35844=CARTESIAN_POINT('Ctrl Pts',(17.5990132779088,-0.594014368327242,
3.96439246823218));
#35845=CARTESIAN_POINT('Ctrl Pts',(17.6149185565964,-0.58222680094655,3.76774911655557));
#35846=CARTESIAN_POINT('Ctrl Pts',(17.6308238352841,-0.463094410724447,
3.5775404310979));
#35847=CARTESIAN_POINT('Ctrl Pts',(17.6467291139717,-0.291317751175132,
3.48110219315546));
#35848=CARTESIAN_POINT('Ctrl Pts',(17.6626343926593,-0.119541091625818,
3.38466395521302));
#35849=CARTESIAN_POINT('Ctrl Pts',(17.6785396713469,0.104879837250709,3.38199616478582));
#35850=CARTESIAN_POINT('Ctrl Pts',(17.6944449500345,0.278900439380867,3.47432375837312));
#35851=CARTESIAN_POINT('Ctrl Pts',(17.7103502287221,0.452921041511034,3.56665135196042));
#35852=CARTESIAN_POINT('Ctrl Pts',(17.7262555074097,0.576541316894826,3.75397432956222));
#35853=CARTESIAN_POINT('Ctrl Pts',(17.7421607860974,0.593000065018554,3.95028190484542));
#35854=CARTESIAN_POINT('Ctrl Pts',(17.758066064785,0.60945881314228,4.1465894801286));
#35855=CARTESIAN_POINT('Ctrl Pts',(17.7739713434726,0.518756034005955,4.35188165309317));
#35856=CARTESIAN_POINT('Ctrl Pts',(17.7898766221602,0.362538606470845,4.47189694310939));
#35857=CARTESIAN_POINT('Ctrl Pts',(17.8003026110209,0.260137309937395,4.55056755941266));
#35858=CARTESIAN_POINT('Ctrl Pts',(17.8107285998817,0.129585238016204,4.59259583028147));
#35859=CARTESIAN_POINT('Ctrl Pts',(17.8211545887425,-0.000441626631060947,
4.59348913571676));
#35860=CARTESIAN_POINT('Origin',(4.,0.,4.));
#35861=CARTESIAN_POINT('',(18.2288454112575,0.000530626821107938,4.59429426521737));
#35862=CARTESIAN_POINT('',(18.1211545887425,-0.000206261771334874,4.59499421029555));
#35863=CARTESIAN_POINT('',(4.,-7.27562663373442E-17,4.5941));
#35864=CARTESIAN_POINT('Ctrl Pts',(18.2288454112575,0.000530626821107938,
4.59429426521737));
#35865=CARTESIAN_POINT('Ctrl Pts',(18.2256568534942,0.0401596894680921,
4.59466101186164));
#35866=CARTESIAN_POINT('Ctrl Pts',(18.2224682957309,0.0797220295111884,
4.5910372210354));
#35867=CARTESIAN_POINT('Ctrl Pts',(18.2192797379675,0.118424305077702,4.58317806034235));
#35868=CARTESIAN_POINT('Ctrl Pts',(18.2033744592799,0.311480390123117,4.54397471188459));
#35869=CARTESIAN_POINT('Ctrl Pts',(18.1874691805923,0.483135922039688,4.39938477867344));
#35870=CARTESIAN_POINT('Ctrl Pts',(18.1715639019047,0.554573942717995,4.21579784094385));
#35871=CARTESIAN_POINT('Ctrl Pts',(18.1556586232171,0.626011963396302,4.03221090321426));
#35872=CARTESIAN_POINT('Ctrl Pts',(18.1397533445295,0.597232472836345,3.80962696096622));
#35873=CARTESIAN_POINT('Ctrl Pts',(18.1238480658419,0.481449795543417,3.65024714373002));
#35874=CARTESIAN_POINT('Ctrl Pts',(18.1079427871543,0.365667118250483,3.49086732649381));
#35875=CARTESIAN_POINT('Ctrl Pts',(18.0920375084667,0.16288125422457,3.39469163426944));
#35876=CARTESIAN_POINT('Ctrl Pts',(18.076132229779,-0.0337971069360236,
3.40587987606835));
#35877=CARTESIAN_POINT('Ctrl Pts',(18.0602269510914,-0.230475468096606,
3.41706811786726));
#35878=CARTESIAN_POINT('Ctrl Pts',(18.0443216724038,-0.421046326391869,
3.53562029368944));
#35879=CARTESIAN_POINT('Ctrl Pts',(18.0284163937162,-0.518007606080761,
3.70710225992629));
#35880=CARTESIAN_POINT('Ctrl Pts',(18.0125111150286,-0.614968885769652,
3.87858422616314));
#35881=CARTESIAN_POINT('Ctrl Pts',(17.996605836341,-0.618320586852172,4.10299598281466));
#35882=CARTESIAN_POINT('Ctrl Pts',(17.9807005576534,-0.526523749990007,
4.27729714530494));
#35883=CARTESIAN_POINT('Ctrl Pts',(17.9647952789658,-0.434726913127837,
4.45159830779523));
#35884=CARTESIAN_POINT('Ctrl Pts',(17.9488900002781,-0.247781538320971,
4.57578887612429));
#35885=CARTESIAN_POINT('Ctrl Pts',(17.9329847215905,-0.0515250326741526,
4.59284579538505));
#35886=CARTESIAN_POINT('Ctrl Pts',(17.9316049514795,-0.0344999389365885,
4.59432546938787));
#35887=CARTESIAN_POINT('Ctrl Pts',(17.9302251813685,-0.0174047750035579,
4.59499891739512));
#35888=CARTESIAN_POINT('Ctrl Pts',(17.9288454112575,-0.000301159635511528,
4.59489313984584));
#35889=CARTESIAN_POINT('Ctrl Pts',(17.8211545887425,-0.000441626631060947,
4.59348913571676));
#35890=CARTESIAN_POINT('Ctrl Pts',(17.8266338785693,-0.0687761401428734,
4.59395860479535));
#35891=CARTESIAN_POINT('Ctrl Pts',(17.8321131683962,-0.136965594625977,
4.58306684864343));
#35892=CARTESIAN_POINT('Ctrl Pts',(17.837592458223,-0.200847632772524,4.56016175744822));
#35893=CARTESIAN_POINT('Ctrl Pts',(17.8534977369106,-0.386284368546891,
4.49367287470298));
#35894=CARTESIAN_POINT('Ctrl Pts',(17.8694030155983,-0.535425764161732,
4.32595670214462));
#35895=CARTESIAN_POINT('Ctrl Pts',(17.8853082942859,-0.579792400402821,
4.13402141072584));
#35896=CARTESIAN_POINT('Ctrl Pts',(17.9012135729735,-0.624159036643913,
3.94208611930704));
#35897=CARTESIAN_POINT('Ctrl Pts',(17.9171188516611,-0.563750913511241,
3.72593170902781));
#35898=CARTESIAN_POINT('Ctrl Pts',(17.9330241303487,-0.426304885490399,
3.58480714034942));
#35899=CARTESIAN_POINT('Ctrl Pts',(17.9489294090363,-0.288858857469565,
3.44368257167104));
#35900=CARTESIAN_POINT('Ctrl Pts',(17.9648346877239,-0.0743749245605683,
3.37758784459349));
#35901=CARTESIAN_POINT('Ctrl Pts',(17.9807399664116,0.118664965311668,3.41687086155347));
#35902=CARTESIAN_POINT('Ctrl Pts',(17.9966452450992,0.311704855183904,3.45615387851346));
#35903=CARTESIAN_POINT('Ctrl Pts',(18.0125505237868,0.483300702019379,3.60081463951098));
#35904=CARTESIAN_POINT('Ctrl Pts',(18.0284558024744,0.554662952572844,3.78443104318807));
#35905=CARTESIAN_POINT('Ctrl Pts',(18.044361081162,0.62602520312631,3.96804744686516));
#35906=CARTESIAN_POINT('Ctrl Pts',(18.0602663598496,0.597153857397765,4.19061949322182));
#35907=CARTESIAN_POINT('Ctrl Pts',(18.0761716385372,0.481305415899848,4.34995151481781));
#35908=CARTESIAN_POINT('Ctrl Pts',(18.0911659552723,0.372092100044007,4.50015792394613));
#35909=CARTESIAN_POINT('Ctrl Pts',(18.1061602720074,0.185579460002099,4.59416090236354));
#35910=CARTESIAN_POINT('Ctrl Pts',(18.1211545887425,-0.000206261771334874,
4.59499421029555));
#35911=CARTESIAN_POINT('Origin',(4.,0.,4.));
#35912=CARTESIAN_POINT('',(18.5288454112575,4.04073003155148E-5,4.59311858068669));
#35913=CARTESIAN_POINT('',(18.4211545887425,0.000547083855738422,4.59411609730493));
#35914=CARTESIAN_POINT('',(4.,-7.27562663373442E-17,4.5941));
#35915=CARTESIAN_POINT('Ctrl Pts',(18.5288454112575,4.04073003155148E-5,
4.59311858068669));
#35916=CARTESIAN_POINT('Ctrl Pts',(18.5210885256199,0.0969311390001333,
4.59317716754242));
#35917=CARTESIAN_POINT('Ctrl Pts',(18.5133316399822,0.193796352446061,4.57078374547556));
#35918=CARTESIAN_POINT('Ctrl Pts',(18.5055747543446,0.27868347559656,4.52579129559858));
#35919=CARTESIAN_POINT('Ctrl Pts',(18.489669475657,0.452742165355285,4.43353552600749));
#35920=CARTESIAN_POINT('Ctrl Pts',(18.4737641969693,0.576439736070726,4.24626358090446));
#35921=CARTESIAN_POINT('Ctrl Pts',(18.4578589182817,0.592979496483005,4.04996281465819));
#35922=CARTESIAN_POINT('Ctrl Pts',(18.4419536395941,0.609519256895283,3.85366204841193));
#35923=CARTESIAN_POINT('Ctrl Pts',(18.4260483609065,0.518901207004412,3.64833246102244));
#35924=CARTESIAN_POINT('Ctrl Pts',(18.4101430822189,0.362733321586741,3.52825271224048));
#35925=CARTESIAN_POINT('Ctrl Pts',(18.3942378035313,0.206565436169079,3.40817296345854));
#35926=CARTESIAN_POINT('Ctrl Pts',(18.3783325248437,-0.015152284775374,
3.37334305328413));
#35927=CARTESIAN_POINT('Ctrl Pts',(18.3624272461561,-0.200616443892158,
3.43975540293737));
#35928=CARTESIAN_POINT('Ctrl Pts',(18.3465219674685,-0.386080603008964,
3.50616775259061));
#35929=CARTESIAN_POINT('Ctrl Pts',(18.3306166887808,-0.535291200298091,
3.67382236207151));
#35930=CARTESIAN_POINT('Ctrl Pts',(18.3147114100932,-0.579737042064157,
3.86573932758804));
#35931=CARTESIAN_POINT('Ctrl Pts',(18.2988061314056,-0.624182883830224,
4.05765629310458));
#35932=CARTESIAN_POINT('Ctrl Pts',(18.282900852718,-0.563863970073232,4.27383561465674));
#35933=CARTESIAN_POINT('Ctrl Pts',(18.2669955740304,-0.426476194107598,
4.41501689358062));
#35934=CARTESIAN_POINT('Ctrl Pts',(18.2542788531061,-0.316630774880643,
4.52789532589669));
#35935=CARTESIAN_POINT('Ctrl Pts',(18.2415621321818,-0.157519428275204,
4.5928315930404));
#35936=CARTESIAN_POINT('Ctrl Pts',(18.2288454112575,0.000530626821107938,
4.59429426521737));
#35937=CARTESIAN_POINT('Ctrl Pts',(18.1211545887425,-0.000206261771334874,
4.59499421029555));
#35938=CARTESIAN_POINT('Ctrl Pts',(18.122065550695,-0.0114934532352288,
4.59504483693191));
#35939=CARTESIAN_POINT('Ctrl Pts',(18.1229765126475,-0.0227779616248223,
4.59475157188293));
#35940=CARTESIAN_POINT('Ctrl Pts',(18.1238874746001,-0.0340422900297544,
4.59410612569417));
#35941=CARTESIAN_POINT('Ctrl Pts',(18.1397927532877,-0.230716017194119,
4.58283671813918));
#35942=CARTESIAN_POINT('Ctrl Pts',(18.1556980319753,-0.421237934255556,
4.46420590619388));
#35943=CARTESIAN_POINT('Ctrl Pts',(18.1716033106629,-0.518128437217054,
4.29268393984778));
#35944=CARTESIAN_POINT('Ctrl Pts',(18.1875085893505,-0.615018940178556,
4.12116197350168));
#35945=CARTESIAN_POINT('Ctrl Pts',(18.2034138680381,-0.618278029040109,
3.89674885275477));
#35946=CARTESIAN_POINT('Ctrl Pts',(18.2193191467258,-0.526409268077163,
3.72248558851787));
#35947=CARTESIAN_POINT('Ctrl Pts',(18.2352244254134,-0.434540507114227,
3.54822232428098));
#35948=CARTESIAN_POINT('Ctrl Pts',(18.251129704101,-0.24754389632682,3.42410891655409));
#35949=CARTESIAN_POINT('Ctrl Pts',(18.2670349827886,-0.0512803682143169,
3.40713299136011));
#35950=CARTESIAN_POINT('Ctrl Pts',(18.2829402614762,0.144983159898198,3.39015706616613));
#35951=CARTESIAN_POINT('Ctrl Pts',(18.2988455401638,0.35051360533581,3.48031862350507));
#35952=CARTESIAN_POINT('Ctrl Pts',(18.3147508188514,0.470940082829639,3.63621929066782));
#35953=CARTESIAN_POINT('Ctrl Pts',(18.330656097539,0.591366560323475,3.79211995783059));
#35954=CARTESIAN_POINT('Ctrl Pts',(18.3465613762266,0.62668906987352,4.01375973481717));
#35955=CARTESIAN_POINT('Ctrl Pts',(18.3624666549143,0.560689009466533,4.199371012841));
#35956=CARTESIAN_POINT('Ctrl Pts',(18.3783719336019,0.49468894905955,4.38498229086483));
#35957=CARTESIAN_POINT('Ctrl Pts',(18.3942772122895,0.327366318695548,4.53456506992591));
#35958=CARTESIAN_POINT('Ctrl Pts',(18.4101824909771,0.135548591400956,4.57943726620491));
#35959=CARTESIAN_POINT('Ctrl Pts',(18.4138398568989,0.0914407431336166,
4.58975547846199));
#35960=CARTESIAN_POINT('Ctrl Pts',(18.4174972228207,0.0460377050408626,
4.59453706917327));
#35961=CARTESIAN_POINT('Ctrl Pts',(18.4211545887425,0.000547083855738422,
4.59411609730493));
#35962=CARTESIAN_POINT('Origin',(4.,0.,4.));
#35963=CARTESIAN_POINT('',(18.8288454112575,-0.000545657836941327,4.59414547262434));
#35964=CARTESIAN_POINT('',(18.7211545887425,-5.63168744233308E-5,4.59312091231189));
#35965=CARTESIAN_POINT('',(4.,-7.27562663373442E-17,4.5941));
#35966=CARTESIAN_POINT('Ctrl Pts',(18.8288454112575,-0.000545657836941327,
4.59414547262434));
#35967=CARTESIAN_POINT('Ctrl Pts',(18.8165201977456,0.15273698101805,4.59272393327212));
#35968=CARTESIAN_POINT('Ctrl Pts',(18.8041949842336,0.307016766534516,4.53213273669464));
#35969=CARTESIAN_POINT('Ctrl Pts',(18.7918697707216,0.416139138999065,4.42538122089617));
#35970=CARTESIAN_POINT('Ctrl Pts',(18.775964492034,0.556957936451544,4.28762193522949));
#35971=CARTESIAN_POINT('Ctrl Pts',(18.7600592133464,0.622575889387102,4.0729916608594));
#35972=CARTESIAN_POINT('Ctrl Pts',(18.7441539346588,0.582864009884755,3.88003953951897));
#35973=CARTESIAN_POINT('Ctrl Pts',(18.7282486559712,0.543152130382401,3.6870874181785));
#35974=CARTESIAN_POINT('Ctrl Pts',(18.7123433772835,0.3981104184421,3.51581344986768));
#35975=CARTESIAN_POINT('Ctrl Pts',(18.6964380985959,0.214335891977863,3.44485939483061));
#35976=CARTESIAN_POINT('Ctrl Pts',(18.6805328199083,0.0305613655136472,
3.37390533979354));
#35977=CARTESIAN_POINT('Ctrl Pts',(18.6646275412207,-0.191945975474496,
3.40327119803019));
#35978=CARTESIAN_POINT('Ctrl Pts',(18.6487222625331,-0.351020173514001,
3.51947340980541));
#35979=CARTESIAN_POINT('Ctrl Pts',(18.6328169838455,-0.510094371553506,
3.63567562158063));
#35980=CARTESIAN_POINT('Ctrl Pts',(18.6169117051579,-0.605735426644373,
3.83871418689441));
#35981=CARTESIAN_POINT('Ctrl Pts',(18.6010064264702,-0.594029012528289,
4.03536238640794));
#35982=CARTESIAN_POINT('Ctrl Pts',(18.5851011477826,-0.582322598412206,
4.23201058592146));
#35983=CARTESIAN_POINT('Ctrl Pts',(18.569195869095,-0.463268715089173,4.42226841963472));
#35984=CARTESIAN_POINT('Ctrl Pts',(18.5532905904074,-0.29153186902666,4.51877753945177));
#35985=CARTESIAN_POINT('Ctrl Pts',(18.5451421973574,-0.203549800283198,
4.56821988225003));
#35986=CARTESIAN_POINT('Ctrl Pts',(18.5369938043075,-0.101740616897797,
4.59305703682098));
#35987=CARTESIAN_POINT('Ctrl Pts',(18.5288454112575,4.04073003155148E-5,
4.59311858068669));
#35988=CARTESIAN_POINT('Ctrl Pts',(18.4211545887425,0.000547083855738422,
4.59411609730493));
#35989=CARTESIAN_POINT('Ctrl Pts',(18.4334025015083,-0.151793472668411,
4.59270633223614));
#35990=CARTESIAN_POINT('Ctrl Pts',(18.4456504142741,-0.305116246576315,
4.53295143150856));
#35991=CARTESIAN_POINT('Ctrl Pts',(18.4578983270399,-0.414068183831284,
4.42739736222451));
#35992=CARTESIAN_POINT('Ctrl Pts',(18.4738036057275,-0.555554407543751,
4.29032364846819));
#35993=CARTESIAN_POINT('Ctrl Pts',(18.4897088844152,-0.622214030743504,
4.07601460745865));
#35994=CARTESIAN_POINT('Ctrl Pts',(18.5056141631028,-0.583439774593308,
3.88287188415962));
#35995=CARTESIAN_POINT('Ctrl Pts',(18.5215194417904,-0.54466551844311,3.68972916086059));
#35996=CARTESIAN_POINT('Ctrl Pts',(18.537424720478,-0.400457382942952,3.51775275527208));
#35997=CARTESIAN_POINT('Ctrl Pts',(18.5533299991656,-0.217029642971419,
3.44590695711865));
#35998=CARTESIAN_POINT('Ctrl Pts',(18.5692352778532,-0.0336019029998957,
3.37406115896522));
#35999=CARTESIAN_POINT('Ctrl Pts',(18.5851405565408,0.189045441442997,3.40234596824686));
#36000=CARTESIAN_POINT('Ctrl Pts',(18.6010458352284,0.348682149221421,3.51777419717301));
#36001=CARTESIAN_POINT('Ctrl Pts',(18.6169511139161,0.508318856999844,3.63320242609916));
#36002=CARTESIAN_POINT('Ctrl Pts',(18.6328563926037,0.604944928113798,3.83577407466982));
#36003=CARTESIAN_POINT('Ctrl Pts',(18.6487616712913,0.594193758619731,4.03247681196108));
#36004=CARTESIAN_POINT('Ctrl Pts',(18.6646669499789,0.583442589125664,4.22917954925235));
#36005=CARTESIAN_POINT('Ctrl Pts',(18.6805722286665,0.465314179023576,4.42001337526422));
#36006=CARTESIAN_POINT('Ctrl Pts',(18.6964775073541,0.294048096631404,4.51735547060535));
#36007=CARTESIAN_POINT('Ctrl Pts',(18.7047032011502,0.205474838715737,4.56769764225005));
#36008=CARTESIAN_POINT('Ctrl Pts',(18.7129288949463,0.102689258835563,4.59303430424318));
#36009=CARTESIAN_POINT('Ctrl Pts',(18.7211545887425,-5.63168744233308E-5,
4.59312091231189));
#36010=CARTESIAN_POINT('Origin',(4.,0.,4.));
#36011=CARTESIAN_POINT('',(19.1288454112575,0.000222628893785728,4.59497983522242));
#36012=CARTESIAN_POINT('',(19.0211545887425,-0.000526118841417405,4.59432346427954));
#36013=CARTESIAN_POINT('',(4.,-7.27562663373442E-17,4.5941));
#36014=CARTESIAN_POINT('Ctrl Pts',(19.1288454112575,0.000222628893785728,
4.59497983522242));
#36015=CARTESIAN_POINT('Ctrl Pts',(19.1278571485589,0.012468395078646,4.59503853204781));
#36016=CARTESIAN_POINT('Ctrl Pts',(19.1268688858602,0.0247107891953784,
4.59469333777414));
#36017=CARTESIAN_POINT('Ctrl Pts',(19.1258806231615,0.0369274203756033,
4.59393377720877));
#36018=CARTESIAN_POINT('Ctrl Pts',(19.1099753444739,0.233544093050454,4.58170927203582));
#36019=CARTESIAN_POINT('Ctrl Pts',(19.0940700657862,0.423487581379576,4.46215450773496));
#36020=CARTESIAN_POINT('Ctrl Pts',(19.0781647870986,0.519543871337238,4.29016397409385));
#36021=CARTESIAN_POINT('Ctrl Pts',(19.062259508411,0.615600161294901,4.11817344045274));
#36022=CARTESIAN_POINT('Ctrl Pts',(19.0463542297234,0.617769252881104,3.89374713747137));
#36023=CARTESIAN_POINT('Ctrl Pts',(19.0304489510358,0.525055191022736,3.71993212880311));
#36024=CARTESIAN_POINT('Ctrl Pts',(19.0145436723482,0.432341129164367,3.54611712013485));
#36025=CARTESIAN_POINT('Ctrl Pts',(18.9986383936606,0.244743913861428,3.42291340577968));
#36026=CARTESIAN_POINT('Ctrl Pts',(18.982733114973,0.0484002497885746,3.40689091904056));
#36027=CARTESIAN_POINT('Ctrl Pts',(18.9668278362853,-0.147943414284278,
3.39086843230144));
#36028=CARTESIAN_POINT('Ctrl Pts',(18.9509225575977,-0.353033527127044,
3.48202717317836));
#36029=CARTESIAN_POINT('Ctrl Pts',(18.9350172789101,-0.472701385564812,
3.63851090447403));
#36030=CARTESIAN_POINT('Ctrl Pts',(18.9191120002225,-0.592369244002587,
3.79499463576972));
#36031=CARTESIAN_POINT('Ctrl Pts',(18.9032067215349,-0.626614848035354,
4.01680335748416));
#36032=CARTESIAN_POINT('Ctrl Pts',(18.8873014428473,-0.559714065105754,
4.20209188855652));
#36033=CARTESIAN_POINT('Ctrl Pts',(18.8713961641597,-0.492813282176159,
4.38738041962887));
#36034=CARTESIAN_POINT('Ctrl Pts',(18.8554908854721,-0.324766112284209,
4.53614876005914));
#36035=CARTESIAN_POINT('Ctrl Pts',(18.8395856067844,-0.132732706353525,
4.58008878179264));
#36036=CARTESIAN_POINT('Ctrl Pts',(18.8360055416088,-0.0895085590353085,
4.5899790920924));
#36037=CARTESIAN_POINT('Ctrl Pts',(18.8324254764332,-0.0450691735440342,
4.59455838259347));
#36038=CARTESIAN_POINT('Ctrl Pts',(18.8288454112575,-0.000545657836941327,
4.59414547262434));
#36039=CARTESIAN_POINT('Ctrl Pts',(18.7211545887425,-5.63168744233308E-5,
4.59312091231189));
#36040=CARTESIAN_POINT('Ctrl Pts',(18.728834173634,-0.0959805501911411,
4.59320177041728));
#36041=CARTESIAN_POINT('Ctrl Pts',(18.7365137585255,-0.191869914813978,
4.57127401300463));
#36042=CARTESIAN_POINT('Ctrl Pts',(18.744193343417,-0.276126457005151,4.5271386400555));
#36043=CARTESIAN_POINT('Ctrl Pts',(18.7600986221046,-0.450631173567243,
4.43572934949413));
#36044=CARTESIAN_POINT('Ctrl Pts',(18.7760039007922,-0.575236852009173,
4.249060403701));
#36045=CARTESIAN_POINT('Ctrl Pts',(18.7919091794798,-0.592729836422094,
4.05284228527226));
#36046=CARTESIAN_POINT('Ctrl Pts',(18.8078144581674,-0.610222820835014,
3.85662416684351));
#36047=CARTESIAN_POINT('Ctrl Pts',(18.823719736855,-0.520603111218926,3.65085687577915));
#36048=CARTESIAN_POINT('Ctrl Pts',(18.8396250155426,-0.365020286731977,
3.53002004684018));
#36049=CARTESIAN_POINT('Ctrl Pts',(18.8555302942302,-0.209437462245028,
3.40918321790122));
#36050=CARTESIAN_POINT('Ctrl Pts',(18.8714355729179,0.0121084771127808,
3.37327685108765));
#36051=CARTESIAN_POINT('Ctrl Pts',(18.8873408516055,0.197893008823487,3.43878763096633));
#36052=CARTESIAN_POINT('Ctrl Pts',(18.9032461302931,0.383677540534204,3.50429841084501));
#36053=CARTESIAN_POINT('Ctrl Pts',(18.9191514089807,0.533700664597814,3.67122633741595));
#36054=CARTESIAN_POINT('Ctrl Pts',(18.9350566876683,0.579078109400399,3.86292516893752));
#36055=CARTESIAN_POINT('Ctrl Pts',(18.9509619663559,0.624455554202981,4.05462400045908));
#36056=CARTESIAN_POINT('Ctrl Pts',(18.9668672450435,0.56518731974455,4.27109373693126));
#36057=CARTESIAN_POINT('Ctrl Pts',(18.9827725237311,0.428486871854059,4.41294063344238));
#36058=CARTESIAN_POINT('Ctrl Pts',(18.9955665454016,0.318526617336051,4.52704063153052));
#36059=CARTESIAN_POINT('Ctrl Pts',(19.008360567072,0.158464569423419,4.5928566151945));
#36060=CARTESIAN_POINT('Ctrl Pts',(19.0211545887425,-0.000526118841417405,
4.59432346427954));
#36061=CARTESIAN_POINT('Origin',(4.,0.,4.));
#36062=CARTESIAN_POINT('',(19.4288454112575,0.000431836873498515,4.59346738712276));
#36063=CARTESIAN_POINT('',(19.3211545887425,0.000315695961457875,4.59487351203822));
#36064=CARTESIAN_POINT('',(4.,-7.27562663373442E-17,4.5941));
#36065=CARTESIAN_POINT('Ctrl Pts',(19.4288454112575,0.000431836873498515,
4.59346738712276));
#36066=CARTESIAN_POINT('Ctrl Pts',(19.4232888206845,0.0697367837969298,
4.59393182999066));
#36067=CARTESIAN_POINT('Ctrl Pts',(19.4177322301115,0.13889623855249,4.58272225272434));
#36068=CARTESIAN_POINT('Ctrl Pts',(19.4121756395385,0.203565929825556,4.55917964700716));
#36069=CARTESIAN_POINT('Ctrl Pts',(19.3962703608509,0.38867754617092,4.49179089484985));
#36070=CARTESIAN_POINT('Ctrl Pts',(19.3803650821633,0.537002597765565,4.32335233206236));
#36071=CARTESIAN_POINT('Ctrl Pts',(19.3644598034757,0.580436494614329,4.13120381907284));
#36072=CARTESIAN_POINT('Ctrl Pts',(19.3485545247881,0.623870391463095,3.93905530608331));
#36073=CARTESIAN_POINT('Ctrl Pts',(19.3326492461004,0.562413133565966,3.72319684289176));
#36074=CARTESIAN_POINT('Ctrl Pts',(19.3167439674128,0.424283294458304,3.58274150440131));
#36075=CARTESIAN_POINT('Ctrl Pts',(19.3008386887252,0.286153455350651,3.44228616591086));
#36076=CARTESIAN_POINT('Ctrl Pts',(19.2849334100376,0.071351035032473,3.37723395212151));
#36077=CARTESIAN_POINT('Ctrl Pts',(19.26902813135,-0.12149578302492,3.4174540870367));
#36078=CARTESIAN_POINT('Ctrl Pts',(19.2531228526624,-0.314342601082313,
3.45767422195189));
#36079=CARTESIAN_POINT('Ctrl Pts',(19.2372175739748,-0.485233816878921,
3.60316670557164));
#36080=CARTESIAN_POINT('Ctrl Pts',(19.2213122952871,-0.555703413721375,
3.78712754492824));
#36081=CARTESIAN_POINT('Ctrl Pts',(19.2054070165995,-0.626173010563829,
3.97108838428485));
#36082=CARTESIAN_POINT('Ctrl Pts',(19.1895017379119,-0.59622098845213,4.19351757937831));
#36083=CARTESIAN_POINT('Ctrl Pts',(19.1735964592243,-0.479600048885993,
4.35228505390253));
#36084=CARTESIAN_POINT('Ctrl Pts',(19.1586794432354,-0.370225264934164,
4.50118762911129));
#36085=CARTESIAN_POINT('Ctrl Pts',(19.1437624272465,-0.184617181632464,
4.59409385471947));
#36086=CARTESIAN_POINT('Ctrl Pts',(19.1288454112575,0.000222628893785728,
4.59497983522242));
#36087=CARTESIAN_POINT('Ctrl Pts',(19.0211545887425,-0.000526118841417405,
4.59432346427954));
#36088=CARTESIAN_POINT('Ctrl Pts',(19.0242658457596,-0.0391895592568775,
4.59468017342281));
#36089=CARTESIAN_POINT('Ctrl Pts',(19.0273771027768,-0.0777896429211806,
4.59123148246997));
#36090=CARTESIAN_POINT('Ctrl Pts',(19.030488359794,-0.115590453236054,4.58374636034569));
#36091=CARTESIAN_POINT('Ctrl Pts',(19.0463936384816,-0.308834669113126,
4.5454811341878));
#36092=CARTESIAN_POINT('Ctrl Pts',(19.0622989171692,-0.481190439544719,
4.40172662532195));
#36093=CARTESIAN_POINT('Ctrl Pts',(19.0782041958568,-0.553519286527586,
4.21848882245705));
#36094=CARTESIAN_POINT('Ctrl Pts',(19.0941094745444,-0.625848133510457,
4.03525101959215));
#36095=CARTESIAN_POINT('Ctrl Pts',(19.1100147532321,-0.598150057044591,
3.81252992272818));
#36096=CARTESIAN_POINT('Ctrl Pts',(19.1259200319197,-0.483142842019737,
3.65258963701249));
#36097=CARTESIAN_POINT('Ctrl Pts',(19.1418253106073,-0.36813562699489,3.49264935129682));
#36098=CARTESIAN_POINT('Ctrl Pts',(19.1577305892949,-0.165819273411065,
3.39548987672941));
#36099=CARTESIAN_POINT('Ctrl Pts',(19.1736358679825,0.0309111084379188,
3.40572273351557));
#36100=CARTESIAN_POINT('Ctrl Pts',(19.1895411466701,0.227641490286902,3.41595559030173));
#36101=CARTESIAN_POINT('Ctrl Pts',(19.2054464253577,0.418785900401045,3.53358077844144));
#36102=CARTESIAN_POINT('Ctrl Pts',(19.2213517040453,0.516578912360374,3.70458978792342));
#36103=CARTESIAN_POINT('Ctrl Pts',(19.237256982733,0.614371924319703,3.87559879740541));
#36104=CARTESIAN_POINT('Ctrl Pts',(19.2531622614206,0.618813538124218,4.09999162822965));
#36105=CARTESIAN_POINT('Ctrl Pts',(19.2690675401082,0.527864352527146,4.27473658562515));
#36106=CARTESIAN_POINT('Ctrl Pts',(19.2849728187958,0.436915166930073,4.44948154302064));
#36107=CARTESIAN_POINT('Ctrl Pts',(19.3008780974834,0.250575181931413,4.5745786269874));
#36108=CARTESIAN_POINT('Ctrl Pts',(19.316783376171,0.0544038354309166,4.59258854924263));
#36109=CARTESIAN_POINT('Ctrl Pts',(19.3182404470282,0.0364327229714708,
4.59423842494573));
#36110=CARTESIAN_POINT('Ctrl Pts',(19.3196975178853,0.0183791031991185,
4.59498959766064));
#36111=CARTESIAN_POINT('Ctrl Pts',(19.3211545887425,0.000315695961457875,
4.59487351203822));
#36112=CARTESIAN_POINT('Origin',(4.,0.,4.));
#36113=CARTESIAN_POINT('',(19.7288454112575,-0.000401422265437046,4.59340756962635));
#36114=CARTESIAN_POINT('',(19.6211545887425,0.000364945106097663,4.59334757974602));
#36115=CARTESIAN_POINT('',(4.,-7.27562663373442E-17,4.5941));
#36116=CARTESIAN_POINT('Ctrl Pts',(19.7288454112575,-0.000401422265437046,
4.59340756962635));
#36117=CARTESIAN_POINT('Ctrl Pts',(19.7187204928102,0.125914276337785,4.59262579220321));
#36118=CARTESIAN_POINT('Ctrl Pts',(19.7085955743629,0.252675872983383,4.55317429478549));
#36119=CARTESIAN_POINT('Ctrl Pts',(19.6984706559155,0.353547469597214,4.47867015725961));
#36120=CARTESIAN_POINT('Ctrl Pts',(19.6825653772279,0.512007102052776,4.36163128164859));
#36121=CARTESIAN_POINT('Ctrl Pts',(19.6666600985403,0.606576931433326,4.15809158444534));
#36122=CARTESIAN_POINT('Ctrl Pts',(19.6507548198527,0.593834428727047,3.9615078130365));
#36123=CARTESIAN_POINT('Ctrl Pts',(19.6348495411651,0.581091926020768,3.76492404162769));
#36124=CARTESIAN_POINT('Ctrl Pts',(19.6189442624775,0.46103709122769,3.57529619601327));
#36125=CARTESIAN_POINT('Ctrl Pts',(19.6030389837899,0.288794059426421,3.47969339775167));
#36126=CARTESIAN_POINT('Ctrl Pts',(19.5871337051022,0.116551027625133,3.38409059949006));
#36127=CARTESIAN_POINT('Ctrl Pts',(19.5712284264146,-0.107880201184358,
3.38251284858128));
#36128=CARTESIAN_POINT('Ctrl Pts',(19.555323147727,-0.281450319664219,3.47568456171554));
#36129=CARTESIAN_POINT('Ctrl Pts',(19.5394178690394,-0.45502043814407,3.5688562748498));
#36130=CARTESIAN_POINT('Ctrl Pts',(19.5235125903518,-0.577729446294298,
3.75677745202708));
#36131=CARTESIAN_POINT('Ctrl Pts',(19.5076073116642,-0.593234549413986,
3.95316264945144));
#36132=CARTESIAN_POINT('Ctrl Pts',(19.4917020329766,-0.608739652533674,
4.1495478468758));
#36133=CARTESIAN_POINT('Ctrl Pts',(19.475796754289,-0.517040850622822,4.35439706454724));
#36134=CARTESIAN_POINT('Ctrl Pts',(19.4598914756013,-0.360242359119356,
4.47365220261941));
#36135=CARTESIAN_POINT('Ctrl Pts',(19.4495427874867,-0.258222223711561,
4.55124494740629));
#36136=CARTESIAN_POINT('Ctrl Pts',(19.4391940993721,-0.128642866595325,
4.59260240088276));
#36137=CARTESIAN_POINT('Ctrl Pts',(19.4288454112575,0.000431836873498515,
4.59346738712276));
#36138=CARTESIAN_POINT('Ctrl Pts',(19.3211545887425,0.000315695961457875,
4.59487351203822));
#36139=CARTESIAN_POINT('Ctrl Pts',(19.3356027965729,-0.178799726336078,
4.59372241551416));
#36140=CARTESIAN_POINT('Ctrl Pts',(19.3500510044034,-0.35887750705714,4.50729762043595));
#36141=CARTESIAN_POINT('Ctrl Pts',(19.3644992122339,-0.469016560662847,
4.36625733020606));
#36142=CARTESIAN_POINT('Ctrl Pts',(19.3804044909215,-0.590262902253753,
4.21099342837053));
#36143=CARTESIAN_POINT('Ctrl Pts',(19.3963097696091,-0.626752877433238,
3.98954286415574));
#36144=CARTESIAN_POINT('Ctrl Pts',(19.4122150482967,-0.561731832709929,
3.80358636875254));
#36145=CARTESIAN_POINT('Ctrl Pts',(19.4281203269843,-0.49671078798662,3.61762987334934));
#36146=CARTESIAN_POINT('Ctrl Pts',(19.4440256056719,-0.330178723360516,
3.46716744675772));
#36147=CARTESIAN_POINT('Ctrl Pts',(19.4599308843595,-0.138600118749324,
3.42128506802099));
#36148=CARTESIAN_POINT('Ctrl Pts',(19.4758361630471,0.0529784858618673,
3.37540268928427));
#36149=CARTESIAN_POINT('Ctrl Pts',(19.4917414417347,0.269603630458146,3.43410035840244));
#36150=CARTESIAN_POINT('Ctrl Pts',(19.5076467204224,0.411810215621333,3.57042659223364));
#36151=CARTESIAN_POINT('Ctrl Pts',(19.52355199911,0.554016800784528,3.70675282606484));
#36152=CARTESIAN_POINT('Ctrl Pts',(19.5394572777976,0.621804826514621,3.92070762460909));
#36153=CARTESIAN_POINT('Ctrl Pts',(19.5553625564852,0.584048894878601,4.11405198996909));
#36154=CARTESIAN_POINT('Ctrl Pts',(19.5712678351728,0.546292963242583,4.30739635532907));
#36155=CARTESIAN_POINT('Ctrl Pts',(19.5871731138604,0.402993074240464,4.4801302875048));
#36156=CARTESIAN_POINT('Ctrl Pts',(19.6030783925481,0.219946482677819,4.55294168410437));
#36157=CARTESIAN_POINT('Ctrl Pts',(19.6091037912795,0.150602919307179,4.5805248346624));
#36158=CARTESIAN_POINT('Ctrl Pts',(19.615129190011,0.0755552166468998,4.59376787586841));
#36159=CARTESIAN_POINT('Ctrl Pts',(19.6211545887425,0.000364945106097663,
4.59334757974602));
#36160=CARTESIAN_POINT('Origin',(4.,0.,4.));
#36161=CARTESIAN_POINT('',(20.0288454112575,-0.000266600559035268,4.5949350414008));
#36162=CARTESIAN_POINT('',(19.9211545887425,-0.000461335262921832,4.59353843444423));
#36163=CARTESIAN_POINT('',(4.,-7.27562663373442E-17,4.5941));
#36164=CARTESIAN_POINT('Ctrl Pts',(20.0288454112575,-0.000266600559035268,
4.5949350414008));
#36165=CARTESIAN_POINT('Ctrl Pts',(20.0141521649359,0.181839152323842,4.59391190659116));
#36166=CARTESIAN_POINT('Ctrl Pts',(19.9994589186142,0.364814066967773,4.50413264800542));
#36167=CARTESIAN_POINT('Ctrl Pts',(19.9847656722925,0.474598868642052,4.35899217880197));
#36168=CARTESIAN_POINT('Ctrl Pts',(19.9688603936049,0.593439717564554,4.20187920587587));
#36169=CARTESIAN_POINT('Ctrl Pts',(19.9529551149173,0.626517665065843,3.97989492921597));
#36170=CARTESIAN_POINT('Ctrl Pts',(19.9370498362297,0.558641803885684,3.79496194153783));
#36171=CARTESIAN_POINT('Ctrl Pts',(19.9211445575421,0.490765942705524,3.61002895385969));
#36172=CARTESIAN_POINT('Ctrl Pts',(19.9052392788545,0.321936272843916,3.46214725516331));
#36173=CARTESIAN_POINT('Ctrl Pts',(19.8893340001669,0.129673778938228,3.41921955761011));
#36174=CARTESIAN_POINT('Ctrl Pts',(19.8734287214793,-0.0625887149674591,
3.37629186005692));
#36175=CARTESIAN_POINT('Ctrl Pts',(19.8575234427916,-0.278284032917226,
3.43831816364691));
#36176=CARTESIAN_POINT('Ctrl Pts',(19.841618164104,-0.418374827314372,3.57681771754473));
#36177=CARTESIAN_POINT('Ctrl Pts',(19.8257128854164,-0.558465621711518,
3.71531727144255));
#36178=CARTESIAN_POINT('Ctrl Pts',(19.8098076067288,-0.622951892556044,
3.9302900756482));
#36179=CARTESIAN_POINT('Ctrl Pts',(19.7939023280412,-0.58222383973146,4.12303018792675));
#36180=CARTESIAN_POINT('Ctrl Pts',(19.7779970493536,-0.541495786906873,
4.3157703002053));
#36181=CARTESIAN_POINT('Ctrl Pts',(19.762091770666,-0.395553410413165,4.48627772055676));
#36182=CARTESIAN_POINT('Ctrl Pts',(19.7461864919784,-0.211407504401025,
4.55626240372308));
#36183=CARTESIAN_POINT('Ctrl Pts',(19.7404061317381,-0.144484459893097,
4.58169651826758));
#36184=CARTESIAN_POINT('Ctrl Pts',(19.7346257714978,-0.0725156072563085,
4.59385388977766));
#36185=CARTESIAN_POINT('Ctrl Pts',(19.7288454112575,-0.000401422265437046,
4.59340756962635));
#36186=CARTESIAN_POINT('Ctrl Pts',(19.6211545887425,0.000364945106097663,
4.59334757974602));
#36187=CARTESIAN_POINT('Ctrl Pts',(19.6310344686986,-0.122924963130536,
4.59265841784648));
#36188=CARTESIAN_POINT('Ctrl Pts',(19.6409143486547,-0.246598186964828,
4.55523353708024));
#36189=CARTESIAN_POINT('Ctrl Pts',(19.6507942286109,-0.346136160298313,
4.48405653351353));
#36190=CARTESIAN_POINT('Ctrl Pts',(19.6666995072985,-0.506378917588675,
4.36947112529969));
#36191=CARTESIAN_POINT('Ctrl Pts',(19.6826047859861,-0.60407113804621,4.16741144784858));
#36192=CARTESIAN_POINT('Ctrl Pts',(19.6985100646737,-0.5943566574826,3.97065479758251));
#36193=CARTESIAN_POINT('Ctrl Pts',(19.7144153433613,-0.584642176918989,
3.77389814731645));
#36194=CARTESIAN_POINT('Ctrl Pts',(19.7303206220489,-0.467520995334232,
3.58244452423543));
#36195=CARTESIAN_POINT('Ctrl Pts',(19.7462259007365,-0.296770260159971,
3.48420125495101));
#36196=CARTESIAN_POINT('Ctrl Pts',(19.7621311794242,-0.12601952498572,3.38595798566659));
#36197=CARTESIAN_POINT('Ctrl Pts',(19.7780364581118,0.098360763778029,3.38092507017875));
#36198=CARTESIAN_POINT('Ctrl Pts',(19.7939417367994,0.27334477570878,3.47141355644931));
#36199=CARTESIAN_POINT('Ctrl Pts',(19.809847015487,0.448328787639532,3.56190204271987));
#36200=CARTESIAN_POINT('Ctrl Pts',(19.8257522941746,0.573916522737285,3.74791193074883));
#36201=CARTESIAN_POINT('Ctrl Pts',(19.8416575728622,0.592443207149574,3.9440350735258));
#36202=CARTESIAN_POINT('Ctrl Pts',(19.8575628515498,0.610969891561863,4.14015821630277));
#36203=CARTESIAN_POINT('Ctrl Pts',(19.8734681302375,0.522435525288687,4.34639461382776));
#36204=CARTESIAN_POINT('Ctrl Pts',(19.8893734089251,0.367491719635661,4.46804975837363));
#36205=CARTESIAN_POINT('Ctrl Pts',(19.8999671355309,0.264291244586565,4.54907828775811));
#36206=CARTESIAN_POINT('Ctrl Pts',(19.9105608621367,0.131629953687138,4.59258455010229));
#36207=CARTESIAN_POINT('Ctrl Pts',(19.9211545887425,-0.000461335262921832,
4.59353843444423));
#36208=CARTESIAN_POINT('Origin',(4.,0.,4.));
#36209=CARTESIAN_POINT('',(20.3288454112575,0.000547175593784699,4.59423670486774));
#36210=CARTESIAN_POINT('',(20.2211545887425,-0.000159442692484791,4.59503650419094));
#36211=CARTESIAN_POINT('',(4.,-7.27562663373442E-17,4.5941));
#36212=CARTESIAN_POINT('Ctrl Pts',(20.3288454112575,0.000547175593784699,
4.59423670486774));
#36213=CARTESIAN_POINT('Ctrl Pts',(20.3254891157492,0.0422991098545892,
4.59465405164581));
#36214=CARTESIAN_POINT('Ctrl Pts',(20.3221328202408,0.0839734681026259,
4.59066114403672));
#36215=CARTESIAN_POINT('Ctrl Pts',(20.3187765247324,0.124636177719752,4.58197547152207));
#36216=CARTESIAN_POINT('Ctrl Pts',(20.3028712460448,0.317334266145104,4.54081460186972));
#36217=CARTESIAN_POINT('Ctrl Pts',(20.2869659673572,0.48731321493246,4.39426577643889));
#36218=CARTESIAN_POINT('Ctrl Pts',(20.2710606886696,0.556778600406793,4.20989870881916));
#36219=CARTESIAN_POINT('Ctrl Pts',(20.255155409982,0.626243985881127,4.02553164119943));
#36220=CARTESIAN_POINT('Ctrl Pts',(20.2392501312944,0.595195808042437,3.80334633139079));
#36221=CARTESIAN_POINT('Ctrl Pts',(20.2233448526068,0.477757630702126,3.64521515909767));
#36222=CARTESIAN_POINT('Ctrl Pts',(20.2074395739191,0.360319453361808,3.48708398680455));
#36223=CARTESIAN_POINT('Ctrl Pts',(20.1915342952315,0.156491276519859,3.39300695202695));
#36224=CARTESIAN_POINT('Ctrl Pts',(20.1756290165439,-0.04006765138094,3.40625706061923));
#36225=CARTESIAN_POINT('Ctrl Pts',(20.1597237378563,-0.236626579281727,
3.4195071692115));
#36226=CARTESIAN_POINT('Ctrl Pts',(20.1438184591687,-0.425916258241364,
3.54008442117362));
#36227=CARTESIAN_POINT('Ctrl Pts',(20.1279131804811,-0.521059912873915,
3.71258420787224));
#36228=CARTESIAN_POINT('Ctrl Pts',(20.1120079017935,-0.616203567506467,
3.88508399457085));
#36229=CARTESIAN_POINT('Ctrl Pts',(20.0961026231058,-0.617201197811932,
4.10950631600596));
#36230=CARTESIAN_POINT('Ctrl Pts',(20.0801973444182,-0.523575121773085,
4.28282745216878));
#36231=CARTESIAN_POINT('Ctrl Pts',(20.0642920657306,-0.429949045734243,
4.45614858833159));
#36232=CARTESIAN_POINT('Ctrl Pts',(20.048386787043,-0.241699263351099,4.57836853922213));
#36233=CARTESIAN_POINT('Ctrl Pts',(20.0324815083554,-0.0452724969876719,
4.59335768007126));
#36234=CARTESIAN_POINT('Ctrl Pts',(20.0312694759895,-0.030304158296608,
4.59449989984645));
#36235=CARTESIAN_POINT('Ctrl Pts',(20.0300574436235,-0.0152883365109376,
4.5950194388496));
#36236=CARTESIAN_POINT('Ctrl Pts',(20.0288454112575,-0.000266600559035268,
4.5949350414008));
#36237=CARTESIAN_POINT('Ctrl Pts',(19.9211545887425,-0.000461335262921832,
4.59353843444423));
#36238=CARTESIAN_POINT('Ctrl Pts',(19.9264661408243,-0.0666901315043342,
4.5940166992278));
#36239=CARTESIAN_POINT('Ctrl Pts',(19.9317776929061,-0.132775635823809,
4.58379778651276));
#36240=CARTESIAN_POINT('Ctrl Pts',(19.9370892449879,-0.194932679790098,
4.56224768701753));
#36241=CARTESIAN_POINT('Ctrl Pts',(19.9529945236755,-0.381060028529917,
4.49771657954882));
#36242=CARTESIAN_POINT('Ctrl Pts',(19.9688998023631,-0.531961480976676,
4.33158047304464));
#36243=CARTESIAN_POINT('Ctrl Pts',(19.9848050810507,-0.578348134104426,
4.14012389605102));
#36244=CARTESIAN_POINT('Ctrl Pts',(20.0007103597384,-0.624734787232175,
3.94866731905739));
#36245=CARTESIAN_POINT('Ctrl Pts',(20.016615638426,-0.566606641040915,3.73189027157431));
#36246=CARTESIAN_POINT('Ctrl Pts',(20.0325209171136,-0.430656211588969,
3.58932409618151));
#36247=CARTESIAN_POINT('Ctrl Pts',(20.0484261958012,-0.294705782137024,
3.44675792078871));
#36248=CARTESIAN_POINT('Ctrl Pts',(20.0643314744888,-0.080933069424392,
3.37840261748619));
#36249=CARTESIAN_POINT('Ctrl Pts',(20.0802367531764,0.112511319004002,3.41565067076361));
#36250=CARTESIAN_POINT('Ctrl Pts',(20.096142031864,0.305955707432406,3.45289872404102));
#36251=CARTESIAN_POINT('Ctrl Pts',(20.1120473105516,0.479071771576571,3.59575013389837));
#36252=CARTESIAN_POINT('Ctrl Pts',(20.1279525892393,0.552362916535151,3.77860107435498));
#36253=CARTESIAN_POINT('Ctrl Pts',(20.1438578679269,0.625654061493722,3.96145201481158));
#36254=CARTESIAN_POINT('Ctrl Pts',(20.1597631466145,0.599120287266732,4.18430248586742));
#36255=CARTESIAN_POINT('Ctrl Pts',(20.1756684253021,0.484961816589866,4.3448525870839));
#36256=CARTESIAN_POINT('Ctrl Pts',(20.1908304797822,0.376137759761604,4.49790047950022));
#36257=CARTESIAN_POINT('Ctrl Pts',(20.2059925342623,0.187686755696174,4.59433432972249));
#36258=CARTESIAN_POINT('Ctrl Pts',(20.2211545887425,-0.000159442692484791,
4.59503650419094));
#36259=CARTESIAN_POINT('Origin',(4.,0.,4.));
#36260=CARTESIAN_POINT('',(20.6288454112575,1.84392275237588E-6,4.59415158619139));
#36261=CARTESIAN_POINT('',(20.5211545887425,0.00014515264107467,4.59408556636595));
#36262=CARTESIAN_POINT('',(4.,-7.27562663373442E-17,4.5941));
#36263=CARTESIAN_POINT('Ctrl Pts',(20.6288454112575,1.84392275237588E-6,
4.59415158619139));
#36264=CARTESIAN_POINT('Ctrl Pts',(20.6209207878748,0.0985777406598016,
4.59414764832452));
#36265=CARTESIAN_POINT('Ctrl Pts',(20.6129961644921,0.197149291092008,4.56908802213256));
#36266=CARTESIAN_POINT('Ctrl Pts',(20.6050715411094,0.283761277174982,4.52200793915563));
#36267=CARTESIAN_POINT('Ctrl Pts',(20.5971189017656,0.370679463050262,4.47476141372331));
#36268=CARTESIAN_POINT('Ctrl Pts',(20.5891662624218,0.445553373684486,4.40533845822152));
#36269=CARTESIAN_POINT('Ctrl Pts',(20.581213623078,0.499196468040806,4.3222224876916));
#36270=CARTESIAN_POINT('Ctrl Pts',(20.5732609837342,0.552839562397126,4.23910651716169));
#36271=CARTESIAN_POINT('Ctrl Pts',(20.5653083443904,0.585251840475543,4.14229753160364));
#36272=CARTESIAN_POINT('Ctrl Pts',(20.5573557050466,0.592531230276538,4.04364021904617));
#36273=CARTESIAN_POINT('Ctrl Pts',(20.5494030657028,0.599810620077534,3.9449829064887));
#36274=CARTESIAN_POINT('Ctrl Pts',(20.541450426359,0.581957121601108,3.84447726693182));
#36275=CARTESIAN_POINT('Ctrl Pts',(20.5334977870152,0.541038843355354,3.75439549632807));
#36276=CARTESIAN_POINT('Ctrl Pts',(20.5255451476714,0.5001205651096,3.66431372572433));
#36277=CARTESIAN_POINT('Ctrl Pts',(20.5175925083276,0.436137507094518,3.58465582407373));
#36278=CARTESIAN_POINT('Ctrl Pts',(20.5096398689838,0.357128912623608,3.5251911792601));
#36279=CARTESIAN_POINT('Ctrl Pts',(20.50168722964,0.278120318152698,3.46572653444646));
#36280=CARTESIAN_POINT('Ctrl Pts',(20.4937345902962,0.184086187225959,3.42645514646979));
#36281=CARTESIAN_POINT('Ctrl Pts',(20.4857819509524,0.0861162623359374,
3.4121221101222));
#36282=CARTESIAN_POINT('Ctrl Pts',(20.4778293116085,-0.0118536625540841,
3.39778907377461));
#36283=CARTESIAN_POINT('Ctrl Pts',(20.4698766722647,-0.113759381407388,
3.4083943890561));
#36284=CARTESIAN_POINT('Ctrl Pts',(20.4619240329209,-0.206384677702653,
3.44274365129583));
#36285=CARTESIAN_POINT('Ctrl Pts',(20.4539713935771,-0.299009973997917,
3.47709291353557));
#36286=CARTESIAN_POINT('Ctrl Pts',(20.4460187542333,-0.382354847735142,
3.53518612273354));
#36287=CARTESIAN_POINT('Ctrl Pts',(20.4380661148895,-0.447563842371028,
3.60976099223211));
#36288=CARTESIAN_POINT('Ctrl Pts',(20.4301134755457,-0.512772837006921,
3.68433586173069));
#36289=CARTESIAN_POINT('Ctrl Pts',(20.4221608362019,-0.559845952541473,
3.77539239152987));
#36290=CARTESIAN_POINT('Ctrl Pts',(20.4142081968581,-0.580888308445953,
3.87190852591559));
#36291=CARTESIAN_POINT('Ctrl Pts',(20.3983029181705,-0.622973020254908,
4.06494079468701));
#36292=CARTESIAN_POINT('Ctrl Pts',(20.3823976394829,-0.5609346935436,4.27981148180459));
#36293=CARTESIAN_POINT('Ctrl Pts',(20.3664923607953,-0.422206916156273,
4.41936036842645));
#36294=CARTESIAN_POINT('Ctrl Pts',(20.353943377616,-0.312753156865475,4.52946196836027));
#36295=CARTESIAN_POINT('Ctrl Pts',(20.3413943944368,-0.155560747392339,
4.59267627084609));
#36296=CARTESIAN_POINT('Ctrl Pts',(20.3288454112575,0.000547175593784699,
4.59423670486774));
#36297=CARTESIAN_POINT('Ctrl Pts',(20.2211545887425,-0.000159442692484791,
4.59503650419094));
#36298=CARTESIAN_POINT('Ctrl Pts',(20.22189781295,-0.00936741923094289,
4.59507092387091));
#36299=CARTESIAN_POINT('Ctrl Pts',(20.2226410371574,-0.0185739425223631,
4.59487531632137));
#36300=CARTESIAN_POINT('Ctrl Pts',(20.2233842613649,-0.0277695625699301,
4.59444507412072));
#36301=CARTESIAN_POINT('Ctrl Pts',(20.2392895400526,-0.224559303926058,
4.58523772856393));
#36302=CARTESIAN_POINT('Ctrl Pts',(20.2551948187402,-0.416355619511548,
4.46857330607325));
#36303=CARTESIAN_POINT('Ctrl Pts',(20.2711000974278,-0.51503297954037,4.29810345018796));
#36304=CARTESIAN_POINT('Ctrl Pts',(20.2870053761154,-0.613710339569191,
4.12763359430267));
#36305=CARTESIAN_POINT('Ctrl Pts',(20.302910654803,-0.619268744041345,3.90335830502277));
#36306=CARTESIAN_POINT('Ctrl Pts',(20.3188159334906,-0.529271009537506,
3.72809546473432));
#36307=CARTESIAN_POINT('Ctrl Pts',(20.3347212121782,-0.439273275033663,
3.55283262444587));
#36308=CARTESIAN_POINT('Ctrl Pts',(20.3506264908658,-0.253719401553817,
3.42658223314887));
#36309=CARTESIAN_POINT('Ctrl Pts',(20.3665317695535,-0.0575887485100287,
3.40762076142476));
#36310=CARTESIAN_POINT('Ctrl Pts',(20.3824370482411,0.138541904533748,3.38865928970065));
#36311=CARTESIAN_POINT('Ctrl Pts',(20.3983423269287,0.345249337141466,3.47698673754941));
#36312=CARTESIAN_POINT('Ctrl Pts',(20.4142476056163,0.467192899405167,3.63141813202173));
#36313=CARTESIAN_POINT('Ctrl Pts',(20.4301528843039,0.589136461668875,3.78584952649406));
#36314=CARTESIAN_POINT('Ctrl Pts',(20.4460581629915,0.626316153588557,4.00638486758996));
#36315=CARTESIAN_POINT('Ctrl Pts',(20.4619634416791,0.562534942182983,4.19337293359078));
#36316=CARTESIAN_POINT('Ctrl Pts',(20.4699160810229,0.530644336480201,4.28686696659118));
#36317=CARTESIAN_POINT('Ctrl Pts',(20.4778687203667,0.473513504946115,4.3719741808178));
#36318=CARTESIAN_POINT('Ctrl Pts',(20.4858213597105,0.400240502138227,4.43864269813793));
#36319=CARTESIAN_POINT('Ctrl Pts',(20.4937739990544,0.326967499330329,4.50531121545807));
#36320=CARTESIAN_POINT('Ctrl Pts',(20.5017266383982,0.237552325248626,4.55354103587171));
#36321=CARTESIAN_POINT('Ctrl Pts',(20.509679277742,0.141619450488441,4.57712494713439));
#36322=CARTESIAN_POINT('Ctrl Pts',(20.5135043814088,0.0954771353210092,
4.58846846487098));
#36323=CARTESIAN_POINT('Ctrl Pts',(20.5173294850756,0.0478269697500401,
4.59411022582368));
#36324=CARTESIAN_POINT('Ctrl Pts',(20.5211545887425,0.00014515264107467,
4.59408556636595));
#36325=CARTESIAN_POINT('Origin',(4.,0.,4.));
#36326=CARTESIAN_POINT('',(20.9288454112575,-6.4040329070536E-6,4.59405282094147));
#36327=CARTESIAN_POINT('',(20.8211545887425,5.65245430726296E-6,4.59414685459231));
#36328=CARTESIAN_POINT('',(4.,-7.27562663373442E-17,4.5941));
#36329=CARTESIAN_POINT('Ctrl Pts',(20.9288454112575,-6.4040329070536E-6,
4.59405282094147));
#36330=CARTESIAN_POINT('Ctrl Pts',(20.9243050993443,0.0564994875152707,
4.59403151438501));
#36331=CARTESIAN_POINT('Ctrl Pts',(20.9197647874311,0.113011285737041,4.58603249222448));
#36332=CARTESIAN_POINT('Ctrl Pts',(20.9152244755179,0.167207550221224,4.57013805289591));
#36333=CARTESIAN_POINT('Ctrl Pts',(20.9072718361741,0.262135685878584,4.5422979516059));
#36334=CARTESIAN_POINT('Ctrl Pts',(20.8993191968303,0.349959832061366,4.49023494241839));
#36335=CARTESIAN_POINT('Ctrl Pts',(20.8913665574865,0.419942299057043,4.42031443844746));
#36336=CARTESIAN_POINT('Ctrl Pts',(20.8834139181427,0.489924766052721,4.35039393447653));
#36337=CARTESIAN_POINT('Ctrl Pts',(20.8754612787989,0.542065553861293,4.26261593572219));
#36338=CARTESIAN_POINT('Ctrl Pts',(20.8675086394551,0.569989725359365,4.16771249585991));
#36339=CARTESIAN_POINT('Ctrl Pts',(20.8595560001113,0.597913896857441,4.07280905599763));
#36340=CARTESIAN_POINT('Ctrl Pts',(20.8516033607674,0.601621452045013,3.97078017502742));
#36341=CARTESIAN_POINT('Ctrl Pts',(20.8436507214236,0.580659121393648,3.87410027737825));
#36342=CARTESIAN_POINT('Ctrl Pts',(20.8356980820798,0.559696790742287,3.77742037972911));
#36343=CARTESIAN_POINT('Ctrl Pts',(20.827745442736,0.514064574252002,3.686089465401));
#36344=CARTESIAN_POINT('Ctrl Pts',(20.8197928033922,0.44934157601673,3.61127397478397));
#36345=CARTESIAN_POINT('Ctrl Pts',(20.8118401640484,0.384618577781443,3.53645848416692));
#36346=CARTESIAN_POINT('Ctrl Pts',(20.8038875247046,0.300804797801161,3.47815841726095));
#36347=CARTESIAN_POINT('Ctrl Pts',(20.7959348853608,0.208147717693743,3.44350176598286));
#36348=CARTESIAN_POINT('Ctrl Pts',(20.787982246017,0.115490637586335,3.40884511470477));
#36349=CARTESIAN_POINT('Ctrl Pts',(20.7800296066732,0.0139902573517945,
3.39783187905454));
#36350=CARTESIAN_POINT('Ctrl Pts',(20.7720769673294,-0.0839438183138644,
3.41180854931868));
#36351=CARTESIAN_POINT('Ctrl Pts',(20.7641243279856,-0.181877893979523,
3.42578521958283));
#36352=CARTESIAN_POINT('Ctrl Pts',(20.7561716886418,-0.2762456650763,3.46475179576135));
#36353=CARTESIAN_POINT('Ctrl Pts',(20.748219049298,-0.355509010203556,3.52394413563581));
#36354=CARTESIAN_POINT('Ctrl Pts',(20.7402664099542,-0.434772355330821,
3.58313647551028));
#36355=CARTESIAN_POINT('Ctrl Pts',(20.7323137706103,-0.498931274488562,
3.66255457908069));
#36356=CARTESIAN_POINT('Ctrl Pts',(20.7243611312665,-0.54014217617541,3.75248840252759));
#36357=CARTESIAN_POINT('Ctrl Pts',(20.7164084919227,-0.581353077862249,
3.84242222597448));
#36358=CARTESIAN_POINT('Ctrl Pts',(20.7084558525789,-0.599615962078206,
3.94287176929784));
#36359=CARTESIAN_POINT('Ctrl Pts',(20.7005032132351,-0.592696601504336,
4.0415558946729));
#36360=CARTESIAN_POINT('Ctrl Pts',(20.6925505738913,-0.585777240930466,
4.14024002004797));
#36361=CARTESIAN_POINT('Ctrl Pts',(20.6845979345475,-0.553675635566762,
4.23715872747472));
#36362=CARTESIAN_POINT('Ctrl Pts',(20.6766452952037,-0.50031917594212,4.32046203197985));
#36363=CARTESIAN_POINT('Ctrl Pts',(20.6686926558599,-0.446962716317479,
4.40376533648498));
#36364=CARTESIAN_POINT('Ctrl Pts',(20.6607400165161,-0.3723514024319,4.47345323806848));
#36365=CARTESIAN_POINT('Ctrl Pts',(20.6527873771723,-0.285602702553558,
4.52100610813718));
#36366=CARTESIAN_POINT('Ctrl Pts',(20.6448347378285,-0.198854002675205,
4.56855897820588));
#36367=CARTESIAN_POINT('Ctrl Pts',(20.6368820984847,-0.099967916804087,
4.59397681675976));
#36368=CARTESIAN_POINT('Ctrl Pts',(20.6289294591409,-0.00104364331035449,
4.59415068835528));
#36369=CARTESIAN_POINT('Ctrl Pts',(20.6289014431798,-0.000695147863829354,
4.59415130087895));
#36370=CARTESIAN_POINT('Ctrl Pts',(20.6288734272186,-0.000346651943377611,
4.59415160011295));
#36371=CARTESIAN_POINT('Ctrl Pts',(20.6288454112575,1.84392275237588E-6,
4.59415158619139));
#36372=CARTESIAN_POINT('Ctrl Pts',(20.5211545887425,0.00014515264107467,
4.59408556636595));
#36373=CARTESIAN_POINT('Ctrl Pts',(20.5252821244194,-0.0513066296901884,
4.59405895720698));
#36374=CARTESIAN_POINT('Ctrl Pts',(20.5294096600964,-0.102795266482965,
4.58743447362686));
#36375=CARTESIAN_POINT('Ctrl Pts',(20.5335371957734,-0.152465997634008,
4.57425651377355));
#36376=CARTESIAN_POINT('Ctrl Pts',(20.5414898351172,-0.248167995557571,
4.5488661670383));
#36377=CARTESIAN_POINT('Ctrl Pts',(20.549442474461,-0.33712141596603,4.49914747145609));
#36378=CARTESIAN_POINT('Ctrl Pts',(20.5573951138048,-0.408848640915227,
4.43107686705031));
#36379=CARTESIAN_POINT('Ctrl Pts',(20.5653477531486,-0.480575865864423,
4.36300626264453));
#36380=CARTESIAN_POINT('Ctrl Pts',(20.5733003924924,-0.535076895354358,
4.27658374941519));
#36381=CARTESIAN_POINT('Ctrl Pts',(20.5812530318362,-0.565476628275392,
4.18243021985824));
#36382=CARTESIAN_POINT('Ctrl Pts',(20.58920567118,-0.595876361196427,4.08827669030129));
#36383=CARTESIAN_POINT('Ctrl Pts',(20.5971583105238,-0.602174797548561,
3.98639214441672));
#36384=CARTESIAN_POINT('Ctrl Pts',(20.6051109498677,-0.58371402745925,3.88920441471463));
#36385=CARTESIAN_POINT('Ctrl Pts',(20.6130635892115,-0.565253257369939,
3.79201668501254));
#36386=CARTESIAN_POINT('Ctrl Pts',(20.6210162285553,-0.522033280839182,
3.69952577149293));
#36387=CARTESIAN_POINT('Ctrl Pts',(20.6289688678991,-0.459278917219465,
3.62305528060961));
#36388=CARTESIAN_POINT('Ctrl Pts',(20.6369215072429,-0.396524553599749,
3.54658478972629));
#36389=CARTESIAN_POINT('Ctrl Pts',(20.6448741465867,-0.314235802891072,
3.48613472147926));
#36390=CARTESIAN_POINT('Ctrl Pts',(20.6528267859305,-0.222505051509483,
3.44908779917463));
#36391=CARTESIAN_POINT('Ctrl Pts',(20.6607794252743,-0.130774300127894,
3.41204087687));
#36392=CARTESIAN_POINT('Ctrl Pts',(20.6687320646181,-0.029601548073392,
3.39839710050778));
#36393=CARTESIAN_POINT('Ctrl Pts',(20.6766847039619,0.0686601223983595,
3.40982890848785));
#36394=CARTESIAN_POINT('Ctrl Pts',(20.6846373433057,0.1669217928701,3.42126071646792));
#36395=CARTESIAN_POINT('Ctrl Pts',(20.6925899826495,0.262272381759091,3.45776810879028));
#36396=CARTESIAN_POINT('Ctrl Pts',(20.7005426219933,0.343045155251024,3.51488528173127));
#36397=CARTESIAN_POINT('Ctrl Pts',(20.7084952613371,0.423817928742975,3.57200245467228));
#36398=CARTESIAN_POINT('Ctrl Pts',(20.7164479006809,0.490012886837861,3.64972940823193));
#36399=CARTESIAN_POINT('Ctrl Pts',(20.7244005400247,0.533541468465666,3.73856417004634));
#36400=CARTESIAN_POINT('Ctrl Pts',(20.7323531793686,0.577070050093471,3.82739893186076));
#36401=CARTESIAN_POINT('Ctrl Pts',(20.7403058187123,0.597932255254196,3.92734150192994));
#36402=CARTESIAN_POINT('Ctrl Pts',(20.7482584580562,0.593574919799613,4.02617190099588));
#36403=CARTESIAN_POINT('Ctrl Pts',(20.7562110974,0.589217584345031,4.1250023000618));
#36404=CARTESIAN_POINT('Ctrl Pts',(20.7641637367438,0.559640708275147,4.22272052812447));
#36405=CARTESIAN_POINT('Ctrl Pts',(20.7721163760876,0.508461778515953,4.30737953925928));
#36406=CARTESIAN_POINT('Ctrl Pts',(20.7800690154314,0.457282848756759,4.39203855039408));
#36407=CARTESIAN_POINT('Ctrl Pts',(20.7880216547752,0.384501865308254,4.46363834460102));
#36408=CARTESIAN_POINT('Ctrl Pts',(20.795974294119,0.299016600344635,4.51342469267633));
#36409=CARTESIAN_POINT('Ctrl Pts',(20.8039269334628,0.213531335381016,4.56321104075164));
#36410=CARTESIAN_POINT('Ctrl Pts',(20.8118795728066,0.115341788902283,4.59118394269532));
#36411=CARTESIAN_POINT('Ctrl Pts',(20.8198322121504,0.0164533379892873,
4.59392342516246));
#36412=CARTESIAN_POINT('Ctrl Pts',(20.8202730043478,0.0109722321971217,
4.59407526688998));
#36413=CARTESIAN_POINT('Ctrl Pts',(20.8207137965451,0.00548897925183007,
4.59414958726715));
#36414=CARTESIAN_POINT('Ctrl Pts',(20.8211545887425,5.65245430726296E-6,
4.59414685459231));
#36415=CARTESIAN_POINT('Origin',(4.,0.,4.));
#36416=CARTESIAN_POINT('',(21.2288454112575,1.28243205298473E-5,4.59412621697841));
#36417=CARTESIAN_POINT('',(21.1211545887425,-1.09306879613159E-5,4.5940621922514));
#36418=CARTESIAN_POINT('',(4.,-7.27562663373442E-17,4.5941));
#36419=CARTESIAN_POINT('Ctrl Pts',(21.2288454112575,1.28243205298473E-5,
4.59412621697841));
#36420=CARTESIAN_POINT('Ctrl Pts',(21.2276894108138,0.0143945780386088,
4.59413985249388));
#36421=CARTESIAN_POINT('Ctrl Pts',(21.2265334103701,0.028775363636007,4.59362827285675));
#36422=CARTESIAN_POINT('Ctrl Pts',(21.2253774099263,0.043117441953227,4.59258471957415));
#36423=CARTESIAN_POINT('Ctrl Pts',(21.2174247705826,0.141782954511012,4.58540565408365));
#36424=CARTESIAN_POINT('Ctrl Pts',(21.2094721312387,0.238616577754522,4.55305001116024));
#36425=CARTESIAN_POINT('Ctrl Pts',(21.2015194918949,0.321779082392626,4.49947370882601));
#36426=CARTESIAN_POINT('Ctrl Pts',(21.1935668525511,0.404941587030731,4.44589740649178));
#36427=CARTESIAN_POINT('Ctrl Pts',(21.1856142132073,0.474432973063433,4.37110044474674));
#36428=CARTESIAN_POINT('Ctrl Pts',(21.1776615738635,0.521756972098598,4.28422777087894));
#36429=CARTESIAN_POINT('Ctrl Pts',(21.1697089345197,0.569080971133768,4.19735509701114));
#36430=CARTESIAN_POINT('Ctrl Pts',(21.1617562951759,0.594237583171398,4.09840671102057));
#36431=CARTESIAN_POINT('Ctrl Pts',(21.1538036558321,0.594151069756079,3.9994804007435));
#36432=CARTESIAN_POINT('Ctrl Pts',(21.1458510164883,0.59406455634076,3.90055409046644));
#36433=CARTESIAN_POINT('Ctrl Pts',(21.1378983771445,0.568734917472505,3.80164985590287));
#36434=CARTESIAN_POINT('Ctrl Pts',(21.1299457378007,0.521259046500119,3.71486008677882));
#36435=CARTESIAN_POINT('Ctrl Pts',(21.1219930984569,0.473783175527722,3.62807031765475));
#36436=CARTESIAN_POINT('Ctrl Pts',(21.114040459113,0.40416107245118,3.5533950139702));
#36437=CARTESIAN_POINT('Ctrl Pts',(21.1060878197692,0.320904987578411,3.49996424865404));
#36438=CARTESIAN_POINT('Ctrl Pts',(21.0981351804254,0.237648902705652,3.44653348333788));
#36439=CARTESIAN_POINT('Ctrl Pts',(21.0901825410817,0.140758836036697,3.41434725639011));
#36440=CARTESIAN_POINT('Ctrl Pts',(21.0822299017378,0.042080917889342,3.40734077242984));
#36441=CARTESIAN_POINT('Ctrl Pts',(21.074277262394,-0.056597000258024,3.40033428846957));
#36442=CARTESIAN_POINT('Ctrl Pts',(21.0663246230502,-0.157062769883762,
3.41850754749682));
#36443=CARTESIAN_POINT('Ctrl Pts',(21.0583719837064,-0.247033082431791,
3.45963862106718));
#36444=CARTESIAN_POINT('Ctrl Pts',(21.0504193443626,-0.337003394979799,
3.50076969463752));
#36445=CARTESIAN_POINT('Ctrl Pts',(21.0424667050188,-0.416478250450111,
3.56485858275095));
#36446=CARTESIAN_POINT('Ctrl Pts',(21.034514065675,-0.475740765152555,3.644069545988));
#36447=CARTESIAN_POINT('Ctrl Pts',(21.0265614263312,-0.535003279855012,
3.72328050922507));
#36448=CARTESIAN_POINT('Ctrl Pts',(21.0186087869874,-0.574053453789596,
3.81761354758578));
#36449=CARTESIAN_POINT('Ctrl Pts',(21.0106561476436,-0.588116871685884,
3.91553516229212));
#36450=CARTESIAN_POINT('Ctrl Pts',(21.0027035082998,-0.60218028958217,4.01345677699845));
#36451=CARTESIAN_POINT('Ctrl Pts',(20.994750868956,-0.591256951440166,4.11496696805043));
#36452=CARTESIAN_POINT('Ctrl Pts',(20.9867982296121,-0.556682383467722,
4.20765473214191));
#36453=CARTESIAN_POINT('Ctrl Pts',(20.9788455902683,-0.522107815495282,
4.30034249623339));
#36454=CARTESIAN_POINT('Ctrl Pts',(20.9708929509246,-0.463882017692404,
4.38420783336438));
#36455=CARTESIAN_POINT('Ctrl Pts',(20.9629403115808,-0.389123888092725,
4.4489970636758));
#36456=CARTESIAN_POINT('Ctrl Pts',(20.9549876722369,-0.314365758493028,
4.51378629398723));
#36457=CARTESIAN_POINT('Ctrl Pts',(20.9470350328931,-0.223075297096518,
4.5594994174791));
#36458=CARTESIAN_POINT('Ctrl Pts',(20.9390823935493,-0.12641400383229,4.58054738252877));
#36459=CARTESIAN_POINT('Ctrl Pts',(20.9356700661187,-0.0849384674446181,
4.58957866703598));
#36460=CARTESIAN_POINT('Ctrl Pts',(20.9322577386881,-0.0424741039190781,
4.59406883414683));
#36461=CARTESIAN_POINT('Ctrl Pts',(20.9288454112575,-6.4040329070536E-6,
4.59405282094147));
#36462=CARTESIAN_POINT('Ctrl Pts',(20.8211545887425,5.65245430726296E-6,
4.59414685459231));
#36463=CARTESIAN_POINT('Ctrl Pts',(20.8286664358889,-0.0934395423672534,
4.59410028517524));
#36464=CARTESIAN_POINT('Ctrl Pts',(20.8361782830354,-0.18690618531264,4.57167601133058));
#36465=CARTESIAN_POINT('Ctrl Pts',(20.8436901301818,-0.270133012248912,
4.529191754035));
#36466=CARTESIAN_POINT('Ctrl Pts',(20.8516427695256,-0.358243556226857,
4.4842145374498));
#36467=CARTESIAN_POINT('Ctrl Pts',(20.8595954088694,-0.434877288835492,
4.41675404128879));
#36468=CARTESIAN_POINT('Ctrl Pts',(20.8675480482133,-0.490664589397756,
4.33505825661903));
#36469=CARTESIAN_POINT('Ctrl Pts',(20.8755006875571,-0.546451889960021,
4.25336247194927));
#36470=CARTESIAN_POINT('Ctrl Pts',(20.8834533269009,-0.581392758475918,
4.15743139877076));
#36471=CARTESIAN_POINT('Ctrl Pts',(20.8914059662447,-0.591215252505097,
4.05899390323763));
#36472=CARTESIAN_POINT('Ctrl Pts',(20.8993586055885,-0.601037746534278,
3.96055640770449));
#36473=CARTESIAN_POINT('Ctrl Pts',(20.9073112449323,-0.585741866076735,
3.85961248981672));
#36474=CARTESIAN_POINT('Ctrl Pts',(20.9152638842761,-0.547197711916726,
3.76850392583047));
#36475=CARTESIAN_POINT('Ctrl Pts',(20.9232165236199,-0.508653557756717,
3.67739536184422));
#36476=CARTESIAN_POINT('Ctrl Pts',(20.9311691629637,-0.446861129894262,
3.59612215175949));
#36477=CARTESIAN_POINT('Ctrl Pts',(20.9391218023075,-0.369375409551539,
3.53462104847409));
#36478=CARTESIAN_POINT('Ctrl Pts',(20.9470744416513,-0.291889689208826,
3.4731199451887));
#36479=CARTESIAN_POINT('Ctrl Pts',(20.9550270809951,-0.198710676385865,
3.43139094870266));
#36480=CARTESIAN_POINT('Ctrl Pts',(20.9629797203389,-0.101230766359376,
3.41453599926792));
#36481=CARTESIAN_POINT('Ctrl Pts',(20.9709323596827,-0.00375085633288601,
3.39768104983318));
#36482=CARTESIAN_POINT('Ctrl Pts',(20.9788849990265,0.0980299508971346,
3.40570014744973));
#36483=CARTESIAN_POINT('Ctrl Pts',(20.9868376383704,0.191667561123074,3.43761284710704));
#36484=CARTESIAN_POINT('Ctrl Pts',(20.9947902777142,0.285305171349014,3.46952554676435));
#36485=CARTESIAN_POINT('Ctrl Pts',(21.002742917058,0.37079958457088,3.52533184846243));
#36486=CARTESIAN_POINT('Ctrl Pts',(21.0106955564018,0.437697946637459,3.59820867233944));
#36487=CARTESIAN_POINT('Ctrl Pts',(21.0186481957456,0.504596308704037,3.67108549621644));
#36488=CARTESIAN_POINT('Ctrl Pts',(21.0266008350894,0.552898619615334,3.76103284227238));
#36489=CARTESIAN_POINT('Ctrl Pts',(21.0345534744332,0.576699262792956,3.8570534220826));
#36490=CARTESIAN_POINT('Ctrl Pts',(21.042506113777,0.600499905970578,3.95307400189282));
#36491=CARTESIAN_POINT('Ctrl Pts',(21.0504587531208,0.599798881414527,4.05516781545734));
#36492=CARTESIAN_POINT('Ctrl Pts',(21.0584113924646,0.574681899562831,4.15085250374278));
#36493=CARTESIAN_POINT('Ctrl Pts',(21.0663640318084,0.549564917711138,4.24653719202821));
#36494=CARTESIAN_POINT('Ctrl Pts',(21.0743166711522,0.500031978563804,4.33581275503458));
#36495=CARTESIAN_POINT('Ctrl Pts',(21.082269310496,0.432139158218639,4.40776403918836));
#36496=CARTESIAN_POINT('Ctrl Pts',(21.0902219498398,0.364246337873458,4.47971532334216));
#36497=CARTESIAN_POINT('Ctrl Pts',(21.0981745891836,0.277993636330433,4.53434232864337));
#36498=CARTESIAN_POINT('Ctrl Pts',(21.1061272285274,0.183926621270441,4.56496615973523));
#36499=CARTESIAN_POINT('Ctrl Pts',(21.1111363485991,0.124676735433976,4.5842551580617));
#36500=CARTESIAN_POINT('Ctrl Pts',(21.1161454686708,0.0623266393968894,
4.59402126159141));
#36501=CARTESIAN_POINT('Ctrl Pts',(21.1211545887425,-1.09306879613159E-5,
4.5940621922514));
#36502=CARTESIAN_POINT('Origin',(4.,0.,4.));
#36503=CARTESIAN_POINT('',(21.5288454112575,-1.51073027558624E-5,4.59408477831653));
#36504=CARTESIAN_POINT('',(21.4211545887425,1.51733402061755E-5,4.59410821609125));
#36505=CARTESIAN_POINT('',(4.,-7.27562663373442E-17,4.5941));
#36506=CARTESIAN_POINT('Ctrl Pts',(21.5288454112575,-1.51073027558624E-5,
4.59408477831653));
#36507=CARTESIAN_POINT('Ctrl Pts',(21.5231210829395,0.0712153309254728,
4.59401644885886));
#36508=CARTESIAN_POINT('Ctrl Pts',(21.5173967546214,0.142469702059594,4.58119587380047));
#36509=CARTESIAN_POINT('Ctrl Pts',(21.5116724263034,0.209120766622247,4.55613331912479));
#36510=CARTESIAN_POINT('Ctrl Pts',(21.5037197869596,0.301717111362981,4.52131465616629));
#36511=CARTESIAN_POINT('Ctrl Pts',(21.4957671476158,0.385428743083265,4.46286809139133));
#36512=CARTESIAN_POINT('Ctrl Pts',(21.4878145082719,0.450020774675764,4.38793951336988));
#36513=CARTESIAN_POINT('Ctrl Pts',(21.4798618689281,0.514612806268249,4.31301093534845));
#36514=CARTESIAN_POINT('Ctrl Pts',(21.4719092295843,0.560085237732952,4.22160034408054));
#36515=CARTESIAN_POINT('Ctrl Pts',(21.4639565902405,0.58087844500124,4.1248839293359));
#36516=CARTESIAN_POINT('Ctrl Pts',(21.4560039508967,0.601671652269532,4.02816751459124));
#36517=CARTESIAN_POINT('Ctrl Pts',(21.4480513115529,0.597785635341394,3.92614527636987));
#36518=CARTESIAN_POINT('Ctrl Pts',(21.4400986722091,0.569695512712777,3.83129082280931));
#36519=CARTESIAN_POINT('Ctrl Pts',(21.4321460328653,0.541605390084162,3.73643636924876));
#36520=CARTESIAN_POINT('Ctrl Pts',(21.4241933935215,0.489311161755075,3.64874970034904));
#36521=CARTESIAN_POINT('Ctrl Pts',(21.4162407541777,0.419206509371839,3.57895170565158));
#36522=CARTESIAN_POINT('Ctrl Pts',(21.4082881148339,0.349101856988603,3.50915371095413));
#36523=CARTESIAN_POINT('Ctrl Pts',(21.4003354754901,0.261186780551223,3.45724439045894));
#36524=CARTESIAN_POINT('Ctrl Pts',(21.3923828361463,0.16621009553345,3.42957036558731));
#36525=CARTESIAN_POINT('Ctrl Pts',(21.3844301968025,0.0712334105156764,
3.40189634071567));
#36526=CARTESIAN_POINT('Ctrl Pts',(21.3764775574587,-0.0308048830825163,
3.3984576114676));
#36527=CARTESIAN_POINT('Ctrl Pts',(21.3685249181149,-0.127429214135013,
3.41967460932821));
#36528=CARTESIAN_POINT('Ctrl Pts',(21.360572278771,-0.22405354518751,3.44089160718882));
#36529=CARTESIAN_POINT('Ctrl Pts',(21.3526196394272,-0.315263913694308,
3.4867643321581));
#36530=CARTESIAN_POINT('Ctrl Pts',(21.3446670000834,-0.389908609845283,
3.5516842188346));
#36531=CARTESIAN_POINT('Ctrl Pts',(21.3367143607396,-0.464553305996249,
3.6166041055111));
#36532=CARTESIAN_POINT('Ctrl Pts',(21.3287617213958,-0.522632329791381,
3.70057115389483));
#36533=CARTESIAN_POINT('Ctrl Pts',(21.320809082052,-0.557044729551177,3.79331924871262));
#36534=CARTESIAN_POINT('Ctrl Pts',(21.3128564427082,-0.591457129310977,
3.88606734353042));
#36535=CARTESIAN_POINT('Ctrl Pts',(21.3049038033644,-0.602202905035458,
3.9875964847823));
#36536=CARTESIAN_POINT('Ctrl Pts',(21.2969511640206,-0.587968239287942,
4.08549335215105));
#36537=CARTESIAN_POINT('Ctrl Pts',(21.2889985246768,-0.573733573540424,
4.18339021951981));
#36538=CARTESIAN_POINT('Ctrl Pts',(21.281045885333,-0.534518466320906,4.27765481300544));
#36539=CARTESIAN_POINT('Ctrl Pts',(21.2730932459892,-0.47511749858569,4.35676200219639));
#36540=CARTESIAN_POINT('Ctrl Pts',(21.2651406066454,-0.415716530850488,
4.43586919138732));
#36541=CARTESIAN_POINT('Ctrl Pts',(21.2571879673016,-0.336129702599601,
4.49981897628356));
#36542=CARTESIAN_POINT('Ctrl Pts',(21.2492353279577,-0.246087587538132,
4.54079262470289));
#36543=CARTESIAN_POINT('Ctrl Pts',(21.2424386890577,-0.169134048541188,
4.57581031891556));
#36544=CARTESIAN_POINT('Ctrl Pts',(21.2356420501576,-0.0845438791841879,
4.59404604774026));
#36545=CARTESIAN_POINT('Ctrl Pts',(21.2288454112575,1.28243205298473E-5,
4.59412621697841));
#36546=CARTESIAN_POINT('Ctrl Pts',(21.1211545887425,-1.09306879613159E-5,
4.5940621922514));
#36547=CARTESIAN_POINT('Ctrl Pts',(21.1240981080146,-0.0366424819978743,
4.5940862444172));
#36548=CARTESIAN_POINT('Ctrl Pts',(21.1270416272867,-0.0732697079540161,
4.59075208378119));
#36549=CARTESIAN_POINT('Ctrl Pts',(21.1299851465589,-0.109260984540888,
4.58401866488291));
#36550=CARTESIAN_POINT('Ctrl Pts',(21.1379377859027,-0.20650024671525,4.56582668205621));
#36551=CARTESIAN_POINT('Ctrl Pts',(21.1458904252465,-0.299097442487026,
4.52282205952027));
#36552=CARTESIAN_POINT('Ctrl Pts',(21.1538430645903,-0.375731303474415,
4.46026269810429));
#36553=CARTESIAN_POINT('Ctrl Pts',(21.1617957039341,-0.452365164461805,
4.3977033366883));
#36554=CARTESIAN_POINT('Ctrl Pts',(21.1697483432779,-0.513035690664809,
4.31558923639226));
#36555=CARTESIAN_POINT('Ctrl Pts',(21.1777009826217,-0.550325083965727,
4.22395996434209));
#36556=CARTESIAN_POINT('Ctrl Pts',(21.1856536219655,-0.587614477266646,
4.13233069229192));
#36557=CARTESIAN_POINT('Ctrl Pts',(21.1936062613093,-0.601522737665479,
4.03118624848761));
#36558=CARTESIAN_POINT('Ctrl Pts',(21.2015589006531,-0.590349390887683,
3.93289291874755));
#36559=CARTESIAN_POINT('Ctrl Pts',(21.2095115399969,-0.579176044109886,
3.83459958900749));
#36560=CARTESIAN_POINT('Ctrl Pts',(21.2174641793407,-0.542921090155459,
3.73915737333167));
#36561=CARTESIAN_POINT('Ctrl Pts',(21.2254168186845,-0.486017190935348,
3.65823538248142));
#36562=CARTESIAN_POINT('Ctrl Pts',(21.2333694580283,-0.429113291715238,
3.57731339163117));
#36563=CARTESIAN_POINT('Ctrl Pts',(21.2413220973721,-0.351560447229444,
3.51091162560648));
#36564=CARTESIAN_POINT('Ctrl Pts',(21.249274736716,-0.262840548960938,3.46714860467879));
#36565=CARTESIAN_POINT('Ctrl Pts',(21.2572273760598,-0.174120650692433,
3.4233855837511));
#36566=CARTESIAN_POINT('Ctrl Pts',(21.2651800154036,-0.0742336986412151,
3.40226130792041));
#36567=CARTESIAN_POINT('Ctrl Pts',(21.2731326547474,0.0246077668693877,
3.40635850761334));
#36568=CARTESIAN_POINT('Ctrl Pts',(21.2810852940912,0.123449232380002,3.41045570730627));
#36569=CARTESIAN_POINT('Ctrl Pts',(21.289037933435,0.221245211350001,3.43977438252282));
#36570=CARTESIAN_POINT('Ctrl Pts',(21.2969905727788,0.306038813396919,3.49072992590572));
#36571=CARTESIAN_POINT('Ctrl Pts',(21.3049432121226,0.390832415443818,3.54168546928862));
#36572=CARTESIAN_POINT('Ctrl Pts',(21.3128958514664,0.462623640567642,3.61427788083785));
#36573=CARTESIAN_POINT('Ctrl Pts',(21.3208484908102,0.512635033719562,3.69963174955258));
#36574=CARTESIAN_POINT('Ctrl Pts',(21.328801130154,0.562646426871494,3.78498561826733));
#36575=CARTESIAN_POINT('Ctrl Pts',(21.3367537694978,0.590877988051513,3.88310094414759));
#36576=CARTESIAN_POINT('Ctrl Pts',(21.3447064088416,0.59387802439953,3.98198179230066));
#36577=CARTESIAN_POINT('Ctrl Pts',(21.3526590481854,0.596878060747546,4.08086264045372));
#36578=CARTESIAN_POINT('Ctrl Pts',(21.3606116875293,0.574646572263566,4.1805090108796));
#36579=CARTESIAN_POINT('Ctrl Pts',(21.3685643268731,0.529901661201384,4.26873777763737));
#36580=CARTESIAN_POINT('Ctrl Pts',(21.3765169662169,0.485156750139203,4.35696654439514));
#36581=CARTESIAN_POINT('Ctrl Pts',(21.3844696055607,0.417898416498819,4.4337777074848));
#36582=CARTESIAN_POINT('Ctrl Pts',(21.3924222449045,0.336349907607971,4.48978005607163));
#36583=CARTESIAN_POINT('Ctrl Pts',(21.4003748842483,0.254801398717122,4.54578240465847));
#36584=CARTESIAN_POINT('Ctrl Pts',(21.4083275235921,0.158962714575808,4.58097593874246));
#36585=CARTESIAN_POINT('Ctrl Pts',(21.4162801629359,0.0605514396169286,
4.59105776945554));
#36586=CARTESIAN_POINT('Ctrl Pts',(21.4179049715381,0.0404449719157324,
4.59311759444699));
#36587=CARTESIAN_POINT('Ctrl Pts',(21.4195297801403,0.0202311170044278,
4.59412918598148));
#36588=CARTESIAN_POINT('Ctrl Pts',(21.4211545887425,1.51733402061755E-5,
4.59410821609125));
#36589=CARTESIAN_POINT('Origin',(4.,0.,4.));
#36590=CARTESIAN_POINT('',(21.8288454112575,1.47252919898561E-5,4.59408074293421));
#36591=CARTESIAN_POINT('',(21.7211545887425,-1.54601956517634E-5,4.59410286710644));
#36592=CARTESIAN_POINT('',(4.,-7.27562663373442E-17,4.5941));
#36593=CARTESIAN_POINT('Ctrl Pts',(21.8288454112575,1.47252919898561E-5,
4.59408074293421));
#36594=CARTESIAN_POINT('Ctrl Pts',(21.826505394409,0.0291331941223908,4.59410767674242));
#36595=CARTESIAN_POINT('Ctrl Pts',(21.8241653775604,0.0582478076928112,
4.59200528777341));
#36596=CARTESIAN_POINT('Ctrl Pts',(21.8218253607118,0.0870422430987805,
4.58774093918134));
#36597=CARTESIAN_POINT('Ctrl Pts',(21.813872721368,0.184901264939656,4.57324838268129));
#36598=CARTESIAN_POINT('Ctrl Pts',(21.8059200820242,0.279062206656402,4.53378504179028));
#36599=CARTESIAN_POINT('Ctrl Pts',(21.7979674426804,0.358012610677869,4.47417584741217));
#36600=CARTESIAN_POINT('Ctrl Pts',(21.7900148033366,0.436963014699336,4.41456665303406));
#36601=CARTESIAN_POINT('Ctrl Pts',(21.7820621639928,0.500702881025523,4.33481160516884));
#36602=CARTESIAN_POINT('Ctrl Pts',(21.774109524649,0.541439142878506,4.24466184465998));
#36603=CARTESIAN_POINT('Ctrl Pts',(21.7661568853052,0.58217540473149,4.15451208415111));
#36604=CARTESIAN_POINT('Ctrl Pts',(21.7582042459614,0.599908062111268,4.0539676109986));
#36605=CARTESIAN_POINT('Ctrl Pts',(21.7502516066176,0.59246905613922,3.95532135643358));
#36606=CARTESIAN_POINT('Ctrl Pts',(21.7422989672738,0.585030050167171,3.85667510186855));
#36607=CARTESIAN_POINT('Ctrl Pts',(21.73434632793,0.552419380843296,3.759927065891));
#36608=CARTESIAN_POINT('Ctrl Pts',(21.7263936885861,0.498624146640836,3.67690601358098));
#36609=CARTESIAN_POINT('Ctrl Pts',(21.7184410492423,0.444828912438376,3.59388496127097));
#36610=CARTESIAN_POINT('Ctrl Pts',(21.7104884098985,0.369849113357332,3.52459089262848));
#36611=CARTESIAN_POINT('Ctrl Pts',(21.7025357705547,0.28285205103972,3.47749595131133));
#36612=CARTESIAN_POINT('Ctrl Pts',(21.6945831312109,0.195854988722108,3.43040100999418));
#36613=CARTESIAN_POINT('Ctrl Pts',(21.6866304918671,0.0968406631679286,
3.40550519600236));
#36614=CARTESIAN_POINT('Ctrl Pts',(21.6786778525233,-0.00208507577578169,
3.40585236167057));
#36615=CARTESIAN_POINT('Ctrl Pts',(21.6707252131795,-0.101010814719503,
3.40619952733877));
#36616=CARTESIAN_POINT('Ctrl Pts',(21.6627725738357,-0.199847967052756,
3.431789672667));
#36617=CARTESIAN_POINT('Ctrl Pts',(21.6548199344919,-0.28651234476781,3.47949405385809));
#36618=CARTESIAN_POINT('Ctrl Pts',(21.6468672951481,-0.373176722482865,
3.52719843504918));
#36619=CARTESIAN_POINT('Ctrl Pts',(21.6389146558043,-0.44766832557972,3.59701705210314));
#36620=CARTESIAN_POINT('Ctrl Pts',(21.6309620164605,-0.500879541024521,
3.68041362817464));
#36621=CARTESIAN_POINT('Ctrl Pts',(21.6230093771167,-0.55409075646931,3.76381020424612));
#36622=CARTESIAN_POINT('Ctrl Pts',(21.6150567377728,-0.586021584262053,
3.86078473933514));
#36623=CARTESIAN_POINT('Ctrl Pts',(21.607104098429,-0.592768045815946,3.95948077576042));
#36624=CARTESIAN_POINT('Ctrl Pts',(21.5991514590852,-0.599514507369841,
4.05817681218572));
#36625=CARTESIAN_POINT('Ctrl Pts',(21.5911988197414,-0.581076602684875,
4.15859434994728));
#36626=CARTESIAN_POINT('Ctrl Pts',(21.5832461803976,-0.539708616728004,
4.24845597739434));
#36627=CARTESIAN_POINT('Ctrl Pts',(21.5752935410538,-0.498340630771147,
4.33831760484137));
#36628=CARTESIAN_POINT('Ctrl Pts',(21.56734090171,-0.434042563542403,4.41762332197391));
#36629=CARTESIAN_POINT('Ctrl Pts',(21.5593882623662,-0.354675729482573,
4.47667692475034));
#36630=CARTESIAN_POINT('Ctrl Pts',(21.5514356230224,-0.275308895422716,
4.53573052752678));
#36631=CARTESIAN_POINT('Ctrl Pts',(21.5434829836786,-0.180873294531764,
4.57453201594709));
#36632=CARTESIAN_POINT('Ctrl Pts',(21.5355303443348,-0.0829149652056982,
4.58833737958621));
#36633=CARTESIAN_POINT('Ctrl Pts',(21.533302033309,-0.055467269432644,4.59220561033096));
#36634=CARTESIAN_POINT('Ctrl Pts',(21.5310737222833,-0.0277430016607059,
4.5941113769453));
#36635=CARTESIAN_POINT('Ctrl Pts',(21.5288454112575,-1.51073027558624E-5,
4.59408477831653));
#36636=CARTESIAN_POINT('Ctrl Pts',(21.4211545887425,1.51733402061755E-5,
4.59410821609125));
#36637=CARTESIAN_POINT('Ctrl Pts',(21.4274824194841,-0.0787159889745399,
4.59402654867773));
#36638=CARTESIAN_POINT('Ctrl Pts',(21.4338102502257,-0.15747883181342,4.57828382012605));
#36639=CARTESIAN_POINT('Ctrl Pts',(21.4401380809673,-0.230053504748576,
4.54780575811717));
#36640=CARTESIAN_POINT('Ctrl Pts',(21.4480907203111,-0.321263308378747,
4.50950178872359));
#36641=CARTESIAN_POINT('Ctrl Pts',(21.4560433596549,-0.402699049862651,
4.44792372259427));
#36642=CARTESIAN_POINT('Ctrl Pts',(21.4639959989987,-0.464404100671371,
4.37060031698995));
#36643=CARTESIAN_POINT('Ctrl Pts',(21.4719486383425,-0.526109151480106,
4.2932769113856));
#36644=CARTESIAN_POINT('Ctrl Pts',(21.4799012776864,-0.568083511613643,
4.20020816630624));
#36645=CARTESIAN_POINT('Ctrl Pts',(21.4878539170302,-0.585195243866348,
4.10277300340868));
#36646=CARTESIAN_POINT('Ctrl Pts',(21.495806556374,-0.602306976119048,4.00533784051114));
#36647=CARTESIAN_POINT('Ctrl Pts',(21.5037591957178,-0.594556080490919,
3.90353625979537));
#36648=CARTESIAN_POINT('Ctrl Pts',(21.5117118350616,-0.562890209537588,
3.80981489101362));
#36649=CARTESIAN_POINT('Ctrl Pts',(21.5196644744054,-0.53122433858425,3.71609352223184));
#36650=CARTESIAN_POINT('Ctrl Pts',(21.5276171137492,-0.47564349230572,3.63045236538409));
#36651=CARTESIAN_POINT('Ctrl Pts',(21.535569753093,-0.402943186155437,3.56336221830407));
#36652=CARTESIAN_POINT('Ctrl Pts',(21.5435223924368,-0.330242880005154,
3.49627207122406));
#36653=CARTESIAN_POINT('Ctrl Pts',(21.5514750317806,-0.24042311398314,3.44773293391182));
#36654=CARTESIAN_POINT('Ctrl Pts',(21.5594276711244,-0.144465577806233,
3.42367937699355));
#36655=CARTESIAN_POINT('Ctrl Pts',(21.5673803104682,-0.0485080416293372,
3.39962582007528));
#36656=CARTESIAN_POINT('Ctrl Pts',(21.575332949812,0.0535872647024426,3.40005784355098));
#36657=CARTESIAN_POINT('Ctrl Pts',(21.5832855891558,0.149337799479898,3.42492262666669));
#36658=CARTESIAN_POINT('Ctrl Pts',(21.5912382284996,0.245088334257342,3.44978740978241));
#36659=CARTESIAN_POINT('Ctrl Pts',(21.5991908678434,0.33449409748049,3.49908495253815));
#36660=CARTESIAN_POINT('Ctrl Pts',(21.6071435071872,0.406624016913212,3.56678795891296));
#36661=CARTESIAN_POINT('Ctrl Pts',(21.6150961465311,0.478753936345942,3.63449096528778));
#36662=CARTESIAN_POINT('Ctrl Pts',(21.6230487858749,0.533608011988269,3.72059943528167));
#36663=CARTESIAN_POINT('Ctrl Pts',(21.6310014252187,0.564479585995414,3.81458543566408));
#36664=CARTESIAN_POINT('Ctrl Pts',(21.6389540645625,0.595351160002559,3.90857143604649));
#36665=CARTESIAN_POINT('Ctrl Pts',(21.6469067039063,0.602240232374519,4.0104349668174));
#36666=CARTESIAN_POINT('Ctrl Pts',(21.6548593432501,0.584304520186539,4.10772182398666));
#36667=CARTESIAN_POINT('Ctrl Pts',(21.6628119825939,0.566368807998562,4.2050086811559));
#36668=CARTESIAN_POINT('Ctrl Pts',(21.6707646219377,0.523608311250652,4.29771886472347));
#36669=CARTESIAN_POINT('Ctrl Pts',(21.6787172612815,0.461251083056512,4.37451729206089));
#36670=CARTESIAN_POINT('Ctrl Pts',(21.6866699006253,0.398893854862358,4.45131571939834));
#36671=CARTESIAN_POINT('Ctrl Pts',(21.6946225399691,0.316939895221968,4.51220239050563));
#36672=CARTESIAN_POINT('Ctrl Pts',(21.7025751793129,0.225409191891896,4.54973308058009));
#36673=CARTESIAN_POINT('Ctrl Pts',(21.7087683157894,0.15412944274098,4.5789601931952));
#36674=CARTESIAN_POINT('Ctrl Pts',(21.7149614522659,0.0770418275534371,
4.59402294959611));
#36675=CARTESIAN_POINT('Ctrl Pts',(21.7211545887425,-1.54601956517634E-5,
4.59410286710644));
#36676=CARTESIAN_POINT('Origin',(4.,0.,4.));
#36677=CARTESIAN_POINT('',(22.1288454112575,-1.19684274697274E-5,4.59413016891312));
#36678=CARTESIAN_POINT('',(22.0211545887425,1.20066176157995E-5,4.59406577061205));
#36679=CARTESIAN_POINT('',(4.,-7.27562663373442E-17,4.5941));
#36680=CARTESIAN_POINT('Ctrl Pts',(22.1288454112575,-1.19684274697274E-5,
4.59413016891312));
#36681=CARTESIAN_POINT('Ctrl Pts',(22.1219370665346,0.0859328098890183,
4.59405244111828));
#36682=CARTESIAN_POINT('Ctrl Pts',(22.1150287218117,0.171910584533005,4.57519344187135));
#36683=CARTESIAN_POINT('Ctrl Pts',(22.1081203770888,0.24987714748571,4.53905210772026));
#36684=CARTESIAN_POINT('Ctrl Pts',(22.100167737745,0.339629466009183,4.49744749656716));
#36685=CARTESIAN_POINT('Ctrl Pts',(22.0922150984012,0.418765494330909,4.4329406966096));
#36686=CARTESIAN_POINT('Ctrl Pts',(22.0842624590574,0.477609775176754,4.35341854270704));
#36687=CARTESIAN_POINT('Ctrl Pts',(22.0763098197136,0.536454056022584,4.2738963888045));
#36688=CARTESIAN_POINT('Ctrl Pts',(22.0683571803698,0.575006589392542,4.17935888095698));
#36689=CARTESIAN_POINT('Ctrl Pts',(22.060404541026,0.588553803007579,4.081364517074));
#36690=CARTESIAN_POINT('Ctrl Pts',(22.0524519016822,0.60210101662262,3.983370153191));
#36691=CARTESIAN_POINT('Ctrl Pts',(22.0444992623384,0.590642910482727,3.88191893327255));
#36692=CARTESIAN_POINT('Ctrl Pts',(22.0365466229946,0.55558039411957,3.78941465069146));
#36693=CARTESIAN_POINT('Ctrl Pts',(22.0285939836508,0.520517877756421,3.69691036811039));
#36694=CARTESIAN_POINT('Ctrl Pts',(22.020641344307,0.461850951170019,3.61335302286667));
#36695=CARTESIAN_POINT('Ctrl Pts',(22.0126887049632,0.386752445163155,3.5489586384446));
#36696=CARTESIAN_POINT('Ctrl Pts',(22.0047360656194,0.311653939156274,3.48456425402251));
#36697=CARTESIAN_POINT('Ctrl Pts',(21.9967834262756,0.220123853728924,3.43933283042207));
#36698=CARTESIAN_POINT('Ctrl Pts',(21.9888307869318,0.123352988439278,3.41879452521803));
#36699=CARTESIAN_POINT('Ctrl Pts',(21.980878147588,0.0265821231496428,3.398256220014));
#36700=CARTESIAN_POINT('Ctrl Pts',(21.9729255082441,-0.075429522002288,
3.40241103320635));
#36701=CARTESIAN_POINT('Ctrl Pts',(21.9649728689003,-0.170209634025949,
3.43075098229493));
#36702=CARTESIAN_POINT('Ctrl Pts',(21.9570202295565,-0.26498974604961,3.4590909313835));
#36703=CARTESIAN_POINT('Ctrl Pts',(21.9490675902127,-0.352538324945002,
3.5116160163683));
#36704=CARTESIAN_POINT('Ctrl Pts',(21.9411149508689,-0.422151364554475,
3.58190433023263));
#36705=CARTESIAN_POINT('Ctrl Pts',(21.9331623115251,-0.491764404163956,
3.65219264409696));
#36706=CARTESIAN_POINT('Ctrl Pts',(21.9252096721813,-0.543441904487514,
3.74024418684083));
#36707=CARTESIAN_POINT('Ctrl Pts',(21.9172570328375,-0.570865587277161,
3.83529345812586));
#36708=CARTESIAN_POINT('Ctrl Pts',(21.9093043934937,-0.598289270066803,
3.93034272941087));
#36709=CARTESIAN_POINT('Ctrl Pts',(21.9013517541499,-0.601459135322544,
4.03238972923704));
#36710=CARTESIAN_POINT('Ctrl Pts',(21.8933991148061,-0.579987623844179,
4.12895782202339));
#36711=CARTESIAN_POINT('Ctrl Pts',(21.8854464754623,-0.558516112365809,
4.22552591480976));
#36712=CARTESIAN_POINT('Ctrl Pts',(21.8774938361185,-0.512403224153321,
4.31661510055631));
#36713=CARTESIAN_POINT('Ctrl Pts',(21.8695411967747,-0.447286887835617,
4.39108848569571));
#36714=CARTESIAN_POINT('Ctrl Pts',(21.8615885574308,-0.38217055151792,4.46556187083511));
#36715=CARTESIAN_POINT('Ctrl Pts',(21.853635918087,-0.298050767095013,4.52341945536736));
#36716=CARTESIAN_POINT('Ctrl Pts',(21.8456832787432,-0.205212323901057,
4.55758736157894));
#36717=CARTESIAN_POINT('Ctrl Pts',(21.840070656248,-0.139691040693493,4.58170156451555));
#36718=CARTESIAN_POINT('Ctrl Pts',(21.8344580337528,-0.0698270680627233,
4.59401614113532));
#36719=CARTESIAN_POINT('Ctrl Pts',(21.8288454112575,1.47252919898561E-5,
4.59408074293421));
#36720=CARTESIAN_POINT('Ctrl Pts',(21.7211545887425,-1.54601956517634E-5,
4.59410286710644));
#36721=CARTESIAN_POINT('Ctrl Pts',(21.7229140916097,-0.0219078436841643,
4.59412557209431));
#36722=CARTESIAN_POINT('Ctrl Pts',(21.724673594477,-0.0437977792686499,
4.59293892497318));
#36723=CARTESIAN_POINT('Ctrl Pts',(21.7264330973443,-0.0655513867134097,
4.59052415646896));
#36724=CARTESIAN_POINT('Ctrl Pts',(21.7343857366881,-0.163873814968881,
4.57960983324176));
#36725=CARTESIAN_POINT('Ctrl Pts',(21.742338376032,-0.259411224460086,4.54360647774573));
#36726=CARTESIAN_POINT('Ctrl Pts',(21.7502910153758,-0.340482865683332,
4.48691599054611));
#36727=CARTESIAN_POINT('Ctrl Pts',(21.7582436547196,-0.421554506906578,
4.4302255033465));
#36728=CARTESIAN_POINT('Ctrl Pts',(21.7661962940634,-0.488160379861865,
4.3528478844433));
#36729=CARTESIAN_POINT('Ctrl Pts',(21.7741489334072,-0.532157009426634,
4.26424360160945));
#36730=CARTESIAN_POINT('Ctrl Pts',(21.782101572751,-0.576153638991403,4.1756393187756));
#36731=CARTESIAN_POINT('Ctrl Pts',(21.7900542120948,-0.597541025165654,
4.0758083720111));
#36732=CARTESIAN_POINT('Ctrl Pts',(21.7980068514386,-0.593704268699233,
3.9769564542281));
#36733=CARTESIAN_POINT('Ctrl Pts',(21.8059594907824,-0.589867512232813,
3.87810453644509));
#36734=CARTESIAN_POINT('Ctrl Pts',(21.8139121301262,-0.560806613125721,
3.78023164764359));
#36735=CARTESIAN_POINT('Ctrl Pts',(21.82186476947,-0.510074662095298,3.69530408148155));
#36736=CARTESIAN_POINT('Ctrl Pts',(21.8298174088138,-0.459342711064876,
3.61037651531951));
#36737=CARTESIAN_POINT('Ctrl Pts',(21.8377700481576,-0.386939708111122,
3.53839427179695));
#36738=CARTESIAN_POINT('Ctrl Pts',(21.8457226875014,-0.301717906454235,
3.48815816056295));
#36739=CARTESIAN_POINT('Ctrl Pts',(21.8536753268452,-0.216496104797349,
3.43792204932895));
#36740=CARTESIAN_POINT('Ctrl Pts',(21.8616279661891,-0.118455504437329,
3.40943207038352));
#36741=CARTESIAN_POINT('Ctrl Pts',(21.8695806055329,-0.0195829040543552,
3.40617151167847));
#36742=CARTESIAN_POINT('Ctrl Pts',(21.8775332448767,0.0792896963286298,
3.40291095297342));
#36743=CARTESIAN_POINT('Ctrl Pts',(21.8854858842205,0.178994296734569,3.42487981450875));
#36744=CARTESIAN_POINT('Ctrl Pts',(21.8934385235643,0.267340651814441,3.46939210375187));
#36745=CARTESIAN_POINT('Ctrl Pts',(21.9013911629081,0.355687006894294,3.51390439299499));
#36746=CARTESIAN_POINT('Ctrl Pts',(21.9093438022519,0.432675116648084,3.58096010994589));
#36747=CARTESIAN_POINT('Ctrl Pts',(21.9172964415957,0.488892136101412,3.66236077992681));
#36748=CARTESIAN_POINT('Ctrl Pts',(21.9252490809395,0.545109155554752,3.74376144990775));
#36749=CARTESIAN_POINT('Ctrl Pts',(21.9332017202833,0.580555084707621,3.8395070729187));
#36750=CARTESIAN_POINT('Ctrl Pts',(21.9411543596271,0.590896175957217,3.93789144251738));
#36751=CARTESIAN_POINT('Ctrl Pts',(21.9491069989709,0.601237267206812,4.03627581211605));
#36752=CARTESIAN_POINT('Ctrl Pts',(21.9570596383147,0.58647352055314,4.13729892830245));
#36753=CARTESIAN_POINT('Ctrl Pts',(21.9650122776585,0.548410005102802,4.22860933921557));
#36754=CARTESIAN_POINT('Ctrl Pts',(21.9729649170023,0.510346489652465,4.31991975012869));
#36755=CARTESIAN_POINT('Ctrl Pts',(21.9809175563462,0.448983205405461,4.40151745576853));
#36756=CARTESIAN_POINT('Ctrl Pts',(21.98887019569,0.371822649612145,4.46342602528218));
#36757=CARTESIAN_POINT('Ctrl Pts',(21.9968228350338,0.29466209381883,4.52533459479583));
#36758=CARTESIAN_POINT('Ctrl Pts',(22.0047754743776,0.201704266479203,4.5675540281833));
#36759=CARTESIAN_POINT('Ctrl Pts',(22.0127281137214,0.104314528045707,4.58492242469582));
#36760=CARTESIAN_POINT('Ctrl Pts',(22.0155369387284,0.069917050565085,4.59105683924014));
#36761=CARTESIAN_POINT('Ctrl Pts',(22.0183457637354,0.0349667096964542,
4.59409118517947));
#36762=CARTESIAN_POINT('Ctrl Pts',(22.0211545887425,1.20066176157995E-5,
4.59406577061205));
#36763=CARTESIAN_POINT('Origin',(4.,0.,4.));
#36764=CARTESIAN_POINT('',(22.4288454112575,5.18920962550018E-6,4.59405135764298));
#36765=CARTESIAN_POINT('',(22.3211545887424,-7.30827440488969E-6,4.59414400810326));
#36766=CARTESIAN_POINT('',(4.,-7.27562663373442E-17,4.5941));
#36767=CARTESIAN_POINT('Ctrl Pts',(22.4288454112575,5.18920962550018E-6,
4.59405135764298));
#36768=CARTESIAN_POINT('Ctrl Pts',(22.4253213780041,0.0438634191921666,
4.5940647188338));
#36769=CARTESIAN_POINT('Ctrl Pts',(22.4217973447507,0.0877187745911938,
4.589273164082));
#36770=CARTESIAN_POINT('Ctrl Pts',(22.4182733114973,0.130485535360993,4.57964583089408));
#36771=CARTESIAN_POINT('Ctrl Pts',(22.4103206721535,0.226996720088313,4.55791995512033));
#36772=CARTESIAN_POINT('Ctrl Pts',(22.4023680328097,0.317964089339764,4.51156722320365));
#36773=CARTESIAN_POINT('Ctrl Pts',(22.3944153934659,0.392265646131591,4.44625488916104));
#36774=CARTESIAN_POINT('Ctrl Pts',(22.3864627541221,0.4665672029234,4.38094255511845));
#36775=CARTESIAN_POINT('Ctrl Pts',(22.3785101147783,0.524202947255594,4.29667061894994));
#36776=CARTESIAN_POINT('Ctrl Pts',(22.3705574754345,0.558126122886914,4.20374247196213));
#36777=CARTESIAN_POINT('Ctrl Pts',(22.3626048360906,0.592049298518242,4.11081432497429));
#36778=CARTESIAN_POINT('Ctrl Pts',(22.3546521967468,0.602259905448686,4.00922996716717));
#36779=CARTESIAN_POINT('Ctrl Pts',(22.346699557403,0.587509558716917,3.91140947017845));
#36780=CARTESIAN_POINT('Ctrl Pts',(22.3387469180592,0.572759211985149,3.81358897318973));
#36781=CARTESIAN_POINT('Ctrl Pts',(22.3307942787154,0.533047911591167,3.71953233701942));
#36782=CARTESIAN_POINT('Ctrl Pts',(22.3228416393716,0.473230904440663,3.6407392662825));
#36783=CARTESIAN_POINT('Ctrl Pts',(22.3148890000278,0.413413897290173,3.5619461955456));
#36784=CARTESIAN_POINT('Ctrl Pts',(22.306936360684,0.333491183383171,3.49841669024209));
#36785=CARTESIAN_POINT('Ctrl Pts',(22.2989837213402,0.243234403245124,3.45791809774646));
#36786=CARTESIAN_POINT('Ctrl Pts',(22.2910310819964,0.152977623107077,3.41741950525082));
#36787=CARTESIAN_POINT('Ctrl Pts',(22.2830784426526,0.0523867767379842,
3.39995182556307));
#36788=CARTESIAN_POINT('Ctrl Pts',(22.2751258033088,-0.0462395349927855,
3.40765072037886));
#36789=CARTESIAN_POINT('Ctrl Pts',(22.267173163965,-0.144865846723578,3.41534961519466));
#36790=CARTESIAN_POINT('Ctrl Pts',(22.2592205246212,-0.241527623816046,
3.448215084514));
#36791=CARTESIAN_POINT('Ctrl Pts',(22.2512678852774,-0.324406647450603,
3.50222887712101));
#36792=CARTESIAN_POINT('Ctrl Pts',(22.2433152459336,-0.40728567108515,3.55624266972802));
#36793=CARTESIAN_POINT('Ctrl Pts',(22.2353626065897,-0.476381941261788,
3.63140478562268));
#36794=CARTESIAN_POINT('Ctrl Pts',(22.2274099672459,-0.523247497912515,
3.71852563243507));
#36795=CARTESIAN_POINT('Ctrl Pts',(22.2194573279021,-0.570113054563243,
3.80564647924745));
#36796=CARTESIAN_POINT('Ctrl Pts',(22.2115046885583,-0.59474789768806,3.90472605697756));
#36797=CARTESIAN_POINT('Ctrl Pts',(22.2035520492145,-0.594140082177443,
4.00365053781872));
#36798=CARTESIAN_POINT('Ctrl Pts',(22.1955994098707,-0.593532266666827,
4.10257501865988));
#36799=CARTESIAN_POINT('Ctrl Pts',(22.1876467705269,-0.567681792520777,
4.2013444026121));
#36800=CARTESIAN_POINT('Ctrl Pts',(22.1796941311831,-0.519749232289404,
4.2878827872712));
#36801=CARTESIAN_POINT('Ctrl Pts',(22.1717414918393,-0.471816672058032,
4.37442117193029));
#36802=CARTESIAN_POINT('Ctrl Pts',(22.1637888524955,-0.401802025741336,
4.44872855729627));
#36803=CARTESIAN_POINT('Ctrl Pts',(22.1558362131517,-0.318265537426909,
4.50171985346399));
#36804=CARTESIAN_POINT('Ctrl Pts',(22.1478835738079,-0.234729049112483,
4.55471114963171));
#36805=CARTESIAN_POINT('Ctrl Pts',(22.1399309344641,-0.137670718800326,
4.58638635660118));
#36806=CARTESIAN_POINT('Ctrl Pts',(22.1319782951203,-0.0389572492816432,
4.5928727489116));
#36807=CARTESIAN_POINT('Ctrl Pts',(22.1309340004994,-0.0259947671705595,
4.5937245044491));
#36808=CARTESIAN_POINT('Ctrl Pts',(22.1298897058784,-0.0130037447923657,
4.5941419185755));
#36809=CARTESIAN_POINT('Ctrl Pts',(22.1288454112575,-1.19684274697274E-5,
4.59413016891312));
#36810=CARTESIAN_POINT('Ctrl Pts',(22.0211545887425,1.20066176157995E-5,
4.59406577061205));
#36811=CARTESIAN_POINT('Ctrl Pts',(22.0262984030792,-0.064000704172389,
4.59401922879619));
#36812=CARTESIAN_POINT('Ctrl Pts',(22.031442217416,-0.128028044405449,4.5837112392356));
#36813=CARTESIAN_POINT('Ctrl Pts',(22.0365860317528,-0.188701337098646,
4.56338935830438));
#36814=CARTESIAN_POINT('Ctrl Pts',(22.0445386710966,-0.282505814282095,
4.53197053576284));
#36815=CARTESIAN_POINT('Ctrl Pts',(22.0524913104404,-0.368293119121642,
4.4766155310422));
#36816=CARTESIAN_POINT('Ctrl Pts',(22.0604439497842,-0.435574585201076,
4.40409224738955));
#36817=CARTESIAN_POINT('Ctrl Pts',(22.068396589128,-0.502856051280518,4.33156896373689));
#36818=CARTESIAN_POINT('Ctrl Pts',(22.0763492284718,-0.551631678599843,
4.24187740115222));
#36819=CARTESIAN_POINT('Ctrl Pts',(22.0843018678156,-0.575937982408454,
4.14598357473613));
#36820=CARTESIAN_POINT('Ctrl Pts',(22.0922545071594,-0.600244286217068,
4.05008974832002));
#36821=CARTESIAN_POINT('Ctrl Pts',(22.1002071465032,-0.600081266514962,
3.94799365807249));
#36822=CARTESIAN_POINT('Ctrl Pts',(22.1081597858471,-0.575468854681199,
3.85217794154701));
#36823=CARTESIAN_POINT('Ctrl Pts',(22.1161124251909,-0.550856442847438,
3.75636222502155));
#36824=CARTESIAN_POINT('Ctrl Pts',(22.1240650645347,-0.501794638882025,
3.66682688221814));
#36825=CARTESIAN_POINT('Ctrl Pts',(22.1320177038785,-0.434281916527717,
3.5945188282416));
#36826=CARTESIAN_POINT('Ctrl Pts',(22.1399703432223,-0.366769194173409,
3.52221077426505));
#36827=CARTESIAN_POINT('Ctrl Pts',(22.1479229825661,-0.280805553430205,
3.46713000911538));
#36828=CARTESIAN_POINT('Ctrl Pts',(22.1558756219099,-0.186901220180937,
3.43601090651668));
#36829=CARTESIAN_POINT('Ctrl Pts',(22.1638282612537,-0.0929968869316588,
3.40489180391798));
#36830=CARTESIAN_POINT('Ctrl Pts',(22.1717809005975,0.00884813882368474,
3.39773436387026));
#36831=CARTESIAN_POINT('Ctrl Pts',(22.1797335399413,0.106181915586414,3.41541368090248));
#36832=CARTESIAN_POINT('Ctrl Pts',(22.1876861792851,0.203515692349121,3.4330929979347));
#36833=CARTESIAN_POINT('Ctrl Pts',(22.1956388186289,0.296338220119215,3.47560907204686));
#36834=CARTESIAN_POINT('Ctrl Pts',(22.2035914579727,0.373300680656879,3.53776373412001));
#36835=CARTESIAN_POINT('Ctrl Pts',(22.2115440973165,0.450263141194552,3.59991839619317));
#36836=CARTESIAN_POINT('Ctrl Pts',(22.2194967366603,0.511365534499791,3.68171164622733));
#36837=CARTESIAN_POINT('Ctrl Pts',(22.2274493760041,0.549137260797828,3.7731431454068));
#36838=CARTESIAN_POINT('Ctrl Pts',(22.2354020153479,0.586908987095865,3.86457464458628));
#36839=CARTESIAN_POINT('Ctrl Pts',(22.2433546546918,0.6013500463867,3.96564439291107));
#36840=CARTESIAN_POINT('Ctrl Pts',(22.2513072940356,0.590694822479903,4.06399523710107));
#36841=CARTESIAN_POINT('Ctrl Pts',(22.2592599333794,0.580039598573106,4.16234608129106));
#36842=CARTESIAN_POINT('Ctrl Pts',(22.2672125727232,0.544288091468676,4.25797802134625));
#36843=CARTESIAN_POINT('Ctrl Pts',(22.275165212067,0.487811409852587,4.33919875012361));
#36844=CARTESIAN_POINT('Ctrl Pts',(22.2831178514108,0.431334728236497,4.42041947890096));
#36845=CARTESIAN_POINT('Ctrl Pts',(22.2910704907546,0.354132872108749,4.48722899640046));
#36846=CARTESIAN_POINT('Ctrl Pts',(22.2990231300984,0.265644819817582,4.53145892916239));
#36847=CARTESIAN_POINT('Ctrl Pts',(22.3064002829798,0.183560135512932,4.57248819778762));
#36848=CARTESIAN_POINT('Ctrl Pts',(22.3137774358611,0.0917635873240076,
4.59408754951618));
#36849=CARTESIAN_POINT('Ctrl Pts',(22.3211545887424,-7.30827440488969E-6,
4.59414400810326));
#36850=CARTESIAN_POINT('Origin',(4.,0.,4.));
#36851=CARTESIAN_POINT('',(22.7288454112575,-7.11440487624268E-7,4.59414971000239));
#36852=CARTESIAN_POINT('',(22.6211545887425,-1.51245797256638E-7,4.59404869726453));
#36853=CARTESIAN_POINT('',(4.,-7.27562663373442E-17,4.5941));
#36854=CARTESIAN_POINT('Ctrl Pts',(22.7288454112575,-7.11440487624268E-7,
4.59414971000239));
#36855=CARTESIAN_POINT('Ctrl Pts',(22.7287056894736,0.0017373052546791,
4.59414999869406));
#36856=CARTESIAN_POINT('Ctrl Pts',(22.7285659676897,0.0034753215591825,
4.59414251282321));
#36857=CARTESIAN_POINT('Ctrl Pts',(22.7284262459057,0.00521327185949689,
4.59412723628209));
#36858=CARTESIAN_POINT('Ctrl Pts',(22.7204736065619,0.104133365400505,4.59325773105135));
#36859=CARTESIAN_POINT('Ctrl Pts',(22.7125209672181,0.202839630323109,4.56714939948764));
#36860=CARTESIAN_POINT('Ctrl Pts',(22.7045683278743,0.289252680684759,4.51898953373575));
#36861=CARTESIAN_POINT('Ctrl Pts',(22.6966156885305,0.375665731046408,4.47082966798385));
#36862=CARTESIAN_POINT('Ctrl Pts',(22.6886630491867,0.449785566847107,4.40061826804377));
#36863=CARTESIAN_POINT('Ctrl Pts',(22.6807104098429,0.502555912967013,4.31694216252228));
#36864=CARTESIAN_POINT('Ctrl Pts',(22.6727577704991,0.555326259086918,4.23326605700079));
#36865=CARTESIAN_POINT('Ctrl Pts',(22.6648051311553,0.586747115526033,4.13612524589788));
#36866=CARTESIAN_POINT('Ctrl Pts',(22.6568524918115,0.592973744123511,4.03739517928057));
#36867=CARTESIAN_POINT('Ctrl Pts',(22.6488998524677,0.59920037272099,3.93866511266326));
#36868=CARTESIAN_POINT('Ctrl Pts',(22.6409472131239,0.580232773476834,3.83834579053153));
#36869=CARTESIAN_POINT('Ctrl Pts',(22.6329945737801,0.538391640361539,3.74870332422701));
#36870=CARTESIAN_POINT('Ctrl Pts',(22.6250419344363,0.496550507246239,3.65906085792248));
#36871=CARTESIAN_POINT('Ctrl Pts',(22.6170892950925,0.431835840259791,3.58009524744515));
#36872=CARTESIAN_POINT('Ctrl Pts',(22.6091366557487,0.35215901686313,3.52146073929621));
#36873=CARTESIAN_POINT('Ctrl Pts',(22.6011840164048,0.272482193466486,3.46282623114728));
#36874=CARTESIAN_POINT('Ctrl Pts',(22.593231377061,0.17784321365963,3.42452282532672));
#36875=CARTESIAN_POINT('Ctrl Pts',(22.5852787377172,0.0798134434713266,
3.41123383340666));
#36876=CARTESIAN_POINT('Ctrl Pts',(22.5773260983734,-0.0182163267169884,
3.3979448414866));
#36877=CARTESIAN_POINT('Ctrl Pts',(22.5693734590296,-0.119636887286728,
3.40967026346704));
#36878=CARTESIAN_POINT('Ctrl Pts',(22.5614208196858,-0.212048437952692,
3.44497640167274));
#36879=CARTESIAN_POINT('Ctrl Pts',(22.553468180342,-0.304459988618666,3.48028253987845));
#36880=CARTESIAN_POINT('Ctrl Pts',(22.5455155409982,-0.387862529380837,
3.53916939430943));
#36881=CARTESIAN_POINT('Ctrl Pts',(22.5375629016544,-0.452058834188948,
3.61443730067171));
#36882=CARTESIAN_POINT('Ctrl Pts',(22.5296102623106,-0.516255138997059,
3.689705207034));
#36883=CARTESIAN_POINT('Ctrl Pts',(22.5216576229668,-0.561245207851117,
3.7813541653276));
#36884=CARTESIAN_POINT('Ctrl Pts',(22.513704983623,-0.581528460676763,3.87817881267738));
#36885=CARTESIAN_POINT('Ctrl Pts',(22.5057523442792,-0.601811713502406,
3.97500346002715));
#36886=CARTESIAN_POINT('Ctrl Pts',(22.4977997049354,-0.597388150299644,
4.07700379643311));
#36887=CARTESIAN_POINT('Ctrl Pts',(22.4898470655916,-0.568798575589296,
4.17170890717095));
#36888=CARTESIAN_POINT('Ctrl Pts',(22.4818944262477,-0.540209000878948,
4.26641401790879));
#36889=CARTESIAN_POINT('Ctrl Pts',(22.4739417869039,-0.487453414661012,
4.35382390297851));
#36890=CARTESIAN_POINT('Ctrl Pts',(22.4659891475601,-0.416981925106977,
4.42325150516024));
#36891=CARTESIAN_POINT('Ctrl Pts',(22.4580365082163,-0.346510435552941,
4.49267910734197));
#36892=CARTESIAN_POINT('Ctrl Pts',(22.4500838688725,-0.258323042662803,
4.54412442663572));
#36893=CARTESIAN_POINT('Ctrl Pts',(22.4421312295287,-0.163201846116148,
4.57129757646718));
#36894=CARTESIAN_POINT('Ctrl Pts',(22.4377026234383,-0.11023146834083,4.58642955613285));
#36895=CARTESIAN_POINT('Ctrl Pts',(22.4332740173479,-0.0551108697057404,
4.59403456681078));
#36896=CARTESIAN_POINT('Ctrl Pts',(22.4288454112575,5.18920962550018E-6,
4.59405135764298));
#36897=CARTESIAN_POINT('Ctrl Pts',(22.3211545887424,-7.30827440488969E-6,
4.59414400810326));
#36898=CARTESIAN_POINT('Ctrl Pts',(22.3217300752049,-0.00716629073194701,
4.59414841239758));
#36899=CARTESIAN_POINT('Ctrl Pts',(22.3223055616673,-0.0143251170819474,
4.59402171850555));
#36900=CARTESIAN_POINT('Ctrl Pts',(22.3228810481298,-0.0214791647150919,
4.59376292335171));
#36901=CARTESIAN_POINT('Ctrl Pts',(22.3308336874736,-0.120340848501978,
4.59018663675477));
#36902=CARTESIAN_POINT('Ctrl Pts',(22.3387863268174,-0.218289967621164,
4.56138371553656));
#36903=CARTESIAN_POINT('Ctrl Pts',(22.3467389661612,-0.303350908332583,
4.51087570903952));
#36904=CARTESIAN_POINT('Ctrl Pts',(22.3546916055051,-0.388411849044011,
4.46036770254246));
#36905=CARTESIAN_POINT('Ctrl Pts',(22.3626442448489,-0.460584611347669,
4.38815461076656));
#36906=CARTESIAN_POINT('Ctrl Pts',(22.3705968841927,-0.511045091866278,
4.3030654678256));
#36907=CARTESIAN_POINT('Ctrl Pts',(22.3785495235365,-0.561505572384874,
4.21797632488466));
#36908=CARTESIAN_POINT('Ctrl Pts',(22.3865021628803,-0.590253771118432,
4.12001113077866));
#36909=CARTESIAN_POINT('Ctrl Pts',(22.3944548022241,-0.593774829630164,
4.02114746451658));
#36910=CARTESIAN_POINT('Ctrl Pts',(22.4024074415679,-0.597295888141896,
3.92228379825449));
#36911=CARTESIAN_POINT('Ctrl Pts',(22.4103600809117,-0.575589806431797,
3.82252165983632));
#36912=CARTESIAN_POINT('Ctrl Pts',(22.4183127202555,-0.531310447862662,
3.73405832985033));
#36913=CARTESIAN_POINT('Ctrl Pts',(22.4262653595993,-0.487031089293526,
3.64559499986435));
#36914=CARTESIAN_POINT('Ctrl Pts',(22.4342179989431,-0.420178453865353,
3.56843047831055));
#36915=CARTESIAN_POINT('Ctrl Pts',(22.4421706382869,-0.338926188203527,
3.51199917808983));
#36916=CARTESIAN_POINT('Ctrl Pts',(22.4501232776307,-0.257673922541701,
3.45556787786912));
#36917=CARTESIAN_POINT('Ctrl Pts',(22.4580759169745,-0.162022026646223,
3.41986979898149));
#36918=CARTESIAN_POINT('Ctrl Pts',(22.4660285563183,-0.0636652448434586,
3.40926951931498));
#36919=CARTESIAN_POINT('Ctrl Pts',(22.4739811956621,0.0346915369593057,
3.39866923964846));
#36920=CARTESIAN_POINT('Ctrl Pts',(22.4819338350059,0.135753204669356,3.41316675920307));
#36921=CARTESIAN_POINT('Ctrl Pts',(22.4898864743497,0.227163587879617,3.45098955584192));
#36922=CARTESIAN_POINT('Ctrl Pts',(22.4978391136936,0.318573971089878,3.48881235248077));
#36923=CARTESIAN_POINT('Ctrl Pts',(22.5057917530374,0.40033306980035,3.54996042620388));
#36924=CARTESIAN_POINT('Ctrl Pts',(22.5137443923812,0.462444730281743,3.62695759769032));
#36925=CARTESIAN_POINT('Ctrl Pts',(22.521697031725,0.524556390763143,3.70395476917678));
#36926=CARTESIAN_POINT('Ctrl Pts',(22.5296496710688,0.567020613015458,3.79680103842659));
#36927=CARTESIAN_POINT('Ctrl Pts',(22.5376023104126,0.584645549343987,3.89414467407578));
#36928=CARTESIAN_POINT('Ctrl Pts',(22.5455549497564,0.602270485672515,3.99148830972497));
#36929=CARTESIAN_POINT('Ctrl Pts',(22.5535075891002,0.595056136077256,4.09332931177355));
#36930=CARTESIAN_POINT('Ctrl Pts',(22.561460228444,0.563884587368514,4.18721625032571));
#36931=CARTESIAN_POINT('Ctrl Pts',(22.5694128677878,0.532713038659782,4.28110318887784));
#36932=CARTESIAN_POINT('Ctrl Pts',(22.5773655071316,0.477584290837583,4.36703606393356));
#36933=CARTESIAN_POINT('Ctrl Pts',(22.5853181464754,0.405238519368296,4.43450837402952));
#36934=CARTESIAN_POINT('Ctrl Pts',(22.5932707858192,0.332892747898984,4.5019806841255));
#36935=CARTESIAN_POINT('Ctrl Pts',(22.601223425163,0.24332995278257,4.55099242926169));
#36936=CARTESIAN_POINT('Ctrl Pts',(22.6091760645068,0.14750052788588,4.57555132613148));
#36937=CARTESIAN_POINT('Ctrl Pts',(22.6131689059187,0.0993867282199646,
4.58788179608141));
#36938=CARTESIAN_POINT('Ctrl Pts',(22.6171617473306,0.0496932250345643,
4.5940481472271));
#36939=CARTESIAN_POINT('Ctrl Pts',(22.6211545887425,-1.51173456864708E-7,
4.59404872180247));
#36940=CARTESIAN_POINT('Origin',(3.42660065607856,0.,4.));
#36941=CARTESIAN_POINT('',(22.7766006560786,-4.98014040841517E-7,4.41590979742004));
#36942=CARTESIAN_POINT('',(22.8,4.87367679877478E-13,4.415875));
#36943=CARTESIAN_POINT('',(3.42660065607856,4.87367679877478E-13,4.415875));
#36944=CARTESIAN_POINT('',(22.8,-0.195748955928421,4.36692555359082));
#36945=CARTESIAN_POINT('Ctrl Pts',(22.7766006560786,-4.98014040834069E-7,
4.41590979742004));
#36946=CARTESIAN_POINT('Ctrl Pts',(22.7844004373857,-0.0679170312443507,
4.41589851620688));
#36947=CARTESIAN_POINT('Ctrl Pts',(22.7922002186928,-0.135834416676695,
4.39892762624317));
#36948=CARTESIAN_POINT('Ctrl Pts',(22.8,-0.195762566582618,4.36695865185838));
#36949=CARTESIAN_POINT('Origin',(22.8,0.,4.));
#36950=CARTESIAN_POINT('Origin',(3.42660065607856,0.,4.));
#36951=CARTESIAN_POINT('',(22.4766006560785,3.63249072247605E-6,4.41584094994071));
#36952=CARTESIAN_POINT('',(22.5733993439214,-1.05822049303872E-7,4.41583910483016));
#36953=CARTESIAN_POINT('',(3.42660065607856,4.87367679877478E-13,4.415875));
#36954=CARTESIAN_POINT('Ctrl Pts',(22.4766006560785,3.63249072248342E-6,
4.41584094994071));
#36955=CARTESIAN_POINT('Ctrl Pts',(22.4810292621689,-0.0385780726118879,
4.41582919621688));
#36956=CARTESIAN_POINT('Ctrl Pts',(22.4934105076031,-0.146451497349971,
4.40094585736882));
#36957=CARTESIAN_POINT('Ctrl Pts',(22.5137443923812,-0.304292138366774,
4.30886736509782));
#36958=CARTESIAN_POINT('Ctrl Pts',(22.5376023104126,-0.415080201412036,
4.12530439950267));
#36959=CARTESIAN_POINT('Ctrl Pts',(22.561460228444,-0.424369795825249,3.91110111771763));
#36960=CARTESIAN_POINT('Ctrl Pts',(22.5853181464754,-0.329889515310188,
3.71863599132299));
#36961=CARTESIAN_POINT('Ctrl Pts',(22.6091760645068,-0.154742073939436,
3.59497211022641));
#36962=CARTESIAN_POINT('Ctrl Pts',(22.6330339825383,0.0582436639512456,
3.57034842802071));
#36963=CARTESIAN_POINT('Ctrl Pts',(22.6568919005697,0.256987911016647,3.65078654733876));
#36964=CARTESIAN_POINT('Ctrl Pts',(22.6807498186011,0.39289034562191,3.81661632308649));
#36965=CARTESIAN_POINT('Ctrl Pts',(22.7046077366325,0.432722782933869,4.02728943245291));
#36966=CARTESIAN_POINT('Ctrl Pts',(22.7284656546639,0.366738191089385,4.2312875884069));
#36967=CARTESIAN_POINT('Ctrl Pts',(22.7523235726953,0.211084664509997,4.37873330099785));
#36968=CARTESIAN_POINT('Ctrl Pts',(22.7683685731669,0.0716802821347026,
4.41560650088387));
#36969=CARTESIAN_POINT('Ctrl Pts',(22.7764609342946,0.00121612829983627,
4.41590999950663));
#36970=CARTESIAN_POINT('Ctrl Pts',(22.7766006560786,-4.98014040834069E-7,
4.41590979742004));
#36971=CARTESIAN_POINT('',(22.8,0.415641328671541,4.01393920819689));
#36972=CARTESIAN_POINT('Origin',(22.8,0.,4.));
#36973=CARTESIAN_POINT('Ctrl Pts',(22.5733993439214,-1.0582204931428E-7,
4.41583910483016));
#36974=CARTESIAN_POINT('Ctrl Pts',(22.5773591418533,-0.034498011376554,
4.41583950370926));
#36975=CARTESIAN_POINT('Ctrl Pts',(22.5892715791291,-0.138279341065089,
4.40307041914735));
#36976=CARTESIAN_POINT('Ctrl Pts',(22.6091366557487,-0.295063722636797,
4.31769517074077));
#36977=CARTESIAN_POINT('Ctrl Pts',(22.6329945737801,-0.411209141905604,
4.13747522778479));
#36978=CARTESIAN_POINT('Ctrl Pts',(22.6568524918115,-0.426804986482714,
3.92363755172126));
#36979=CARTESIAN_POINT('Ctrl Pts',(22.6807104098429,-0.33803111495158,3.72847502015617));
#36980=CARTESIAN_POINT('Ctrl Pts',(22.7045683278743,-0.16660749730952,3.59970312177549));
#36981=CARTESIAN_POINT('Ctrl Pts',(22.7284262459057,0.0455714674079685,
3.56882345794434));
#36982=CARTESIAN_POINT('Ctrl Pts',(22.7522841639372,0.246577802732478,3.64336153500176));
#36983=CARTESIAN_POINT('Ctrl Pts',(22.7761420819686,0.387346815298129,3.80514019809748));
#36984=CARTESIAN_POINT('Ctrl Pts',(22.7920473606562,0.417963038852713,3.94471011778788));
#36985=CARTESIAN_POINT('Ctrl Pts',(22.8,0.415641328671541,4.01393920819689));
#36986=CARTESIAN_POINT('Origin',(3.42660065607856,0.,4.));
#36987=CARTESIAN_POINT('',(22.1766006560786,-8.37799962078257E-6,4.41589611849309));
#36988=CARTESIAN_POINT('',(22.2733993439214,-5.11585294796223E-6,4.41590580604266));
#36989=CARTESIAN_POINT('',(3.42660065607856,4.87367679877478E-13,4.415875));
#36990=CARTESIAN_POINT('Ctrl Pts',(22.1766006560786,-8.37799962077716E-6,
4.41589611849309));
#36991=CARTESIAN_POINT('Ctrl Pts',(22.1776449506995,-0.0091027307950905,
4.41590434335565));
#36992=CARTESIAN_POINT('Ctrl Pts',(22.1866418846642,-0.0874489573854402,
4.4133870032437));
#36993=CARTESIAN_POINT('Ctrl Pts',(22.2035914579727,-0.232253957950086,
4.36612956178204));
#36994=CARTESIAN_POINT('Ctrl Pts',(22.2274493760041,-0.379286482964224,
4.21008217638027));
#36995=CARTESIAN_POINT('Ctrl Pts',(22.2513072940356,-0.433573131350875,
4.00266397632408));
#36996=CARTESIAN_POINT('Ctrl Pts',(22.275165212067,-0.381839338801546,3.79459436150246));
#36997=CARTESIAN_POINT('Ctrl Pts',(22.2990231300984,-0.236735426869051,
3.63675202040985));
#36998=CARTESIAN_POINT('Ctrl Pts',(22.3228810481298,-0.0337432544318164,
3.56773370504276));
#36999=CARTESIAN_POINT('Ctrl Pts',(22.3467389661613,0.177500062688638,3.60441627341574));
#37000=CARTESIAN_POINT('Ctrl Pts',(22.3705968841926,0.345339779804043,3.73782983856348));
#37001=CARTESIAN_POINT('Ctrl Pts',(22.3944548022241,0.428734513273282,3.93535114928888));
#37002=CARTESIAN_POINT('Ctrl Pts',(22.4183127202555,0.407291980919218,4.1486808655136));
#37003=CARTESIAN_POINT('Ctrl Pts',(22.4421706382869,0.286255462618544,4.32565405918856));
#37004=CARTESIAN_POINT('Ctrl Pts',(22.4615999502279,0.130682174689606,4.40492695636159));
#37005=CARTESIAN_POINT('Ctrl Pts',(22.4730766228251,0.0307047625933256,
4.41585030288671));
#37006=CARTESIAN_POINT('Ctrl Pts',(22.4766006560785,3.63249072248342E-6,
4.41584094994071));
#37007=CARTESIAN_POINT('Ctrl Pts',(22.2733993439214,-5.11585294797612E-6,
4.41590580604266));
#37008=CARTESIAN_POINT('Ctrl Pts',(22.2739748303838,-0.0050164638240448,
4.41590888908576));
#37009=CARTESIAN_POINT('Ctrl Pts',(22.2825029561901,-0.0792779396689182,
4.41459464077989));
#37010=CARTESIAN_POINT('Ctrl Pts',(22.2989837213402,-0.221370022215225,
4.37281103827166));
#37011=CARTESIAN_POINT('Ctrl Pts',(22.3228416393716,-0.372934645290675,
4.22116172228637));
#37012=CARTESIAN_POINT('Ctrl Pts',(22.346699557403,-0.43330658847365,4.01543234121164));
#37013=CARTESIAN_POINT('Ctrl Pts',(22.3705574754345,-0.387723268841402,
3.80592933171158));
#37014=CARTESIAN_POINT('Ctrl Pts',(22.3944153934659,-0.247331046528593,
3.64388188817752));
#37015=CARTESIAN_POINT('Ctrl Pts',(22.4182733114973,-0.0464596501027702,
3.56891502119853));
#37016=CARTESIAN_POINT('Ctrl Pts',(22.4421312295287,0.165772403721094,3.59936017830047));
#37017=CARTESIAN_POINT('Ctrl Pts',(22.4659891475602,0.337468575289321,3.7277726770023));
#37018=CARTESIAN_POINT('Ctrl Pts',(22.4898470655915,0.426644514167594,3.92275218663495));
#37019=CARTESIAN_POINT('Ctrl Pts',(22.513704983623,0.411494197867752,4.13662086224655));
#37020=CARTESIAN_POINT('Ctrl Pts',(22.5375629016544,0.295722435535401,4.31708206952049));
#37021=CARTESIAN_POINT('Ctrl Pts',(22.5574610217539,0.138855410360913,4.40292493148274));
#37022=CARTESIAN_POINT('Ctrl Pts',(22.5694065025095,0.0347856757474044,
4.41583870262252));
#37023=CARTESIAN_POINT('Ctrl Pts',(22.5733993439214,-1.0582204931428E-7,
4.41583910483016));
#37024=CARTESIAN_POINT('Origin',(3.42660065607856,0.,4.));
#37025=CARTESIAN_POINT('',(21.8766006560786,1.03078286340212E-5,4.41586151989188));
#37026=CARTESIAN_POINT('',(21.9733993439214,8.40473402259622E-6,4.41585103914036));
#37027=CARTESIAN_POINT('',(3.42660065607856,4.87367679877478E-13,4.415875));
#37028=CARTESIAN_POINT('Ctrl Pts',(21.8766006560786,1.03078286340201E-5,
4.41586151989188));
#37029=CARTESIAN_POINT('Ctrl Pts',(21.8822132785738,-0.0488795353146484,
4.415816298089));
#37030=CARTESIAN_POINT('Ctrl Pts',(21.8957785404128,-0.167079919178725,
4.39498170153279));
#37031=CARTESIAN_POINT('Ctrl Pts',(21.9172964415957,-0.326407159500644,
4.28539643168872));
#37032=CARTESIAN_POINT('Ctrl Pts',(21.9411543596271,-0.423245389017799,
4.09410684177624));
#37033=CARTESIAN_POINT('Ctrl Pts',(21.9650122776585,-0.416588591947193,
3.87980556563057));
#37034=CARTESIAN_POINT('Ctrl Pts',(21.98887019569,-0.30806453650007,3.69489510271888));
#37035=CARTESIAN_POINT('Ctrl Pts',(22.0127281137213,-0.12421031036921,3.58459109808296));
#37036=CARTESIAN_POINT('Ctrl Pts',(22.0365860317528,0.0900167200678817,
3.57586588547707));
#37037=CARTESIAN_POINT('Ctrl Pts',(22.0604439497842,0.282232210442068,3.67085301705332));
#37038=CARTESIAN_POINT('Ctrl Pts',(22.0843018678157,0.405434237512275,3.8463255517439));
#37039=CARTESIAN_POINT('Ctrl Pts',(22.108159785847,0.429496549703537,4.05937567504088));
#37040=CARTESIAN_POINT('Ctrl Pts',(22.1320177038785,0.348535256241736,4.25790682842971));
#37041=CARTESIAN_POINT('Ctrl Pts',(22.1548313272889,0.18962186617866,4.38744320371645));
#37042=CARTESIAN_POINT('Ctrl Pts',(22.1696923113557,0.0601536901409818,
4.41584170838249));
#37043=CARTESIAN_POINT('Ctrl Pts',(22.1766006560786,-8.37799962077716E-6,
4.41589611849309));
#37044=CARTESIAN_POINT('Ctrl Pts',(21.9733993439214,8.40473402260317E-6,
4.41585103914036));
#37045=CARTESIAN_POINT('Ctrl Pts',(21.9785431582582,-0.044801031555974,
4.41581845947763));
#37046=CARTESIAN_POINT('Ctrl Pts',(21.9916396119388,-0.158914563981884,
4.39744691543598));
#37047=CARTESIAN_POINT('Ctrl Pts',(22.0126887049632,-0.317860118355158,
4.29488591379237));
#37048=CARTESIAN_POINT('Ctrl Pts',(22.0365466229946,-0.420290167226249,
4.10653136780738));
#37049=CARTESIAN_POINT('Ctrl Pts',(22.060404541026,-0.419947821735935,3.89212700053744));
#37050=CARTESIAN_POINT('Ctrl Pts',(22.0842624590574,-0.316916794682727,
3.70410052003731));
#37051=CARTESIAN_POINT('Ctrl Pts',(22.1081203770888,-0.136390978688423,
3.58842952252864));
#37052=CARTESIAN_POINT('Ctrl Pts',(22.1319782951203,0.0774861468089536,
3.57339871771534));
#37053=CARTESIAN_POINT('Ctrl Pts',(22.1558362131517,0.27241579873489,3.66268354680831));
#37054=CARTESIAN_POINT('Ctrl Pts',(22.1796941311831,0.400732367405962,3.83445143701846));
#37055=CARTESIAN_POINT('Ctrl Pts',(22.2035520492145,0.431058956528623,4.04670046033727));
#37056=CARTESIAN_POINT('Ctrl Pts',(22.227409967246,0.355979888945518,4.24752994899471));
#37057=CARTESIAN_POINT('Ctrl Pts',(22.2506923988149,0.197764744804664,4.38444734931837));
#37058=CARTESIAN_POINT('Ctrl Pts',(22.26602219104,0.064235283418036,4.41586628455644));
#37059=CARTESIAN_POINT('Ctrl Pts',(22.2733993439214,-5.11585294797612E-6,
4.41590580604266));
#37060=CARTESIAN_POINT('Origin',(3.42660065607856,0.,4.));
#37061=CARTESIAN_POINT('',(21.5766006560785,-1.05752387382048E-5,4.41586434469346));
#37062=CARTESIAN_POINT('',(21.6733993439214,-1.08222664516599E-5,4.41587700699864));
#37063=CARTESIAN_POINT('',(3.42660065607856,4.87367679877478E-13,4.415875));
#37064=CARTESIAN_POINT('Ctrl Pts',(21.5766006560785,-1.05752387381843E-5,
4.41586434469346));
#37065=CARTESIAN_POINT('Ctrl Pts',(21.5788289671043,-0.0194203346498642,
4.41588296395747));
#37066=CARTESIAN_POINT('Ctrl Pts',(21.5890099174739,-0.10809016089515,4.40978779866957));
#37067=CARTESIAN_POINT('Ctrl Pts',(21.6071435071872,-0.258824259222961,
4.34785450957493));
#37068=CARTESIAN_POINT('Ctrl Pts',(21.6310014252187,-0.39385182381868,4.18131050126406));
#37069=CARTESIAN_POINT('Ctrl Pts',(21.6548593432501,-0.432571889182456,
3.97043113659525));
#37070=CARTESIAN_POINT('Ctrl Pts',(21.6787172612815,-0.365516344619441,
3.76678216446856));
#37071=CARTESIAN_POINT('Ctrl Pts',(21.702575179313,-0.209082097331647,3.62016130585559));
#37072=CARTESIAN_POINT('Ctrl Pts',(21.7264330973443,-0.00152158196427748,
3.56642135455923));
#37073=CARTESIAN_POINT('Ctrl Pts',(21.7502910153758,0.206411001640417,3.61870319251831));
#37074=CARTESIAN_POINT('Ctrl Pts',(21.7741489334072,0.363870472821225,3.76422248622317));
#37075=CARTESIAN_POINT('Ctrl Pts',(21.7980068514386,0.432353701764573,3.96739580449697));
#37076=CARTESIAN_POINT('Ctrl Pts',(21.82186476947,0.395114673548107,4.17854173669174));
#37077=CARTESIAN_POINT('Ctrl Pts',(21.8457226875014,0.261259344941517,4.3460293508861));
#37078=CARTESIAN_POINT('Ctrl Pts',(21.8639679830376,0.110037800305057,4.4094070875278));
#37079=CARTESIAN_POINT('Ctrl Pts',(21.87426063923,0.0203934810735595,4.41588037378429));
#37080=CARTESIAN_POINT('Ctrl Pts',(21.8766006560786,1.03078286340201E-5,
4.41586151989188));
#37081=CARTESIAN_POINT('Ctrl Pts',(21.6733993439214,-1.0822266451653E-5,
4.41587700699864));
#37082=CARTESIAN_POINT('Ctrl Pts',(21.6751588467887,-0.0153356749568721,
4.41589290068126));
#37083=CARTESIAN_POINT('Ctrl Pts',(21.6848709889998,-0.0999166717736498,
4.41130778913604));
#37084=CARTESIAN_POINT('Ctrl Pts',(21.7025357705547,-0.248467031045983,
4.35532645760922));
#37085=CARTESIAN_POINT('Ctrl Pts',(21.7263936885861,-0.388341045935521,
4.1928315042612));
#37086=CARTESIAN_POINT('Ctrl Pts',(21.7502516066176,-0.433255096896122,
3.98318399549658));
#37087=CARTESIAN_POINT('Ctrl Pts',(21.774109524649,-0.372226475033738,3.77764845789182));
#37088=CARTESIAN_POINT('Ctrl Pts',(21.7979674426804,-0.220178340780001,
3.62648392906691));
#37089=CARTESIAN_POINT('Ctrl Pts',(21.8218253607118,-0.0142906046679706,
3.56665425395863));
#37090=CARTESIAN_POINT('Ctrl Pts',(21.8456832787432,0.195091573553633,3.61278941785858));
#37091=CARTESIAN_POINT('Ctrl Pts',(21.8695411967747,0.356768547853618,3.75360811649661));
#37092=CARTESIAN_POINT('Ctrl Pts',(21.8933991148061,0.431205894023261,3.95467634223136));
#37093=CARTESIAN_POINT('Ctrl Pts',(21.9172570328375,0.400201653291494,4.16682743688221));
#37094=CARTESIAN_POINT('Ctrl Pts',(21.941114950869,0.271337207055788,4.33818467892719));
#37095=CARTESIAN_POINT('Ctrl Pts',(21.9598290545635,0.118211900824938,4.40773087908456));
#37096=CARTESIAN_POINT('Ctrl Pts',(21.9705905189143,0.0244769910710258,
4.41586882955141));
#37097=CARTESIAN_POINT('Ctrl Pts',(21.9733993439214,8.40473402260317E-6,
4.41585103914036));
#37098=CARTESIAN_POINT('Origin',(3.42660065607856,0.,4.));
#37099=CARTESIAN_POINT('',(21.2766006560785,8.9771325895615E-6,4.41589335210553));
#37100=CARTESIAN_POINT('',(21.3733993439214,1.06214664634743E-5,4.41588075133303));
#37101=CARTESIAN_POINT('',(3.42660065607856,4.87367679877478E-13,4.415875));
#37102=CARTESIAN_POINT('Ctrl Pts',(21.2766006560785,8.97713258955941E-6,
4.41589335210553));
#37103=CARTESIAN_POINT('Ctrl Pts',(21.2833972949786,-0.0591814269577189,
4.41583723296416));
#37104=CARTESIAN_POINT('Ctrl Pts',(21.2981465732225,-0.187680420990878,
4.38813575385326));
#37105=CARTESIAN_POINT('Ctrl Pts',(21.3208484908102,-0.346716519889314,
4.26034671465164));
#37106=CARTESIAN_POINT('Ctrl Pts',(21.3447064088417,-0.429069235164158,
4.0623886883135));
#37107=CARTESIAN_POINT('Ctrl Pts',(21.368564326873,-0.406502834830527,3.8491749282489));
#37108=CARTESIAN_POINT('Ctrl Pts',(21.3924222449045,-0.284535418465691,
3.67284200661995));
#37109=CARTESIAN_POINT('Ctrl Pts',(21.4162801629359,-0.0929913416969399,
3.5765081259772));
#37110=CARTESIAN_POINT('Ctrl Pts',(21.4401380809674,0.121291651150069,3.58372954422009));
#37111=CARTESIAN_POINT('Ctrl Pts',(21.4639959989987,0.305915531372611,3.69274042788069));
#37112=CARTESIAN_POINT('Ctrl Pts',(21.4878539170302,0.415734731202803,3.87688464650718));
#37113=CARTESIAN_POINT('Ctrl Pts',(21.5117118350615,0.423895464867194,4.09113392265755));
#37114=CARTESIAN_POINT('Ctrl Pts',(21.535569753093,0.328402210690932,4.28309847227994));
#37115=CARTESIAN_POINT('Ctrl Pts',(21.5571993600986,0.169024930905334,4.39437398220882));
#37116=CARTESIAN_POINT('Ctrl Pts',(21.5708763277605,0.0498513310028489,
4.41581651349798));
#37117=CARTESIAN_POINT('Ctrl Pts',(21.5766006560785,-1.05752387381843E-5,
4.41586434469346));
#37118=CARTESIAN_POINT('Ctrl Pts',(21.3733993439214,1.06214664634605E-5,
4.41588075133303));
#37119=CARTESIAN_POINT('Ctrl Pts',(21.379727174663,-0.0551018547626871,
4.41582358345633));
#37120=CARTESIAN_POINT('Ctrl Pts',(21.3940076447484,-0.1795281855266,4.39095386216025));
#37121=CARTESIAN_POINT('Ctrl Pts',(21.4162407541777,-0.338898428465248,
4.27044521104599));
#37122=CARTESIAN_POINT('Ctrl Pts',(21.4400986722091,-0.427045644525908,
4.07499849655415));
#37123=CARTESIAN_POINT('Ctrl Pts',(21.4639565902406,-0.410768568010174,
3.86121260673678));
#37124=CARTESIAN_POINT('Ctrl Pts',(21.4878145082719,-0.294047387504818,
3.68136401506497));
#37125=CARTESIAN_POINT('Ctrl Pts',(21.5116724263034,-0.105423611064507,
3.57943060117972));
#37126=CARTESIAN_POINT('Ctrl Pts',(21.5355303443348,0.108979109962582,3.58033786138646));
#37127=CARTESIAN_POINT('Ctrl Pts',(21.5593882623662,0.296733470072461,3.68386394585134));
#37128=CARTESIAN_POINT('Ctrl Pts',(21.5832461803976,0.411928413892185,3.86469390692879));
#37129=CARTESIAN_POINT('Ctrl Pts',(21.6071040984291,0.426395639810567,4.07860989342611));
#37130=CARTESIAN_POINT('Ctrl Pts',(21.6309620164605,0.33659751701124,4.27330361969026));
#37131=CARTESIAN_POINT('Ctrl Pts',(21.6530604316246,0.177184770587036,4.39173732935402));
#37132=CARTESIAN_POINT('Ctrl Pts',(21.6672062074449,0.0539299276789421,
4.41582106406873));
#37133=CARTESIAN_POINT('Ctrl Pts',(21.6733993439214,-1.0822266451653E-5,
4.41587700699864));
#37134=CARTESIAN_POINT('Origin',(3.42660065607856,0.,4.));
#37135=CARTESIAN_POINT('',(20.9766006560786,-4.48287659654576E-6,4.41584197426197));
#37136=CARTESIAN_POINT('',(21.0733993439214,-7.65157297119567E-6,4.41584853425778));
#37137=CARTESIAN_POINT('',(3.42660065607856,4.87367679877478E-13,4.415875));
#37138=CARTESIAN_POINT('Ctrl Pts',(20.9766006560786,-4.48287659652116E-6,
4.41584197426197));
#37139=CARTESIAN_POINT('Ctrl Pts',(20.9800129835092,-0.0297322302090305,
4.41585318364051));
#37140=CARTESIAN_POINT('Ctrl Pts',(20.9913779502836,-0.128734546054536,
4.40538471300776));
#37141=CARTESIAN_POINT('Ctrl Pts',(21.0106955564018,-0.28396276796243,4.32765515869354));
#37142=CARTESIAN_POINT('Ctrl Pts',(21.0345534744332,-0.40623841344949,4.15153583326342));
#37143=CARTESIAN_POINT('Ctrl Pts',(21.0584113924646,-0.429177699343215,
3.93836186909709));
#37144=CARTESIAN_POINT('Ctrl Pts',(21.082269310496,-0.347171348131155,3.74026010679315));
#37145=CARTESIAN_POINT('Ctrl Pts',(21.1061272285274,-0.180272145040548,
3.605671823621));
#37146=CARTESIAN_POINT('Ctrl Pts',(21.1299851465589,0.0307085077608185,
3.56750752082027));
#37147=CARTESIAN_POINT('Ctrl Pts',(21.1538430645903,0.234180094072738,3.63509941005724));
#37148=CARTESIAN_POINT('Ctrl Pts',(21.1777009826217,0.380388268371489,3.79191943321731));
#37149=CARTESIAN_POINT('Ctrl Pts',(21.2015589006531,0.433581149524578,3.99962082296209));
#37150=CARTESIAN_POINT('Ctrl Pts',(21.2254168186846,0.380751629084578,4.2074149318183));
#37151=CARTESIAN_POINT('Ctrl Pts',(21.2492747367159,0.234817963878357,4.36449043997717));
#37152=CARTESIAN_POINT('Ctrl Pts',(21.2663360158473,0.0893960873046664,
4.41308118928586));
#37153=CARTESIAN_POINT('Ctrl Pts',(21.2754446556348,0.0100763257733538,
4.41590289708112));
#37154=CARTESIAN_POINT('Ctrl Pts',(21.2766006560785,8.97713258955941E-6,
4.41589335210553));
#37155=CARTESIAN_POINT('Ctrl Pts',(21.0733993439214,-7.65157297121996E-6,
4.41584853425778));
#37156=CARTESIAN_POINT('Ctrl Pts',(21.0763428631935,-0.0256500457845501,
4.41586537097631));
#37157=CARTESIAN_POINT('Ctrl Pts',(21.0872390218095,-0.120560449820324,
4.40722571769055));
#37158=CARTESIAN_POINT('Ctrl Pts',(21.1060878197692,-0.274189543318984,
4.33587624407661));
#37159=CARTESIAN_POINT('Ctrl Pts',(21.1299457378007,-0.401599180171465,
4.16343456021562));
#37160=CARTESIAN_POINT('Ctrl Pts',(21.1538036558321,-0.430806878168669,
3.95102867450389));
#37161=CARTESIAN_POINT('Ctrl Pts',(21.1776615738635,-0.354670559489406,
3.75059761183336));
#37162=CARTESIAN_POINT('Ctrl Pts',(21.2015194918949,-0.191807627993766,
3.61115222665144));
#37163=CARTESIAN_POINT('Ctrl Pts',(21.2253774099264,0.0179574932869785,
3.56679071405539));
#37164=CARTESIAN_POINT('Ctrl Pts',(21.2492353279577,0.223331518303719,3.62836067225603));
#37165=CARTESIAN_POINT('Ctrl Pts',(21.2730932459892,0.374094903668402,3.78080656934254));
#37166=CARTESIAN_POINT('Ctrl Pts',(21.2969511640206,0.433381894944723,3.98685123093373));
#37167=CARTESIAN_POINT('Ctrl Pts',(21.320809082052,0.386695207821707,4.19611112472705));
#37168=CARTESIAN_POINT('Ctrl Pts',(21.3446670000834,0.245451009020076,4.35741650656472));
#37169=CARTESIAN_POINT('Ctrl Pts',(21.3621970873732,0.0975684711839555,
4.41172139589413));
#37170=CARTESIAN_POINT('Ctrl Pts',(21.3717745353192,0.014161952170494,4.41589543043265));
#37171=CARTESIAN_POINT('Ctrl Pts',(21.3733993439214,1.06214664634605E-5,
4.41588075133303));
#37172=CARTESIAN_POINT('Origin',(3.42660065607856,0.,4.));
#37173=CARTESIAN_POINT('',(20.6766006560786,1.29204965968245E-6,4.41591114679826));
#37174=CARTESIAN_POINT('',(20.7733993439214,3.9567662055099E-6,4.41590779860895));
#37175=CARTESIAN_POINT('',(3.42660065607856,4.87367679877478E-13,4.415875));
#37176=CARTESIAN_POINT('Ctrl Pts',(20.6766006560786,1.29076178055295E-6,
4.41591111076812));
#37177=CARTESIAN_POINT('Ctrl Pts',(20.6766286720397,-0.000242659277546582,
4.41591112051333));
#37178=CARTESIAN_POINT('Ctrl Pts',(20.6846093273446,-0.0697345275278937,
4.41585145172406));
#37179=CARTESIAN_POINT('Ctrl Pts',(20.7005426219933,-0.208420567790133,
4.38020336888205));
#37180=CARTESIAN_POINT('Ctrl Pts',(20.7244005400248,-0.365106210756856,
4.23385701605743));
#37181=CARTESIAN_POINT('Ctrl Pts',(20.7482584580562,-0.432520392530856,
4.03032528343114));
#37182=CARTESIAN_POINT('Ctrl Pts',(20.7721163760876,-0.394167874571092,
3.81937870627435));
#37183=CARTESIAN_POINT('Ctrl Pts',(20.795974294119,-0.259432524437891,3.65259868360638));
#37184=CARTESIAN_POINT('Ctrl Pts',(20.8198322121504,-0.0612578225112809,
3.57076788979259));
#37185=CARTESIAN_POINT('Ctrl Pts',(20.8436901301819,0.151895538690754,3.5938959627232));
#37186=CARTESIAN_POINT('Ctrl Pts',(20.8675480482132,0.327906592802717,3.71632757520176));
#37187=CARTESIAN_POINT('Ctrl Pts',(20.8914059662447,0.423735399567132,3.90812480123879));
#37188=CARTESIAN_POINT('Ctrl Pts',(20.9152638842761,0.415949440063929,4.12238802732943));
#37189=CARTESIAN_POINT('Ctrl Pts',(20.9391218023075,0.30645246920106,4.30672404095661));
#37190=CARTESIAN_POINT('Ctrl Pts',(20.9595673929083,0.148398440326279,4.40042000858165));
#37191=CARTESIAN_POINT('Ctrl Pts',(20.9720603441653,0.0395501167658222,
4.4158270594931));
#37192=CARTESIAN_POINT('Ctrl Pts',(20.9766006560786,-4.48287659652116E-6,
4.41584197426197));
#37193=CARTESIAN_POINT('Ctrl Pts',(20.7733993439214,3.95676620551077E-6,
4.41590779860895));
#37194=CARTESIAN_POINT('Ctrl Pts',(20.7809111910678,-0.0654084660523611,
4.41587519962517));
#37195=CARTESIAN_POINT('Ctrl Pts',(20.7963756775582,-0.200102595337945,
4.3835597345012));
#37196=CARTESIAN_POINT('Ctrl Pts',(20.8197928033922,-0.358062019934396,
4.24450842127602));
#37197=CARTESIAN_POINT('Ctrl Pts',(20.8436507214237,-0.431438726014498,
4.04305074550709));
#37198=CARTESIAN_POINT('Ctrl Pts',(20.867508639455,-0.399316990859146,3.83106596928302));
#37199=CARTESIAN_POINT('Ctrl Pts',(20.8913665574865,-0.269551332195825,
3.66039017609669));
#37200=CARTESIAN_POINT('Ctrl Pts',(20.9152244755179,-0.0738730526583281,
3.57275822989076));
#37201=CARTESIAN_POINT('Ctrl Pts',(20.9390823935493,0.139869212314499,3.58959853735383));
#37202=CARTESIAN_POINT('Ctrl Pts',(20.9629403115807,0.319409638666883,3.70679317993256));
#37203=CARTESIAN_POINT('Ctrl Pts',(20.9867982296122,0.420845711130686,3.8956848776653));
#37204=CARTESIAN_POINT('Ctrl Pts',(21.0106561476436,0.419373541863394,4.11008446384341));
#37205=CARTESIAN_POINT('Ctrl Pts',(21.034514065675,0.315353119032788,4.29756540021079));
#37206=CARTESIAN_POINT('Ctrl Pts',(21.0554284644342,0.156567902793621,4.39812991232556));
#37207=CARTESIAN_POINT('Ctrl Pts',(21.0683902238497,0.0436291721249729,
4.41581988245125));
#37208=CARTESIAN_POINT('Ctrl Pts',(21.0733993439214,-7.65157297121996E-6,
4.41584853425778));
#37209=CARTESIAN_POINT('Origin',(3.42660065607856,0.,4.));
#37210=CARTESIAN_POINT('',(20.3766006560786,0.000383027521040961,4.41597069455794));
#37211=CARTESIAN_POINT('',(20.4733993439214,0.000101608071013781,4.41586489633469));
#37212=CARTESIAN_POINT('',(3.42660065607856,4.87367679877478E-13,4.415875));
#37213=CARTESIAN_POINT('Ctrl Pts',(20.3766006560786,0.000383027521040954,
4.41597069455794));
#37214=CARTESIAN_POINT('Ctrl Pts',(20.3891496392578,-0.108893832387875,
4.41487837761012));
#37215=CARTESIAN_POINT('Ctrl Pts',(20.4176039011246,-0.35839559572325,4.31454223548297));
#37216=CARTESIAN_POINT('Ctrl Pts',(20.4540108023354,-0.457800032585507,
3.97025345815189));
#37217=CARTESIAN_POINT('Ctrl Pts',(20.4858213597105,-0.325993724402262,
3.71529210935379));
#37218=CARTESIAN_POINT('Ctrl Pts',(20.509679277742,-0.15096738523986,3.59329490328468));
#37219=CARTESIAN_POINT('Ctrl Pts',(20.5335371957734,0.0630371972956549,
3.57102347342756));
#37220=CARTESIAN_POINT('Ctrl Pts',(20.5573951138048,0.260511246441404,3.65349437971329));
#37221=CARTESIAN_POINT('Ctrl Pts',(20.5812530318362,0.394877283734959,3.82077798440408));
#37222=CARTESIAN_POINT('Ctrl Pts',(20.6051109498677,0.432370081305563,4.03184236506754));
#37223=CARTESIAN_POINT('Ctrl Pts',(20.6289688678991,0.364303478986858,4.23514367899931));
#37224=CARTESIAN_POINT('Ctrl Pts',(20.6527987699694,0.207251017164088,4.38076243960928));
#37225=CARTESIAN_POINT('Ctrl Pts',(20.6686760326959,0.0690052481014253,
4.41590835422812));
#37226=CARTESIAN_POINT('Ctrl Pts',(20.6766006560786,1.29076178055295E-6,
4.41591111076812));
#37227=CARTESIAN_POINT('Ctrl Pts',(20.4733993439214,0.000101608071013788,
4.4158648963347));
#37228=CARTESIAN_POINT('Ctrl Pts',(20.4775268795984,-0.0359150725839473,
4.41584626969953));
#37229=CARTESIAN_POINT('Ctrl Pts',(20.4896070546192,-0.141401612166324,
4.40227446254147));
#37230=CARTESIAN_POINT('Ctrl Pts',(20.5096398689838,-0.298255971346869,
4.31460392554555));
#37231=CARTESIAN_POINT('Ctrl Pts',(20.5334977870152,-0.412709509332759,
4.13311446574462));
#37232=CARTESIAN_POINT('Ctrl Pts',(20.5573557050466,-0.425936384696969,
3.91915434697803));
#37233=CARTESIAN_POINT('Ctrl Pts',(20.581213623078,-0.335173342752607,3.72492109335083));
#37234=CARTESIAN_POINT('Ctrl Pts',(20.6050715411095,-0.162364888615448,
3.59797442377207));
#37235=CARTESIAN_POINT('Ctrl Pts',(20.6289294591408,0.0501004451364318,
3.56932214892951));
#37236=CARTESIAN_POINT('Ctrl Pts',(20.6527873771723,0.250339089241223,3.64598859455508));
#37237=CARTESIAN_POINT('Ctrl Pts',(20.6766452952037,0.389350172549011,3.80921715950176));
#37238=CARTESIAN_POINT('Ctrl Pts',(20.7005032132352,0.433161330121289,4.01909908002448));
#37239=CARTESIAN_POINT('Ctrl Pts',(20.7243611312665,0.371049143609512,4.22430982617278));
#37240=CARTESIAN_POINT('Ctrl Pts',(20.748219049298,0.218207240773441,4.37467120177868));
#37241=CARTESIAN_POINT('Ctrl Pts',(20.7645651201829,0.0769305199015265,
4.41491906931248));
#37242=CARTESIAN_POINT('Ctrl Pts',(20.772958551724,0.00384233167249433,
4.41590971150433));
#37243=CARTESIAN_POINT('Ctrl Pts',(20.7733993439214,3.95676620551077E-6,
4.41590779860895));
#37244=CARTESIAN_POINT('Origin',(3.42660065607856,0.,4.));
#37245=CARTESIAN_POINT('',(20.0766006560786,-0.000186622634748148,4.41645953600834));
#37246=CARTESIAN_POINT('',(20.1733993439214,-0.000111611226006447,4.41653056081536));
#37247=CARTESIAN_POINT('',(3.42660065607856,4.87367679877478E-13,4.415875));
#37248=CARTESIAN_POINT('Ctrl Pts',(20.0766006560786,-0.000186622634748109,
4.41645953600834));
#37249=CARTESIAN_POINT('Ctrl Pts',(20.0778126884445,-0.0107019642254321,
4.4165186149328));
#37250=CARTESIAN_POINT('Ctrl Pts',(20.0949299994981,-0.159149739060163,
4.41138240526969));
#37251=CARTESIAN_POINT('Ctrl Pts',(20.1279525892393,-0.432744382500041,
4.23375285658289));
#37252=CARTESIAN_POINT('Ctrl Pts',(20.1756684253021,-0.430649333670284,
3.76246031529274));
#37253=CARTESIAN_POINT('Ctrl Pts',(20.223384261365,-0.033136228617316,3.50924504180455));
#37254=CARTESIAN_POINT('Ctrl Pts',(20.2711000974278,0.394908089060633,3.70680919012016));
#37255=CARTESIAN_POINT('Ctrl Pts',(20.3188159334906,0.460110046434968,4.17340395051402));
#37256=CARTESIAN_POINT('Ctrl Pts',(20.3539827863742,0.197028357007358,4.40022211154544));
#37257=CARTESIAN_POINT('Ctrl Pts',(20.3732443605702,0.0296097328916507,
4.416262840815));
#37258=CARTESIAN_POINT('Ctrl Pts',(20.3766006560786,0.000383027521040954,
4.41597069455794));
#37259=CARTESIAN_POINT('Ctrl Pts',(20.1733993439214,-0.000111611226006447,
4.41653056081536));
#37260=CARTESIAN_POINT('Ctrl Pts',(20.1741425681289,-0.00655727229825777,
4.41655465488103));
#37261=CARTESIAN_POINT('Ctrl Pts',(20.190791071024,-0.150919726673813,4.41348743992374));
#37262=CARTESIAN_POINT('Ctrl Pts',(20.2233448526067,-0.425711472830213,
4.24633918020534));
#37263=CARTESIAN_POINT('Ctrl Pts',(20.2710606886696,-0.437384262562023,
3.77535541015343));
#37264=CARTESIAN_POINT('Ctrl Pts',(20.3187765247324,-0.0477164433392854,
3.51022640082505));
#37265=CARTESIAN_POINT('Ctrl Pts',(20.3664923607953,0.386374384143037,3.69571627142296));
#37266=CARTESIAN_POINT('Ctrl Pts',(20.4062555575143,0.45143962727185,4.08165775845481));
#37267=CARTESIAN_POINT('Ctrl Pts',(20.4380661148895,0.291471375703242,4.31996082336987));
#37268=CARTESIAN_POINT('Ctrl Pts',(20.4577964972439,0.136183087716603,4.40372206768731));
#37269=CARTESIAN_POINT('Ctrl Pts',(20.4695742402546,0.0334792813416625,
4.41588215816259));
#37270=CARTESIAN_POINT('Ctrl Pts',(20.4733993439214,0.000101608071013788,
4.4158648963347));
#37271=CARTESIAN_POINT('Origin',(3.42660065607856,0.,4.));
#37272=CARTESIAN_POINT('',(19.7766006560786,-0.000280998963924209,4.41539029291088));
#37273=CARTESIAN_POINT('',(19.8733993439214,-0.000322938566065189,4.41548189938477));
#37274=CARTESIAN_POINT('',(3.42660065607856,4.87367679877478E-13,4.415875));
#37275=CARTESIAN_POINT('Ctrl Pts',(19.7766006560786,-0.000280998963924181,
4.41539029291088));
#37276=CARTESIAN_POINT('Ctrl Pts',(19.7823810163188,-0.0507615353771658,
4.41570272077311));
#37277=CARTESIAN_POINT('Ctrl Pts',(19.8040666552467,-0.23976299482565,4.3837755623668));
#37278=CARTESIAN_POINT('Ctrl Pts',(19.8416575728622,-0.481212499922896,
4.10168523844358));
#37279=CARTESIAN_POINT('Ctrl Pts',(19.8893734089251,-0.345789702982467,
3.65023692191923));
#37280=CARTESIAN_POINT('Ctrl Pts',(19.9370892449879,0.107175910646637,3.51998011832295));
#37281=CARTESIAN_POINT('Ctrl Pts',(19.9848050810508,0.461722480014006,3.83053541934297));
#37282=CARTESIAN_POINT('Ctrl Pts',(20.0313088847476,0.394022427012164,4.28486673161383));
#37283=CARTESIAN_POINT('Ctrl Pts',(20.0619074097569,0.127288937001902,4.4157433330307));
#37284=CARTESIAN_POINT('Ctrl Pts',(20.0766006560786,-0.000186622634748109,
4.41645953600834));
#37285=CARTESIAN_POINT('Ctrl Pts',(19.8733993439214,-0.000322938566065196,
4.41548189938477));
#37286=CARTESIAN_POINT('Ctrl Pts',(19.8787108960032,-0.0466836533228258,
4.41581668875846));
#37287=CARTESIAN_POINT('Ctrl Pts',(19.8999277267727,-0.231469429366377,
4.38724295332581));
#37288=CARTESIAN_POINT('Ctrl Pts',(19.9370498362297,-0.47800980043334,4.11581244897344));
#37289=CARTESIAN_POINT('Ctrl Pts',(19.9847656722926,-0.355939225796451,
3.66057517601247));
#37290=CARTESIAN_POINT('Ctrl Pts',(20.0324815083554,0.0929888682922082,
3.51702731322357));
#37291=CARTESIAN_POINT('Ctrl Pts',(20.0801973444182,0.456536973876988,3.81701888067549));
#37292=CARTESIAN_POINT('Ctrl Pts',(20.1271699562736,0.401683300383188,4.27772103607547));
#37293=CARTESIAN_POINT('Ctrl Pts',(20.1582372894413,0.131382308576697,4.41603903277767));
#37294=CARTESIAN_POINT('Ctrl Pts',(20.1733993439214,-0.000111611226006447,
4.41653056081536));
#37295=CARTESIAN_POINT('Origin',(3.42660065607856,0.,4.));
#37296=CARTESIAN_POINT('',(19.4766006560786,0.000302289446139524,4.41543216566181));
#37297=CARTESIAN_POINT('',(19.5733993439214,0.000255464646300079,4.41534829948978));
#37298=CARTESIAN_POINT('',(3.42660065607856,4.87367679877478E-13,4.415875));
#37299=CARTESIAN_POINT('Ctrl Pts',(19.4766006560786,0.000302289446139546,
4.41543216566181));
#37300=CARTESIAN_POINT('Ctrl Pts',(19.4869493441932,-0.0900510892866153,
4.41482666801407));
#37301=CARTESIAN_POINT('Ctrl Pts',(19.5132033109954,-0.320168095705801,
4.3413809155508));
#37302=CARTESIAN_POINT('Ctrl Pts',(19.5553625564852,-0.490312813065352,
3.96128857502183));
#37303=CARTESIAN_POINT('Ctrl Pts',(19.603078392548,-0.232620797759261,3.56664935826393));
#37304=CARTESIAN_POINT('Ctrl Pts',(19.6507942286109,0.238690449241969,3.56996267500769));
#37305=CARTESIAN_POINT('Ctrl Pts',(19.6985100646737,0.490808633485035,3.96818593857384));
#37306=CARTESIAN_POINT('Ctrl Pts',(19.7404455404963,0.316268156276861,4.34384396940031));
#37307=CARTESIAN_POINT('Ctrl Pts',(19.7664757376312,0.0881410531427697,
4.41484304213512));
#37308=CARTESIAN_POINT('Ctrl Pts',(19.7766006560786,-0.000280998963924181,
4.41539029291088));
#37309=CARTESIAN_POINT('Ctrl Pts',(19.5733993439214,0.000255464646300094,
4.41534829948978));
#37310=CARTESIAN_POINT('Ctrl Pts',(19.5832792238775,-0.0860485087386658,
4.41486588036018));
#37311=CARTESIAN_POINT('Ctrl Pts',(19.6090643825213,-0.311990568344336,
4.34649332259355));
#37312=CARTESIAN_POINT('Ctrl Pts',(19.6507548198527,-0.491240257057309,
3.97574594767572));
#37313=CARTESIAN_POINT('Ctrl Pts',(19.6984706559155,-0.245282818621706,
3.57368850533185));
#37314=CARTESIAN_POINT('Ctrl Pts',(19.7461864919783,0.225921452997342,3.56311925573479));
#37315=CARTESIAN_POINT('Ctrl Pts',(19.7939023280412,0.489658867576397,3.95374471702426));
#37316=CARTESIAN_POINT('Ctrl Pts',(19.8363066120222,0.324430886710512,4.33863507066385));
#37317=CARTESIAN_POINT('Ctrl Pts',(19.8628056173156,0.0921420753912029,
4.4148141723173));
#37318=CARTESIAN_POINT('Ctrl Pts',(19.8733993439214,-0.000322938566065196,
4.41548189938477));
#37319=CARTESIAN_POINT('Origin',(3.42660065607856,0.,4.));
#37320=CARTESIAN_POINT('',(19.1766006560786,0.000155842099650094,4.41649089206047));
#37321=CARTESIAN_POINT('',(19.2733993439214,0.000220989830587742,4.4164164649367));
#37322=CARTESIAN_POINT('',(3.42660065607856,4.87367679877478E-13,4.415875));
#37323=CARTESIAN_POINT('Ctrl Pts',(19.1766006560786,0.000155842099650088,
4.41649089206047));
#37324=CARTESIAN_POINT('Ctrl Pts',(19.1915176720675,-0.129233580897558,
4.41587069825202));
#37325=CARTESIAN_POINT('Ctrl Pts',(19.2223399667441,-0.397695790553126,
4.28149179527637));
#37326=CARTESIAN_POINT('Ctrl Pts',(19.2690675401082,-0.459293044881286,
3.82405931712685));
#37327=CARTESIAN_POINT('Ctrl Pts',(19.316783376171,-0.100417177000157,3.51852142809106));
#37328=CARTESIAN_POINT('Ctrl Pts',(19.3644992122339,0.350673329058588,3.65513271950473));
#37329=CARTESIAN_POINT('Ctrl Pts',(19.4122150482967,0.479735122332443,4.10844094226069));
#37330=CARTESIAN_POINT('Ctrl Pts',(19.4495821962449,0.235804435834584,4.38544967282755));
#37331=CARTESIAN_POINT('Ctrl Pts',(19.4710440655056,0.0488163355692654,
4.4157572795781));
#37332=CARTESIAN_POINT('Ctrl Pts',(19.4766006560786,0.000302289446139546,
4.41543216566181));
#37333=CARTESIAN_POINT('Ctrl Pts',(19.2733993439214,0.000220989830587761,
4.4164164649367));
#37334=CARTESIAN_POINT('Ctrl Pts',(19.2878475517519,-0.125161313229646,
4.41561068768233));
#37335=CARTESIAN_POINT('Ctrl Pts',(19.31820103827,-0.389985711500173,4.28851341748863));
#37336=CARTESIAN_POINT('Ctrl Pts',(19.3644598034757,-0.464275578741542,
3.8376626582024));
#37337=CARTESIAN_POINT('Ctrl Pts',(19.4121756395385,-0.114554038379521,
3.52168776344319));
#37338=CARTESIAN_POINT('Ctrl Pts',(19.4598914756013,0.340364234683876,3.64495435060606));
#37339=CARTESIAN_POINT('Ctrl Pts',(19.5076073116642,0.482720800247919,4.09426482953845));
#37340=CARTESIAN_POINT('Ctrl Pts',(19.5454432677708,0.244097666198316,4.38190156491584));
#37341=CARTESIAN_POINT('Ctrl Pts',(19.5673739451899,0.0528892875329133,
4.41564251031262));
#37342=CARTESIAN_POINT('Ctrl Pts',(19.5733993439214,0.000255464646300094,
4.41534829948978));
#37343=CARTESIAN_POINT('Origin',(3.42660065607856,0.,4.));
#37344=CARTESIAN_POINT('',(18.8766006560785,-0.00038196507782994,4.41590683121974));
#37345=CARTESIAN_POINT('',(18.9733993439214,-0.000368287616214491,4.41603142687637));
#37346=CARTESIAN_POINT('',(3.42660065607856,4.87367679877478E-13,4.415875));
#37347=CARTESIAN_POINT('Ctrl Pts',(18.8766006560785,-0.000381965077829925,
4.41590683121974));
#37348=CARTESIAN_POINT('Ctrl Pts',(18.8801807212542,-0.0315488007868432,
4.41619587167324));
#37349=CARTESIAN_POINT('Ctrl Pts',(18.8996660651174,-0.200861076696893,
4.39874895857547));
#37350=CARTESIAN_POINT('Ctrl Pts',(18.9350566876684,-0.462607878309702,
4.16703046362027));
#37351=CARTESIAN_POINT('Ctrl Pts',(18.9827725237311,-0.39069124519864,3.70122654773242));
#37352=CARTESIAN_POINT('Ctrl Pts',(19.030488359794,0.0400031699426168,3.50979089028978));
#37353=CARTESIAN_POINT('Ctrl Pts',(19.0782041958568,0.433962058584907,3.76852180111673));
#37354=CARTESIAN_POINT('Ctrl Pts',(19.1259200319197,0.429406911488226,4.23982270375453));
#37355=CARTESIAN_POINT('Ctrl Pts',(19.1587188519936,0.155221332864305,4.41240136130926));
#37356=CARTESIAN_POINT('Ctrl Pts',(19.1756123933799,0.00872798149047904,
4.41653198033223));
#37357=CARTESIAN_POINT('Ctrl Pts',(19.1766006560786,0.000155842099650088,
4.41649089206047));
#37358=CARTESIAN_POINT('Ctrl Pts',(18.9733993439214,-0.000368287616214533,
4.41603142687637));
#37359=CARTESIAN_POINT('Ctrl Pts',(18.9765106009386,-0.0274330213022572,
4.4162811262788));
#37360=CARTESIAN_POINT('Ctrl Pts',(18.9955271366434,-0.192586232161443,
4.40152565608163));
#37361=CARTESIAN_POINT('Ctrl Pts',(19.0304489510358,-0.457487847288108,
4.18058265263639));
#37362=CARTESIAN_POINT('Ctrl Pts',(19.0781647870987,-0.399321187381313,
3.71286272589862));
#37363=CARTESIAN_POINT('Ctrl Pts',(19.1258806231614,0.0255482632835279,
3.50882537619781));
#37364=CARTESIAN_POINT('Ctrl Pts',(19.1735964592243,0.426956350589889,3.75584124112414));
#37365=CARTESIAN_POINT('Ctrl Pts',(19.2213122952871,0.436283851722622,4.22707185138688));
#37366=CARTESIAN_POINT('Ctrl Pts',(19.2545799235195,0.163455264474221,4.41023200720537));
#37367=CARTESIAN_POINT('Ctrl Pts',(19.2719422730642,0.0128655269200745,
4.41649772584937));
#37368=CARTESIAN_POINT('Ctrl Pts',(19.2733993439214,0.000220989830587761,
4.4164164649367));
#37369=CARTESIAN_POINT('Origin',(3.42660065607856,0.,4.));
#37370=CARTESIAN_POINT('',(18.5766006560786,2.82854505807383E-5,4.41518799822097));
#37371=CARTESIAN_POINT('',(18.6733993439214,-3.94222854199766E-5,4.41518963037823));
#37372=CARTESIAN_POINT('',(3.42660065607856,4.87367679877478E-13,4.415875));
#37373=CARTESIAN_POINT('Ctrl Pts',(18.5766006560786,2.82854505807215E-5,
4.41518799822097));
#37374=CARTESIAN_POINT('Ctrl Pts',(18.5847490491285,-0.0712192880865648,
4.41514491699706));
#37375=CARTESIAN_POINT('Ctrl Pts',(18.6088027208661,-0.281596950705947,
4.36382162423513));
#37376=CARTESIAN_POINT('Ctrl Pts',(18.6487616712913,-0.49096944006335,4.0292272779409));
#37377=CARTESIAN_POINT('Ctrl Pts',(18.6964775073541,-0.290120809601049,
3.60284116440841));
#37378=CARTESIAN_POINT('Ctrl Pts',(18.744193343417,0.177150224400508,3.54117212067402));
#37379=CARTESIAN_POINT('Ctrl Pts',(18.7919091794797,0.481741481528227,3.90085177849878));
#37380=CARTESIAN_POINT('Ctrl Pts',(18.836044950367,0.354281053487698,4.31776308733785));
#37381=CARTESIAN_POINT('Ctrl Pts',(18.8642754425666,0.106917172161326,4.4149117417093));
#37382=CARTESIAN_POINT('Ctrl Pts',(18.8766006560785,-0.000381965077829925,
4.41590683121974));
#37383=CARTESIAN_POINT('Ctrl Pts',(18.6733993439214,-3.94222854199489E-5,
4.41518963037823));
#37384=CARTESIAN_POINT('Ctrl Pts',(18.6810789288129,-0.0671871929144198,
4.41524623173262));
#37385=CARTESIAN_POINT('Ctrl Pts',(18.704663792392,-0.273330541024821,4.36810584919535));
#37386=CARTESIAN_POINT('Ctrl Pts',(18.7441539346588,-0.489895661254576,
4.0436745456279));
#37387=CARTESIAN_POINT('Ctrl Pts',(18.7918697707216,-0.301692008317894,
3.6115580391236));
#37388=CARTESIAN_POINT('Ctrl Pts',(18.8395856067845,0.163560057986223,3.53615376224111));
#37389=CARTESIAN_POINT('Ctrl Pts',(18.8873014428472,0.478612406344963,3.88670662268212));
#37390=CARTESIAN_POINT('Ctrl Pts',(18.9319060218929,0.362263203066427,4.31165738429376));
#37391=CARTESIAN_POINT('Ctrl Pts',(18.960605322251,0.110926532249199,4.41500462017153));
#37392=CARTESIAN_POINT('Ctrl Pts',(18.9733993439214,-0.000368287616214533,
4.41603142687637));
#37393=CARTESIAN_POINT('Origin',(3.42660065607856,0.,4.));
#37394=CARTESIAN_POINT('',(18.2766006560786,0.000371443240938316,4.41601098728712));
#37395=CARTESIAN_POINT('',(18.3733993439214,0.000382963303967143,4.41588626824893));
#37396=CARTESIAN_POINT('',(3.42660065607856,4.87367679877478E-13,4.415875));
#37397=CARTESIAN_POINT('Ctrl Pts',(18.2766006560785,0.000371443240938293,
4.41601098728712));
#37398=CARTESIAN_POINT('Ctrl Pts',(18.2893173770028,-0.110264925490287,
4.41498710445335));
#37399=CARTESIAN_POINT('Ctrl Pts',(18.3179393766147,-0.360950442388199,
4.31267773405576));
#37400=CARTESIAN_POINT('Ctrl Pts',(18.3624666549143,-0.479157019140895,
3.88903254594255));
#37401=CARTESIAN_POINT('Ctrl Pts',(18.4101824909771,-0.165810997523729,
3.5369536330429));
#37402=CARTESIAN_POINT('Ctrl Pts',(18.4578983270399,0.299801814449608,3.61009732380414));
#37403=CARTESIAN_POINT('Ctrl Pts',(18.5056141631028,0.49010200717001,4.04129464153984));
#37404=CARTESIAN_POINT('Ctrl Pts',(18.5451816061157,0.274694351318236,4.36741107590602));
#37405=CARTESIAN_POINT('Ctrl Pts',(18.5688437704409,0.0678526130816757,
4.41522900951301));
#37406=CARTESIAN_POINT('Ctrl Pts',(18.5766006560786,2.82854505807215E-5,
4.41518799822097));
#37407=CARTESIAN_POINT('Ctrl Pts',(18.3733993439214,0.000382963303967157,
4.41588626824893));
#37408=CARTESIAN_POINT('Ctrl Pts',(18.3856472566872,-0.106256708375174,
4.41489942083623));
#37409=CARTESIAN_POINT('Ctrl Pts',(18.4138004481407,-0.352960303644862,
4.31875095920395));
#37410=CARTESIAN_POINT('Ctrl Pts',(18.4578589182817,-0.482217355384067,
3.90319273261591));
#37411=CARTESIAN_POINT('Ctrl Pts',(18.5055747543446,-0.179376629827252,
3.54203793877243));
#37412=CARTESIAN_POINT('Ctrl Pts',(18.5532905904074,0.288188414964166,3.60143675240633));
#37413=CARTESIAN_POINT('Ctrl Pts',(18.6010064264702,0.491105603945206,4.02684232898929));
#37414=CARTESIAN_POINT('Ctrl Pts',(18.6410426776416,0.282958802096416,4.36309886994028));
#37415=CARTESIAN_POINT('Ctrl Pts',(18.6651736501253,0.0718833454275778,
4.41512900400112));
#37416=CARTESIAN_POINT('Ctrl Pts',(18.6733993439214,-3.94222854199489E-5,
4.41518963037823));
#37417=CARTESIAN_POINT('Origin',(3.42660065607856,0.,4.));
#37418=CARTESIAN_POINT('',(17.9766006560786,-0.000210814279110197,4.41643020456723));
#37419=CARTESIAN_POINT('',(18.0733993439214,-0.000144384975211464,4.41650095473263));
#37420=CARTESIAN_POINT('',(3.42660065607856,4.87367679877478E-13,4.415875));
#37421=CARTESIAN_POINT('Ctrl Pts',(17.9766006560786,-0.000210814279110157,
4.41643020456723));
#37422=CARTESIAN_POINT('Ctrl Pts',(17.9779804261896,-0.0121834889824064,
4.41650424974197));
#37423=CARTESIAN_POINT('Ctrl Pts',(17.9952654749882,-0.162096873242269,
4.41059855206721));
#37424=CARTESIAN_POINT('Ctrl Pts',(18.0284558024744,-0.435175833605105,
4.22918817311999));
#37425=CARTESIAN_POINT('Ctrl Pts',(18.0761716385373,-0.428137176707308,
3.75791781814212));
#37426=CARTESIAN_POINT('Ctrl Pts',(18.1238874746,-0.0279335627019553,3.5089552556775));
#37427=CARTESIAN_POINT('Ctrl Pts',(18.1716033106629,0.397921871745719,3.71092663761881));
#37428=CARTESIAN_POINT('Ctrl Pts',(18.2193191467257,0.458359528554279,4.17835853620019));
#37429=CARTESIAN_POINT('Ctrl Pts',(18.2543182618643,0.193950155243433,4.40107745006558));
#37430=CARTESIAN_POINT('Ctrl Pts',(18.2734120983152,0.0281121206155762,
4.41626771302466));
#37431=CARTESIAN_POINT('Ctrl Pts',(18.2766006560785,0.000371443240938293,
4.41601098728712));
#37432=CARTESIAN_POINT('Ctrl Pts',(18.0733993439214,-0.000144384975211439,
4.41650095473263));
#37433=CARTESIAN_POINT('Ctrl Pts',(18.0743103058739,-0.00804551399413891,
4.41653639380418));
#37434=CARTESIAN_POINT('Ctrl Pts',(18.0911265465141,-0.153864670001157,
4.41274680364665));
#37435=CARTESIAN_POINT('Ctrl Pts',(18.1238480658419,-0.428237044548737,
4.24190547436581));
#37436=CARTESIAN_POINT('Ctrl Pts',(18.1715639019047,-0.435081213444543,
3.7706322547532));
#37437=CARTESIAN_POINT('Ctrl Pts',(18.2192797379675,-0.0423836094492617,
3.50999096487715));
#37438=CARTESIAN_POINT('Ctrl Pts',(18.2669955740304,0.389235515258945,3.69933251171255));
#37439=CARTESIAN_POINT('Ctrl Pts',(18.3147114100932,0.463413677146622,4.16478163940629));
#37440=CARTESIAN_POINT('Ctrl Pts',(18.3501793333902,0.202226156869028,4.39827758107438));
#37441=CARTESIAN_POINT('Ctrl Pts',(18.3697419779996,0.0322267809866215,
4.41618095209965));
#37442=CARTESIAN_POINT('Ctrl Pts',(18.3733993439214,0.000382963303967157,
4.41588626824893));
#37443=CARTESIAN_POINT('Origin',(3.42660065607856,0.,4.));
#37444=CARTESIAN_POINT('',(17.6766006560786,-0.000263771022561219,4.41536107794487));
#37445=CARTESIAN_POINT('',(17.7733993439214,-0.000309142357869163,4.41544738986064));
#37446=CARTESIAN_POINT('',(3.42660065607856,4.87367679877478E-13,4.415875));
#37447=CARTESIAN_POINT('Ctrl Pts',(17.6766006560786,-0.000263771022561289,
4.41536107794487));
#37448=CARTESIAN_POINT('Ctrl Pts',(17.6825487540639,-0.0522183410383149,
4.41566152300153));
#37449=CARTESIAN_POINT('Ctrl Pts',(17.7044021307368,-0.24273028972288,4.38249735042552));
#37450=CARTESIAN_POINT('Ctrl Pts',(17.7421607860973,-0.48225726547346,4.09660825404716));
#37451=CARTESIAN_POINT('Ctrl Pts',(17.7898766221602,-0.342084653792828,
3.64661166616396));
#37452=CARTESIAN_POINT('Ctrl Pts',(17.837592458223,0.112229559114723,3.52113702282083));
#37453=CARTESIAN_POINT('Ctrl Pts',(17.8853082942859,0.463481641013499,3.83540961967535));
#37454=CARTESIAN_POINT('Ctrl Pts',(17.9316443602377,0.391261919872151,4.28736986940801));
#37455=CARTESIAN_POINT('Ctrl Pts',(17.962075147502,0.125831334120538,4.41565069513148));
#37456=CARTESIAN_POINT('Ctrl Pts',(17.9766006560786,-0.000210814279110157,
4.41643020456723));
#37457=CARTESIAN_POINT('Ctrl Pts',(17.7733993439214,-0.000309142357869142,
4.41544738986064));
#37458=CARTESIAN_POINT('Ctrl Pts',(17.7788786337482,-0.0481438769258273,
4.41577602216682));
#37459=CARTESIAN_POINT('Ctrl Pts',(17.8002632022627,-0.23443694547481,4.38601982759396));
#37460=CARTESIAN_POINT('Ctrl Pts',(17.8375530494648,-0.479202773223469,
4.11076970247734));
#37461=CARTESIAN_POINT('Ctrl Pts',(17.8852688855277,-0.352344189444135,
3.65683998336499));
#37462=CARTESIAN_POINT('Ctrl Pts',(17.9329847215905,0.0980774850139738,
3.51803938772416));
#37463=CARTESIAN_POINT('Ctrl Pts',(17.9807005576534,0.458433095867658,3.82183063825345));
#37464=CARTESIAN_POINT('Ctrl Pts',(18.0275054317636,0.3989600628602,4.28031410431705));
#37465=CARTESIAN_POINT('Ctrl Pts',(18.0584050271863,0.129907183855675,4.41591763216682));
#37466=CARTESIAN_POINT('Ctrl Pts',(18.0733993439214,-0.000144384975211439,
4.41650095473263));
#37467=CARTESIAN_POINT('Origin',(3.42660065607856,0.,4.));
#37468=CARTESIAN_POINT('',(17.3766006560786,0.000316824918469052,4.41546566829253));
#37469=CARTESIAN_POINT('',(17.4733993439214,0.000273208168652644,4.41537657040552));
#37470=CARTESIAN_POINT('',(3.42660065607856,4.87367679877478E-13,4.415875));
#37471=CARTESIAN_POINT('Ctrl Pts',(17.3766006560786,0.000316824918469058,
4.41546566829253));
#37472=CARTESIAN_POINT('Ctrl Pts',(17.3871170819382,-0.0914824399419538,
4.4148173972429));
#37473=CARTESIAN_POINT('Ctrl Pts',(17.4135387864855,-0.323087181591141,
4.33950699049548));
#37474=CARTESIAN_POINT('Ctrl Pts',(17.4558657697204,-0.489877595596684,
3.956123284257));
#37475=CARTESIAN_POINT('Ctrl Pts',(17.5035816057832,-0.228040769637767,
3.56422180844494));
#37476=CARTESIAN_POINT('Ctrl Pts',(17.551297441846,0.243209403937772,3.57250215124727));
#37477=CARTESIAN_POINT('Ctrl Pts',(17.5990132779089,0.491116639619549,3.97336034645914));
#37478=CARTESIAN_POINT('Ctrl Pts',(17.6407810159864,0.313340775136121,4.34566293955037));
#37479=CARTESIAN_POINT('Ctrl Pts',(17.6666434753763,0.0867087440962768,
4.41485812965324));
#37480=CARTESIAN_POINT('Ctrl Pts',(17.6766006560786,-0.000263771022561289,
4.41536107794487));
#37481=CARTESIAN_POINT('Ctrl Pts',(17.4733993439214,0.000273208168652693,
4.41537657040552));
#37482=CARTESIAN_POINT('Ctrl Pts',(17.4834469616226,-0.0874810350323011,
4.41484969107387));
#37483=CARTESIAN_POINT('Ctrl Pts',(17.5093998580114,-0.314919534962053,
4.34468516187688));
#37484=CARTESIAN_POINT('Ctrl Pts',(17.5512580330878,-0.490957336521241,
3.97057010757845));
#37485=CARTESIAN_POINT('Ctrl Pts',(17.5989738691507,-0.240776309167652,
3.57112706567612));
#37486=CARTESIAN_POINT('Ctrl Pts',(17.6466897052135,0.230513307714322,3.56552463842171));
#37487=CARTESIAN_POINT('Ctrl Pts',(17.6944055412763,0.490119007219086,3.95890762096741));
#37488=CARTESIAN_POINT('Ctrl Pts',(17.7366420875123,0.321513805022658,4.34052027563639));
#37489=CARTESIAN_POINT('Ctrl Pts',(17.7629733550606,0.090710757213051,4.41482206853766));
#37490=CARTESIAN_POINT('Ctrl Pts',(17.7733993439214,-0.000309142357869142,
4.41544738986064));
#37491=CARTESIAN_POINT('Origin',(3.42660065607856,0.,4.));
#37492=CARTESIAN_POINT('',(17.0766006560786,0.000130763213737631,4.41651185352269));
#37493=CARTESIAN_POINT('',(17.1733993439214,0.000198609043858391,4.41644558073401));
#37494=CARTESIAN_POINT('',(3.42660065607856,4.87367679877478E-13,4.415875));
#37495=CARTESIAN_POINT('Ctrl Pts',(17.0766006560786,0.000130763213737628,
4.41651185352269));
#37496=CARTESIAN_POINT('Ctrl Pts',(17.0916854098125,-0.130696083011285,
4.41597403242798));
#37497=CARTESIAN_POINT('Ctrl Pts',(17.1226754422341,-0.400436570105288,
4.2789290971087));
#37498=CARTESIAN_POINT('Ctrl Pts',(17.1695707533433,-0.457413284126125,
3.81922856321607));
#37499=CARTESIAN_POINT('Ctrl Pts',(17.2172865894061,-0.0953372598908034,
3.51748986360026));
#37500=CARTESIAN_POINT('Ctrl Pts',(17.265002425469,0.354288437054553,3.6588476466131));
#37501=CARTESIAN_POINT('Ctrl Pts',(17.3127182615318,0.478565610824392,4.11349088504481));
#37502=CARTESIAN_POINT('Ctrl Pts',(17.349917671735,0.232837083242772,4.38668157013213));
#37503=CARTESIAN_POINT('Ctrl Pts',(17.3712118032506,0.0473568302064652,
4.41579785693967));
#37504=CARTESIAN_POINT('Ctrl Pts',(17.3766006560786,0.000316824918469058,
4.41546566829253));
#37505=CARTESIAN_POINT('Ctrl Pts',(17.1733993439214,0.000198609043858397,
4.41644558073401));
#37506=CARTESIAN_POINT('Ctrl Pts',(17.1880152894969,-0.126615914365149,
4.41569892234974));
#37507=CARTESIAN_POINT('Ctrl Pts',(17.2185365137601,-0.392752582168809,
4.28602487069057));
#37508=CARTESIAN_POINT('Ctrl Pts',(17.2649630167107,-0.462538907526291,
3.83277863809798));
#37509=CARTESIAN_POINT('Ctrl Pts',(17.3126788527736,-0.109506707187599,
3.52050703244687));
#37510=CARTESIAN_POINT('Ctrl Pts',(17.3603946888365,0.344087187338735,3.64856119684745));
#37511=CARTESIAN_POINT('Ctrl Pts',(17.4081105248993,0.481700523269991,4.09934702176407));
#37512=CARTESIAN_POINT('Ctrl Pts',(17.4457787432609,0.241130489326423,4.3831889686244));
#37513=CARTESIAN_POINT('Ctrl Pts',(17.467541682935,0.0514330574063097,4.41568373580506));
#37514=CARTESIAN_POINT('Ctrl Pts',(17.4733993439214,0.000273208168652693,
4.41537657040552));
#37515=CARTESIAN_POINT('Origin',(3.42660065607856,0.,4.));
#37516=CARTESIAN_POINT('',(16.7766006560786,-0.000383680820852129,4.41586226484778));
#37517=CARTESIAN_POINT('',(16.8733993439214,-0.000374684679869397,4.41598699190495));
#37518=CARTESIAN_POINT('',(3.42660065607856,4.87367679877478E-13,4.415875));
#37519=CARTESIAN_POINT('Ctrl Pts',(16.7766006560786,-0.000383680820852189,
4.41586226484779));
#37520=CARTESIAN_POINT('Ctrl Pts',(16.7803484589992,-0.0330197262611539,
4.41616320579436));
#37521=CARTESIAN_POINT('Ctrl Pts',(16.8000015406075,-0.203823433586872,
4.39772119122577));
#37522=CARTESIAN_POINT('Ctrl Pts',(16.8355599009034,-0.464342533291602,
4.16214572651883));
#37523=CARTESIAN_POINT('Ctrl Pts',(16.8832757369663,-0.387520750342007,
3.69712561530174));
#37524=CARTESIAN_POINT('Ctrl Pts',(16.9309915730291,0.0451673004198413,
3.51023971187451));
#37525=CARTESIAN_POINT('Ctrl Pts',(16.978707409092,0.436377524217892,3.7731082169636));
#37526=CARTESIAN_POINT('Ctrl Pts',(17.0264232451548,0.426855552995382,4.24433493759383));
#37527=CARTESIAN_POINT('Ctrl Pts',(17.0590543274837,0.152277829190936,4.41314658311127));
#37528=CARTESIAN_POINT('Ctrl Pts',(17.0757801311249,0.00724700082869906,
4.41654110793655));
#37529=CARTESIAN_POINT('Ctrl Pts',(17.0766006560786,0.000130763213737628,
4.41651185352269));
#37530=CARTESIAN_POINT('Ctrl Pts',(16.8733993439214,-0.000374684679869387,
4.41598699190495));
#37531=CARTESIAN_POINT('Ctrl Pts',(16.8766783386836,-0.0289064002234668,
4.4162516892709));
#37532=CARTESIAN_POINT('Ctrl Pts',(16.8958626121335,-0.195546116663039,
4.40054826733105));
#37533=CARTESIAN_POINT('Ctrl Pts',(16.9309521642709,-0.459365614209645,
4.17575112327883));
#37534=CARTESIAN_POINT('Ctrl Pts',(16.9786680003337,-0.396272847821079,
3.70867019559999));
#37535=CARTESIAN_POINT('Ctrl Pts',(17.0263838363966,0.0307233721630972,
3.5091219099869));
#37536=CARTESIAN_POINT('Ctrl Pts',(17.0740996724594,0.429505846750062,3.76035452756312));
#37537=CARTESIAN_POINT('Ctrl Pts',(17.1218155085223,0.433866493469502,4.23165726989771));
#37538=CARTESIAN_POINT('Ctrl Pts',(17.1549153990096,0.160507997039396,4.41102293437065));
#37539=CARTESIAN_POINT('Ctrl Pts',(17.1721100108093,0.0113854435377776,
4.41651144656345));
#37540=CARTESIAN_POINT('Ctrl Pts',(17.1733993439214,0.000198609043858397,
4.41644558073401));
#37541=CARTESIAN_POINT('Origin',(3.42660065607856,0.,4.));
#37542=CARTESIAN_POINT('',(16.4766006560786,5.2409936866527E-5,4.41519222098806));
#37543=CARTESIAN_POINT('',(16.5733993439214,-1.52272386678698E-5,4.41518677123726));
#37544=CARTESIAN_POINT('',(3.42660065607856,4.87367679877478E-13,4.415875));
#37545=CARTESIAN_POINT('Ctrl Pts',(16.4766006560786,5.2409936866539E-5,
4.41519222098806));
#37546=CARTESIAN_POINT('Ctrl Pts',(16.4849167868736,-0.0726599781719204,
4.41511070701236));
#37547=CARTESIAN_POINT('Ctrl Pts',(16.5091381963562,-0.284551613766983,
4.36224737480062));
#37548=CARTESIAN_POINT('Ctrl Pts',(16.5492648845264,-0.4912502013546,4.02405128938415));
#37549=CARTESIAN_POINT('Ctrl Pts',(16.5969807205893,-0.285919008936969,
3.59980561575594));
#37550=CARTESIAN_POINT('Ctrl Pts',(16.6446965566521,0.181976008816936,3.54306460296116));
#37551=CARTESIAN_POINT('Ctrl Pts',(16.6924123927149,0.482759657613431,3.90593439612197));
#37552=CARTESIAN_POINT('Ctrl Pts',(16.7363804258571,0.351413532087107,4.31989995948535));
#37553=CARTESIAN_POINT('Ctrl Pts',(16.7644431803116,0.105484194296011,4.41488604428797));
#37554=CARTESIAN_POINT('Ctrl Pts',(16.7766006560786,-0.000383680820852189,
4.41586226484779));
#37555=CARTESIAN_POINT('Ctrl Pts',(16.5733993439214,-1.52272386678906E-5,
4.41518677123726));
#37556=CARTESIAN_POINT('Ctrl Pts',(16.5812466665579,-0.0686308195205231,
4.41520910309265));
#37557=CARTESIAN_POINT('Ctrl Pts',(16.6049992678821,-0.276289552895371,
4.36659242126669));
#37558=CARTESIAN_POINT('Ctrl Pts',(16.6446571478939,-0.490328743065594,
4.03850907134293));
#37559=CARTESIAN_POINT('Ctrl Pts',(16.6923729839567,-0.297581432841348,
3.60840005658827));
#37560=CARTESIAN_POINT('Ctrl Pts',(16.7400888200196,0.168439486040012,3.53790329540825));
#37561=CARTESIAN_POINT('Ctrl Pts',(16.7878046560824,0.479779833116189,3.89175704832657));
#37562=CARTESIAN_POINT('Ctrl Pts',(16.832241497383,0.359412856911567,4.31386464726761));
#37563=CARTESIAN_POINT('Ctrl Pts',(16.860773059996,0.109491163683573,4.41496773315674));
#37564=CARTESIAN_POINT('Ctrl Pts',(16.8733993439214,-0.000374684679869387,
4.41598699190495));
#37565=CARTESIAN_POINT('Origin',(3.42660065607856,0.,4.));
#37566=CARTESIAN_POINT('',(16.1766006560786,0.000364146841390381,4.41605523138122));
#37567=CARTESIAN_POINT('',(16.2733993439214,0.000380345806842055,4.41593091837313));
#37568=CARTESIAN_POINT('',(3.42660065607856,4.87367679877478E-13,4.415875));
#37569=CARTESIAN_POINT('Ctrl Pts',(16.1766006560786,0.000364146841390366,
4.41605523138122));
#37570=CARTESIAN_POINT('Ctrl Pts',(16.1894851147479,-0.111700864104492,
4.41502624848758));
#37571=CARTESIAN_POINT('Ctrl Pts',(16.2182748521048,-0.363797281821349,
4.31045679267864));
#37572=CARTESIAN_POINT('Ctrl Pts',(16.2629698681494,-0.477960913216358,
3.88398883549692));
#37573=CARTESIAN_POINT('Ctrl Pts',(16.3106857042122,-0.160921706883503,
3.53523185446324));
#37574=CARTESIAN_POINT('Ctrl Pts',(16.358401540275,0.303894378979202,3.6132786128531));
#37575=CARTESIAN_POINT('Ctrl Pts',(16.4061173763379,0.489639580609251,4.04645757153336));
#37576=CARTESIAN_POINT('Ctrl Pts',(16.4455170816057,0.271734615807756,4.36891289568356));
#37577=CARTESIAN_POINT('Ctrl Pts',(16.4690115081859,0.0664083969439258,
4.41526660914191));
#37578=CARTESIAN_POINT('Ctrl Pts',(16.4766006560786,5.2409936866539E-5,
4.41519222098806));
#37579=CARTESIAN_POINT('Ctrl Pts',(16.2733993439214,0.000380345806842052,
4.41593091837313));
#37580=CARTESIAN_POINT('Ctrl Pts',(16.2858149944323,-0.107690075887363,
4.41492720978183));
#37581=CARTESIAN_POINT('Ctrl Pts',(16.3141359236307,-0.35582464097624,4.31660057631701));
#37582=CARTESIAN_POINT('Ctrl Pts',(16.3583621315169,-0.481170314810987,
3.89811598262401));
#37583=CARTESIAN_POINT('Ctrl Pts',(16.4060779675797,-0.174540169679895,
3.54017290856226));
#37584=CARTESIAN_POINT('Ctrl Pts',(16.4537938036425,0.292372898913969,3.60449612791703));
#37585=CARTESIAN_POINT('Ctrl Pts',(16.5015096397054,0.490795435699827,4.0320166386149));
#37586=CARTESIAN_POINT('Ctrl Pts',(16.5413781531317,0.280003220364278,4.36466130212541));
#37587=CARTESIAN_POINT('Ctrl Pts',(16.5653413878703,0.0704421061260754,
4.4151638399628));
#37588=CARTESIAN_POINT('Ctrl Pts',(16.5733993439214,-1.52272386678906E-5,
4.41518677123726));
#37589=CARTESIAN_POINT('Origin',(3.42660065607856,0.,4.));
#37590=CARTESIAN_POINT('',(15.8766006560786,-0.00023258108979477,4.41639972388928));
#37591=CARTESIAN_POINT('',(15.9733993439214,-0.000169011902647176,4.4164782780785));
#37592=CARTESIAN_POINT('',(3.42660065607856,4.87367679877478E-13,4.415875));
#37593=CARTESIAN_POINT('Ctrl Pts',(15.8766006560786,-0.000232581089794846,
4.41639972388928));
#37594=CARTESIAN_POINT('Ctrl Pts',(15.8781481639346,-0.0136633580705269,
4.41648966084242));
#37595=CARTESIAN_POINT('Ctrl Pts',(15.8956009504782,-0.165044849757219,
4.40979870506104));
#37596=CARTESIAN_POINT('Ctrl Pts',(15.9289590157095,-0.437567097060412,
4.22458909239344));
#37597=CARTESIAN_POINT('Ctrl Pts',(15.9766748517724,-0.425562075928853,
3.75341909160864));
#37598=CARTESIAN_POINT('Ctrl Pts',(16.0243906878352,-0.0227568523576073,
3.50868813313462));
#37599=CARTESIAN_POINT('Ctrl Pts',(16.072106523898,0.400946338892803,3.71513642180785));
#37600=CARTESIAN_POINT('Ctrl Pts',(16.1198223599609,0.456454337785543,4.1831793175245));
#37601=CARTESIAN_POINT('Ctrl Pts',(16.1546537373544,0.190990792023167,4.40204523666471));
#37602=CARTESIAN_POINT('Ctrl Pts',(16.1735798360603,0.0266382990664043,
4.41629648110721));
#37603=CARTESIAN_POINT('Ctrl Pts',(16.1766006560786,0.000364146841390366,
4.41605523138122));
#37604=CARTESIAN_POINT('Ctrl Pts',(15.9733993439214,-0.000169011902647174,
4.4164782780785));
#37605=CARTESIAN_POINT('Ctrl Pts',(15.974478043619,-0.00952634975615679,
4.4165263696097));
#37606=CARTESIAN_POINT('Ctrl Pts',(15.9914620220042,-0.156808910032117,
4.4119928338179));
#37607=CARTESIAN_POINT('Ctrl Pts',(16.024351279077,-0.430762722000766,4.23737881579128));
#37608=CARTESIAN_POINT('Ctrl Pts',(16.0720671151398,-0.432639725453012,
3.76605963834362));
#37609=CARTESIAN_POINT('Ctrl Pts',(16.1197829512026,-0.0372170120039125,
3.50957149464017));
#37610=CARTESIAN_POINT('Ctrl Pts',(16.1674987872655,0.392382656225717,3.70345139362117));
#37611=CARTESIAN_POINT('Ctrl Pts',(16.2152146233283,0.461651293660056,4.16965644082667));
#37612=CARTESIAN_POINT('Ctrl Pts',(16.2505148088803,0.199264245432362,4.39929555075695));
#37613=CARTESIAN_POINT('Ctrl Pts',(16.2699097157447,0.0307553622657438,
4.41621302761729));
#37614=CARTESIAN_POINT('Ctrl Pts',(16.2733993439214,0.000380345806842052,
4.41593091837313));
#37615=CARTESIAN_POINT('Origin',(3.42660065607856,0.,4.));
#37616=CARTESIAN_POINT('',(15.5766006560786,-0.000245472137683418,4.41533389801214));
#37617=CARTESIAN_POINT('',(15.6733993439214,-0.00029394562308721,4.41541483535501));
#37618=CARTESIAN_POINT('',(3.42660065607856,4.87367679877478E-13,4.415875));
#37619=CARTESIAN_POINT('Ctrl Pts',(15.5766006560786,-0.000245472137683396,
4.41533389801214));
#37620=CARTESIAN_POINT('Ctrl Pts',(15.5827164918089,-0.0536739331835165,
4.41562024719655));
#37621=CARTESIAN_POINT('Ctrl Pts',(15.6047376062269,-0.245697356182912,
4.38119912149661));
#37622=CARTESIAN_POINT('Ctrl Pts',(15.6426639993325,-0.483248643997369,
4.09152034160055));
#37623=CARTESIAN_POINT('Ctrl Pts',(15.6903798353953,-0.338341267922855,
3.64302603558196));
#37624=CARTESIAN_POINT('Ctrl Pts',(15.7380956714582,0.117270100534806,3.52234641383892));
#37625=CARTESIAN_POINT('Ctrl Pts',(15.785811507521,0.465190531238913,3.84030342991275));
#37626=CARTESIAN_POINT('Ctrl Pts',(15.8319798357278,0.388490242362186,4.28984418805176));
#37627=CARTESIAN_POINT('Ctrl Pts',(15.862242885247,0.124378106492246,4.41556528924811));
#37628=CARTESIAN_POINT('Ctrl Pts',(15.8766006560786,-0.000232581089794846,
4.41639972388928));
#37629=CARTESIAN_POINT('Ctrl Pts',(15.6733993439214,-0.000293945623087231,
4.41541483535501));
#37630=CARTESIAN_POINT('Ctrl Pts',(15.6790463714933,-0.0496027558454661,
4.41573527017753));
#37631=CARTESIAN_POINT('Ctrl Pts',(15.7005986777528,-0.23740431922453,4.38477730872224));
#37632=CARTESIAN_POINT('Ctrl Pts',(15.7380562626999,-0.480343569999647,
4.1057131950703));
#37633=CARTESIAN_POINT('Ctrl Pts',(15.7857720987628,-0.348708030819167,
3.6531456586776));
#37634=CARTESIAN_POINT('Ctrl Pts',(15.8334879348256,0.103151458625294,3.5190998009613));
#37635=CARTESIAN_POINT('Ctrl Pts',(15.8812037708885,0.460285376424935,3.82667199562295));
#37636=CARTESIAN_POINT('Ctrl Pts',(15.9278409072537,0.396214095655672,4.28286244744368));
#37637=CARTESIAN_POINT('Ctrl Pts',(15.9585727649314,0.128446309981357,4.41581726659612));
#37638=CARTESIAN_POINT('Ctrl Pts',(15.9733993439214,-0.000169011902647174,
4.4164782780785));
#37639=CARTESIAN_POINT('Origin',(3.42660065607856,0.,4.));
#37640=CARTESIAN_POINT('',(15.2766006560786,0.000330084823988869,4.41550084660604));
#37641=CARTESIAN_POINT('',(15.3733993439214,0.000289868078815952,4.41540680128743));
#37642=CARTESIAN_POINT('',(3.42660065607856,4.87367679877478E-13,4.415875));
#37643=CARTESIAN_POINT('Ctrl Pts',(15.2766006560786,0.000330084823988861,
4.41550084660604));
#37644=CARTESIAN_POINT('Ctrl Pts',(15.2872848196833,-0.0929135079625664,
4.41481081573461));
#37645=CARTESIAN_POINT('Ctrl Pts',(15.3138742619755,-0.32600240339937,4.33760928826424));
#37646=CARTESIAN_POINT('Ctrl Pts',(15.3563689829555,-0.489387968817152,
3.95096286275689));
#37647=CARTESIAN_POINT('Ctrl Pts',(15.4040848190183,-0.223435404337718,
3.56184267101825));
#37648=CARTESIAN_POINT('Ctrl Pts',(15.4518006550811,0.24770132994065,3.57508909640066));
#37649=CARTESIAN_POINT('Ctrl Pts',(15.499516491144,0.491370121559653,3.97853774265298));
#37650=CARTESIAN_POINT('Ctrl Pts',(15.5411164914764,0.310410063586636,4.3474585185963));
#37651=CARTESIAN_POINT('Ctrl Pts',(15.5668112131213,0.0852759340546689,
4.41487554708019));
#37652=CARTESIAN_POINT('Ctrl Pts',(15.5766006560786,-0.000245472137683396,
4.41533389801214));
#37653=CARTESIAN_POINT('Ctrl Pts',(15.3733993439214,0.000289868078815973,
4.41540680128743));
#37654=CARTESIAN_POINT('Ctrl Pts',(15.3836146993676,-0.0889130762729256,
4.41483587894927));
#37655=CARTESIAN_POINT('Ctrl Pts',(15.4097353335015,-0.317845114095608,
4.34285359523591));
#37656=CARTESIAN_POINT('Ctrl Pts',(15.4517612463229,-0.490619905976795,
3.96539750426199));
#37657=CARTESIAN_POINT('Ctrl Pts',(15.4994770823858,-0.236243011612202,
3.56861332390027));
#37658=CARTESIAN_POINT('Ctrl Pts',(15.5471929184486,0.235079475381852,3.56797816593814));
#37659=CARTESIAN_POINT('Ctrl Pts',(15.5949087545115,0.490524862970081,3.9640753057054));
#37660=CARTESIAN_POINT('Ctrl Pts',(15.6369775630024,0.318592711010818,4.34238143198936));
#37661=CARTESIAN_POINT('Ctrl Pts',(15.6631410928057,0.0892792238074376,
4.41483274135358));
#37662=CARTESIAN_POINT('Ctrl Pts',(15.6733993439214,-0.000293945623087231,
4.41541483535501));
#37663=CARTESIAN_POINT('Origin',(3.42660065607856,0.,4.));
#37664=CARTESIAN_POINT('',(14.9766006560786,0.000104941934236194,4.41652945172571));
#37665=CARTESIAN_POINT('',(15.0733993439214,0.000175165248676303,4.41647198785975));
#37666=CARTESIAN_POINT('',(3.42660065607856,4.87367679877478E-13,4.415875));
#37667=CARTESIAN_POINT('Ctrl Pts',(14.9766006560786,0.000104941934236227,
4.41652945172572));
#37668=CARTESIAN_POINT('Ctrl Pts',(14.9918531475576,-0.132161740438444,
4.41608294134065));
#37669=CARTESIAN_POINT('Ctrl Pts',(15.0230109177242,-0.40316752945992,4.27633971254324));
#37670=CARTESIAN_POINT('Ctrl Pts',(15.0700739665785,-0.455482716161518,
3.8144178884426));
#37671=CARTESIAN_POINT('Ctrl Pts',(15.1177898026413,-0.0902467530057116,
3.51651189422706));
#37672=CARTESIAN_POINT('Ctrl Pts',(15.1655056387041,0.357864192060027,3.66260046696357));
#37673=CARTESIAN_POINT('Ctrl Pts',(15.2132214747669,0.47734294310866,4.11852822244656));
#37674=CARTESIAN_POINT('Ctrl Pts',(15.2502531472251,0.229869832763757,4.3878938710325));
#37675=CARTESIAN_POINT('Ctrl Pts',(15.2713795409956,0.0458961718568525,
4.41583804947224));
#37676=CARTESIAN_POINT('Ctrl Pts',(15.2766006560786,0.000330084823988861,
4.41550084660604));
#37677=CARTESIAN_POINT('Ctrl Pts',(15.0733993439214,0.000175165248676341,
4.41647198785975));
#37678=CARTESIAN_POINT('Ctrl Pts',(15.0881830272419,-0.128073190246274,
4.41579247653651));
#37679=CARTESIAN_POINT('Ctrl Pts',(15.1188719892501,-0.395510344386944,
4.28350986851547));
#37680=CARTESIAN_POINT('Ctrl Pts',(15.1654662299459,-0.46075086019608,3.82791319143947));
#37681=CARTESIAN_POINT('Ctrl Pts',(15.2131820660087,-0.104447211543591,
3.51937956259357));
#37682=CARTESIAN_POINT('Ctrl Pts',(15.2608979020716,0.347771918596306,3.652207076714));
#37683=CARTESIAN_POINT('Ctrl Pts',(15.3086137381344,0.480626744730421,4.10441818376995));
#37684=CARTESIAN_POINT('Ctrl Pts',(15.346114218751,0.238163166260598,4.38445638366753));
#37685=CARTESIAN_POINT('Ctrl Pts',(15.36770942068,0.0499756483669043,4.41572480336754));
#37686=CARTESIAN_POINT('Ctrl Pts',(15.3733993439214,0.000289868078815973,
4.41540680128743));
#37687=CARTESIAN_POINT('Origin',(3.42660065607856,0.,4.));
#37688=CARTESIAN_POINT('',(14.6766006560786,-0.000383732061438463,4.41581798673635));
#37689=CARTESIAN_POINT('',(14.7733993439214,-0.000379407362125217,4.41594234696178));
#37690=CARTESIAN_POINT('',(3.42660065607856,4.87367679877478E-13,4.415875));
#37691=CARTESIAN_POINT('Ctrl Pts',(14.6766006560786,-0.000383732061438387,
4.41581798673635));
#37692=CARTESIAN_POINT('Ctrl Pts',(14.6805161967443,-0.0344897130604965,
4.41612948839573));
#37693=CARTESIAN_POINT('Ctrl Pts',(14.7003370160976,-0.206786574235377,
4.39667515056147));
#37694=CARTESIAN_POINT('Ctrl Pts',(14.7360631141386,-0.466025611307368,
4.15724297904063));
#37695=CARTESIAN_POINT('Ctrl Pts',(14.7837789502014,-0.38430721152129,3.69305832471834));
#37696=CARTESIAN_POINT('Ctrl Pts',(14.8314947862642,0.0503264139313189,
3.51074293371195));
#37697=CARTESIAN_POINT('Ctrl Pts',(14.8792106223271,0.438744519099385,3.77771983486548));
#37698=CARTESIAN_POINT('Ctrl Pts',(14.9269264583899,0.42425678142631,4.24882003188202));
#37699=CARTESIAN_POINT('Ctrl Pts',(14.9593898029737,0.149335702075518,4.41387566524124));
#37700=CARTESIAN_POINT('Ctrl Pts',(14.97594786887,0.00576578747519492,4.41654856180149));
#37701=CARTESIAN_POINT('Ctrl Pts',(14.9766006560786,0.000104941934236227,
4.41652945172572));
#37702=CARTESIAN_POINT('Ctrl Pts',(14.7733993439214,-0.000379407362125234,
4.41594234696178));
#37703=CARTESIAN_POINT('Ctrl Pts',(14.7768460764287,-0.0303789312965351,
4.41622104989506));
#37704=CARTESIAN_POINT('Ctrl Pts',(14.7961980876235,-0.198506931257387,
4.39955296987463));
#37705=CARTESIAN_POINT('Ctrl Pts',(14.831455377506,-0.461192356972643,4.17090007232882));
#37706=CARTESIAN_POINT('Ctrl Pts',(14.8791712135689,-0.393180492164677,
3.7045100248179));
#37707=CARTESIAN_POINT('Ctrl Pts',(14.9268870496317,0.0358950684576197,
3.50947296821438));
#37708=CARTESIAN_POINT('Ctrl Pts',(14.9746028856945,0.432007635398663,3.76489443262817));
#37709=CARTESIAN_POINT('Ctrl Pts',(15.0223187217574,0.431400943461215,4.23621695712364));
#37710=CARTESIAN_POINT('Ctrl Pts',(15.0552508744997,0.157562060208247,4.41179740605063));
#37711=CARTESIAN_POINT('Ctrl Pts',(15.0722777485543,0.00990499767517082,
4.41652354042182));
#37712=CARTESIAN_POINT('Ctrl Pts',(15.0733993439214,0.000175165248676341,
4.41647198785975));
#37713=CARTESIAN_POINT('Origin',(3.42660065607856,0.,4.));
#37714=CARTESIAN_POINT('',(14.3766006560786,7.63317591858645E-5,4.41519896243726));
#37715=CARTESIAN_POINT('',(14.4733993439214,9.02664646690309E-6,4.41518644689786));
#37716=CARTESIAN_POINT('',(3.42660065607856,4.87367679877478E-13,4.415875));
#37717=CARTESIAN_POINT('Ctrl Pts',(14.3766006560786,7.63317591858798E-5,
4.41519896243726));
#37718=CARTESIAN_POINT('Ctrl Pts',(14.3850845246186,-0.0740996743586071,
4.41507773880187));
#37719=CARTESIAN_POINT('Ctrl Pts',(14.4094736718463,-0.287504468978829,
4.360651101065));
#37720=CARTESIAN_POINT('Ctrl Pts',(14.4497680977616,-0.491476396904638,
4.01887262932433));
#37721=CARTESIAN_POINT('Ctrl Pts',(14.4974839338244,-0.281685449746218,
3.59681451879656));
#37722=CARTESIAN_POINT('Ctrl Pts',(14.5451997698872,0.186781580201919,3.54500783946397));
#37723=CARTESIAN_POINT('Ctrl Pts',(14.59291560595,0.483724211046603,3.91102746210588));
#37724=CARTESIAN_POINT('Ctrl Pts',(14.6367159013472,0.348540265561382,4.32201186060262));
#37725=CARTESIAN_POINT('Ctrl Pts',(14.6646109180567,0.104051852208848,4.41486414061182));
#37726=CARTESIAN_POINT('Ctrl Pts',(14.6766006560786,-0.000383732061438387,
4.41581798673635));
#37727=CARTESIAN_POINT('Ctrl Pts',(14.4733993439214,9.0266464668684E-6,
4.41518644689786));
#37728=CARTESIAN_POINT('Ctrl Pts',(14.481414404303,-0.0700733710850898,
4.41517292627706));
#37729=CARTESIAN_POINT('Ctrl Pts',(14.5053347433722,-0.279247125311621,
4.3650573561381));
#37730=CARTESIAN_POINT('Ctrl Pts',(14.545160361129,-0.490707361486496,4.03333931965322));
#37731=CARTESIAN_POINT('Ctrl Pts',(14.5928761971918,-0.293437803431633,
3.60528557111603));
#37732=CARTESIAN_POINT('Ctrl Pts',(14.6405920332547,0.173300204635467,3.53970415608515));
#37733=CARTESIAN_POINT('Ctrl Pts',(14.6883078693175,0.480893968219416,3.89681949708321));
#37734=CARTESIAN_POINT('Ctrl Pts',(14.7325769728731,0.356556173733762,4.31604662460621));
#37735=CARTESIAN_POINT('Ctrl Pts',(14.760940797741,0.10805675748006,4.41493494840171));
#37736=CARTESIAN_POINT('Ctrl Pts',(14.7733993439214,-0.000379407362125234,
4.41594234696178));
#37737=CARTESIAN_POINT('Origin',(3.42660065607856,0.,4.));
#37738=CARTESIAN_POINT('',(14.0766006560786,0.000355193352615291,4.41609897421413));
#37739=CARTESIAN_POINT('',(14.1733993439214,0.000376051973931104,4.41597558743442));
#37740=CARTESIAN_POINT('',(3.42660065607856,4.87367679877478E-13,4.415875));
#37741=CARTESIAN_POINT('Ctrl Pts',(14.0766006560786,0.000355193352615277,
4.41609897421413));
#37742=CARTESIAN_POINT('Ctrl Pts',(14.0896528524929,-0.113137957382804,
4.41506966208575));
#37743=CARTESIAN_POINT('Ctrl Pts',(14.1186103275949,-0.366637448157006,
4.30821039815648));
#37744=CARTESIAN_POINT('Ctrl Pts',(14.1634730813845,-0.476711717661702,
3.87895801102093));
#37745=CARTESIAN_POINT('Ctrl Pts',(14.2111889174473,-0.156014541823709,
3.53356170012368));
#37746=CARTESIAN_POINT('Ctrl Pts',(14.2589047535102,0.307953188363286,3.61650285707861));
#37747=CARTESIAN_POINT('Ctrl Pts',(14.306620589573,0.4891227672074,4.05161534124029));
#37748=CARTESIAN_POINT('Ctrl Pts',(14.3458525570958,0.268773633406098,4.37039329245586));
#37749=CARTESIAN_POINT('Ctrl Pts',(14.369179245931,0.0649630708582953,4.4153050049005));
#37750=CARTESIAN_POINT('Ctrl Pts',(14.3766006560786,7.63317591858798E-5,
4.41519896243726));
#37751=CARTESIAN_POINT('Ctrl Pts',(14.1733993439214,0.000376051973931098,
4.41597558743442));
#37752=CARTESIAN_POINT('Ctrl Pts',(14.1859827321773,-0.109124255432428,
4.41495896305428));
#37753=CARTESIAN_POINT('Ctrl Pts',(14.2144713991208,-0.358682910161539,
4.31442504752535));
#37754=CARTESIAN_POINT('Ctrl Pts',(14.258865344752,-0.480069828122688,3.8930505494253));
#37755=CARTESIAN_POINT('Ctrl Pts',(14.3065811808148,-0.169684322438749,
3.53835895376334));
#37756=CARTESIAN_POINT('Ctrl Pts',(14.3542970168777,0.296524907469595,3.60759943412104));
#37757=CARTESIAN_POINT('Ctrl Pts',(14.4020128529405,0.49043075222644,4.0371873919842));
#37758=CARTESIAN_POINT('Ctrl Pts',(14.4417136286217,0.277046036654804,4.36620192284859));
#37759=CARTESIAN_POINT('Ctrl Pts',(14.4655091256154,0.0689998253659925,
4.41519975692232));
#37760=CARTESIAN_POINT('Ctrl Pts',(14.4733993439214,9.0266464668684E-6,
4.41518644689786));
#37761=CARTESIAN_POINT('Origin',(3.42660065607856,0.,4.));
#37762=CARTESIAN_POINT('',(13.7766006560786,-0.000253139125078747,4.41636688691614));
#37763=CARTESIAN_POINT('',(13.8733993439214,-0.000192710833643805,4.4164526008213));
#37764=CARTESIAN_POINT('',(3.42660065607856,4.87367679877478E-13,4.415875));
#37765=CARTESIAN_POINT('Ctrl Pts',(13.7766006560786,-0.000253139125078718,
4.41636688691614));
#37766=CARTESIAN_POINT('Ctrl Pts',(13.7783159016796,-0.0151427949580853,
4.41647347977994));
#37767=CARTESIAN_POINT('Ctrl Pts',(13.7959364259683,-0.167994124135391,
4.40898222403799));
#37768=CARTESIAN_POINT('Ctrl Pts',(13.8294622289446,-0.439909757638992,
4.21996506537626));
#37769=CARTESIAN_POINT('Ctrl Pts',(13.8771780650075,-0.422939705734467,
3.74894775411238));
#37770=CARTESIAN_POINT('Ctrl Pts',(13.9248939010703,-0.0175776142901187,
3.50847558318244));
#37771=CARTESIAN_POINT('Ctrl Pts',(13.9726097371332,0.403926270823208,3.71937784729135));
#37772=CARTESIAN_POINT('Ctrl Pts',(14.020325573196,0.454498446235019,4.18797975215946));
#37773=CARTESIAN_POINT('Ctrl Pts',(14.0549892128445,0.188032430710383,4.40299531219535));
#37774=CARTESIAN_POINT('Ctrl Pts',(14.0737475738053,0.0251636842930195,
4.41632397176197));
#37775=CARTESIAN_POINT('Ctrl Pts',(14.0766006560786,0.000355193352615277,
4.41609897421413));
#37776=CARTESIAN_POINT('Ctrl Pts',(13.8733993439214,-0.000192710833643682,
4.4164526008213));
#37777=CARTESIAN_POINT('Ctrl Pts',(13.874645781364,-0.0110068809386406,
4.41651469495978));
#37778=CARTESIAN_POINT('Ctrl Pts',(13.8917974974943,-0.15975450351916,4.41122255187585));
#37779=CARTESIAN_POINT('Ctrl Pts',(13.9248544923121,-0.433240552373761,
4.23282579030437));
#37780=CARTESIAN_POINT('Ctrl Pts',(13.9725703283749,-0.430150181893835,
3.76151300691929));
#37781=CARTESIAN_POINT('Ctrl Pts',(14.0202861644378,-0.032046280669499,
3.50920649887429));
#37782=CARTESIAN_POINT('Ctrl Pts',(14.0680020005006,0.39548621318905,3.70760321474174));
#37783=CARTESIAN_POINT('Ctrl Pts',(14.1157178365634,0.459837632138507,4.1745123976147));
#37784=CARTESIAN_POINT('Ctrl Pts',(14.1508502843704,0.196303200904851,4.40029544879449));
#37785=CARTESIAN_POINT('Ctrl Pts',(14.1700774534897,0.0292830534939708,
4.41624396624722));
#37786=CARTESIAN_POINT('Ctrl Pts',(14.1733993439214,0.000376051973931098,
4.41597558743442));
#37787=CARTESIAN_POINT('Origin',(3.42660065607856,0.,4.));
#37788=CARTESIAN_POINT('',(13.4766006560786,-0.000226204729293368,4.4153088088013));
#37789=CARTESIAN_POINT('',(13.5733993439214,-0.000277574767750837,4.41538411867388));
#37790=CARTESIAN_POINT('',(3.42660065607856,4.87367679877478E-13,4.415875));
#37791=CARTESIAN_POINT('Ctrl Pts',(13.4766006560786,-0.000226204729293314,
4.4153088088013));
#37792=CARTESIAN_POINT('Ctrl Pts',(13.482884229554,-0.0551283395969922,
4.41557894444213));
#37793=CARTESIAN_POINT('Ctrl Pts',(13.505073081717,-0.248664136397309,4.37988069596112));
#37794=CARTESIAN_POINT('Ctrl Pts',(13.5431672125676,-0.484186345555107,
4.08642226350871));
#37795=CARTESIAN_POINT('Ctrl Pts',(13.5908830486304,-0.334560300710407,
3.63948005597396));
#37796=CARTESIAN_POINT('Ctrl Pts',(13.6385988846933,0.122297616148583,3.52360886035071));
#37797=CARTESIAN_POINT('Ctrl Pts',(13.6863147207561,0.466847750307624,3.8452149784873));
#37798=CARTESIAN_POINT('Ctrl Pts',(13.7323153112179,0.38570983934117,4.29229218593957));
#37799=CARTESIAN_POINT('Ctrl Pts',(13.762410622992,0.122927301498021,4.41548505619568));
#37800=CARTESIAN_POINT('Ctrl Pts',(13.7766006560786,-0.000253139125078718,
4.41636688691614));
#37801=CARTESIAN_POINT('Ctrl Pts',(13.5733993439214,-0.000277574767750817,
4.41538411867388));
#37802=CARTESIAN_POINT('Ctrl Pts',(13.5792141092383,-0.0510604653080308,
4.41569425641003));
#37803=CARTESIAN_POINT('Ctrl Pts',(13.6009341532429,-0.240371663949131,
4.38351498152559));
#37804=CARTESIAN_POINT('Ctrl Pts',(13.6385594759351,-0.481431012491488,
4.10064494554323));
#37805=CARTESIAN_POINT('Ctrl Pts',(13.6862753119979,-0.345033139360895,
3.64948986092447));
#37806=CARTESIAN_POINT('Ctrl Pts',(13.7339911480608,0.108213974662067,3.52021363031051));
#37807=CARTESIAN_POINT('Ctrl Pts',(13.7817069841236,0.462086530666827,3.83153260544464));
#37808=CARTESIAN_POINT('Ctrl Pts',(13.8281763827438,0.393458703070077,4.28538422885222));
#37809=CARTESIAN_POINT('Ctrl Pts',(13.8587405026764,0.126988323162951,4.4157223370415));
#37810=CARTESIAN_POINT('Ctrl Pts',(13.8733993439214,-0.000192710833643682,
4.4164526008213));
#37811=CARTESIAN_POINT('Origin',(3.42660065607856,0.,4.));
#37812=CARTESIAN_POINT('',(13.1766006560786,0.000342007958933446,4.41553758638116));
#37813=CARTESIAN_POINT('',(13.2733993439214,0.000305371599794934,4.41543889539504));
#37814=CARTESIAN_POINT('',(3.42660065607856,4.87367679877478E-13,4.415875));
#37815=CARTESIAN_POINT('Ctrl Pts',(13.1766006560786,0.000342007958933428,
4.41553758638117));
#37816=CARTESIAN_POINT('Ctrl Pts',(13.1874525574283,-0.0943443719380771,
4.41480703635833));
#37817=CARTESIAN_POINT('Ctrl Pts',(13.2142097374657,-0.328913583769224,
4.33568767983454));
#37818=CARTESIAN_POINT('Ctrl Pts',(13.2568721961906,-0.488843983144383,
3.94580788806928));
#37819=CARTESIAN_POINT('Ctrl Pts',(13.3045880322534,-0.218805220893238,
3.55951220202843));
#37820=CARTESIAN_POINT('Ctrl Pts',(13.3523038683163,0.252165742455243,3.57772323864086));
#37821=CARTESIAN_POINT('Ctrl Pts',(13.4000197043791,0.491569024438394,3.98371752277252));
#37822=CARTESIAN_POINT('Ctrl Pts',(13.4414519669665,0.307476227900318,4.34923088347422));
#37823=CARTESIAN_POINT('Ctrl Pts',(13.4669789508664,0.0838425436168888,
4.41489516431802));
#37824=CARTESIAN_POINT('Ctrl Pts',(13.4766006560786,-0.000226204729293314,
4.4153088088013));
#37825=CARTESIAN_POINT('Ctrl Pts',(13.2733993439214,0.000305371599794949,
4.41543889539504));
#37826=CARTESIAN_POINT('Ctrl Pts',(13.2837824371127,-0.0903447040275099,
4.41482455235666));
#37827=CARTESIAN_POINT('Ctrl Pts',(13.3100708089916,-0.320767143545349,
4.3409984814332));
#37828=CARTESIAN_POINT('Ctrl Pts',(13.352264459558,-0.490227979701372,3.96022874442655));
#37829=CARTESIAN_POINT('Ctrl Pts',(13.3999802956209,-0.23168347330409,3.56614749850931));
#37830=CARTESIAN_POINT('Ctrl Pts',(13.4476961316837,0.239619531536799,3.57047968038978));
#37831=CARTESIAN_POINT('Ctrl Pts',(13.4954119677466,0.490876233547033,3.96924698078795));
#37832=CARTESIAN_POINT('Ctrl Pts',(13.5373130384925,0.315668023336251,4.34421900798688));
#37833=CARTESIAN_POINT('Ctrl Pts',(13.5633088305507,0.0878472949503496,
4.41484592860038));
#37834=CARTESIAN_POINT('Ctrl Pts',(13.5733993439214,-0.000277574767750817,
4.41538411867388));
#37835=CARTESIAN_POINT('Origin',(3.42660065607856,0.,4.));
#37836=CARTESIAN_POINT('',(12.8766006560786,7.85109994957766E-5,4.41654344863055));
#37837=CARTESIAN_POINT('',(12.9733993439214,0.000150764780949702,4.41649545414489));
#37838=CARTESIAN_POINT('',(3.42660065607856,4.87367679877478E-13,4.415875));
#37839=CARTESIAN_POINT('Ctrl Pts',(12.8766006560786,7.85109994958138E-5,
4.41654344863055));
#37840=CARTESIAN_POINT('Ctrl Pts',(12.8920208853026,-0.133630732206743,
4.41619751255639));
#37841=CARTESIAN_POINT('Ctrl Pts',(12.9233463932143,-0.405888408666218,
4.27372356364211));
#37842=CARTESIAN_POINT('Ctrl Pts',(12.9705771798136,-0.453501555338242,
3.80962782724943));
#37843=CARTESIAN_POINT('Ctrl Pts',(13.0182930158764,-0.0851462219395619,
3.51558762841831));
#37844=CARTESIAN_POINT('Ctrl Pts',(13.0660088519392,0.361400197209248,3.66639076405307));
#37845=CARTESIAN_POINT('Ctrl Pts',(13.1137246880021,0.476067254403989,4.1235523942958));
#37846=CARTESIAN_POINT('Ctrl Pts',(13.1505886227152,0.226902767145371,4.38908671404106));
#37847=CARTESIAN_POINT('Ctrl Pts',(13.1715472787407,0.0444343739838573,
4.41587777975472));
#37848=CARTESIAN_POINT('Ctrl Pts',(13.1766006560786,0.000342007958933428,
4.41553758638117));
#37849=CARTESIAN_POINT('Ctrl Pts',(12.9733993439214,0.000150764780949724,
4.4164954541449));
#37850=CARTESIAN_POINT('Ctrl Pts',(12.988350764987,-0.12953330947047,4.41589144324702));
#37851=CARTESIAN_POINT('Ctrl Pts',(13.0192074647402,-0.39825874617628,4.28096832590395));
#37852=CARTESIAN_POINT('Ctrl Pts',(13.065969443181,-0.458911634846768,3.82306685936703));
#37853=CARTESIAN_POINT('Ctrl Pts',(13.1136852792439,-0.0993761143989603,
3.51830547777773));
#37854=CARTESIAN_POINT('Ctrl Pts',(13.1614011153067,0.351418020999476,3.65589158776806));
#37855=CARTESIAN_POINT('Ctrl Pts',(13.2091169513695,0.479499580452807,4.10947774749948));
#37856=CARTESIAN_POINT('Ctrl Pts',(13.2464496942411,0.235195791588524,4.38570395495548));
#37857=CARTESIAN_POINT('Ctrl Pts',(13.2678771584251,0.0485170676377186,
4.41576563003508));
#37858=CARTESIAN_POINT('Ctrl Pts',(13.2733993439214,0.000305371599794949,
4.41543889539504));
#37859=CARTESIAN_POINT('Origin',(3.42660065607856,0.,4.));
#37860=CARTESIAN_POINT('',(12.5766006560786,-0.000382134531266273,4.41577416496379));
#37861=CARTESIAN_POINT('',(12.6733993439214,-0.000382453243898073,4.41589767499446));
#37862=CARTESIAN_POINT('',(3.42660065607856,4.87367679877478E-13,4.415875));
#37863=CARTESIAN_POINT('Ctrl Pts',(12.5766006560786,-0.000382134531266193,
4.41577416496379));
#37864=CARTESIAN_POINT('Ctrl Pts',(12.5806839344893,-0.0359587315295452,
4.41609477791077));
#37865=CARTESIAN_POINT('Ctrl Pts',(12.6006724915877,-0.209750441210566,
4.39561070447123));
#37866=CARTESIAN_POINT('Ctrl Pts',(12.6365663273737,-0.4676569254097,4.15232276575852));
#37867=CARTESIAN_POINT('Ctrl Pts',(12.6842821634365,-0.381050985679211,
3.68902512775968));
#37868=CARTESIAN_POINT('Ctrl Pts',(12.7319979994994,0.0554799374235607,
3.5113004999026));
#37869=CARTESIAN_POINT('Ctrl Pts',(12.7797138355622,0.441062780321708,3.78235614259331));
#37870=CARTESIAN_POINT('Ctrl Pts',(12.8274296716251,0.421610885427219,4.2532774884218));
#37871=CARTESIAN_POINT('Ctrl Pts',(12.8597252784638,0.146394963767536,4.4145887178469));
#37872=CARTESIAN_POINT('Ctrl Pts',(12.876115606615,0.00428438860018927,
4.4165543301878));
#37873=CARTESIAN_POINT('Ctrl Pts',(12.8766006560786,7.85109994958138E-5,
4.41654344863055));
#37874=CARTESIAN_POINT('Ctrl Pts',(12.6733993439214,-0.000382453243898042,
4.41589767499447));
#37875=CARTESIAN_POINT('Ctrl Pts',(12.6770138141737,-0.0318505807336982,
4.4161892599907));
#37876=CARTESIAN_POINT('Ctrl Pts',(12.6965335631136,-0.201468625965512,
4.39853963407534));
#37877=CARTESIAN_POINT('Ctrl Pts',(12.7319585907412,-0.462967872677167,
4.16603003860975));
#37878=CARTESIAN_POINT('Ctrl Pts',(12.779674426804,-0.390044463885,3.70038267566003));
#37879=CARTESIAN_POINT('Ctrl Pts',(12.8273902628668,0.0410627776982723,
3.50987851185683));
#37880=CARTESIAN_POINT('Ctrl Pts',(12.8751060989297,0.434461438689172,3.76946045210395));
#37881=CARTESIAN_POINT('Ctrl Pts',(12.9228219349925,0.42888747548329,4.24075040649094));
#37882=CARTESIAN_POINT('Ctrl Pts',(12.9555863499897,0.154617472482897,4.41255553662561));
#37883=CARTESIAN_POINT('Ctrl Pts',(12.9724454862994,0.00842423538524961,
4.41653398830136));
#37884=CARTESIAN_POINT('Ctrl Pts',(12.9733993439214,0.000150764780949724,
4.4164954541449));
#37885=CARTESIAN_POINT('Origin',(3.42660065607856,0.,4.));
#37886=CARTESIAN_POINT('',(12.2766006560786,9.99581421417901E-5,4.41520820259509));
#37887=CARTESIAN_POINT('',(12.3733993439214,3.32456539758885E-5,4.41518865831861));
#37888=CARTESIAN_POINT('',(3.42660065607856,4.87367679877478E-13,4.415875));
#37889=CARTESIAN_POINT('Ctrl Pts',(12.2766006560786,9.99581421418094E-5,
4.41520820259509));
#37890=CARTESIAN_POINT('Ctrl Pts',(12.2852522623637,-0.0755384113923865,
4.41504611816934));
#37891=CARTESIAN_POINT('Ctrl Pts',(12.3098091473364,-0.290455378639464,
4.35903266527152));
#37892=CARTESIAN_POINT('Ctrl Pts',(12.3502713109967,-0.49164800158875,4.0136918729824));
#37893=CARTESIAN_POINT('Ctrl Pts',(12.3979871470595,-0.277420602272412,
3.59386820576715));
#37894=CARTESIAN_POINT('Ctrl Pts',(12.4457029831224,0.191566404775332,3.54700161433684));
#37895=CARTESIAN_POINT('Ctrl Pts',(12.4934188191852,0.484635034689867,3.91613041073711));
#37896=CARTESIAN_POINT('Ctrl Pts',(12.5370513768373,0.345661459897227,4.32409890635003));
#37897=CARTESIAN_POINT('Ctrl Pts',(12.5647786558017,0.102620036091023,4.41484591908716));
#37898=CARTESIAN_POINT('Ctrl Pts',(12.5766006560786,-0.000382134531266193,
4.41577416496379));
#37899=CARTESIAN_POINT('Ctrl Pts',(12.3733993439214,3.32456539758746E-5,
4.41518865831861));
#37900=CARTESIAN_POINT('Ctrl Pts',(12.381582142048,-0.071514873974996,4.41513780400291));
#37901=CARTESIAN_POINT('Ctrl Pts',(12.4056702188623,-0.282203129244181,
4.36350051499509));
#37902=CARTESIAN_POINT('Ctrl Pts',(12.4456635743641,-0.491031474462283,
4.0281658647901));
#37903=CARTESIAN_POINT('Ctrl Pts',(12.493379410427,-0.289261580343189,3.60221492864948));
#37904=CARTESIAN_POINT('Ctrl Pts',(12.5410952464898,0.178141673866572,3.54155614424011));
#37905=CARTESIAN_POINT('Ctrl Pts',(12.5888110825527,0.481954687902679,3.90189340664049));
#37906=CARTESIAN_POINT('Ctrl Pts',(12.6329124483632,0.353693368040787,4.31820342736526));
#37907=CARTESIAN_POINT('Ctrl Pts',(12.6611085354861,0.106623193447456,4.41490615616012));
#37908=CARTESIAN_POINT('Ctrl Pts',(12.6733993439214,-0.000382453243898042,
4.41589767499447));
#37909=CARTESIAN_POINT('Origin',(3.42660065607856,0.,4.));
#37910=CARTESIAN_POINT('',(11.9766006560786,0.000344603143201134,4.41614202049347));
#37911=CARTESIAN_POINT('',(12.0733993439214,0.00037008249145147,4.41602009379307));
#37912=CARTESIAN_POINT('',(3.42660065607856,4.87367679877478E-13,4.415875));
#37913=CARTESIAN_POINT('Ctrl Pts',(11.9766006560786,0.000344603143201134,
4.41614202049347));
#37914=CARTESIAN_POINT('Ctrl Pts',(11.989820590238,-0.114576335025177,4.41511745277426));
#37915=CARTESIAN_POINT('Ctrl Pts',(12.018945803085,-0.369470719226983,4.30593844396252));
#37916=CARTESIAN_POINT('Ctrl Pts',(12.0639762946196,-0.475409571231627,
3.87394063131468));
#37917=CARTESIAN_POINT('Ctrl Pts',(12.1116921306825,-0.151090047408964,
3.53194335553704));
#37918=CARTESIAN_POINT('Ctrl Pts',(12.1594079667453,0.311977791768556,3.61976969834691));
#37919=CARTESIAN_POINT('Ctrl Pts',(12.2071238028081,0.488551624369653,4.05676737776005));
#37920=CARTESIAN_POINT('Ctrl Pts',(12.2461880325859,0.265811525316043,4.37185240566124));
#37921=CARTESIAN_POINT('Ctrl Pts',(12.269346983676,0.0635166157645696,4.41534409728183));
#37922=CARTESIAN_POINT('Ctrl Pts',(12.2766006560786,9.99581421418094E-5,
4.41520820259509));
#37923=CARTESIAN_POINT('Ctrl Pts',(12.0733993439214,0.000370082491451453,
4.41602009379308));
#37924=CARTESIAN_POINT('Ctrl Pts',(12.0861504699224,-0.110559366248508,
4.41499479059613));
#37925=CARTESIAN_POINT('Ctrl Pts',(12.1148068746109,-0.361534897467509,
4.3122242613332));
#37926=CARTESIAN_POINT('Ctrl Pts',(12.1593685579871,-0.478916017555994,
3.88799699566402));
#37927=CARTESIAN_POINT('Ctrl Pts',(12.2070843940499,-0.164809627468288,
3.53659627586117));
#37928=CARTESIAN_POINT('Ctrl Pts',(12.2548002301128,0.300643979445627,3.61074632631782));
#37929=CARTESIAN_POINT('Ctrl Pts',(12.3025160661756,0.490011594032383,4.04235401475446));
#37930=CARTESIAN_POINT('Ctrl Pts',(12.3420491041118,0.274087380788525,4.36772087084377));
#37931=CARTESIAN_POINT('Ctrl Pts',(12.3656768633604,0.0675564760281007,
4.41523665186048));
#37932=CARTESIAN_POINT('Ctrl Pts',(12.3733993439214,3.32456539758746E-5,
4.41518865831861));
#37933=CARTESIAN_POINT('Origin',(3.42660065607856,0.,4.));
#37934=CARTESIAN_POINT('',(11.6766006560786,-0.000272404999166542,4.41633191892761));
#37935=CARTESIAN_POINT('',(11.7733993439214,-0.000215373091504267,4.41642415578018));
#37936=CARTESIAN_POINT('',(3.42660065607856,4.87367679877478E-13,4.415875));
#37937=CARTESIAN_POINT('Ctrl Pts',(11.6766006560786,-0.000272404999166455,
4.41633191892761));
#37938=CARTESIAN_POINT('Ctrl Pts',(11.6784836394247,-0.0166217551361539,
4.41645573239506));
#37939=CARTESIAN_POINT('Ctrl Pts',(11.6962719014584,-0.170944672110958,
4.40814899119985));
#37940=CARTESIAN_POINT('Ctrl Pts',(11.7299654421798,-0.44220355512924,4.21531660568344));
#37941=CARTESIAN_POINT('Ctrl Pts',(11.7776812782426,-0.420270357404582,
3.74450430230823));
#37942=CARTESIAN_POINT('Ctrl Pts',(11.8253971143054,-0.0123964237846327,
3.50831762943));
#37943=CARTESIAN_POINT('Ctrl Pts',(11.8731129503683,0.406861336540243,3.72365044295193));
#37944=CARTESIAN_POINT('Ctrl Pts',(11.9208287864311,0.452492071153857,4.1927593068956));
#37945=CARTESIAN_POINT('Ctrl Pts',(11.9553246883346,0.185075114683736,4.40392780377));
#37946=CARTESIAN_POINT('Ctrl Pts',(11.9739153115504,0.0236883133891,4.41635013933017));
#37947=CARTESIAN_POINT('Ctrl Pts',(11.9766006560786,0.000344603143201134,
4.41614202049347));
#37948=CARTESIAN_POINT('Ctrl Pts',(11.7733993439214,-0.000215373091504231,
4.41642415578018));
#37949=CARTESIAN_POINT('Ctrl Pts',(11.7748135191091,-0.0124870613922979,
4.41650138834433));
#37950=CARTESIAN_POINT('Ctrl Pts',(11.7921329729843,-0.162701432614141,
4.41043584391465));
#37951=CARTESIAN_POINT('Ctrl Pts',(11.8253577055472,-0.435670260442099,
4.22824690363353));
#37952=CARTESIAN_POINT('Ctrl Pts',(11.8730735416101,-0.427612859293677,
3.75699286549843));
#37953=CARTESIAN_POINT('Ctrl Pts',(11.9207893776729,-0.0268719897862959,
3.50889601812151));
#37954=CARTESIAN_POINT('Ctrl Pts',(11.9685052137357,0.398545841420554,3.71178751390968));
#37955=CARTESIAN_POINT('Ctrl Pts',(12.0162210497986,0.457972894034889,4.17934897039372));
#37956=CARTESIAN_POINT('Ctrl Pts',(12.0511857598605,0.193343073938706,4.40127740506484));
#37957=CARTESIAN_POINT('Ctrl Pts',(12.0702451912347,0.0278098881012828,
4.41627371553856));
#37958=CARTESIAN_POINT('Ctrl Pts',(12.0733993439214,0.000370082491451453,
4.41602009379308));
#37959=CARTESIAN_POINT('Origin',(3.42660065607856,0.,4.));
#37960=CARTESIAN_POINT('',(11.3766006560786,-0.000206048103233091,4.41528588740701));
#37961=CARTESIAN_POINT('',(11.4733993439214,-0.000260100423148973,4.41535533657191));
#37962=CARTESIAN_POINT('',(3.42660065607856,4.87367679877478E-13,4.415875));
#37963=CARTESIAN_POINT('Ctrl Pts',(11.3766006560786,-0.000206048103232999,
4.41528588740701));
#37964=CARTESIAN_POINT('Ctrl Pts',(11.383051967299,-0.0565815589273492,
4.41553770218085));
#37965=CARTESIAN_POINT('Ctrl Pts',(11.4054085572071,-0.251630532720247,
4.37854193442951));
#37966=CARTESIAN_POINT('Ctrl Pts',(11.4436704258028,-0.485070265991237,
4.08131458604192));
#37967=CARTESIAN_POINT('Ctrl Pts',(11.4913862618656,-0.330742172127369,
3.63597412121053));
#37968=CARTESIAN_POINT('Ctrl Pts',(11.5391020979284,0.127311547523522,3.52492422212962));
#37969=CARTESIAN_POINT('Ctrl Pts',(11.5868179339912,0.468453114143607,3.85014371984754));
#37970=CARTESIAN_POINT('Ctrl Pts',(11.632650786708,0.382920955827079,4.29471395365306));
#37971=CARTESIAN_POINT('Ctrl Pts',(11.6625783607371,0.121478760105588,4.41540989855421));
#37972=CARTESIAN_POINT('Ctrl Pts',(11.6766006560786,-0.000272404999166455,
4.41633191892761));
#37973=CARTESIAN_POINT('Ctrl Pts',(11.4733993439214,-0.000260100423148869,
4.41535533657191));
#37974=CARTESIAN_POINT('Ctrl Pts',(11.4793818469834,-0.0525169974224216,
4.41565306322741));
#37975=CARTESIAN_POINT('Ctrl Pts',(11.501269628733,-0.243338890257842,4.3822327073369));
#37976=CARTESIAN_POINT('Ctrl Pts',(11.5390626891702,-0.482464979911041,
4.09556551685319));
#37977=CARTESIAN_POINT('Ctrl Pts',(11.586778525233,-0.341319923258817,3.64587299617429));
#37978=CARTESIAN_POINT('Ctrl Pts',(11.6344943612959,0.113264470804062,3.5213807520529));
#37979=CARTESIAN_POINT('Ctrl Pts',(11.6822101973587,0.463836358529674,3.83641192782507));
#37980=CARTESIAN_POINT('Ctrl Pts',(11.7285118582339,0.390694138047139,4.28787953265104));
#37981=CARTESIAN_POINT('Ctrl Pts',(11.7589082404215,0.125533053862222,4.41563275094549));
#37982=CARTESIAN_POINT('Ctrl Pts',(11.7733993439214,-0.000215373091504231,
4.41642415578018));
#37983=CARTESIAN_POINT('Origin',(3.42660065607856,0.,4.));
#37984=CARTESIAN_POINT('',(11.0766006560786,0.000352537510456688,4.41557576695298));
#37985=CARTESIAN_POINT('',(11.1733993439214,0.000319650745578964,4.41547275084625));
#37986=CARTESIAN_POINT('',(3.42660065607856,4.87367679877478E-13,4.415875));
#37987=CARTESIAN_POINT('Ctrl Pts',(11.0766006560786,0.000352537510456667,
4.41557576695298));
#37988=CARTESIAN_POINT('Ctrl Pts',(11.0876202951733,-0.0957751134661499,
4.41480617263661));
#37989=CARTESIAN_POINT('Ctrl Pts',(11.1145452129557,-0.331820540820521,
4.33374203885914));
#37990=CARTESIAN_POINT('Ctrl Pts',(11.1573754094257,-0.488245699001722,
3.94065893278431));
#37991=CARTESIAN_POINT('Ctrl Pts',(11.2050912454886,-0.214150733603143,
3.55723066033293));
#37992=CARTESIAN_POINT('Ctrl Pts',(11.2528070815514,0.256602145595791,3.58040428537983));
#37993=CARTESIAN_POINT('Ctrl Pts',(11.3005229176142,0.491713326162588,3.98889911147238));
#37994=CARTESIAN_POINT('Ctrl Pts',(11.3417874424566,0.304539430122629,4.35098016691413));
#37995=CARTESIAN_POINT('Ctrl Pts',(11.3671466886114,0.0824085130402235,
4.41491686960609));
#37996=CARTESIAN_POINT('Ctrl Pts',(11.3766006560786,-0.000206048103232999,
4.41528588740701));
#37997=CARTESIAN_POINT('Ctrl Pts',(11.1733993439214,0.000319650745578978,
4.41547275084625));
#37998=CARTESIAN_POINT('Ctrl Pts',(11.1839501748577,-0.0917759901056567,
4.4148158243975));
#37999=CARTESIAN_POINT('Ctrl Pts',(11.2104062844816,-0.32368545017211,4.33911969104981));
#38000=CARTESIAN_POINT('Ctrl Pts',(11.2527676727932,-0.489781601228288,
3.95506440219344));
#38001=CARTESIAN_POINT('Ctrl Pts',(11.300483508856,-0.227098200695192,3.56372986339542));
#38002=CARTESIAN_POINT('Ctrl Pts',(11.3481993449188,0.244132971891272,3.57302890392028));
#38003=CARTESIAN_POINT('Ctrl Pts',(11.3959151809817,0.491173079921361,3.97442207176994));
#38004=CARTESIAN_POINT('Ctrl Pts',(11.4376485139825,0.312739912806573,4.34603313379779));
#38005=CARTESIAN_POINT('Ctrl Pts',(11.4634765682958,0.0864149014017155,
4.41486151738456));
#38006=CARTESIAN_POINT('Ctrl Pts',(11.4733993439214,-0.000260100423148869,
4.41535533657191));
#38007=CARTESIAN_POINT('Origin',(3.42660065607856,0.,4.));
#38008=CARTESIAN_POINT('',(10.7766006560786,5.16128798610187E-5,4.41655360457584));
#38009=CARTESIAN_POINT('',(10.8733993439214,0.000125523266313186,4.41651574507477));
#38010=CARTESIAN_POINT('',(3.42660065607856,4.87367679877478E-13,4.415875));
#38011=CARTESIAN_POINT('Ctrl Pts',(10.7766006560786,5.16128798610299E-5,
4.41655360457584));
#38012=CARTESIAN_POINT('Ctrl Pts',(10.7921886230477,-0.135103241057852,
4.41631783152902));
#38013=CARTESIAN_POINT('Ctrl Pts',(10.8236818687044,-0.408598944994929,
4.27108057505162));
#38014=CARTESIAN_POINT('Ctrl Pts',(10.8710803930487,-0.451470021714238,
3.80485891169382));
#38015=CARTESIAN_POINT('Ctrl Pts',(10.9187962291115,-0.080036233235122,
3.51471716883706));
#38016=CARTESIAN_POINT('Ctrl Pts',(10.9665120651743,0.364896059739551,3.6702181168734));
#38017=CARTESIAN_POINT('Ctrl Pts',(11.0142279012372,0.47473868640782,4.1285628425314));
#38018=CARTESIAN_POINT('Ctrl Pts',(11.0509240982053,0.223935965514619,4.3902602363912));
#38019=CARTESIAN_POINT('Ctrl Pts',(11.0717150164857,0.0429714521173939,
4.4159169723618));
#38020=CARTESIAN_POINT('Ctrl Pts',(11.0766006560786,0.000352537510456667,
4.41557576695298));
#38021=CARTESIAN_POINT('Ctrl Pts',(10.8733993439214,0.000125523266313226,
4.41651574507477));
#38022=CARTESIAN_POINT('Ctrl Pts',(10.888518502732,-0.130996444363694,4.41599591363288));
#38023=CARTESIAN_POINT('Ctrl Pts',(10.9195429402303,-0.400997532511054,
4.27840016053723));
#38024=CARTESIAN_POINT('Ctrl Pts',(10.9664726564161,-0.45702143577077,3.81824018018824));
#38025=CARTESIAN_POINT('Ctrl Pts',(11.014188492479,-0.0942939790271268,
3.51728489730359));
#38026=CARTESIAN_POINT('Ctrl Pts',(11.0619043285418,0.355025089556487,3.65961432075161));
#38027=CARTESIAN_POINT('Ctrl Pts',(11.1096201646047,0.478319155637209,4.11452515096033));
#38028=CARTESIAN_POINT('Ctrl Pts',(11.1467851697312,0.23222845252417,4.38693182090163));
#38029=CARTESIAN_POINT('Ctrl Pts',(11.1680448961701,0.0470573247768451,
4.41580613485813));
#38030=CARTESIAN_POINT('Ctrl Pts',(11.1733993439214,0.000319650745578978,
4.41547275084625));
#38031=CARTESIAN_POINT('Origin',(3.42660065607856,0.,4.));
#38032=CARTESIAN_POINT('',(10.4766006560786,-0.000378910032885682,4.4157309619862));
#38033=CARTESIAN_POINT('',(10.5733993439214,-0.000383826598418624,4.41585315377736));
#38034=CARTESIAN_POINT('',(3.42660065607856,4.87367679877478E-13,4.415875));
#38035=CARTESIAN_POINT('Ctrl Pts',(10.4766006560786,-0.000378910032885704,
4.4157309619862));
#38036=CARTESIAN_POINT('Ctrl Pts',(10.4808516722344,-0.0374267536145521,
4.41605913507464));
#38037=CARTESIAN_POINT('Ctrl Pts',(10.5010079670778,-0.212714974368116,
4.3945277200383));
#38038=CARTESIAN_POINT('Ctrl Pts',(10.5370695406088,-0.469236294399976,
4.14738563318641));
#38039=CARTESIAN_POINT('Ctrl Pts',(10.5847853766716,-0.377752434501872,
3.68502647241413));
#38040=CARTESIAN_POINT('Ctrl Pts',(10.6325012127345,0.0606272984676223,
3.51191234851464));
#38041=CARTESIAN_POINT('Ctrl Pts',(10.6802170487973,0.443332050383407,3.78701662516801));
#38042=CARTESIAN_POINT('Ctrl Pts',(10.7279328848602,0.418918158891686,4.25770681210006));
#38043=CARTESIAN_POINT('Ctrl Pts',(10.7600607539539,0.143455624352724,4.41528584951654));
#38044=CARTESIAN_POINT('Ctrl Pts',(10.7762833443601,0.00280285164340033,
4.41655840401831));
#38045=CARTESIAN_POINT('Ctrl Pts',(10.7766006560786,5.16128798610299E-5,
4.41655360457584));
#38046=CARTESIAN_POINT('Ctrl Pts',(10.5733993439214,-0.000383826598418617,
4.41585315377736));
#38047=CARTESIAN_POINT('Ctrl Pts',(10.5771815519187,-0.0333213161677604,
4.41615637378185));
#38048=CARTESIAN_POINT('Ctrl Pts',(10.5968690386037,-0.20443114816448,4.39750812937281));
#38049=CARTESIAN_POINT('Ctrl Pts',(10.6324618039763,-0.464691964107356,
4.16114156306187));
#38050=CARTESIAN_POINT('Ctrl Pts',(10.6801776400391,-0.386865111317189,
3.69628860657276));
#38051=CARTESIAN_POINT('Ctrl Pts',(10.7278934761019,0.0462259258804368,
3.51033849586834));
#38052=CARTESIAN_POINT('Ctrl Pts',(10.7756093121648,0.436866984064762,3.77405207881873));
#38053=CARTESIAN_POINT('Ctrl Pts',(10.8233251482276,0.426326368719826,4.24525711444552));
#38054=CARTESIAN_POINT('Ctrl Pts',(10.8559218254798,0.151674250044741,4.4132974389186));
#38055=CARTESIAN_POINT('Ctrl Pts',(10.8726132240444,0.00694320316194716,
4.41654277368359));
#38056=CARTESIAN_POINT('Ctrl Pts',(10.8733993439214,0.000125523266313226,
4.41651574507477));
#38057=CARTESIAN_POINT('Origin',(3.42660065607856,0.,4.));
#38058=CARTESIAN_POINT('',(10.1766006560786,0.000123197149224082,4.41521991402453));
#38059=CARTESIAN_POINT('',(10.2733993439214,5.7336166378985E-5,4.41519339896199));
#38060=CARTESIAN_POINT('',(3.42660065607856,4.87367679877478E-13,4.415875));
#38061=CARTESIAN_POINT('Ctrl Pts',(10.1766006560786,0.000123197149224097,
4.41521991402453));
#38062=CARTESIAN_POINT('Ctrl Pts',(10.1854200001087,-0.0769762270984491,
4.41501595190525));
#38063=CARTESIAN_POINT('Ctrl Pts',(10.2101446228264,-0.293404201931947,
4.35739193013711));
#38064=CARTESIAN_POINT('Ctrl Pts',(10.2507745242318,-0.491764996345908,
4.00850959581219));
#38065=CARTESIAN_POINT('Ctrl Pts',(10.2984903602946,-0.273124940234581,
3.59096700393021));
#38066=CARTESIAN_POINT('Ctrl Pts',(10.3462061963575,0.196329951061554,3.54904570612073));
#38067=CARTESIAN_POINT('Ctrl Pts',(10.3939220324203,0.485492027373267,3.92124267520431));
#38068=CARTESIAN_POINT('Ctrl Pts',(10.4373868523273,0.34277731801193,4.32616121393696));
#38069=CARTESIAN_POINT('Ctrl Pts',(10.4649463935468,0.101188639822117,4.41483126760997));
#38070=CARTESIAN_POINT('Ctrl Pts',(10.4766006560786,-0.000378910032885704,
4.4157309619862));
#38071=CARTESIAN_POINT('Ctrl Pts',(10.2733993439214,5.73361663789851E-5,
4.41519339896199));
#38072=CARTESIAN_POINT('Ctrl Pts',(10.2817498797931,-0.0729553575157724,
4.41510384014646));
#38073=CARTESIAN_POINT('Ctrl Pts',(10.3060056943524,-0.285157432566911,
4.36192175935665));
#38074=CARTESIAN_POINT('Ctrl Pts',(10.3461667875993,-0.491301045992024,
4.02298928139638));
#38075=CARTESIAN_POINT('Ctrl Pts',(10.3938826236621,-0.285053227451061,
3.599188470261));
#38076=CARTESIAN_POINT('Ctrl Pts',(10.4415984597249,0.182963355965895,3.54345905416307));
#38077=CARTESIAN_POINT('Ctrl Pts',(10.4893142957878,0.482961874346273,3.9069782134126));
#38078=CARTESIAN_POINT('Ctrl Pts',(10.5332479238533,0.35082465130295,4.32033516829581));
#38079=CARTESIAN_POINT('Ctrl Pts',(10.5612762732311,0.105190355120073,4.41488124595214));
#38080=CARTESIAN_POINT('Ctrl Pts',(10.5733993439214,-0.000383826598418617,
4.41585315377736));
#38081=CARTESIAN_POINT('Origin',(3.42660065607856,0.,4.));
#38082=CARTESIAN_POINT('',(9.87660065607859,0.000332404019580576,4.41618417038907));
#38083=CARTESIAN_POINT('',(9.9733993439214,0.000362444897862246,4.41606425076498));
#38084=CARTESIAN_POINT('',(3.42660065607856,4.87367679877478E-13,4.415875));
#38085=CARTESIAN_POINT('Ctrl Pts',(9.87660065607859,0.000332404019580564,
4.41618417038907));
#38086=CARTESIAN_POINT('Ctrl Pts',(9.88998832798303,-0.116016130490024,
4.41516972706101));
#38087=CARTESIAN_POINT('Ctrl Pts',(9.91928127857509,-0.372296869871387,
4.30364082544554));
#38088=CARTESIAN_POINT('Ctrl Pts',(9.96447950785476,-0.474054618562381,
3.8689372536849));
#38089=CARTESIAN_POINT('Ctrl Pts',(10.0121953439176,-0.146148770628728,
3.53037700046135));
#38090=CARTESIAN_POINT('Ctrl Pts',(10.0599111799804,0.315967742161179,3.62307877379278));
#38091=CARTESIAN_POINT('Ctrl Pts',(10.1076270160433,0.487926215535836,4.06191310882887));
#38092=CARTESIAN_POINT('Ctrl Pts',(10.146523508076,0.262848409674369,4.37329037489646));
#38093=CARTESIAN_POINT('Ctrl Pts',(10.1695147214211,0.062069015396409,4.41538378814543));
#38094=CARTESIAN_POINT('Ctrl Pts',(10.1766006560786,0.000123197149224097,
4.41521991402453));
#38095=CARTESIAN_POINT('Ctrl Pts',(9.9733993439214,0.000362444897862267,
4.41606425076498));
#38096=CARTESIAN_POINT('Ctrl Pts',(9.9863182076674,-0.111995531308361,4.41503480155798));
#38097=CARTESIAN_POINT('Ctrl Pts',(10.015142350101,-0.364380386131072,4.30999810797653));
#38098=CARTESIAN_POINT('Ctrl Pts',(10.0598717712222,-0.477709011270712,
3.88295588266498));
#38099=CARTESIAN_POINT('Ctrl Pts',(10.1075876072851,-0.159916626226494,
3.53488507064564));
#38100=CARTESIAN_POINT('Ctrl Pts',(10.1553034433479,0.304729657315094,3.61393645496551));
#38101=CARTESIAN_POINT('Ctrl Pts',(10.2030192794107,0.489538007675758,4.04751593304174));
#38102=CARTESIAN_POINT('Ctrl Pts',(10.2423845796019,0.271127379494919,4.3692182851415));
#38103=CARTESIAN_POINT('Ctrl Pts',(10.2658446011055,0.0661120339180705,
4.41527442296197));
#38104=CARTESIAN_POINT('Ctrl Pts',(10.2733993439214,5.73361663789851E-5,
4.41519339896199));
#38105=CARTESIAN_POINT('Origin',(3.42660065607856,0.,4.));
#38106=CARTESIAN_POINT('',(9.57660065607859,-0.000290304052950346,4.41629504206998));
#38107=CARTESIAN_POINT('',(9.6733993439214,-0.000236899196693507,4.41639317328699));
#38108=CARTESIAN_POINT('',(3.42660065607856,4.87367679877478E-13,4.415875));
#38109=CARTESIAN_POINT('Ctrl Pts',(9.57660065607859,-0.000290304052950335,
4.41629504206998));
#38110=CARTESIAN_POINT('Ctrl Pts',(9.57865137716975,-0.0181001948149981,
4.41643644713422));
#38111=CARTESIAN_POINT('Ctrl Pts',(9.59660737694851,-0.173896467062472,
4.40729888742394));
#38112=CARTESIAN_POINT('Ctrl Pts',(9.63046865541489,-0.444448234747017,
4.21064422964382));
#38113=CARTESIAN_POINT('Ctrl Pts',(9.67818449147773,-0.41755432743774,3.74008922975375));
#38114=CARTESIAN_POINT('Ctrl Pts',(9.72590032754057,-0.00721385634321597,
3.50821428942208));
#38115=CARTESIAN_POINT('Ctrl Pts',(9.77361616360341,0.40975121003073,3.72795373420991));
#38116=CARTESIAN_POINT('Ctrl Pts',(9.82133199966624,0.450435435400681,4.19751745084266));
#38117=CARTESIAN_POINT('Ctrl Pts',(9.85566016382464,0.182118884769847,4.40484283743537));
#38118=CARTESIAN_POINT('Ctrl Pts',(9.87408304929542,0.0222122246324328,
4.41637494063069));
#38119=CARTESIAN_POINT('Ctrl Pts',(9.87660065607859,0.000332404019580564,
4.41618417038907));
#38120=CARTESIAN_POINT('Ctrl Pts',(9.6733993439214,-0.00023689919669354,
4.41639317328699));
#38121=CARTESIAN_POINT('Ctrl Pts',(9.67498125685411,-0.0139668454918635,
4.4164864708936));
#38122=CARTESIAN_POINT('Ctrl Pts',(9.69246844847443,-0.165649677201134,
4.40963259460397));
#38123=CARTESIAN_POINT('Ctrl Pts',(9.72586091878235,-0.438051576325333,
4.22364266437974));
#38124=CARTESIAN_POINT('Ctrl Pts',(9.77357675484519,-0.425028039486299,
3.75249971615691));
#38125=CARTESIAN_POINT('Ctrl Pts',(9.82129259090803,-0.0216947140899849,
3.50864008686857));
#38126=CARTESIAN_POINT('Ctrl Pts',(9.86900842697087,0.401561201071248,3.7160038263529));
#38127=CARTESIAN_POINT('Ctrl Pts',(9.91672426303371,0.456057286475463,4.18416562194019));
#38128=CARTESIAN_POINT('Ctrl Pts',(9.95152123535055,0.190383912560376,4.40224154849284));
#38129=CARTESIAN_POINT('Ctrl Pts',(9.97041292897978,0.0263359008882403,
4.4163022254471));
#38130=CARTESIAN_POINT('Ctrl Pts',(9.9733993439214,0.000362444897862267,
4.41606425076498));
#38131=CARTESIAN_POINT('Origin',(3.42660065607856,0.,4.));
#38132=CARTESIAN_POINT('',(9.27660065607858,-0.000185084181660103,4.41526520375254));
#38133=CARTESIAN_POINT('',(9.37339934392141,-0.000241596553487405,4.41532857883968));
#38134=CARTESIAN_POINT('',(3.42660065607856,4.87367679877478E-13,4.415875));
#38135=CARTESIAN_POINT('Ctrl Pts',(9.27660065607858,-0.000185084181660189,
4.41526520375254));
#38136=CARTESIAN_POINT('Ctrl Pts',(9.28321970504406,-0.0580335922681754,
4.4154966095816));
#38137=CARTESIAN_POINT('Ctrl Pts',(9.30574403269715,-0.254596444523232,
4.37718269734299));
#38138=CARTESIAN_POINT('Ctrl Pts',(9.34417363903789,-0.485900307124067,
4.07619787653679));
#38139=CARTESIAN_POINT('Ctrl Pts',(9.39188947510068,-0.326887306273347,
3.63250862071426));
#38140=CARTESIAN_POINT('Ctrl Pts',(9.43960531116356,0.13231133773591,3.52629235307153));
#38141=CARTESIAN_POINT('Ctrl Pts',(9.48732114722637,0.470006444430667,3.85508910653225));
#38142=CARTESIAN_POINT('Ctrl Pts',(9.53298626219807,0.380123833963086,4.29710958399465));
#38143=CARTESIAN_POINT('Ctrl Pts',(9.56274609848214,0.120032327051623,4.41533971732329));
#38144=CARTESIAN_POINT('Ctrl Pts',(9.57660065607859,-0.000290304052950335,
4.41629504206998));
#38145=CARTESIAN_POINT('Ctrl Pts',(9.3733993439214,-0.000241596553487357,
4.41532857883968));
#38146=CARTESIAN_POINT('Ctrl Pts',(9.37954958472843,-0.0539723465869793,
4.41561177485228));
#38147=CARTESIAN_POINT('Ctrl Pts',(9.40160510422307,-0.246305905820531,
4.3809303471886));
#38148=CARTESIAN_POINT('Ctrl Pts',(9.43956590240532,-0.483445357410111,
4.09047547319903));
#38149=CARTESIAN_POINT('Ctrl Pts',(9.48728173846818,-0.337568794959357,
3.64229546617122));
#38150=CARTESIAN_POINT('Ctrl Pts',(9.53499757453099,0.118302386066128,3.5226010365501));
#38151=CARTESIAN_POINT('Ctrl Pts',(9.58271341059386,0.465534665650901,3.84130942079228));
#38152=CARTESIAN_POINT('Ctrl Pts',(9.62884733372396,0.387920650713885,4.29034844530944));
#38153=CARTESIAN_POINT('Ctrl Pts',(9.65907597816649,0.124080336294106,4.41554841393524));
#38154=CARTESIAN_POINT('Ctrl Pts',(9.6733993439214,-0.00023689919669354,
4.41639317328699));
#38155=CARTESIAN_POINT('Origin',(3.42660065607856,0.,4.));
#38156=CARTESIAN_POINT('',(8.97660065607858,0.000361621133123973,4.41561526113518));
#38157=CARTESIAN_POINT('',(9.0733993439214,0.00033264130393823,4.41550825894961));
#38158=CARTESIAN_POINT('',(3.42660065607856,4.87367679877478E-13,4.415875));
#38159=CARTESIAN_POINT('Ctrl Pts',(8.97660065607858,0.000361621133123963,
4.41561526113518));
#38160=CARTESIAN_POINT('Ctrl Pts',(8.98778803291839,-0.097205817696177,
4.41480833810253));
#38161=CARTESIAN_POINT('Ctrl Pts',(9.01488068844582,-0.334723089553266,
4.33177224018802));
#38162=CARTESIAN_POINT('Ctrl Pts',(9.05787862266083,-0.487593182843731,
3.93551656882348));
#38163=CARTESIAN_POINT('Ctrl Pts',(9.10559445872368,-0.209472459465777,
3.55499829935456));
#38164=CARTESIAN_POINT('Ctrl Pts',(9.15331029478651,0.261010046587687,3.58313193881964));
#38165=CARTESIAN_POINT('Ctrl Pts',(9.20102613084934,0.491803010703882,3.99408193320625));
#38166=CARTESIAN_POINT('Ctrl Pts',(9.24212291794672,0.301599829163518,4.35270650246492));
#38167=CARTESIAN_POINT('Ctrl Pts',(9.26731442635645,0.0809737859182142,
4.41494055172187));
#38168=CARTESIAN_POINT('Ctrl Pts',(9.27660065607858,-0.000185084181660189,
4.41526520375254));
#38169=CARTESIAN_POINT('Ctrl Pts',(9.0733993439214,0.000332641303938268,
4.41550825894961));
#38170=CARTESIAN_POINT('Ctrl Pts',(9.08411791260276,-0.093207009794584,
4.4148098083896));
#38171=CARTESIAN_POINT('Ctrl Pts',(9.11074175997173,-0.326599857706223,
4.33721709571948));
#38172=CARTESIAN_POINT('Ctrl Pts',(9.1532708860283,-0.489280820139143,3.94990505119329));
#38173=CARTESIAN_POINT('Ctrl Pts',(9.20098672209113,-0.222487703095825,
3.56136068709803));
#38174=CARTESIAN_POINT('Ctrl Pts',(9.24870255815399,0.248619295113741,3.57562555337399));
#38175=CARTESIAN_POINT('Ctrl Pts',(9.29641839421681,0.49141536912078,3.97960000382683));
#38176=CARTESIAN_POINT('Ctrl Pts',(9.33798398947263,0.309808547095179,4.34782394055348));
#38177=CARTESIAN_POINT('Ctrl Pts',(9.36364430604082,0.0849819773478622,
4.41487939515448));
#38178=CARTESIAN_POINT('Ctrl Pts',(9.3733993439214,-0.000241596553487357,
4.41532857883968));
#38179=CARTESIAN_POINT('Origin',(3.42660065607856,0.,4.));
#38180=CARTESIAN_POINT('',(8.67660065607859,2.43999233753954E-5,4.41655967853978));
#38181=CARTESIAN_POINT('',(8.77339934392141,9.9565801791445E-5,4.41653262406943));
#38182=CARTESIAN_POINT('',(3.42660065607856,4.87367679877478E-13,4.415875));
#38183=CARTESIAN_POINT('Ctrl Pts',(8.67660065607859,2.43999233753836E-5,
4.41655967853978));
#38184=CARTESIAN_POINT('Ctrl Pts',(8.69235636079272,-0.136579453435425,
4.41644398151286));
#38185=CARTESIAN_POINT('Ctrl Pts',(8.72401734419445,-0.411298873006737,
4.26841067400337));
#38186=CARTESIAN_POINT('Ctrl Pts',(8.7715836062838,-0.449388340942622,3.80011167148426));
#38187=CARTESIAN_POINT('Ctrl Pts',(8.81929944234665,-0.0749173544856965,
3.51390061216986));
#38188=CARTESIAN_POINT('Ctrl Pts',(8.86701527840948,0.368351391347115,3.67408210030036));
#38189=CARTESIAN_POINT('Ctrl Pts',(8.91473111447233,0.473357386691186,4.13355901061654));
#38190=CARTESIAN_POINT('Ctrl Pts',(8.95125957369535,0.220969504140389,4.39141457480799));
#38191=CARTESIAN_POINT('Ctrl Pts',(8.97188275423077,0.0415074238114615,
4.41595555392421));
#38192=CARTESIAN_POINT('Ctrl Pts',(8.97660065607858,0.000361621133123963,
4.41561526113518));
#38193=CARTESIAN_POINT('Ctrl Pts',(8.77339934392141,9.95658017914599E-5,
4.41653262406943));
#38194=CARTESIAN_POINT('Ctrl Pts',(8.78868624047708,-0.132462770989084,
4.416105976883));
#38195=CARTESIAN_POINT('Ctrl Pts',(8.81987841572037,-0.403726445587972,
4.27580529254432));
#38196=CARTESIAN_POINT('Ctrl Pts',(8.86697586965126,-0.455080472922433,
3.81343369002772));
#38197=CARTESIAN_POINT('Ctrl Pts',(8.91469170571412,-0.0892013699275644,
3.51631793453238));
#38198=CARTESIAN_POINT('Ctrl Pts',(8.96240754177693,0.358592723611288,3.66337486216116));
#38199=CARTESIAN_POINT('Ctrl Pts',(9.0101233778398,0.477085601399612,4.11955983351088));
#38200=CARTESIAN_POINT('Ctrl Pts',(9.04712064522126,0.229261233371815,4.38814011953822));
#38201=CARTESIAN_POINT('Ctrl Pts',(9.06821263391514,0.0455964315317218,
4.41584623882512));
#38202=CARTESIAN_POINT('Ctrl Pts',(9.0733993439214,0.000332641303938268,
4.41550825894961));
#38203=CARTESIAN_POINT('Origin',(3.42660065607856,0.,4.));
#38204=CARTESIAN_POINT('',(8.37660065607859,-0.000374086211409503,4.41568853448753));
#38205=CARTESIAN_POINT('',(8.47339934392141,-0.000383538171196851,4.41580895574666));
#38206=CARTESIAN_POINT('',(3.42660065607856,4.87367679877478E-13,4.415875));
#38207=CARTESIAN_POINT('Ctrl Pts',(8.37660065607859,-0.000374086211409545,
4.41568853448753));
#38208=CARTESIAN_POINT('Ctrl Pts',(8.38101940997943,-0.0388937529272332,
4.41602262289185));
#38209=CARTESIAN_POINT('Ctrl Pts',(8.40134344256788,-0.215680110827853,
4.3934260635833));
#38210=CARTESIAN_POINT('Ctrl Pts',(8.43757275384394,-0.470763542849379,
4.14243212971755));
#38211=CARTESIAN_POINT('Ctrl Pts',(8.48528858990678,-0.37441192437669,3.68106280283335));
#38212=CARTESIAN_POINT('Ctrl Pts',(8.53300442596962,0.0657679253190804,
3.51257841158684));
#38213=CARTESIAN_POINT('Ctrl Pts',(8.58072026203246,0.445552077224736,3.79170076492532));
#38214=CARTESIAN_POINT('Ctrl Pts',(8.62843609809529,0.41617890091499,4.26210751092856));
#38215=CARTESIAN_POINT('Ctrl Pts',(8.66039622944401,0.140517691799823,4.41596716726027));
#38216=CARTESIAN_POINT('Ctrl Pts',(8.6764510821051,0.00132122424898086,
4.41656077688887));
#38217=CARTESIAN_POINT('Ctrl Pts',(8.67660065607859,2.43999233753836E-5,
4.41655967853978));
#38218=CARTESIAN_POINT('Ctrl Pts',(8.47339934392141,-0.000383538171196768,
4.41580895574666));
#38219=CARTESIAN_POINT('Ctrl Pts',(8.47734928966379,-0.0347911067166248,
4.41612244784963));
#38220=CARTESIAN_POINT('Ctrl Pts',(8.4972045140938,-0.207394442561863,4.39645832432586));
#38221=CARTESIAN_POINT('Ctrl Pts',(8.5329650172114,-0.466364439759318,4.15623518867385));
#38222=CARTESIAN_POINT('Ctrl Pts',(8.58068085327425,-0.383642787608637,
3.69222827230584));
#38223=CARTESIAN_POINT('Ctrl Pts',(8.62839668933707,0.0513839395061145,
3.51085286915611));
#38224=CARTESIAN_POINT('Ctrl Pts',(8.67611252539993,0.439224004328866,3.77866880275638));
#38225=CARTESIAN_POINT('Ctrl Pts',(8.72382836146275,0.42371790764641,4.24973658040369));
#38226=CARTESIAN_POINT('Ctrl Pts',(8.75625730096992,0.148732406864234,4.41402322426773));
#38227=CARTESIAN_POINT('Ctrl Pts',(8.77278096178947,0.00546194790078228,
4.41654988270631));
#38228=CARTESIAN_POINT('Ctrl Pts',(8.77339934392141,9.95658017914599E-5,
4.41653262406943));
#38229=CARTESIAN_POINT('Origin',(3.42660065607856,0.,4.));
#38230=CARTESIAN_POINT('',(8.07660065607859,0.000145957947245773,4.41523406184916));
#38231=CARTESIAN_POINT('',(8.1733993439214,8.12049300508987E-5,4.41520065480005));
#38232=CARTESIAN_POINT('',(3.42660065607856,4.87367679877478E-13,4.415875));
#38233=CARTESIAN_POINT('Ctrl Pts',(8.07660065607858,0.00014595794724577,
4.41523406184916));
#38234=CARTESIAN_POINT('Ctrl Pts',(8.08558773785375,-0.0784131624224431,
4.41498734772332));
#38235=CARTESIAN_POINT('Ctrl Pts',(8.11048009831652,-0.296350794919178,
4.35572875890285));
#38236=CARTESIAN_POINT('Ctrl Pts',(8.15127773746691,-0.491827368180951,
4.00332637343646));
#38237=CARTESIAN_POINT('Ctrl Pts',(8.19899357352975,-0.268798940774433,
3.58811123553743));
#38238=CARTESIAN_POINT('Ctrl Pts',(8.24670940959259,0.201071689948468,3.55113988776764));
#38239=CARTESIAN_POINT('Ctrl Pts',(8.29442524565542,0.486295093906121,3.92636368766143));
#38240=CARTESIAN_POINT('Ctrl Pts',(8.33772232781743,0.339888039743562,4.32819890206972));
#38241=CARTESIAN_POINT('Ctrl Pts',(8.36511413129181,0.0997575609540166,
4.41482007364463));
#38242=CARTESIAN_POINT('Ctrl Pts',(8.37660065607859,-0.000374086211409545,
4.41568853448753));
#38243=CARTESIAN_POINT('Ctrl Pts',(8.1733993439214,8.12049300509751E-5,
4.41520065480005));
#38244=CARTESIAN_POINT('Ctrl Pts',(8.18191761753811,-0.0743948540356096,
4.41507113968239));
#38245=CARTESIAN_POINT('Ctrl Pts',(8.20634116984244,-0.288109900049694,
4.36032095112539));
#38246=CARTESIAN_POINT('Ctrl Pts',(8.24667000083438,-0.491516046133,4.01781014446235));
#38247=CARTESIAN_POINT('Ctrl Pts',(8.29438583689722,-0.280813212199106,
3.59620653211525));
#38248=CARTESIAN_POINT('Ctrl Pts',(8.34210167296004,0.187764715363875,3.54541267448783));
#38249=CARTESIAN_POINT('Ctrl Pts',(8.38981750902289,0.483915415676709,3.91207335260334));
#38250=CARTESIAN_POINT('Ctrl Pts',(8.43358339934334,0.347950231939931,4.32244196179047));
#38251=CARTESIAN_POINT('Ctrl Pts',(8.46144401097618,0.1037581297464,4.41486010664565));
#38252=CARTESIAN_POINT('Ctrl Pts',(8.47339934392141,-0.000383538171196768,
4.41580895574666));
#38253=CARTESIAN_POINT('Origin',(3.42660065607856,0.,4.));
#38254=CARTESIAN_POINT('',(7.77660065607858,0.000318631424802313,4.41622521972442));
#38255=CARTESIAN_POINT('',(7.8733993439214,0.000353153796088606,4.4161078667978));
#38256=CARTESIAN_POINT('',(3.42660065607856,4.87367679877478E-13,4.415875));
#38257=CARTESIAN_POINT('Ctrl Pts',(7.77660065607859,0.000318631424802297,
4.41622521972442));
#38258=CARTESIAN_POINT('Ctrl Pts',(7.79015606572807,-0.117457481003694,
4.41522659035305));
#38259=CARTESIAN_POINT('Ctrl Pts',(7.81961675406517,-0.375115671948731,
4.30131743988157));
#38260=CARTESIAN_POINT('Ctrl Pts',(7.86498272108989,-0.472647010158531,
3.86394843388276));
#38261=CARTESIAN_POINT('Ctrl Pts',(7.91269855715272,-0.141191260335066,
3.52886280888004));
#38262=CARTESIAN_POINT('Ctrl Pts',(7.96041439321556,0.31992259635559,3.62642971585976));
#38263=CARTESIAN_POINT('Ctrl Pts',(8.0081302292784,0.48724661017382,4.0670519628834));
#38264=CARTESIAN_POINT('Ctrl Pts',(8.04685898356608,0.259884401562094,4.37470733986759));
#38265=CARTESIAN_POINT('Ctrl Pts',(8.06968245916614,0.0606202562326388,
4.41542398077349));
#38266=CARTESIAN_POINT('Ctrl Pts',(8.07660065607858,0.00014595794724577,
4.41523406184916));
#38267=CARTESIAN_POINT('Ctrl Pts',(7.8733993439214,0.000353153796088627,
4.4161078667978));
#38268=CARTESIAN_POINT('Ctrl Pts',(7.88648594541244,-0.113432877329791,
4.41507910421771));
#38269=CARTESIAN_POINT('Ctrl Pts',(7.9154778255911,-0.367219156371593,4.30774647947464));
#38270=CARTESIAN_POINT('Ctrl Pts',(7.96037498445733,-0.476448943335793,
3.87792777037096));
#38271=CARTESIAN_POINT('Ctrl Pts',(8.0080908205202,-0.1550058622045,3.53322552818936));
#38272=CARTESIAN_POINT('Ctrl Pts',(8.05580665658301,0.308781487260178,3.61716946571973));
#38273=CARTESIAN_POINT('Ctrl Pts',(8.10352249264587,0.489010045760349,4.0526725734847));
#38274=CARTESIAN_POINT('Ctrl Pts',(8.14272005509199,0.26816615642074,4.37069430501912));
#38275=CARTESIAN_POINT('Ctrl Pts',(8.1660123388505,0.064666477720629,4.4153129696744));
#38276=CARTESIAN_POINT('Ctrl Pts',(8.1733993439214,8.12049300509751E-5,
4.41520065480005));
#38277=CARTESIAN_POINT('Origin',(3.42660065607856,0.,4.));
#38278=CARTESIAN_POINT('',(7.47660065607859,-0.000306770237538029,4.41625647512786));
#38279=CARTESIAN_POINT('',(7.5733993439214,-0.000257198714157858,4.41635988094829));
#38280=CARTESIAN_POINT('',(3.42660065607856,4.87367679877478E-13,4.415875));
#38281=CARTESIAN_POINT('Ctrl Pts',(7.47660065607859,-0.00030677023753798,
4.41625647512786));
#38282=CARTESIAN_POINT('Ctrl Pts',(7.47881911491479,-0.0195780710793754,
4.41641565502598));
#38283=CARTESIAN_POINT('Ctrl Pts',(7.4969428524386,-0.176849480241104,4.4064317922735));
#38284=CARTESIAN_POINT('Ctrl Pts',(7.53097186865002,-0.44664354691983,4.20594845626764));
#38285=CARTESIAN_POINT('Ctrl Pts',(7.57868770471286,-0.414791917646955,
3.73570302684109));
#38286=CARTESIAN_POINT('Ctrl Pts',(7.62640354077569,-0.00203048755240202,
3.50816557464413));
#38287=CARTESIAN_POINT('Ctrl Pts',(7.67411937683853,0.412595570264971,3.73228724307244));
#38288=CARTESIAN_POINT('Ctrl Pts',(7.72183521290137,0.448328767436039,4.20225365549051));
#38289=CARTESIAN_POINT('Ctrl Pts',(7.75599563931472,0.179163779268806,4.40574053813273));
#38290=CARTESIAN_POINT('Ctrl Pts',(7.77425078704046,0.0207354574140521,
4.41639833498254));
#38291=CARTESIAN_POINT('Ctrl Pts',(7.77660065607859,0.000318631424802297,
4.41622521972442));
#38292=CARTESIAN_POINT('Ctrl Pts',(7.5733993439214,-0.000257198714157839,
4.41635988094829));
#38293=CARTESIAN_POINT('Ctrl Pts',(7.57514899459915,-0.0154461882200338,
4.41646996636401));
#38294=CARTESIAN_POINT('Ctrl Pts',(7.59280392396451,-0.168599214901356,
4.40881268721627));
#38295=CARTESIAN_POINT('Ctrl Pts',(7.62636413201748,-0.440384235482588,
4.21901358396786));
#38296=CARTESIAN_POINT('Ctrl Pts',(7.67407996808031,-0.422396009600076,
3.7480340579683));
#38297=CARTESIAN_POINT('Ctrl Pts',(7.72179580414317,-0.0165150286377962,
3.50843873354525));
#38298=CARTESIAN_POINT('Ctrl Pts',(7.76951164020598,0.404531957204003,3.72025168374225));
#38299=CARTESIAN_POINT('Ctrl Pts',(7.81722747626884,0.454091022239626,4.18896181724392));
#38300=CARTESIAN_POINT('Ctrl Pts',(7.85185671084063,0.187425762196077,4.40318800700955));
#38301=CARTESIAN_POINT('Ctrl Pts',(7.87058066672482,0.02486112795907,4.41632944836175));
#38302=CARTESIAN_POINT('Ctrl Pts',(7.8733993439214,0.000353153796088627,
4.4161078667978));
#38303=CARTESIAN_POINT('Origin',(3.42660065607856,0.,4.));
#38304=CARTESIAN_POINT('',(7.17660065607858,-0.000163391746992416,4.4152468210878));
#38305=CARTESIAN_POINT('',(7.2733993439214,-0.000222139526412562,4.4153039283715));
#38306=CARTESIAN_POINT('',(3.42660065607856,4.87367679877478E-13,4.415875));
#38307=CARTESIAN_POINT('Ctrl Pts',(7.17660065607859,-0.000163391746992363,
4.4152468210878));
#38308=CARTESIAN_POINT('Ctrl Pts',(7.18338744278911,-0.0594844418834033,
4.41545575762517));
#38309=CARTESIAN_POINT('Ctrl Pts',(7.20607950818724,-0.257561782965025,
4.37580284351512));
#38310=CARTESIAN_POINT('Ctrl Pts',(7.24467685227299,-0.486676365692783,
4.07107270446015));
#38311=CARTESIAN_POINT('Ctrl Pts',(7.29239268833582,-0.322996137187983,
3.62908393881966));
#38312=CARTESIAN_POINT('Ctrl Pts',(7.34010852439867,0.137296434535941,3.52771310152703));
#38313=CARTESIAN_POINT('Ctrl Pts',(7.3878243604615,0.471507566988788,3.86005058906394));
#38314=CARTESIAN_POINT('Ctrl Pts',(7.43332173768814,0.377318713751663,4.29947917201381));
#38315=CARTESIAN_POINT('Ctrl Pts',(7.46291383622717,0.118587850938607,4.41527441201542));
#38316=CARTESIAN_POINT('Ctrl Pts',(7.47660065607859,-0.00030677023753798,
4.41625647512786));
#38317=CARTESIAN_POINT('Ctrl Pts',(7.2733993439214,-0.000222139526412493,
4.4153039283715));
#38318=CARTESIAN_POINT('Ctrl Pts',(7.27971732247348,-0.0554265094472961,
4.41557047734173));
#38319=CARTESIAN_POINT('Ctrl Pts',(7.30194057971316,-0.249272617462211,
4.37960776139715));
#38320=CARTESIAN_POINT('Ctrl Pts',(7.34006911564044,-0.484372034479295,
4.08537538031203));
#38321=CARTESIAN_POINT('Ctrl Pts',(7.3877849517033,-0.333780171974684,3.63875766810317));
#38322=CARTESIAN_POINT('Ctrl Pts',(7.43550078776612,0.123327161313159,3.52387434835784));
#38323=CARTESIAN_POINT('Ctrl Pts',(7.48321662382897,0.467181263150904,3.84622454030349));
#38324=CARTESIAN_POINT('Ctrl Pts',(7.52918280921405,0.385138488472668,4.29279105563264));
#38325=CARTESIAN_POINT('Ctrl Pts',(7.55924371591154,0.122630008444172,4.41546922990911));
#38326=CARTESIAN_POINT('Ctrl Pts',(7.5733993439214,-0.000257198714157839,
4.41635988094829));
#38327=CARTESIAN_POINT('Origin',(3.42660065607856,0.,4.));
#38328=CARTESIAN_POINT('',(6.87660065607859,0.000369753976522709,4.4156559906262));
#38329=CARTESIAN_POINT('',(6.9733993439214,0.000344359613660638,4.41554532105972));
#38330=CARTESIAN_POINT('',(3.42660065607856,4.87367679877478E-13,4.415875));
#38331=CARTESIAN_POINT('Ctrl Pts',(6.87660065607859,0.000369753976522759,
4.4156559906262));
#38332=CARTESIAN_POINT('Ctrl Pts',(6.88795577066343,-0.0986361616094132,
4.41481368816743));
#38333=CARTESIAN_POINT('Ctrl Pts',(6.91521616393589,-0.337621850525623,
4.32977807754403));
#38334=CARTESIAN_POINT('Ctrl Pts',(6.95838183589596,-0.486886005735063,
3.93038141845316));
#38335=CARTESIAN_POINT('Ctrl Pts',(7.0060976719588,-0.204771183672361,3.55281534000283));
#38336=CARTESIAN_POINT('Ctrl Pts',(7.05381350802163,0.265389096458903,3.58590591031157));
#38337=CARTESIAN_POINT('Ctrl Pts',(7.10152934408448,0.491837993618785,3.99926540470374));
#38338=CARTESIAN_POINT('Ctrl Pts',(7.14245839343679,0.298657604039877,4.35441002681052));
#38339=CARTESIAN_POINT('Ctrl Pts',(7.16748216410149,0.0795383202432945,
4.41496610118));
#38340=CARTESIAN_POINT('Ctrl Pts',(7.17660065607859,-0.000163391746992363,
4.4152468210878));
#38341=CARTESIAN_POINT('Ctrl Pts',(6.9733993439214,0.00034435961366068,
4.41554532105972));
#38342=CARTESIAN_POINT('Ctrl Pts',(6.9842856503478,-0.0946377878655052,
4.41480662962373));
#38343=CARTESIAN_POINT('Ctrl Pts',(7.0110772354618,-0.329510302625179,4.33529054280597));
#38344=CARTESIAN_POINT('Ctrl Pts',(7.05377409926342,-0.488725618924084,
3.94475128051735));
#38345=CARTESIAN_POINT('Ctrl Pts',(7.10148993532626,-0.21785253135038,3.55904022429238));
#38346=CARTESIAN_POINT('Ctrl Pts',(7.14920577138909,0.253078023397415,3.57826934481931));
#38347=CARTESIAN_POINT('Ctrl Pts',(7.19692160745195,0.491603063369337,3.98478019943955));
#38348=CARTESIAN_POINT('Ctrl Pts',(7.2383194649627,0.306874094293292,4.34959156107453));
#38349=CARTESIAN_POINT('Ctrl Pts',(7.26381204378586,0.0835484619188193,
4.41489945011039));
#38350=CARTESIAN_POINT('Ctrl Pts',(7.2733993439214,-0.000222139526412493,
4.4153039283715));
#38351=CARTESIAN_POINT('Origin',(3.42660065607856,0.,4.));
#38352=CARTESIAN_POINT('',(6.57660065607858,1.8302248101926E-5,4.41656360501758));
#38353=CARTESIAN_POINT('',(6.6733993439214,7.63499956435865E-5,4.4165465803965));
#38354=CARTESIAN_POINT('',(3.42660065607856,4.87367679877478E-13,4.415875));
#38355=CARTESIAN_POINT('Ctrl Pts',(6.57660065607858,1.83022481018748E-5,
4.41656360501758));
#38356=CARTESIAN_POINT('Ctrl Pts',(6.57661881985014,-0.000139156870309867,
4.41656362372179));
#38357=CARTESIAN_POINT('Ctrl Pts',(6.59254226230931,-0.138177237712184,
4.41649399470799));
#38358=CARTESIAN_POINT('Ctrl Pts',(6.62437098345609,-0.41404349770976,4.26553045144514));
#38359=CARTESIAN_POINT('Ctrl Pts',(6.67208681951894,-0.447234019333667,
3.79538894860702));
#38360=CARTESIAN_POINT('Ctrl Pts',(6.71980265558177,-0.0698021891909718,
3.51313682319347));
#38361=CARTESIAN_POINT('Ctrl Pts',(6.76751849164461,0.371772181936036,3.67798293440124));
#38362=CARTESIAN_POINT('Ctrl Pts',(6.81523432770745,0.471920133146607,4.13853999974893));
#38363=CARTESIAN_POINT('Ctrl Pts',(6.85159504918544,0.21800401543618,4.39254992240466));
#38364=CARTESIAN_POINT('Ctrl Pts',(6.87205049197582,0.0400429038769189,
4.41599351380864));
#38365=CARTESIAN_POINT('Ctrl Pts',(6.87660065607859,0.000369753976522759,
4.4156559906262));
#38366=CARTESIAN_POINT('Ctrl Pts',(6.6733993439214,7.63499956435956E-5,
4.4165465803965));
#38367=CARTESIAN_POINT('Ctrl Pts',(6.68885397822212,-0.133927014866661,
4.41622291450327));
#38368=CARTESIAN_POINT('Ctrl Pts',(6.72021389121046,-0.406451392834186,
4.27318229388465));
#38369=CARTESIAN_POINT('Ctrl Pts',(6.76747908288639,-0.453085647428837,
3.80864864857145));
#38370=CARTESIAN_POINT('Ctrl Pts',(6.81519491894923,-0.0841006081168706,
3.51540431248109));
#38371=CARTESIAN_POINT('Ctrl Pts',(6.86291075501207,0.362121456530253,3.66717299786736));
#38372=CARTESIAN_POINT('Ctrl Pts',(6.91062659107491,0.475798562415156,4.124581128109));
#38373=CARTESIAN_POINT('Ctrl Pts',(6.94745612071136,0.226294304474162,4.38932900794447));
#38374=CARTESIAN_POINT('Ctrl Pts',(6.96838037166019,0.0441344886838037,
4.41588588393584));
#38375=CARTESIAN_POINT('Ctrl Pts',(6.9733993439214,0.00034435961366068,
4.41554532105972));
#38376=CARTESIAN_POINT('Origin',(3.42660065607856,0.,4.));
#38377=CARTESIAN_POINT('',(6.27660065607859,-8.94903747701068E-6,4.41582842213685));
#38378=CARTESIAN_POINT('',(6.3733993439214,-0.000441664590319634,4.4157663968931));
#38379=CARTESIAN_POINT('',(3.42660065607856,4.87367679877478E-13,4.415875));
#38380=CARTESIAN_POINT('Ctrl Pts',(6.27660065607859,-8.94903747701223E-6,
4.41582842213685));
#38381=CARTESIAN_POINT('Ctrl Pts',(6.28118714772447,-0.0399801639742102,
4.41579747358059));
#38382=CARTESIAN_POINT('Ctrl Pts',(6.29372627871415,-0.149263049162913,
4.40013952362907));
#38383=CARTESIAN_POINT('Ctrl Pts',(6.31421804904765,-0.307151379675736,
4.3060270879454));
#38384=CARTESIAN_POINT('Ctrl Pts',(6.33807596707907,-0.416657206472865,
4.12081787696614));
#38385=CARTESIAN_POINT('Ctrl Pts',(6.36193388511048,-0.422829889105799,
3.9075587958503));
#38386=CARTESIAN_POINT('Ctrl Pts',(6.39374444248571,-0.296437506874183,
3.64987069373525));
#38387=CARTESIAN_POINT('Ctrl Pts',(6.43350763920474,0.0703302468340302,
3.51324810367198));
#38388=CARTESIAN_POINT('Ctrl Pts',(6.48122347526758,0.448014600657906,3.7964368525222));
#38389=CARTESIAN_POINT('Ctrl Pts',(6.52892114755886,0.413253290380966,4.26628466471864));
#38390=CARTESIAN_POINT('Ctrl Pts',(6.56071354116253,0.137741412285014,4.41654724519979));
#38391=CARTESIAN_POINT('Ctrl Pts',(6.57660065607858,1.83022481018748E-5,
4.41656360501758));
#38392=CARTESIAN_POINT('Ctrl Pts',(6.3733993439214,-0.000441664590319611,
4.4157663968931));
#38393=CARTESIAN_POINT('Ctrl Pts',(6.37751702740883,-0.0362476131304844,
4.41610293027605));
#38394=CARTESIAN_POINT('Ctrl Pts',(6.39753998958387,-0.210006484715375,
4.39546152579387));
#38395=CARTESIAN_POINT('Ctrl Pts',(6.43346823044653,-0.468271923807345,
4.15124960425567));
#38396=CARTESIAN_POINT('Ctrl Pts',(6.48118406650937,-0.380227249479543,
3.6882349865083));
#38397=CARTESIAN_POINT('Ctrl Pts',(6.52889990257221,0.0564566449812287,
3.51140415777354));
#38398=CARTESIAN_POINT('Ctrl Pts',(6.57661573863504,0.441574375138847,3.78331933667001));
#38399=CARTESIAN_POINT('Ctrl Pts',(6.62433157469789,0.421040068198854,4.25418342072721));
#38400=CARTESIAN_POINT('Ctrl Pts',(6.65659277646,0.145792717270209,4.41473316952435));
#38401=CARTESIAN_POINT('Ctrl Pts',(6.6729486995345,0.00398377756883227,
4.41655601822694));
#38402=CARTESIAN_POINT('Ctrl Pts',(6.6733993439214,7.63499956435956E-5,
4.4165465803965));
#38403=CARTESIAN_POINT('Origin',(3.42660065607856,0.,4.));
#38404=CARTESIAN_POINT('',(5.97660065607859,-9.19412645702589E-6,4.41589218083175));
#38405=CARTESIAN_POINT('',(6.0733993439214,-6.65563173402051E-6,4.41590255337155));
#38406=CARTESIAN_POINT('',(3.42660065607856,4.87367679877478E-13,4.415875));
#38407=CARTESIAN_POINT('Ctrl Pts',(5.97660065607858,-9.19412645705893E-6,
4.41589218083175));
#38408=CARTESIAN_POINT('Ctrl Pts',(5.97780283625498,-0.0104787976275591,
4.4159022685469));
#38409=CARTESIAN_POINT('Ctrl Pts',(5.98695765577519,-0.0902010538040918,
4.41295272969856));
#38410=CARTESIAN_POINT('Ctrl Pts',(6.0040651146392,-0.23587461323539,4.36380751861078));
#38411=CARTESIAN_POINT('Ctrl Pts',(6.02792303267061,-0.381351759249696,
4.20630938167977));
#38412=CARTESIAN_POINT('Ctrl Pts',(6.05178095070204,-0.433578399193506,
3.9983625870902));
#38413=CARTESIAN_POINT('Ctrl Pts',(6.07563886873346,-0.379782579589031,
3.79081692866841));
#38414=CARTESIAN_POINT('Ctrl Pts',(6.09949678676487,-0.233120953551068,
3.63442082419035));
#38415=CARTESIAN_POINT('Ctrl Pts',(6.12335470479629,-0.0294522997972467,
3.5674214393556));
#38416=CARTESIAN_POINT('Ctrl Pts',(6.14721262282771,0.181413325723775,3.60619428643423));
#38417=CARTESIAN_POINT('Ctrl Pts',(6.17107054085913,0.347927737305898,3.74127281623538));
#38418=CARTESIAN_POINT('Ctrl Pts',(6.19492845889055,0.429346806292137,3.93959933010928));
#38419=CARTESIAN_POINT('Ctrl Pts',(6.21878637692197,0.405811992579865,4.15272917617017));
#38420=CARTESIAN_POINT('Ctrl Pts',(6.24264429495339,0.282982581651336,4.32844890303245));
#38421=CARTESIAN_POINT('Ctrl Pts',(6.26191572133893,0.127967070080381,4.40561019629887));
#38422=CARTESIAN_POINT('Ctrl Pts',(6.27323450838066,0.029326984292613,4.415851136102));
#38423=CARTESIAN_POINT('Ctrl Pts',(6.27660065607859,-8.94903747701223E-6,
4.41582842213685));
#38424=CARTESIAN_POINT('Ctrl Pts',(6.0733993439214,-6.65563173397714E-6,
4.41590255337156));
#38425=CARTESIAN_POINT('Ctrl Pts',(6.07413271593935,-0.00639299139291402,
4.41590724351385));
#38426=CARTESIAN_POINT('Ctrl Pts',(6.0828187273011,-0.0820297780542147,
4.41420140028919));
#38427=CARTESIAN_POINT('Ctrl Pts',(6.09945737800665,-0.2250554921608,4.3705991908187));
#38428=CARTESIAN_POINT('Ctrl Pts',(6.12331529603809,-0.375113923638194,
4.21744656883549));
#38429=CARTESIAN_POINT('Ctrl Pts',(6.1471732140695,-0.433431396087355,4.01114207710762));
#38430=CARTESIAN_POINT('Ctrl Pts',(6.17103113210093,-0.385792139046387,
3.80207577201042));
#38431=CARTESIAN_POINT('Ctrl Pts',(6.19488905013233,-0.243761337718234,
3.64147770828707));
#38432=CARTESIAN_POINT('Ctrl Pts',(6.21874696816376,-0.042227823444436,
3.56841523311022));
#38433=CARTESIAN_POINT('Ctrl Pts',(6.24260488619517,0.16982704650124,3.60113783246665));
#38434=CARTESIAN_POINT('Ctrl Pts',(6.2664628042266,0.339985970990829,3.73091992247201));
#38435=CARTESIAN_POINT('Ctrl Pts',(6.29032072225801,0.427700638223926,3.92738904240251));
#38436=CARTESIAN_POINT('Ctrl Pts',(6.31417864028943,0.409561128158778,4.13996490148311));
#38437=CARTESIAN_POINT('Ctrl Pts',(6.34187151417723,0.27471212230801,4.35031587281991));
#38438=CARTESIAN_POINT('Ctrl Pts',(6.36161174872122,0.102059178040878,4.41480301073152));
#38439=CARTESIAN_POINT('Ctrl Pts',(6.3733993439214,-0.000441664590319611,
4.4157663968931));
#38440=CARTESIAN_POINT('Origin',(3.42660065607856,0.,4.));
#38441=CARTESIAN_POINT('',(5.67660065607858,1.06631253201556E-5,4.41586554077139));
#38442=CARTESIAN_POINT('',(5.7733993439214,9.17748676071416E-6,4.4158542849441));
#38443=CARTESIAN_POINT('',(3.42660065607856,4.87367679877478E-13,4.415875));
#38444=CARTESIAN_POINT('Ctrl Pts',(5.67660065607858,1.06631253201268E-5,
4.41586554077139));
#38445=CARTESIAN_POINT('Ctrl Pts',(5.68237116412931,-0.050253077703417,
4.41581669384736));
#38446=CARTESIAN_POINT('Ctrl Pts',(5.69609431152383,-0.169828933264711,
4.3941204493343));
#38447=CARTESIAN_POINT('Ctrl Pts',(5.71777009826218,-0.329222253834466,
4.28214440376531));
#38448=CARTESIAN_POINT('Ctrl Pts',(5.74162801629359,-0.424158110434281,
4.08990358344764));
#38449=CARTESIAN_POINT('Ctrl Pts',(5.76548593432501,-0.415375755386326,
3.8756788878607));
#38450=CARTESIAN_POINT('Ctrl Pts',(5.78934385235642,-0.305022713182347,
3.69185409099321));
#38451=CARTESIAN_POINT('Ctrl Pts',(5.81320177038785,-0.120083309624962,
3.58337936191985));
#38452=CARTESIAN_POINT('Ctrl Pts',(5.83705968841926,0.0942197354074567,
3.57677972866706));
#38453=CARTESIAN_POINT('Ctrl Pts',(5.86091760645069,0.285483486244351,3.673668977605));
#38454=CARTESIAN_POINT('Ctrl Pts',(5.8847755244821,0.406938752801468,3.85035505520226));
#38455=CARTESIAN_POINT('Ctrl Pts',(5.90863344251353,0.428886400972996,4.06363338935351));
#38456=CARTESIAN_POINT('Ctrl Pts',(5.93249136054494,0.345959657594393,4.261351642888));
#38457=CARTESIAN_POINT('Ctrl Pts',(5.95514709839996,0.186877681905787,4.38841966610496));
#38458=CARTESIAN_POINT('Ctrl Pts',(5.96985019691118,0.0587795235055939,
4.41583553648629));
#38459=CARTESIAN_POINT('Ctrl Pts',(5.97660065607858,-9.19412645705893E-6,
4.41589218083175));
#38460=CARTESIAN_POINT('Ctrl Pts',(5.7733993439214,9.17748676073846E-6,
4.4158542849441));
#38461=CARTESIAN_POINT('Ctrl Pts',(5.77870104381367,-0.0461746181927863,
4.41581721944429));
#38462=CARTESIAN_POINT('Ctrl Pts',(5.79195538304975,-0.161664917198308,
4.3966319946429));
#38463=CARTESIAN_POINT('Ctrl Pts',(5.81316236162963,-0.320769768688322,
4.29171820750724));
#38464=CARTESIAN_POINT('Ctrl Pts',(5.83702027966105,-0.421326288178809,
4.10235681181338));
#38465=CARTESIAN_POINT('Ctrl Pts',(5.86087819769247,-0.418857046020503,
3.88796639709818));
#38466=CARTESIAN_POINT('Ctrl Pts',(5.88473611572389,-0.313965860818636,
3.70097123187977));
#38467=CARTESIAN_POINT('Ctrl Pts',(5.90859403375531,-0.132301443679057,
3.58709678011166));
#38468=CARTESIAN_POINT('Ctrl Pts',(5.93245195178673,0.0817142298265842,
3.57418834816524));
#38469=CARTESIAN_POINT('Ctrl Pts',(5.95630986981814,0.275748643515392,3.66540258613358));
#38470=CARTESIAN_POINT('Ctrl Pts',(5.98016778784957,0.402354822815078,3.83843477537114));
#38471=CARTESIAN_POINT('Ctrl Pts',(6.00402570588098,0.430574627524036,4.05097449853386));
#38472=CARTESIAN_POINT('Ctrl Pts',(6.02788362391241,0.353506566116634,4.25104874587108));
#38473=CARTESIAN_POINT('Ctrl Pts',(6.05100816992587,0.195023852357142,4.38547315270063));
#38474=CARTESIAN_POINT('Ctrl Pts',(6.06618007659554,0.06286002589468,4.4158563839102));
#38475=CARTESIAN_POINT('Ctrl Pts',(6.0733993439214,-6.65563173397714E-6,
4.41590255337156));
#38476=CARTESIAN_POINT('Origin',(3.42660065607856,0.,4.));
#38477=CARTESIAN_POINT('',(5.37660065607858,-1.01751121954902E-5,4.41586038335289));
#38478=CARTESIAN_POINT('',(5.4733993439214,-1.09014992595302E-5,4.41587264340464));
#38479=CARTESIAN_POINT('',(3.42660065607856,4.87367679877478E-13,4.415875));
#38480=CARTESIAN_POINT('Ctrl Pts',(5.37660065607859,-1.01751121954468E-5,
4.41586038335289));
#38481=CARTESIAN_POINT('Ctrl Pts',(5.37898685265982,-0.0207957689391596,
4.41587928195339));
#38482=CARTESIAN_POINT('Ctrl Pts',(5.38932568858487,-0.110842971866809,
4.40924760552439));
#38483=CARTESIAN_POINT('Ctrl Pts',(5.40761716385372,-0.26226226804932,4.34526983614494));
#38484=CARTESIAN_POINT('Ctrl Pts',(5.43147508188515,-0.395631058815178,
4.17739453851434));
#38485=CARTESIAN_POINT('Ctrl Pts',(5.45533299991656,-0.432257278927009,
3.96614144408682));
#38486=CARTESIAN_POINT('Ctrl Pts',(5.47919091794798,-0.363184819889405,
3.76316768886851));
#38487=CARTESIAN_POINT('Ctrl Pts',(5.5030488359794,-0.205303779432806,3.61810588490468));
#38488=CARTESIAN_POINT('Ctrl Pts',(5.52690675401082,0.00277962745745752,
3.56642759466814));
#38489=CARTESIAN_POINT('Ctrl Pts',(5.55076467204224,0.210183339719457,3.62076956781107));
#38490=CARTESIAN_POINT('Ctrl Pts',(5.57462259007365,0.36619150013966,3.76784371165257));
#38491=CARTESIAN_POINT('Ctrl Pts',(5.59848050810508,0.432655863921731,3.97168639180759));
#38492=CARTESIAN_POINT('Ctrl Pts',(5.62233842613649,0.393324083661671,4.18245252040861));
#38493=CARTESIAN_POINT('Ctrl Pts',(5.64619634416792,0.257813851021257,4.34860403787086));
#38494=CARTESIAN_POINT('Ctrl Pts',(5.66428375414861,0.107285005985459,4.40994309575933));
#38495=CARTESIAN_POINT('Ctrl Pts',(5.6744185247855,0.0190180158238588,4.41588401235146));
#38496=CARTESIAN_POINT('Ctrl Pts',(5.67660065607858,1.06631253201268E-5,
4.41586554077139));
#38497=CARTESIAN_POINT('Ctrl Pts',(5.4733993439214,-1.0901499259525E-5,
4.41587264340464));
#38498=CARTESIAN_POINT('Ctrl Pts',(5.47531673234419,-0.0167114040746605,
4.41588973972128));
#38499=CARTESIAN_POINT('Ctrl Pts',(5.48518676011079,-0.102669266038577,
4.41080986982701));
#38500=CARTESIAN_POINT('Ctrl Pts',(5.50300942722118,-0.251979671819092,
4.35284416104532));
#38501=CARTESIAN_POINT('Ctrl Pts',(5.52686734525261,-0.390234841353927,
4.18896964197264));
#38502=CARTESIAN_POINT('Ctrl Pts',(5.55072526328402,-0.433066962396004,
3.97888689800548));
#38503=CARTESIAN_POINT('Ctrl Pts',(5.57458318131544,-0.370002414621403,
3.77396688259));
#38504=CARTESIAN_POINT('Ctrl Pts',(5.59844109934686,-0.21646219781534,3.62431812139094));
#38505=CARTESIAN_POINT('Ctrl Pts',(5.62229901737828,-0.00999107731853999,
3.56653381289738));
#38506=CARTESIAN_POINT('Ctrl Pts',(5.64615693540971,0.198923133709572,3.61474379450078));
#38507=CARTESIAN_POINT('Ctrl Pts',(5.67001485344111,0.359195220034686,3.75715941257656));
#38508=CARTESIAN_POINT('Ctrl Pts',(5.69387277147254,0.431634290692432,3.95895616900985));
#38509=CARTESIAN_POINT('Ctrl Pts',(5.71773068950395,0.398527019959163,4.1707892603438));
#38510=CARTESIAN_POINT('Ctrl Pts',(5.74158860753538,0.267969036875697,4.34085972491723));
#38511=CARTESIAN_POINT('Ctrl Pts',(5.76014482567452,0.115458993192439,4.40830959117706));
#38512=CARTESIAN_POINT('Ctrl Pts',(5.77074840446986,0.0231018550196917,
4.41587281831976));
#38513=CARTESIAN_POINT('Ctrl Pts',(5.7733993439214,9.17748676073846E-6,
4.4158542849441));
#38514=CARTESIAN_POINT('Origin',(3.42660065607856,0.,4.));
#38515=CARTESIAN_POINT('',(5.07660065607859,8.10857529294212E-6,4.41589722116852));
#38516=CARTESIAN_POINT('',(5.1733993439214,1.02299162792543E-5,4.4158851107878));
#38517=CARTESIAN_POINT('',(3.42660065607856,4.87367679877478E-13,4.415875));
#38518=CARTESIAN_POINT('Ctrl Pts',(5.07660065607858,8.10857529294148E-6,
4.41589722116852));
#38519=CARTESIAN_POINT('Ctrl Pts',(5.08355518053415,-0.060555656273516,
4.41584370653314));
#38520=CARTESIAN_POINT('Ctrl Pts',(5.09846234433351,-0.190424342306974,
4.38715451669839));
#38521=CARTESIAN_POINT('Ctrl Pts',(5.1213221474767,-0.349282119693095,4.256894448863));
#38522=CARTESIAN_POINT('Ctrl Pts',(5.1451800655081,-0.4296670234643,4.05812921762123));
#38523=CARTESIAN_POINT('Ctrl Pts',(5.16903798353954,-0.404986636103755,
3.84514980926298));
#38524=CARTESIAN_POINT('Ctrl Pts',(5.19289590157095,-0.281275984601366,
3.67003549057442));
#38525=CARTESIAN_POINT('Ctrl Pts',(5.21675381960238,-0.0887856930599551,
3.5756064824932));
#38526=CARTESIAN_POINT('Ctrl Pts',(5.24061173763379,0.125415118908336,3.58495324968971));
#38527=CARTESIAN_POINT('Ctrl Pts',(5.26446965566521,0.308948518064291,3.69579025298356));
#38528=CARTESIAN_POINT('Ctrl Pts',(5.28832757369662,0.416935588964862,3.88101482593007));
#38529=CARTESIAN_POINT('Ctrl Pts',(5.31218549172805,0.422970551266107,4.09533451502773));
#38530=CARTESIAN_POINT('Ctrl Pts',(5.33604340975946,0.325577692296299,4.28634231834109));
#38531=CARTESIAN_POINT('Ctrl Pts',(5.35751513120965,0.166275769440666,4.39523064161658));
#38532=CARTESIAN_POINT('Ctrl Pts',(5.37103421331602,0.0484777907299229,
4.41581629730449));
#38533=CARTESIAN_POINT('Ctrl Pts',(5.37660065607859,-1.01751121954468E-5,
4.41586038335289));
#38534=CARTESIAN_POINT('Ctrl Pts',(5.1733993439214,1.02299162792474E-5,
4.4158851107878));
#38535=CARTESIAN_POINT('Ctrl Pts',(5.17988506021851,-0.0564756498766958,
4.41582730150705));
#38536=CARTESIAN_POINT('Ctrl Pts',(5.19432341585943,-0.182274442988225,
4.39002065289559));
#38537=CARTESIAN_POINT('Ctrl Pts',(5.21671441084416,-0.341564590845109,
4.26707000444592));
#38538=CARTESIAN_POINT('Ctrl Pts',(5.24057232887557,-0.427768622694993,
4.07075847957352));
#38539=CARTESIAN_POINT('Ctrl Pts',(5.264430246907,-0.409371574112622,3.85714457902312));
#38540=CARTESIAN_POINT('Ctrl Pts',(5.2882881649384,-0.290872024601924,3.6784627202051));
#38541=CARTESIAN_POINT('Ctrl Pts',(5.31214608296984,-0.101246341881189,
3.57840548479658));
#38542=CARTESIAN_POINT('Ctrl Pts',(5.33600400100125,0.113136829324483,3.58143959235932));
#38543=CARTESIAN_POINT('Ctrl Pts',(5.35986191903268,0.299854963974951,3.68682312094679));
#38544=CARTESIAN_POINT('Ctrl Pts',(5.38371983706408,0.413250392048343,3.8687869272297));
#38545=CARTESIAN_POINT('Ctrl Pts',(5.40757775509551,0.425594842551202,4.08283590397723));
#38546=CARTESIAN_POINT('Ctrl Pts',(5.43143567312693,0.333869761079625,4.27662924579771));
#38547=CARTESIAN_POINT('Ctrl Pts',(5.45337620273556,0.174437273907163,4.39264091290779));
#38548=CARTESIAN_POINT('Ctrl Pts',(5.46736409300038,0.0525562895569378,
4.41581883033293));
#38549=CARTESIAN_POINT('Ctrl Pts',(5.4733993439214,-1.0901499259525E-5,
4.41587264340464));
#38550=CARTESIAN_POINT('Origin',(3.42660065607856,0.,4.));
#38551=CARTESIAN_POINT('',(4.77660065607858,-3.27394476109793E-6,4.41584059078716));
#38552=CARTESIAN_POINT('',(4.8733993439214,-6.67049670156904E-6,4.4158459349409));
#38553=CARTESIAN_POINT('',(3.42660065607856,4.87367679877478E-13,4.415875));
#38554=CARTESIAN_POINT('Ctrl Pts',(4.77660065607858,-3.27394476113199E-6,
4.41584059078717));
#38555=CARTESIAN_POINT('Ctrl Pts',(4.78017086906467,-0.0311067951354469,
4.4158491206715));
#38556=CARTESIAN_POINT('Ctrl Pts',(4.79169372139456,-0.131487321212171,
4.40473555835468));
#38557=CARTESIAN_POINT('Ctrl Pts',(4.81116921306824,-0.287199161490599,
4.32482210305491));
#38558=CARTESIAN_POINT('Ctrl Pts',(4.83502713109967,-0.407721671464292,
4.14749845969467));
#38559=CARTESIAN_POINT('Ctrl Pts',(4.85888504913109,-0.42854512664958,3.93410742516172));
#38560=CARTESIAN_POINT('Ctrl Pts',(4.8827429671625,-0.344577625034195,3.73682892005441));
#38561=CARTESIAN_POINT('Ctrl Pts',(4.90660088519393,-0.176351507991885,
3.60390291263011));
#38562=CARTESIAN_POINT('Ctrl Pts',(4.93045880322534,0.0349973564730633,
3.56783343253575));
#38563=CARTESIAN_POINT('Ctrl Pts',(4.95431672125677,0.237788413971502,3.63744045016736));
#38564=CARTESIAN_POINT('Ctrl Pts',(4.97817463928818,0.382433727027559,3.79570315365689));
#38565=CARTESIAN_POINT('Ctrl Pts',(5.0020325573196,0.433563576539811,4.00392200101168));
#38566=CARTESIAN_POINT('Ctrl Pts',(5.02589047535102,0.378675321553375,4.21118181228595));
#38567=CARTESIAN_POINT('Ctrl Pts',(5.04974839338244,0.231190635538481,4.36680191797922));
#38568=CARTESIAN_POINT('Ctrl Pts',(5.0666517869583,0.086644022961884,4.4135113916189));
#38569=CARTESIAN_POINT('Ctrl Pts',(5.07560254119034,0.00870023350343714,
4.41590490160082));
#38570=CARTESIAN_POINT('Ctrl Pts',(5.07660065607858,8.10857529294148E-6,
4.41589722116852));
#38571=CARTESIAN_POINT('Ctrl Pts',(4.8733993439214,-6.67049670157252E-6,
4.41584593494091));
#38572=CARTESIAN_POINT('Ctrl Pts',(4.87650074874903,-0.0270249643080214,
4.41586127519519));
#38573=CARTESIAN_POINT('Ctrl Pts',(4.88755479292047,-0.123313358466266,
4.40662010077424));
#38574=CARTESIAN_POINT('Ctrl Pts',(4.90656147643571,-0.277507970732168,
4.33313973520738));
#38575=CARTESIAN_POINT('Ctrl Pts',(4.93041939446713,-0.403200703213916,
4.15944262266324));
#38576=CARTESIAN_POINT('Ctrl Pts',(4.95427731249855,-0.430299880793222,
3.94675744574809));
#38577=CARTESIAN_POINT('Ctrl Pts',(4.97813523052996,-0.352179016385168,
3.7470915236456));
#38578=CARTESIAN_POINT('Ctrl Pts',(5.00199314856139,-0.187940789307144,
3.60926861310034));
#38579=CARTESIAN_POINT('Ctrl Pts',(5.0258510665928,0.0222540801607904,3.56699016996131));
#38580=CARTESIAN_POINT('Ctrl Pts',(5.04970898462423,0.227007220840439,3.63059442521772));
#38581=CARTESIAN_POINT('Ctrl Pts',(5.07356690265564,0.376250912472057,3.7845284059142));
#38582=CARTESIAN_POINT('Ctrl Pts',(5.09742482068706,0.433491007135177,3.99115106069306));
#38583=CARTESIAN_POINT('Ctrl Pts',(5.12128273871848,0.384730742495793,4.19993752217271));
#38584=CARTESIAN_POINT('Ctrl Pts',(5.1451406567499,0.241893331461176,4.35983381329239));
#38585=CARTESIAN_POINT('Ctrl Pts',(5.16251285848421,0.0948160588051851,
4.41219316122439));
#38586=CARTESIAN_POINT('Ctrl Pts',(5.17193242087471,0.0127860645481494,
4.41589818594594));
#38587=CARTESIAN_POINT('Ctrl Pts',(5.1733993439214,1.02299162792474E-5,
4.4158851107878));
#38588=CARTESIAN_POINT('Origin',(3.42660065607856,0.,4.));
#38589=CARTESIAN_POINT('',(4.47660065607858,-1.72413508574122E-6,4.41591032029986));
#38590=CARTESIAN_POINT('',(4.5733993439214,2.6062779713001E-6,4.4159095790646));
#38591=CARTESIAN_POINT('',(3.42660065607856,4.87367679877478E-13,4.415875));
#38592=CARTESIAN_POINT('Ctrl Pts',(4.47660065607858,-1.72413508575881E-6,
4.41591032029986));
#38593=CARTESIAN_POINT('Ctrl Pts',(4.47678655759518,-0.00162050728124812,
4.41591069657345));
#38594=CARTESIAN_POINT('Ctrl Pts',(4.48492509845559,-0.0724886630755744,
4.4155056303295));
#38595=CARTESIAN_POINT('Ctrl Pts',(4.5010162786598,-0.212178818846594,4.37811758201071));
#38596=CARTESIAN_POINT('Ctrl Pts',(4.52487419669122,-0.367409789343613,
4.23022337776645));
#38597=CARTESIAN_POINT('Ctrl Pts',(4.54873211472264,-0.432799058467291,
4.02603328640456));
#38598=CARTESIAN_POINT('Ctrl Pts',(4.57259003275406,-0.392357168499796,
3.8154773474345));
#38599=CARTESIAN_POINT('Ctrl Pts',(4.59644795078547,-0.255973263285106,
3.65004222328625));
#38600=CARTESIAN_POINT('Ctrl Pts',(4.6203058688169,-0.0569969226013119,
3.57018130821703));
#38601=CARTESIAN_POINT('Ctrl Pts',(4.64416378684831,0.155916718210686,3.59542277130738));
#38602=CARTESIAN_POINT('Ctrl Pts',(4.66802170487973,0.330704474340828,3.71959438727947));
#38603=CARTESIAN_POINT('Ctrl Pts',(4.69187962291115,0.424625978282027,3.91233281365517));
#38604=CARTESIAN_POINT('Ctrl Pts',(4.71573754094257,0.41471486395576,4.1265082550995));
#38605=CARTESIAN_POINT('Ctrl Pts',(4.73959545897399,0.303394668785218,4.30974898215573));
#38606=CARTESIAN_POINT('Ctrl Pts',(4.75988316401932,0.145646585585232,4.40116103141851));
#38607=CARTESIAN_POINT('Ctrl Pts',(4.77221822972086,0.0381762104768988,
4.41583012037823));
#38608=CARTESIAN_POINT('Ctrl Pts',(4.77660065607858,-3.27394476113199E-6,
4.41584059078717));
#38609=CARTESIAN_POINT('Ctrl Pts',(4.5733993439214,2.60627797130011E-6,
4.4159095790646));
#38610=CARTESIAN_POINT('Ctrl Pts',(4.58106907662335,-0.0667838229435618,
4.4158868274511));
#38611=CARTESIAN_POINT('Ctrl Pts',(4.59669144866912,-0.202842099803805,
4.38250385602613));
#38612=CARTESIAN_POINT('Ctrl Pts',(4.62026646005868,-0.360469908510665,
4.24094439618412));
#38613=CARTESIAN_POINT('Ctrl Pts',(4.6441243780901,-0.431844582779732,4.03876871570463));
#38614=CARTESIAN_POINT('Ctrl Pts',(4.66798229612152,-0.397621493350665,
3.82711302819544));
#38615=CARTESIAN_POINT('Ctrl Pts',(4.69184021415294,-0.266169117804412,
3.65773291463971));
#38616=CARTESIAN_POINT('Ctrl Pts',(4.71569813218436,-0.0696311426542753,
3.57204642662242));
#38617=CARTESIAN_POINT('Ctrl Pts',(4.73955605021577,0.143933543589337,3.59100624451743));
#38618=CARTESIAN_POINT('Ctrl Pts',(4.76341396824719,0.322302557754209,3.70997617639404));
#38619=CARTESIAN_POINT('Ctrl Pts',(4.78727188627862,0.421859817202848,3.8998648332327));
#38620=CARTESIAN_POINT('Ctrl Pts',(4.81112980431003,0.41826086011465,4.11423926597311));
#38621=CARTESIAN_POINT('Ctrl Pts',(4.83498772234146,0.312385729531365,4.30067908636799));
#38622=CARTESIAN_POINT('Ctrl Pts',(4.85574423554524,0.15381688120809,4.39891624198015));
#38623=CARTESIAN_POINT('Ctrl Pts',(4.86854810940522,0.04225549351942,4.41582193963064));
#38624=CARTESIAN_POINT('Ctrl Pts',(4.8733993439214,-6.67049670157252E-6,
4.41584593494091));
#38625=CARTESIAN_POINT('Origin',(3.42660065607856,0.,4.));
#38626=CARTESIAN_POINT('',(4.17660065607858,5.88453344125852E-6,4.41584444980552));
#38627=CARTESIAN_POINT('',(4.2733993439214,2.51014653358805E-6,4.41583996132385));
#38628=CARTESIAN_POINT('',(3.42660065607856,4.87367679877478E-13,4.415875));
#38629=CARTESIAN_POINT('Ctrl Pts',(4.17660065607858,5.88453344126799E-6,
4.41584444980552));
#38630=CARTESIAN_POINT('Ctrl Pts',(4.18135488546951,-0.0414115481342504,
4.41582334930757));
#38631=CARTESIAN_POINT('Ctrl Pts',(4.19406175420423,-0.152126265423154,
4.3993918905015));
#38632=CARTESIAN_POINT('Ctrl Pts',(4.21472126228278,-0.310547447266788,
4.30257739619942));
#38633=CARTESIAN_POINT('Ctrl Pts',(4.23857918031418,-0.417556725585918,
4.11678647978038));
#38634=CARTESIAN_POINT('Ctrl Pts',(4.26243709834561,-0.422462345057068,
3.90243789311793));
#38635=CARTESIAN_POINT('Ctrl Pts',(4.28629501637703,-0.324064236326554,
3.71194600226016));
#38636=CARTESIAN_POINT('Ctrl Pts',(4.31015293440845,-0.146423688323203,
3.59189110566319));
#38637=CARTESIAN_POINT('Ctrl Pts',(4.33401085243986,0.0670214896752265,
3.5716299793216));
#38638=CARTESIAN_POINT('Ctrl Pts',(4.35786877047129,0.264078061498623,3.65611697628114));
#38639=CARTESIAN_POINT('Ctrl Pts',(4.38172668850271,0.396560367883193,3.82469274783887));
#38640=CARTESIAN_POINT('Ctrl Pts',(4.40558460653412,0.432072854850341,4.03613591352675));
#38641=CARTESIAN_POINT('Ctrl Pts',(4.42944252456555,0.361931763288092,4.23874286631049));
#38642=CARTESIAN_POINT('Ctrl Pts',(4.45311454108036,0.204524647174786,4.38184685695289));
#38643=CARTESIAN_POINT('Ctrl Pts',(4.46883391825138,0.0676290543833733,
4.4158946000499));
#38644=CARTESIAN_POINT('Ctrl Pts',(4.47660065607858,-1.72413508575881E-6,
4.41591032029986));
#38645=CARTESIAN_POINT('Ctrl Pts',(4.2733993439214,2.51014653359152E-6,
4.41583996132385));
#38646=CARTESIAN_POINT('Ctrl Pts',(4.27768476515387,-0.0373320337329404,
4.41583213221101));
#38647=CARTESIAN_POINT('Ctrl Pts',(4.28992282573015,-0.143955736965383,
4.40160880992953));
#38648=CARTESIAN_POINT('Ctrl Pts',(4.31011352565024,-0.301501118270308,
4.3115924136571));
#38649=CARTESIAN_POINT('Ctrl Pts',(4.33397144368164,-0.413936097932681,
4.12903358037428));
#38650=CARTESIAN_POINT('Ctrl Pts',(4.35782936171308,-0.425152419412173,
3.91492252699502));
#38651=CARTESIAN_POINT('Ctrl Pts',(4.38168727974448,-0.332407397051365,
3.72161523052345));
#38652=CARTESIAN_POINT('Ctrl Pts',(4.40554519777592,-0.158379709595794,
3.5963805946708));
#38653=CARTESIAN_POINT('Ctrl Pts',(4.42940311580732,0.0543761300157755,
3.56984189703405));
#38654=CARTESIAN_POINT('Ctrl Pts',(4.45326103383876,0.25383552520097,3.64848857324589));
#38655=CARTESIAN_POINT('Ctrl Pts',(4.47711895187016,0.39122521984844,3.81308936806525));
#38656=CARTESIAN_POINT('Ctrl Pts',(4.50097686990159,0.432949691632991,4.02339490384879));
#38657=CARTESIAN_POINT('Ctrl Pts',(4.524834787933,0.368806170420464,4.22797974831721));
#38658=CARTESIAN_POINT('Ctrl Pts',(4.54869270596443,0.214479494504121,4.37681733431002));
#38659=CARTESIAN_POINT('Ctrl Pts',(4.56488089129389,0.0741790848482271,
4.4152866170047));
#38660=CARTESIAN_POINT('Ctrl Pts',(4.57311643727954,0.0024660981813593,
4.41591041828323));
#38661=CARTESIAN_POINT('Ctrl Pts',(4.5733993439214,2.60627797130011E-6,
4.4159095790646));
#38662=CARTESIAN_POINT('Origin',(4.,0.,4.));
#38663=CARTESIAN_POINT('',(4.,-7.34788079488412E-17,4.6));
#38664=CARTESIAN_POINT('Origin',(4.,0.,4.));
#38665=CARTESIAN_POINT('',(4.,-0.219892372742957,4.3529863453938));
#38666=CARTESIAN_POINT('Ctrl Pts',(4.,-0.219914231356238,4.35301468169996));
#38667=CARTESIAN_POINT('Ctrl Pts',(4.,-0.219843051329574,4.3531167999744));
#38668=CARTESIAN_POINT('Ctrl Pts',(4.,-0.219771822781512,4.35321888245988));
#38669=CARTESIAN_POINT('Ctrl Pts',(4.,-0.21970054575756,4.3533209291203));
#38670=CARTESIAN_POINT('Ctrl Pts',(4.,-0.207925336055227,4.3701793886806));
#38671=CARTESIAN_POINT('Ctrl Pts',(4.,-0.194831304039315,4.38605734350833));
#38672=CARTESIAN_POINT('Ctrl Pts',(4.,-0.18064579384139,4.40088380688851));
#38673=CARTESIAN_POINT('Ctrl Pts',(4.,-0.168975273508986,4.41308164397169));
#38674=CARTESIAN_POINT('Ctrl Pts',(4.,-0.156565051628872,4.42456888924957));
#38675=CARTESIAN_POINT('Ctrl Pts',(4.,-0.143515931303371,4.43531683418355));
#38676=CARTESIAN_POINT('Ctrl Pts',(4.,-0.133182439541062,4.44382804395605));
#38677=CARTESIAN_POINT('Ctrl Pts',(4.,-0.122447811630206,4.45187590303098));
#38678=CARTESIAN_POINT('Ctrl Pts',(4.,-0.111352162047151,4.45944712768208));
#38679=CARTESIAN_POINT('Ctrl Pts',(4.,-0.105068105051177,4.46373511522897));
#38680=CARTESIAN_POINT('Ctrl Pts',(4.,-0.0986661212125077,4.46787107983396));
#38681=CARTESIAN_POINT('Ctrl Pts',(4.,-0.0921733602714696,4.47184061613108));
#38682=CARTESIAN_POINT('Ctrl Pts',(4.,-0.0718171345235072,4.48428598070136));
#38683=CARTESIAN_POINT('Ctrl Pts',(4.,-0.0505350523745213,4.49512244469223));
#38684=CARTESIAN_POINT('Ctrl Pts',(4.,-0.0285775088988711,4.50429938857761));
#38685=CARTESIAN_POINT('Ctrl Pts',(4.,-0.00645956782426854,4.51354336909515));
#38686=CARTESIAN_POINT('Ctrl Pts',(4.,0.0163444141029789,4.52110543571878));
#38687=CARTESIAN_POINT('Ctrl Pts',(4.,0.0396343143342583,4.52702898180467));
#38688=CARTESIAN_POINT('Ctrl Pts',(4.,0.0479455316904685,4.52914285427945));
#38689=CARTESIAN_POINT('Ctrl Pts',(4.,0.0563191235587283,4.53104786585874));
#38690=CARTESIAN_POINT('Ctrl Pts',(4.,0.0647475081636451,4.53274519105122));
#38691=CARTESIAN_POINT('Ctrl Pts',(4.,0.0709442475001029,4.53399310299165));
#38692=CARTESIAN_POINT('Ctrl Pts',(4.,0.0771669940275102,4.53512789739638));
#38693=CARTESIAN_POINT('Ctrl Pts',(4.,0.0834037601527001,4.53614909266968));
#38694=CARTESIAN_POINT('Ctrl Pts',(4.,0.108500755516298,4.54025842313435));
#38695=CARTESIAN_POINT('Ctrl Pts',(4.,0.133859781029961,4.54253781872753));
#38696=CARTESIAN_POINT('Ctrl Pts',(3.99999999999999,0.159256593756596,4.54305292380224));
#38697=CARTESIAN_POINT('Ctrl Pts',(3.99999999999999,0.185497795908202,4.5435851550133));
#38698=CARTESIAN_POINT('Ctrl Pts',(3.99999999999998,0.211780221987087,4.54223483664603));
#38699=CARTESIAN_POINT('Ctrl Pts',(3.99999999999998,0.237902321580844,4.5390442708621));
#38700=CARTESIAN_POINT('Ctrl Pts',(3.99999999999998,0.243507595489062,4.53835964001621));
#38701=CARTESIAN_POINT('Ctrl Pts',(3.99999999999998,0.249105619801251,4.53759013757336));
#38702=CARTESIAN_POINT('Ctrl Pts',(3.99999999999998,0.254694598474614,4.53673594206822));
#38703=CARTESIAN_POINT('',(4.,-0.219892372743086,3.64701365460628));
#38704=CARTESIAN_POINT('Ctrl Pts',(4.,0.254721014554616,3.46322028700966));
#38705=CARTESIAN_POINT('Ctrl Pts',(4.,0.254552373521139,3.46319452321125));
#38706=CARTESIAN_POINT('Ctrl Pts',(4.,0.254383724765285,3.46316883668624));
#38707=CARTESIAN_POINT('Ctrl Pts',(4.,0.254215068323085,3.46314322746093));
#38708=CARTESIAN_POINT('Ctrl Pts',(4.,0.228435861761457,3.4592288468388));
#38709=CARTESIAN_POINT('Ctrl Pts',(4.,0.202474691352968,3.45711700011808));
#38710=CARTESIAN_POINT('Ctrl Pts',(4.,0.176517231963435,3.45683380906617));
#38711=CARTESIAN_POINT('Ctrl Pts',(4.,0.151199179447316,3.45655759382427));
#38712=CARTESIAN_POINT('Ctrl Pts',(4.,0.125883695414598,3.45802192769867));
#38713=CARTESIAN_POINT('Ctrl Pts',(4.,0.1007794950383,3.46128259448669));
#38714=CARTESIAN_POINT('Ctrl Pts',(4.,0.0854593772715275,3.46327245269535));
#38715=CARTESIAN_POINT('Ctrl Pts',(4.,0.0702187270328167,3.46593187194604));
#38716=CARTESIAN_POINT('Ctrl Pts',(4.,0.0551140352340102,3.4692772918897));
#38717=CARTESIAN_POINT('Ctrl Pts',(4.,0.0468842919617017,3.47110003330284));
#38718=CARTESIAN_POINT('Ctrl Pts',(4.,0.0386923719445779,3.47312744960567));
#38719=CARTESIAN_POINT('Ctrl Pts',(4.,0.0305707631998946,3.47535548770785));
#38720=CARTESIAN_POINT('Ctrl Pts',(4.,0.0102648423897012,3.48092610391051));
#38721=CARTESIAN_POINT('Ctrl Pts',(4.,-0.00963556638195036,3.48775588581666));
#38722=CARTESIAN_POINT('Ctrl Pts',(4.,-0.0289965775380143,3.49587186612014));
#38723=CARTESIAN_POINT('Ctrl Pts',(4.,-0.047965755796229,3.50382359322137));
#38724=CARTESIAN_POINT('Ctrl Pts',(4.,-0.0664174073931304,3.51301096346156));
#38725=CARTESIAN_POINT('Ctrl Pts',(4.,-0.0841982143338667,3.52340033683134));
#38726=CARTESIAN_POINT('Ctrl Pts',(4.,-0.0930898199841631,3.5285957259532));
#38727=CARTESIAN_POINT('Ctrl Pts',(4.,-0.101813128894432,3.53409169793663));
#38728=CARTESIAN_POINT('Ctrl Pts',(4.,-0.110345561972859,3.53988353361915));
#38729=CARTESIAN_POINT('Ctrl Pts',(4.,-0.11586100642067,3.5436274303089));
#38730=CARTESIAN_POINT('Ctrl Pts',(4.,-0.121288652521606,3.54748953413154));
#38731=CARTESIAN_POINT('Ctrl Pts',(4.,-0.126621987542688,3.55146681430013));
#38732=CARTESIAN_POINT('Ctrl Pts',(4.,-0.143297831161627,3.56390265451229));
#38733=CARTESIAN_POINT('Ctrl Pts',(4.,-0.159061930875806,3.57746928852925));
#38734=CARTESIAN_POINT('Ctrl Pts',(4.,-0.173743808224101,3.59211536896244));
#38735=CARTESIAN_POINT('Ctrl Pts',(4.,-0.187864697165731,3.60620182877415));
#38736=CARTESIAN_POINT('Ctrl Pts',(4.,-0.200984288190684,3.62128798311348));
#38737=CARTESIAN_POINT('Ctrl Pts',(4.,-0.212904831975564,3.63731335989365));
#38738=CARTESIAN_POINT('Ctrl Pts',(4.,-0.21528245268753,3.64050971304978));
#38739=CARTESIAN_POINT('Ctrl Pts',(4.,-0.217612227418936,3.64374335030505));
#38740=CARTESIAN_POINT('Ctrl Pts',(4.,-0.219892372743211,3.64701365460636));
#38741=CARTESIAN_POINT('Origin',(4.,0.,4.));
#38742=CARTESIAN_POINT('Origin',(2.,0.,4.));
#38743=CARTESIAN_POINT('',(2.,-7.34788079488412E-17,4.6));
#38744=CARTESIAN_POINT('',(2.,-7.34788079488412E-17,4.6));
#38745=CARTESIAN_POINT('Origin',(2.,0.,4.));
#38746=CARTESIAN_POINT('Origin',(2.,0.,4.));
#38747=CARTESIAN_POINT('Ctrl Pts',(3.95224475517895,0.178288362465424,4.37571967666652));
#38748=CARTESIAN_POINT('Ctrl Pts',(3.96019739452275,0.115708609995841,4.40541533085819));
#38749=CARTESIAN_POINT('Ctrl Pts',(3.97610267321037,-0.0245105356436035,
4.43290545314371));
#38750=CARTESIAN_POINT('Ctrl Pts',(3.99996059124178,-0.228962993402626,
4.36819499612132));
#38751=CARTESIAN_POINT('Ctrl Pts',(4.0238185092732,-0.377374743411151,4.21349068386271));
#38752=CARTESIAN_POINT('Ctrl Pts',(4.04767642730463,-0.433534992178268,
4.00656196868444));
#38753=CARTESIAN_POINT('Ctrl Pts',(4.07153434533603,-0.383670022685343,
3.79803920418254));
#38754=CARTESIAN_POINT('Ctrl Pts',(4.09539226336747,-0.239994733226421,
3.63889579340969));
#38755=CARTESIAN_POINT('Ctrl Pts',(4.11925018139887,-0.0376302499649443,
3.56805514133307));
#38756=CARTESIAN_POINT('Ctrl Pts',(4.1431080994303,0.173933765839147,3.60283521426327));
#38757=CARTESIAN_POINT('Ctrl Pts',(4.16696601746172,0.342967344134064,3.73473372141871));
#38758=CARTESIAN_POINT('Ctrl Pts',(4.19082393549313,0.428135478754777,3.93149662217858));
#38759=CARTESIAN_POINT('Ctrl Pts',(4.21468185352456,0.40861313688017,4.1450106963618));
#38760=CARTESIAN_POINT('Ctrl Pts',(4.23853977155597,0.289173588337559,4.32306558264197));
#38761=CARTESIAN_POINT('Ctrl Pts',(4.2623976895874,0.0990233075312312,4.42212219878201));
#38762=CARTESIAN_POINT('Ctrl Pts',(4.28625560761881,-0.115340915390822,
4.41795840454656));
#38763=CARTESIAN_POINT('Ctrl Pts',(4.31011352565024,-0.301501118270308,
4.3115924136571));
#38764=CARTESIAN_POINT('Ctrl Pts',(4.33397144368164,-0.413936097932681,
4.12903358037428));
#38765=CARTESIAN_POINT('Ctrl Pts',(4.35782936171308,-0.425152419412173,
3.91492252699502));
#38766=CARTESIAN_POINT('Ctrl Pts',(4.38168727974448,-0.332407397051365,
3.72161523052345));
#38767=CARTESIAN_POINT('Ctrl Pts',(4.40554519777592,-0.158379709595794,
3.5963805946708));
#38768=CARTESIAN_POINT('Ctrl Pts',(4.42940311580732,0.0543761300157755,
3.56984189703405));
#38769=CARTESIAN_POINT('Ctrl Pts',(4.45326103383876,0.25383552520097,3.64848857324589));
#38770=CARTESIAN_POINT('Ctrl Pts',(4.47711895187016,0.39122521984844,3.81308936806525));
#38771=CARTESIAN_POINT('Ctrl Pts',(4.50097686990159,0.432949691632991,4.02339490384879));
#38772=CARTESIAN_POINT('Ctrl Pts',(4.524834787933,0.368806170420464,4.22797974831721));
#38773=CARTESIAN_POINT('Ctrl Pts',(4.54869270596443,0.214479494504121,4.37681733431002));
#38774=CARTESIAN_POINT('Ctrl Pts',(4.57255062399584,0.00770673985495463,
4.4335128177492));
#38775=CARTESIAN_POINT('Ctrl Pts',(4.59640854202726,-0.200950522604244,
4.38420260860549));
#38776=CARTESIAN_POINT('Ctrl Pts',(4.62026646005868,-0.360469908510665,
4.24094439618412));
#38777=CARTESIAN_POINT('Ctrl Pts',(4.6441243780901,-0.431844582779732,4.03876871570463));
#38778=CARTESIAN_POINT('Ctrl Pts',(4.66798229612152,-0.397621493350665,
3.82711302819544));
#38779=CARTESIAN_POINT('Ctrl Pts',(4.69184021415294,-0.266169117804412,
3.65773291463971));
#38780=CARTESIAN_POINT('Ctrl Pts',(4.71569813218436,-0.0696311426542753,
3.57204642662242));
#38781=CARTESIAN_POINT('Ctrl Pts',(4.73955605021577,0.143933543589337,3.59100624451743));
#38782=CARTESIAN_POINT('Ctrl Pts',(4.76341396824719,0.322302557754209,3.70997617639404));
#38783=CARTESIAN_POINT('Ctrl Pts',(4.78727188627862,0.421859817202848,3.8998648332327));
#38784=CARTESIAN_POINT('Ctrl Pts',(4.81112980431003,0.41826086011465,4.11423926597311));
#38785=CARTESIAN_POINT('Ctrl Pts',(4.83498772234146,0.312385729531365,4.30067908636799));
#38786=CARTESIAN_POINT('Ctrl Pts',(4.85884564037287,0.130123778861223,4.41359467981201));
#38787=CARTESIAN_POINT('Ctrl Pts',(4.88270355840429,-0.0839569802410516,
4.42537510794913));
#38788=CARTESIAN_POINT('Ctrl Pts',(4.90656147643571,-0.277507970732168,
4.33313973520738));
#38789=CARTESIAN_POINT('Ctrl Pts',(4.93041939446713,-0.403200703213916,
4.15944262266324));
#38790=CARTESIAN_POINT('Ctrl Pts',(4.95427731249855,-0.430299880793222,
3.94675744574809));
#38791=CARTESIAN_POINT('Ctrl Pts',(4.97813523052996,-0.352179016385168,
3.7470915236456));
#38792=CARTESIAN_POINT('Ctrl Pts',(5.00199314856139,-0.187940789307144,
3.60926861310034));
#38793=CARTESIAN_POINT('Ctrl Pts',(5.0258510665928,0.0222540801607904,3.56699016996131));
#38794=CARTESIAN_POINT('Ctrl Pts',(5.04970898462423,0.227007220840439,3.63059442521772));
#38795=CARTESIAN_POINT('Ctrl Pts',(5.07356690265564,0.376250912472057,3.7845284059142));
#38796=CARTESIAN_POINT('Ctrl Pts',(5.09742482068706,0.433491007135177,3.99115106069306));
#38797=CARTESIAN_POINT('Ctrl Pts',(5.12128273871848,0.384730742495793,4.19993752217271));
#38798=CARTESIAN_POINT('Ctrl Pts',(5.1451406567499,0.241893331461176,4.35983381329239));
#38799=CARTESIAN_POINT('Ctrl Pts',(5.16899857478132,0.0399064118422473,
4.43174093538579));
#38800=CARTESIAN_POINT('Ctrl Pts',(5.19285649281273,-0.171838712500945,
4.39807563839043));
#38801=CARTESIAN_POINT('Ctrl Pts',(5.21671441084416,-0.341564590845109,
4.26707000444592));
#38802=CARTESIAN_POINT('Ctrl Pts',(5.24057232887557,-0.427768622694993,
4.07075847957352));
#38803=CARTESIAN_POINT('Ctrl Pts',(5.264430246907,-0.409371574112622,3.85714457902312));
#38804=CARTESIAN_POINT('Ctrl Pts',(5.2882881649384,-0.290872024601924,3.6784627202051));
#38805=CARTESIAN_POINT('Ctrl Pts',(5.31214608296984,-0.101246341881189,
3.57840548479658));
#38806=CARTESIAN_POINT('Ctrl Pts',(5.33600400100125,0.113136829324483,3.58143959235932));
#38807=CARTESIAN_POINT('Ctrl Pts',(5.35986191903268,0.299854963974951,3.68682312094679));
#38808=CARTESIAN_POINT('Ctrl Pts',(5.38371983706408,0.413250392048343,3.8687869272297));
#38809=CARTESIAN_POINT('Ctrl Pts',(5.40757775509551,0.425594842551202,4.08283590397723));
#38810=CARTESIAN_POINT('Ctrl Pts',(5.43143567312693,0.333869761079625,4.27662924579771));
#38811=CARTESIAN_POINT('Ctrl Pts',(5.45529359115834,0.160504428594232,4.4027792017911));
#38812=CARTESIAN_POINT('Ctrl Pts',(5.47915150918977,-0.0521086087350157,
4.43043867146175));
#38813=CARTESIAN_POINT('Ctrl Pts',(5.50300942722118,-0.251979671819092,
4.35284416104532));
#38814=CARTESIAN_POINT('Ctrl Pts',(5.52686734525261,-0.390234841353927,
4.18896964197264));
#38815=CARTESIAN_POINT('Ctrl Pts',(5.55072526328402,-0.433066962396004,
3.97888689800548));
#38816=CARTESIAN_POINT('Ctrl Pts',(5.57458318131544,-0.370002414621403,
3.77396688259));
#38817=CARTESIAN_POINT('Ctrl Pts',(5.59844109934686,-0.21646219781534,3.62431812139094));
#38818=CARTESIAN_POINT('Ctrl Pts',(5.62229901737828,-0.00999107731853999,
3.56653381289738));
#38819=CARTESIAN_POINT('Ctrl Pts',(5.64615693540971,0.198923133709572,3.61474379450078));
#38820=CARTESIAN_POINT('Ctrl Pts',(5.67001485344111,0.359195220034686,3.75715941257656));
#38821=CARTESIAN_POINT('Ctrl Pts',(5.69387277147254,0.431634290692432,3.95895616900985));
#38822=CARTESIAN_POINT('Ctrl Pts',(5.71773068950395,0.398527019959163,4.1707892603438));
#38823=CARTESIAN_POINT('Ctrl Pts',(5.74158860753538,0.267969036875697,4.34085972491723));
#38824=CARTESIAN_POINT('Ctrl Pts',(5.76544652556679,0.0718853255354575,
4.42758070267197));
#38825=CARTESIAN_POINT('Ctrl Pts',(5.78930444359821,-0.141776307127955,
4.40974655013133));
#38826=CARTESIAN_POINT('Ctrl Pts',(5.81316236162963,-0.320769768688322,
4.29171820750724));
#38827=CARTESIAN_POINT('Ctrl Pts',(5.83702027966105,-0.421326288178809,
4.10235681181338));
#38828=CARTESIAN_POINT('Ctrl Pts',(5.86087819769247,-0.418857046020503,
3.88796639709818));
#38829=CARTESIAN_POINT('Ctrl Pts',(5.88473611572389,-0.313965860818636,
3.70097123187977));
#38830=CARTESIAN_POINT('Ctrl Pts',(5.90859403375531,-0.132301443679057,
3.58709678011166));
#38831=CARTESIAN_POINT('Ctrl Pts',(5.93245195178673,0.0817142298265842,
3.57418834816524));
#38832=CARTESIAN_POINT('Ctrl Pts',(5.95630986981814,0.275748643515392,3.66540258613358));
#38833=CARTESIAN_POINT('Ctrl Pts',(5.98016778784957,0.402354822815078,3.83843477537114));
#38834=CARTESIAN_POINT('Ctrl Pts',(6.00402570588098,0.430574627524036,4.05097449853386));
#38835=CARTESIAN_POINT('Ctrl Pts',(6.02788362391241,0.353506566116634,4.25104874587108));
#38836=CARTESIAN_POINT('Ctrl Pts',(6.05174154194382,0.189997730437525,4.38973628930191));
#38837=CARTESIAN_POINT('Ctrl Pts',(6.07559945997525,-0.0199730113800777,
4.43311976162365));
#38838=CARTESIAN_POINT('Ctrl Pts',(6.09945737800665,-0.2250554921608,4.3705991908187));
#38839=CARTESIAN_POINT('Ctrl Pts',(6.12331529603809,-0.375113923638194,
4.21744656883549));
#38840=CARTESIAN_POINT('Ctrl Pts',(6.1471732140695,-0.433431396087355,4.01114207710762));
#38841=CARTESIAN_POINT('Ctrl Pts',(6.17103113210093,-0.385792139046387,
3.80207577201042));
#38842=CARTESIAN_POINT('Ctrl Pts',(6.19488905013233,-0.243761337718234,
3.64147770828707));
#38843=CARTESIAN_POINT('Ctrl Pts',(6.21874696816376,-0.042227823444436,
3.56841523311022));
#38844=CARTESIAN_POINT('Ctrl Pts',(6.24260488619517,0.16982704650124,3.60113783246665));
#38845=CARTESIAN_POINT('Ctrl Pts',(6.2664628042266,0.339985970990829,3.73091992247201));
#38846=CARTESIAN_POINT('Ctrl Pts',(6.29032072225801,0.427700638223926,3.92738904240251));
#38847=CARTESIAN_POINT('Ctrl Pts',(6.31417864028943,0.409561128158778,4.13996490148311));
#38848=CARTESIAN_POINT('Ctrl Pts',(6.34598919766466,0.254661277208374,4.38159318714805));
#38849=CARTESIAN_POINT('Ctrl Pts',(6.38575239438369,-0.125272905304917,
4.47558432627151));
#38850=CARTESIAN_POINT('Ctrl Pts',(6.43346823044653,-0.468271923807345,
4.15124960425567));
#38851=CARTESIAN_POINT('Ctrl Pts',(6.48118406650937,-0.380227249479543,
3.6882349865083));
#38852=CARTESIAN_POINT('Ctrl Pts',(6.52889990257221,0.0564566449812287,
3.51140415777354));
#38853=CARTESIAN_POINT('Ctrl Pts',(6.57661573863504,0.441574375138847,3.78331933667001));
#38854=CARTESIAN_POINT('Ctrl Pts',(6.62433157469789,0.421040068198854,4.25418342072721));
#38855=CARTESIAN_POINT('Ctrl Pts',(6.67204741076071,0.0139362792425842,
4.49164405688148));
#38856=CARTESIAN_POINT('Ctrl Pts',(6.71976324682356,-0.406006764042365,
4.27761133505345));
#38857=CARTESIAN_POINT('Ctrl Pts',(6.76747908288639,-0.453085647428837,
3.80864864857145));
#38858=CARTESIAN_POINT('Ctrl Pts',(6.81519491894923,-0.0841006081168706,
3.51540431248109));
#38859=CARTESIAN_POINT('Ctrl Pts',(6.86291075501207,0.362121456530253,3.66717299786736));
#38860=CARTESIAN_POINT('Ctrl Pts',(6.91062659107491,0.475798562415156,4.124581128109));
#38861=CARTESIAN_POINT('Ctrl Pts',(6.95834242713775,0.152544250279933,4.46758486877347));
#38862=CARTESIAN_POINT('Ctrl Pts',(7.00605826320058,-0.310794706562241,
4.38119802990972));
#38863=CARTESIAN_POINT('Ctrl Pts',(7.05377409926342,-0.488725618924084,
3.94475128051735));
#38864=CARTESIAN_POINT('Ctrl Pts',(7.10148993532626,-0.21785253135038,3.55904022429238));
#38865=CARTESIAN_POINT('Ctrl Pts',(7.14920577138909,0.253078023397415,3.57826934481931));
#38866=CARTESIAN_POINT('Ctrl Pts',(7.19692160745195,0.491603063369337,3.98478019943955));
#38867=CARTESIAN_POINT('Ctrl Pts',(7.24463744351477,0.278681483980911,4.40526763942622));
#38868=CARTESIAN_POINT('Ctrl Pts',(7.29235327957762,-0.190157610347023,
4.45359156587464));
#38869=CARTESIAN_POINT('Ctrl Pts',(7.34006911564044,-0.484372034479295,
4.08537538031203));
#38870=CARTESIAN_POINT('Ctrl Pts',(7.3877849517033,-0.333780171974684,3.63875766810317));
#38871=CARTESIAN_POINT('Ctrl Pts',(7.43550078776612,0.123327161313159,3.52387434835784));
#38872=CARTESIAN_POINT('Ctrl Pts',(7.48321662382897,0.467181263150904,3.84622454030349));
#38873=CARTESIAN_POINT('Ctrl Pts',(7.5309324598918,0.382015623368301,4.30978910321172));
#38874=CARTESIAN_POINT('Ctrl Pts',(7.57864829595465,-0.0539608418635878,
4.4888695658253));
#38875=CARTESIAN_POINT('Ctrl Pts',(7.62636413201748,-0.440384235482588,
4.21901358396786));
#38876=CARTESIAN_POINT('Ctrl Pts',(7.67407996808031,-0.422396009600076,
3.7480340579683));
#38877=CARTESIAN_POINT('Ctrl Pts',(7.72179580414317,-0.0165150286377962,
3.50843873354525));
#38878=CARTESIAN_POINT('Ctrl Pts',(7.76951164020598,0.404531957204003,3.72025168374225));
#38879=CARTESIAN_POINT('Ctrl Pts',(7.81722747626884,0.454091022239626,4.18896181724392));
#38880=CARTESIAN_POINT('Ctrl Pts',(7.86494331233166,0.0866513144543145,
4.48414540641706));
#38881=CARTESIAN_POINT('Ctrl Pts',(7.91265914839452,-0.360361628691054,
4.33473081934393));
#38882=CARTESIAN_POINT('Ctrl Pts',(7.96037498445733,-0.476448943335793,
3.87792777037096));
#38883=CARTESIAN_POINT('Ctrl Pts',(8.0080908205202,-0.1550058622045,3.53322552818936));
#38884=CARTESIAN_POINT('Ctrl Pts',(8.05580665658301,0.308781487260178,3.61716946571973));
#38885=CARTESIAN_POINT('Ctrl Pts',(8.10352249264587,0.489010045760349,4.0526725734847));
#38886=CARTESIAN_POINT('Ctrl Pts',(8.1512383287087,0.220173154851853,4.43980564654689));
#38887=CARTESIAN_POINT('Ctrl Pts',(8.19895416477154,-0.250852131956433,
4.4230584271054));
#38888=CARTESIAN_POINT('Ctrl Pts',(8.24667000083438,-0.491516046133,4.01781014446235));
#38889=CARTESIAN_POINT('Ctrl Pts',(8.29438583689722,-0.280813212199106,
3.59620653211525));
#38890=CARTESIAN_POINT('Ctrl Pts',(8.34210167296004,0.187764715363875,3.54541267448783));
#38891=CARTESIAN_POINT('Ctrl Pts',(8.38981750902289,0.483915415676709,3.91207335260334));
#38892=CARTESIAN_POINT('Ctrl Pts',(8.43753334508573,0.335679143777854,4.35947842394856));
#38893=CARTESIAN_POINT('Ctrl Pts',(8.48524918114857,-0.120816450939738,
4.4767689272953));
#38894=CARTESIAN_POINT('Ctrl Pts',(8.5329650172114,-0.466364439759318,4.15623518867385));
#38895=CARTESIAN_POINT('Ctrl Pts',(8.58068085327425,-0.383642787608637,
3.69222827230584));
#38896=CARTESIAN_POINT('Ctrl Pts',(8.62839668933707,0.0513839395061145,
3.51085286915611));
#38897=CARTESIAN_POINT('Ctrl Pts',(8.67611252539993,0.439224004328866,3.77866880275638));
#38898=CARTESIAN_POINT('Ctrl Pts',(8.72382836146275,0.42371790764641,4.24973658040369));
#38899=CARTESIAN_POINT('Ctrl Pts',(8.7715441975256,0.0191051366342138,4.49146741357506));
#38900=CARTESIAN_POINT('Ctrl Pts',(8.81926003358843,-0.403052175319494,
4.28187615866228));
#38901=CARTESIAN_POINT('Ctrl Pts',(8.86697586965126,-0.455080472922433,
3.81343369002772));
#38902=CARTESIAN_POINT('Ctrl Pts',(8.91469170571412,-0.0892013699275644,
3.51631793453238));
#38903=CARTESIAN_POINT('Ctrl Pts',(8.96240754177693,0.358592723611288,3.66337486216116));
#38904=CARTESIAN_POINT('Ctrl Pts',(9.0101233778398,0.477085601399612,4.11955983351088));
#38905=CARTESIAN_POINT('Ctrl Pts',(9.05783921390261,0.157463430517111,4.46595117008304));
#38906=CARTESIAN_POINT('Ctrl Pts',(9.10555504996547,-0.306759831495564,
4.38445237758765));
#38907=CARTESIAN_POINT('Ctrl Pts',(9.1532708860283,-0.489280820139143,3.94990505119329));
#38908=CARTESIAN_POINT('Ctrl Pts',(9.20098672209113,-0.222487703095825,
3.56136068709803));
#38909=CARTESIAN_POINT('Ctrl Pts',(9.24870255815399,0.248619295113741,3.57562555337399));
#38910=CARTESIAN_POINT('Ctrl Pts',(9.29641839421681,0.49141536912078,3.97960000382683));
#38911=CARTESIAN_POINT('Ctrl Pts',(9.34413423027966,0.282937148266828,4.40230808465976));
#38912=CARTESIAN_POINT('Ctrl Pts',(9.39185006634249,-0.185366609388173,
4.45557046104408));
#38913=CARTESIAN_POINT('Ctrl Pts',(9.43956590240532,-0.483445357410111,
4.09047547319903));
#38914=CARTESIAN_POINT('Ctrl Pts',(9.48728173846818,-0.337568794959357,
3.64229546617122));
#38915=CARTESIAN_POINT('Ctrl Pts',(9.53499757453099,0.118302386066128,3.5226010365501));
#38916=CARTESIAN_POINT('Ctrl Pts',(9.58271341059386,0.465534665650901,3.84130942079228));
#38917=CARTESIAN_POINT('Ctrl Pts',(9.63042924665667,0.385259298596883,4.30574580568933));
#38918=CARTESIAN_POINT('Ctrl Pts',(9.67814508271952,-0.0488056103349303,
4.48941111271794));
#38919=CARTESIAN_POINT('Ctrl Pts',(9.72586091878235,-0.438051576325333,
4.22364266437974));
#38920=CARTESIAN_POINT('Ctrl Pts',(9.77357675484519,-0.425028039486299,
3.75249971615691));
#38921=CARTESIAN_POINT('Ctrl Pts',(9.82129259090803,-0.0216947140899849,
3.50864008686857));
#38922=CARTESIAN_POINT('Ctrl Pts',(9.86900842697087,0.401561201071248,3.7160038263529));
#38923=CARTESIAN_POINT('Ctrl Pts',(9.91672426303371,0.456057286475463,4.18416562194019));
#38924=CARTESIAN_POINT('Ctrl Pts',(9.96444009909655,0.0917489483659128,
4.48320529314746));
#38925=CARTESIAN_POINT('Ctrl Pts',(10.0121559351594,-0.356813860767086,
4.3385101085883));
#38926=CARTESIAN_POINT('Ctrl Pts',(10.0598717712222,-0.477709011270712,
3.88295588266498));
#38927=CARTESIAN_POINT('Ctrl Pts',(10.1075876072851,-0.159916626226494,
3.53488507064564));
#38928=CARTESIAN_POINT('Ctrl Pts',(10.1553034433479,0.304729657315094,3.61393645496551));
#38929=CARTESIAN_POINT('Ctrl Pts',(10.2030192794107,0.489538007675758,4.04751593304174));
#38930=CARTESIAN_POINT('Ctrl Pts',(10.2507351154736,0.224796073077312,4.43746079867915));
#38931=CARTESIAN_POINT('Ctrl Pts',(10.2984509515364,-0.246379554360218,
4.42567868168988));
#38932=CARTESIAN_POINT('Ctrl Pts',(10.3461667875993,-0.491301045992024,
4.02298928139638));
#38933=CARTESIAN_POINT('Ctrl Pts',(10.3938826236621,-0.285053227451061,
3.599188470261));
#38934=CARTESIAN_POINT('Ctrl Pts',(10.4415984597249,0.182963355965895,3.54345905416307));
#38935=CARTESIAN_POINT('Ctrl Pts',(10.4893142957878,0.482961874346273,3.9069782134126));
#38936=CARTESIAN_POINT('Ctrl Pts',(10.5370301318506,0.339449072190825,4.35592071060949));
#38937=CARTESIAN_POINT('Ctrl Pts',(10.5847459679134,-0.115785036052801,
4.47801574270962));
#38938=CARTESIAN_POINT('Ctrl Pts',(10.6324618039763,-0.464691964107356,
4.16114156306187));
#38939=CARTESIAN_POINT('Ctrl Pts',(10.6801776400391,-0.386865111317189,
3.69628860657276));
#38940=CARTESIAN_POINT('Ctrl Pts',(10.7278934761019,0.0462259258804368,
3.51033849586834));
#38941=CARTESIAN_POINT('Ctrl Pts',(10.7756093121648,0.436866984064762,3.77405207881873));
#38942=CARTESIAN_POINT('Ctrl Pts',(10.8233251482276,0.426326368719826,4.24525711444552));
#38943=CARTESIAN_POINT('Ctrl Pts',(10.8710409842905,0.0242836891050981,
4.49123876811122));
#38944=CARTESIAN_POINT('Ctrl Pts',(10.9187568203533,-0.400059075867425,
4.28610830234036));
#38945=CARTESIAN_POINT('Ctrl Pts',(10.9664726564161,-0.45702143577077,3.81824018018824));
#38946=CARTESIAN_POINT('Ctrl Pts',(11.014188492479,-0.0942939790271268,
3.51728489730359));
#38947=CARTESIAN_POINT('Ctrl Pts',(11.0619043285418,0.355025089556487,3.65961432075161));
#38948=CARTESIAN_POINT('Ctrl Pts',(11.1096201646047,0.478319155637209,4.11452515096033));
#38949=CARTESIAN_POINT('Ctrl Pts',(11.1573360006675,0.16236538121005,4.46426577284621));
#38950=CARTESIAN_POINT('Ctrl Pts',(11.2050518367304,-0.302691021094817,
4.38766399188028));
#38951=CARTESIAN_POINT('Ctrl Pts',(11.2527676727932,-0.489781601228288,
3.95506440219344));
#38952=CARTESIAN_POINT('Ctrl Pts',(11.300483508856,-0.227098200695192,3.56372986339542));
#38953=CARTESIAN_POINT('Ctrl Pts',(11.3481993449188,0.244132971891272,3.57302890392028));
#38954=CARTESIAN_POINT('Ctrl Pts',(11.3959151809817,0.491173079921361,3.97442207176994));
#38955=CARTESIAN_POINT('Ctrl Pts',(11.4436310170445,0.287161390990383,4.39930384468027));
#38956=CARTESIAN_POINT('Ctrl Pts',(11.4913468531074,-0.180555021833016,
4.45749875294131));
#38957=CARTESIAN_POINT('Ctrl Pts',(11.5390626891702,-0.482464979911041,
4.09556551685319));
#38958=CARTESIAN_POINT('Ctrl Pts',(11.586778525233,-0.341319923258817,3.64587299617429));
#38959=CARTESIAN_POINT('Ctrl Pts',(11.6344943612959,0.113264470804062,3.5213807520529));
#38960=CARTESIAN_POINT('Ctrl Pts',(11.6822101973587,0.463836358529674,3.83641192782507));
#38961=CARTESIAN_POINT('Ctrl Pts',(11.7299260334216,0.38846018117773,4.30166854740152));
#38962=CARTESIAN_POINT('Ctrl Pts',(11.7776418694844,-0.0436449577779122,
4.48989829813191));
#38963=CARTESIAN_POINT('Ctrl Pts',(11.8253577055472,-0.435670260442099,
4.22824690363353));
#38964=CARTESIAN_POINT('Ctrl Pts',(11.8730735416101,-0.427612859293677,
3.75699286549843));
#38965=CARTESIAN_POINT('Ctrl Pts',(11.9207893776729,-0.0268719897862959,
3.50889601812151));
#38966=CARTESIAN_POINT('Ctrl Pts',(11.9685052137357,0.398545841420554,3.71178751390968));
#38967=CARTESIAN_POINT('Ctrl Pts',(12.0162210497986,0.457972894034889,4.17934897039372));
#38968=CARTESIAN_POINT('Ctrl Pts',(12.0639368858614,0.0968363912382316,
4.48221150772657));
#38969=CARTESIAN_POINT('Ctrl Pts',(12.1116527219243,-0.353226459651896,
4.34225179773635));
#38970=CARTESIAN_POINT('Ctrl Pts',(12.1593685579871,-0.478916017555994,
3.88799699566402));
#38971=CARTESIAN_POINT('Ctrl Pts',(12.2070843940499,-0.164809627468288,
3.53659627586117));
#38972=CARTESIAN_POINT('Ctrl Pts',(12.2548002301128,0.300643979445627,3.61074632631782));
#38973=CARTESIAN_POINT('Ctrl Pts',(12.3025160661756,0.490011594032383,4.04235401475446));
#38974=CARTESIAN_POINT('Ctrl Pts',(12.3502319022385,0.229394022021679,4.43506735974179));
#38975=CARTESIAN_POINT('Ctrl Pts',(12.3979477383013,-0.241879610092261,
4.42825165390643));
#38976=CARTESIAN_POINT('Ctrl Pts',(12.4456635743641,-0.491031474462283,
4.0281658647901));
#38977=CARTESIAN_POINT('Ctrl Pts',(12.493379410427,-0.289261580343189,3.60221492864948));
#38978=CARTESIAN_POINT('Ctrl Pts',(12.5410952464898,0.178141673866572,3.54155614424011));
#38979=CARTESIAN_POINT('Ctrl Pts',(12.5888110825527,0.481954687902679,3.90189340664049));
#38980=CARTESIAN_POINT('Ctrl Pts',(12.6365269186155,0.343181296211668,4.35232346328687));
#38981=CARTESIAN_POINT('Ctrl Pts',(12.6842427546783,-0.110740760313508,
4.47920946240362));
#38982=CARTESIAN_POINT('Ctrl Pts',(12.7319585907412,-0.462967872677167,
4.16603003860975));
#38983=CARTESIAN_POINT('Ctrl Pts',(12.779674426804,-0.390044463885,3.70038267566003));
#38984=CARTESIAN_POINT('Ctrl Pts',(12.8273902628668,0.0410627776982723,
3.50987851185683));
#38985=CARTESIAN_POINT('Ctrl Pts',(12.8751060989297,0.434461438689172,3.76946045210395));
#38986=CARTESIAN_POINT('Ctrl Pts',(12.9228219349925,0.42888747548329,4.24075040649094));
#38987=CARTESIAN_POINT('Ctrl Pts',(12.9705377710553,0.0294595442590321,
4.49095555817611));
#38988=CARTESIAN_POINT('Ctrl Pts',(13.0182536071182,-0.397021539751646,
4.29030866646591));
#38989=CARTESIAN_POINT('Ctrl Pts',(13.065969443181,-0.458911634846768,3.82306685936703));
#38990=CARTESIAN_POINT('Ctrl Pts',(13.1136852792439,-0.0993761143989603,
3.51830547777773));
#38991=CARTESIAN_POINT('Ctrl Pts',(13.1614011153067,0.351418020999476,3.65589158776806));
#38992=CARTESIAN_POINT('Ctrl Pts',(13.2091169513695,0.479499580452807,4.10947774749948));
#38993=CARTESIAN_POINT('Ctrl Pts',(13.2568327874324,0.167249297126924,4.46252880717046));
#38994=CARTESIAN_POINT('Ctrl Pts',(13.3045486234952,-0.298588589211839,
4.39083254629632));
#38995=CARTESIAN_POINT('Ctrl Pts',(13.352264459558,-0.490227979701372,3.96022874442655));
#38996=CARTESIAN_POINT('Ctrl Pts',(13.3999802956209,-0.23168347330409,3.56614749850931));
#38997=CARTESIAN_POINT('Ctrl Pts',(13.4476961316837,0.239619531536799,3.57047968038978));
#38998=CARTESIAN_POINT('Ctrl Pts',(13.4954119677466,0.490876233547033,3.96924698078795));
#38999=CARTESIAN_POINT('Ctrl Pts',(13.5431278038094,0.291353737189313,4.39625525192456));
#39000=CARTESIAN_POINT('Ctrl Pts',(13.5908436398722,-0.175723379082843,
4.45937622804808));
#39001=CARTESIAN_POINT('Ctrl Pts',(13.6385594759351,-0.481431012491488,
4.10064494554323));
#39002=CARTESIAN_POINT('Ctrl Pts',(13.6862753119979,-0.345033139360895,
3.64948986092447));
#39003=CARTESIAN_POINT('Ctrl Pts',(13.7339911480608,0.108213974662067,3.52021363031051));
#39004=CARTESIAN_POINT('Ctrl Pts',(13.7817069841236,0.462086530666827,3.83153260544464));
#39005=CARTESIAN_POINT('Ctrl Pts',(13.8294228201864,0.391617915445045,4.297557781203));
#39006=CARTESIAN_POINT('Ctrl Pts',(13.8771386562493,-0.0384794573460961,
4.49033106796769));
#39007=CARTESIAN_POINT('Ctrl Pts',(13.9248544923121,-0.433240552373761,
4.23282579030437));
#39008=CARTESIAN_POINT('Ctrl Pts',(13.9725703283749,-0.430150181893835,
3.76151300691929));
#39009=CARTESIAN_POINT('Ctrl Pts',(14.0202861644378,-0.032046280669499,
3.50920649887429));
#39010=CARTESIAN_POINT('Ctrl Pts',(14.0680020005006,0.39548621318905,3.70760321474174));
#39011=CARTESIAN_POINT('Ctrl Pts',(14.1157178365634,0.459837632138507,4.1745123976147));
#39012=CARTESIAN_POINT('Ctrl Pts',(14.1634336726263,0.101913077983734,4.48116416053968));
#39013=CARTESIAN_POINT('Ctrl Pts',(14.2111495086891,-0.349599823817769,
4.34595547117883));
#39014=CARTESIAN_POINT('Ctrl Pts',(14.258865344752,-0.480069828122688,3.8930505494253));
#39015=CARTESIAN_POINT('Ctrl Pts',(14.3065811808148,-0.169684322438749,
3.53835895376334));
#39016=CARTESIAN_POINT('Ctrl Pts',(14.3542970168777,0.296524907469595,3.60759943412104));
#39017=CARTESIAN_POINT('Ctrl Pts',(14.4020128529405,0.49043075222644,4.0371873919842));
#39018=CARTESIAN_POINT('Ctrl Pts',(14.4497286890033,0.233966490966644,4.43262559558668));
#39019=CARTESIAN_POINT('Ctrl Pts',(14.4974445250662,-0.237352798985028,
4.43077705796148));
#39020=CARTESIAN_POINT('Ctrl Pts',(14.545160361129,-0.490707361486496,4.03333931965322));
#39021=CARTESIAN_POINT('Ctrl Pts',(14.5928761971918,-0.293437803431633,
3.60528557111603));
#39022=CARTESIAN_POINT('Ctrl Pts',(14.6405920332547,0.173300204635467,3.53970415608515));
#39023=CARTESIAN_POINT('Ctrl Pts',(14.6883078693175,0.480893968219416,3.89681949708321));
#39024=CARTESIAN_POINT('Ctrl Pts',(14.7360237053804,0.346875401282657,4.34868708154587));
#39025=CARTESIAN_POINT('Ctrl Pts',(14.7837395414432,-0.10568418401607,4.48034995378457));
#39026=CARTESIAN_POINT('Ctrl Pts',(14.831455377506,-0.461192356972643,4.17090007232882));
#39027=CARTESIAN_POINT('Ctrl Pts',(14.8791712135689,-0.393180492164677,
3.7045100248179));
#39028=CARTESIAN_POINT('Ctrl Pts',(14.9268870496317,0.0358950684576197,
3.50947296821438));
#39029=CARTESIAN_POINT('Ctrl Pts',(14.9746028856945,0.432007635398663,3.76489443262817));
#39030=CARTESIAN_POINT('Ctrl Pts',(15.0223187217574,0.431400943461215,4.23621695712364));
#39031=CARTESIAN_POINT('Ctrl Pts',(15.0700345578202,0.0346321271865876,
4.4906178152274));
#39032=CARTESIAN_POINT('Ctrl Pts',(15.1177503938831,-0.393939904367254,
4.2944767844824));
#39033=CARTESIAN_POINT('Ctrl Pts',(15.1654662299459,-0.46075086019608,3.82791319143947));
#39034=CARTESIAN_POINT('Ctrl Pts',(15.2131820660087,-0.104447211543591,
3.51937956259357));
#39035=CARTESIAN_POINT('Ctrl Pts',(15.2608979020716,0.347771918596306,3.652207076714));
#39036=CARTESIAN_POINT('Ctrl Pts',(15.3086137381344,0.480626744730421,4.10441818376995));
#39037=CARTESIAN_POINT('Ctrl Pts',(15.3563295741973,0.172114635785536,4.46074046598969));
#39038=CARTESIAN_POINT('Ctrl Pts',(15.4040454102601,-0.294452991525291,
4.39395768888776));
#39039=CARTESIAN_POINT('Ctrl Pts',(15.4517612463229,-0.490619905976795,
3.96539750426199));
#39040=CARTESIAN_POINT('Ctrl Pts',(15.4994770823858,-0.236243011612202,
3.56861332390027));
#39041=CARTESIAN_POINT('Ctrl Pts',(15.5471929184486,0.235079475381852,3.56797816593814));
#39042=CARTESIAN_POINT('Ctrl Pts',(15.5949087545115,0.490524862970081,3.9640753057054));
#39043=CARTESIAN_POINT('Ctrl Pts',(15.6426245905743,0.295513721197704,4.39316264501585));
#39044=CARTESIAN_POINT('Ctrl Pts',(15.6903404266371,-0.170872217813597,
4.46120267782338));
#39045=CARTESIAN_POINT('Ctrl Pts',(15.7380562626999,-0.480343569999647,
4.1057131950703));
#39046=CARTESIAN_POINT('Ctrl Pts',(15.7857720987628,-0.348708030819167,
3.6531456586776));
#39047=CARTESIAN_POINT('Ctrl Pts',(15.8334879348256,0.103151458625294,3.5190998009613));
#39048=CARTESIAN_POINT('Ctrl Pts',(15.8812037708885,0.460285376424935,3.82667199562295));
#39049=CARTESIAN_POINT('Ctrl Pts',(15.9289196069513,0.39473215065269,4.29341396369818));
#39050=CARTESIAN_POINT('Ctrl Pts',(15.9766354430142,-0.033309682798763,
4.49070937415524));
#39051=CARTESIAN_POINT('Ctrl Pts',(16.024351279077,-0.430762722000766,4.23737881579128));
#39052=CARTESIAN_POINT('Ctrl Pts',(16.0720671151398,-0.432639725453012,
3.76605963834362));
#39053=CARTESIAN_POINT('Ctrl Pts',(16.1197829512026,-0.0372170120039125,
3.50957149464017));
#39054=CARTESIAN_POINT('Ctrl Pts',(16.1674987872655,0.392382656225717,3.70345139362117));
#39055=CARTESIAN_POINT('Ctrl Pts',(16.2152146233283,0.461651293660056,4.16965644082667));
#39056=CARTESIAN_POINT('Ctrl Pts',(16.2629304593912,0.106978444708158,4.48006336792116));
#39057=CARTESIAN_POINT('Ctrl Pts',(16.310646295454,-0.345934356094203,4.34962071752925));
#39058=CARTESIAN_POINT('Ctrl Pts',(16.3583621315169,-0.481170314810987,
3.89811598262401));
#39059=CARTESIAN_POINT('Ctrl Pts',(16.4060779675797,-0.174540169679895,
3.54017290856226));
#39060=CARTESIAN_POINT('Ctrl Pts',(16.4537938036425,0.292372898913969,3.60449612791703));
#39061=CARTESIAN_POINT('Ctrl Pts',(16.5015096397054,0.490795435699827,4.0320166386149));
#39062=CARTESIAN_POINT('Ctrl Pts',(16.5492254757682,0.238512972024049,4.4301357774334));
#39063=CARTESIAN_POINT('Ctrl Pts',(16.596941311831,-0.23279962385521,4.43325461334514));
#39064=CARTESIAN_POINT('Ctrl Pts',(16.6446571478939,-0.490328743065594,
4.03850907134293));
#39065=CARTESIAN_POINT('Ctrl Pts',(16.6923729839567,-0.297581432841348,
3.60840005658827));
#39066=CARTESIAN_POINT('Ctrl Pts',(16.7400888200196,0.168439486040012,3.53790329540825));
#39067=CARTESIAN_POINT('Ctrl Pts',(16.7878046560824,0.479779833116189,3.89175704832657));
#39068=CARTESIAN_POINT('Ctrl Pts',(16.8355204921452,0.350530977080134,4.3450119692985));
#39069=CARTESIAN_POINT('Ctrl Pts',(16.8832363282081,-0.100615868820984,
4.4814370901721));
#39070=CARTESIAN_POINT('Ctrl Pts',(16.9309521642709,-0.459365614209645,
4.17575112327883));
#39071=CARTESIAN_POINT('Ctrl Pts',(16.9786680003337,-0.396272847821079,
3.70867019559999));
#39072=CARTESIAN_POINT('Ctrl Pts',(17.0263838363966,0.0307233721630972,
3.5091219099869));
#39073=CARTESIAN_POINT('Ctrl Pts',(17.0740996724594,0.429505846750062,3.76035452756312));
#39074=CARTESIAN_POINT('Ctrl Pts',(17.1218155085223,0.433866493469502,4.23165726989771));
#39075=CARTESIAN_POINT('Ctrl Pts',(17.1695313445851,0.039800863341802,4.49022557677993));
#39076=CARTESIAN_POINT('Ctrl Pts',(17.217247180648,-0.390814512007675,4.29861219341511));
#39077=CARTESIAN_POINT('Ctrl Pts',(17.2649630167107,-0.462538907526291,
3.83277863809798));
#39078=CARTESIAN_POINT('Ctrl Pts',(17.3126788527736,-0.109506707187599,
3.52050703244687));
#39079=CARTESIAN_POINT('Ctrl Pts',(17.3603946888365,0.344087187338735,3.64856119684745));
#39080=CARTESIAN_POINT('Ctrl Pts',(17.4081105248993,0.481700523269991,4.09934702176407));
#39081=CARTESIAN_POINT('Ctrl Pts',(17.4558263609621,0.176960856767158,4.45890094794434));
#39082=CARTESIAN_POINT('Ctrl Pts',(17.503542197025,-0.290284687397741,4.39703907252861));
#39083=CARTESIAN_POINT('Ctrl Pts',(17.5512580330878,-0.490957336521241,
3.97057010757845));
#39084=CARTESIAN_POINT('Ctrl Pts',(17.5989738691507,-0.240776309167652,
3.57112706567612));
#39085=CARTESIAN_POINT('Ctrl Pts',(17.6466897052135,0.230513307714322,3.56552463842171));
#39086=CARTESIAN_POINT('Ctrl Pts',(17.6944055412763,0.490119007219086,3.95890762096741));
#39087=CARTESIAN_POINT('Ctrl Pts',(17.7421213773392,0.299640880944266,4.39002636746625));
#39088=CARTESIAN_POINT('Ctrl Pts',(17.789837213402,-0.166002076869247,4.46297789939377));
#39089=CARTESIAN_POINT('Ctrl Pts',(17.8375530494648,-0.479202773223469,
4.11076970247734));
#39090=CARTESIAN_POINT('Ctrl Pts',(17.8852688855277,-0.352344189444135,
3.65683998336499));
#39091=CARTESIAN_POINT('Ctrl Pts',(17.9329847215905,0.0980774850139738,
3.51803938772416));
#39092=CARTESIAN_POINT('Ctrl Pts',(17.9807005576534,0.458433095867658,3.82183063825345));
#39093=CARTESIAN_POINT('Ctrl Pts',(18.0284163937162,0.397802540886209,4.28923755516265));
#39094=CARTESIAN_POINT('Ctrl Pts',(18.076132229779,-0.0281362083699241,
4.49103317467411));
#39095=CARTESIAN_POINT('Ctrl Pts',(18.1238480658419,-0.428237044548737,
4.24190547436581));
#39096=CARTESIAN_POINT('Ctrl Pts',(18.1715639019047,-0.435081213444543,
3.7706322547532));
#39097=CARTESIAN_POINT('Ctrl Pts',(18.2192797379675,-0.0423836094492617,
3.50999096487715));
#39098=CARTESIAN_POINT('Ctrl Pts',(18.2669955740304,0.389235515258945,3.69933251171255));
#39099=CARTESIAN_POINT('Ctrl Pts',(18.3147114100932,0.463413677146622,4.16478163940629));
#39100=CARTESIAN_POINT('Ctrl Pts',(18.3624272461561,0.112031928774586,4.4789092521418));
#39101=CARTESIAN_POINT('Ctrl Pts',(18.4101430822189,-0.342230463623947,
4.35324712966946));
#39102=CARTESIAN_POINT('Ctrl Pts',(18.4578589182817,-0.482217355384067,
3.90319273261591));
#39103=CARTESIAN_POINT('Ctrl Pts',(18.5055747543446,-0.179376629827252,
3.54203793877243));
#39104=CARTESIAN_POINT('Ctrl Pts',(18.5532905904074,0.288188414964166,3.60143675240633));
#39105=CARTESIAN_POINT('Ctrl Pts',(18.6010064264702,0.491105603945206,4.02684232898929));
#39106=CARTESIAN_POINT('Ctrl Pts',(18.6487222625331,0.243032960192409,4.42759818183915));
#39107=CARTESIAN_POINT('Ctrl Pts',(18.6964380985959,-0.228220590447982,
4.43568404486223));
#39108=CARTESIAN_POINT('Ctrl Pts',(18.7441539346588,-0.489895661254576,
4.0436745456279));
#39109=CARTESIAN_POINT('Ctrl Pts',(18.7918697707216,-0.301692008317894,
3.6115580391236));
#39110=CARTESIAN_POINT('Ctrl Pts',(18.8395856067845,0.163560057986223,3.53615376224111));
#39111=CARTESIAN_POINT('Ctrl Pts',(18.8873014428472,0.478612406344963,3.88670662268212));
#39112=CARTESIAN_POINT('Ctrl Pts',(18.9350172789101,0.35414761756175,4.34129853476112));
#39113=CARTESIAN_POINT('Ctrl Pts',(18.982733114973,-0.0955363776958117,
4.48247075080787));
#39114=CARTESIAN_POINT('Ctrl Pts',(19.0304489510358,-0.457487847288108,
4.18058265263639));
#39115=CARTESIAN_POINT('Ctrl Pts',(19.0781647870987,-0.399321187381313,
3.71286272589862));
#39116=CARTESIAN_POINT('Ctrl Pts',(19.1258806231614,0.0255482632835279,
3.50882537619781));
#39117=CARTESIAN_POINT('Ctrl Pts',(19.1735964592243,0.426956350589889,3.75584124112414));
#39118=CARTESIAN_POINT('Ctrl Pts',(19.2213122952871,0.436283851722622,4.22707185138688));
#39119=CARTESIAN_POINT('Ctrl Pts',(19.26902813135,0.0449651784623906,4.48977888620274));
#39120=CARTESIAN_POINT('Ctrl Pts',(19.3167439674128,-0.387645709555542,
4.3027144342981));
#39121=CARTESIAN_POINT('Ctrl Pts',(19.3644598034757,-0.464275578741542,
3.8376626582024));
#39122=CARTESIAN_POINT('Ctrl Pts',(19.4121756395385,-0.114554038379521,
3.52168776344319));
#39123=CARTESIAN_POINT('Ctrl Pts',(19.4598914756013,0.340364234683876,3.64495435060606));
#39124=CARTESIAN_POINT('Ctrl Pts',(19.5076073116642,0.482720800247919,4.09426482953845));
#39125=CARTESIAN_POINT('Ctrl Pts',(19.555323147727,0.181787415268628,4.45701044834135));
#39126=CARTESIAN_POINT('Ctrl Pts',(19.6030389837899,-0.28608412753634,4.40007637198121));
#39127=CARTESIAN_POINT('Ctrl Pts',(19.6507548198527,-0.491240257057309,
3.97574594767572));
#39128=CARTESIAN_POINT('Ctrl Pts',(19.6984706559155,-0.245282818621706,
3.57368850533185));
#39129=CARTESIAN_POINT('Ctrl Pts',(19.7461864919783,0.225921452997342,3.56311925573479));
#39130=CARTESIAN_POINT('Ctrl Pts',(19.7939023280412,0.489658867576397,3.95374471702426));
#39131=CARTESIAN_POINT('Ctrl Pts',(19.841618164104,0.303734463062876,4.38684635894002));
#39132=CARTESIAN_POINT('Ctrl Pts',(19.8893340001669,-0.161112940293692,
4.46470246728215));
#39133=CARTESIAN_POINT('Ctrl Pts',(19.9370498362297,-0.47800980043334,4.11581244897344));
#39134=CARTESIAN_POINT('Ctrl Pts',(19.9847656722926,-0.355939225796451,
3.66057517601247));
#39135=CARTESIAN_POINT('Ctrl Pts',(20.0324815083554,0.0929888682922082,
3.51702731322357));
#39136=CARTESIAN_POINT('Ctrl Pts',(20.0801973444182,0.456536973876988,3.81701888067549));
#39137=CARTESIAN_POINT('Ctrl Pts',(20.1279131804811,0.400815378068436,4.28501049648274));
#39138=CARTESIAN_POINT('Ctrl Pts',(20.1756290165439,-0.022934367574535,
4.49133741301101));
#39139=CARTESIAN_POINT('Ctrl Pts',(20.2233448526067,-0.425711472830213,
4.24633918020534));
#39140=CARTESIAN_POINT('Ctrl Pts',(20.2710606886696,-0.437384262562023,
3.77535541015343));
#39141=CARTESIAN_POINT('Ctrl Pts',(20.3187765247324,-0.0477164433392854,
3.51022640082505));
#39142=CARTESIAN_POINT('Ctrl Pts',(20.3664923607953,0.386374384143037,3.69571627142296));
#39143=CARTESIAN_POINT('Ctrl Pts',(20.4062555575143,0.45143962727185,4.08165775845481));
#39144=CARTESIAN_POINT('Ctrl Pts',(20.4380661148895,0.291471375703242,4.31996082336987));
#39145=CARTESIAN_POINT('Ctrl Pts',(20.461924032921,0.103697252552815,4.42124466395835));
#39146=CARTESIAN_POINT('Ctrl Pts',(20.4857819509523,-0.111451542568667,
4.41901444157942));
#39147=CARTESIAN_POINT('Ctrl Pts',(20.5096398689838,-0.298255971346869,
4.31460392554555));
#39148=CARTESIAN_POINT('Ctrl Pts',(20.5334977870152,-0.412709509332759,
4.13311446574462));
#39149=CARTESIAN_POINT('Ctrl Pts',(20.5573557050466,-0.425936384696969,
3.91915434697803));
#39150=CARTESIAN_POINT('Ctrl Pts',(20.581213623078,-0.335173342752607,3.72492109335083));
#39151=CARTESIAN_POINT('Ctrl Pts',(20.6050715411095,-0.162364888615448,
3.59797442377207));
#39152=CARTESIAN_POINT('Ctrl Pts',(20.6289294591408,0.0501004451364318,
3.56932214892951));
#39153=CARTESIAN_POINT('Ctrl Pts',(20.6527873771723,0.250339089241223,3.64598859455508));
#39154=CARTESIAN_POINT('Ctrl Pts',(20.6766452952037,0.389350172549011,3.80921715950176));
#39155=CARTESIAN_POINT('Ctrl Pts',(20.7005032132352,0.433161330121289,4.01909908002448));
#39156=CARTESIAN_POINT('Ctrl Pts',(20.7243611312665,0.371049143609512,4.22430982617278));
#39157=CARTESIAN_POINT('Ctrl Pts',(20.748219049298,0.218207240773441,4.37467120177868));
#39158=CARTESIAN_POINT('Ctrl Pts',(20.7720769673293,0.01200671405148,4.43341500212799));
#39159=CARTESIAN_POINT('Ctrl Pts',(20.7959348853608,-0.197129246586683,
4.38617716647524));
#39160=CARTESIAN_POINT('Ctrl Pts',(20.8197928033922,-0.358062019934396,
4.24450842127602));
#39161=CARTESIAN_POINT('Ctrl Pts',(20.8436507214237,-0.431438726014498,
4.04305074550709));
#39162=CARTESIAN_POINT('Ctrl Pts',(20.867508639455,-0.399316990859146,3.83106596928302));
#39163=CARTESIAN_POINT('Ctrl Pts',(20.8913665574865,-0.269551332195825,
3.66039017609669));
#39164=CARTESIAN_POINT('Ctrl Pts',(20.9152244755179,-0.0738730526583281,
3.57275822989076));
#39165=CARTESIAN_POINT('Ctrl Pts',(20.9390823935493,0.139869212314499,3.58959853735383));
#39166=CARTESIAN_POINT('Ctrl Pts',(20.9629403115807,0.319409638666883,3.70679317993256));
#39167=CARTESIAN_POINT('Ctrl Pts',(20.9867982296122,0.420845711130686,3.8956848776653));
#39168=CARTESIAN_POINT('Ctrl Pts',(21.0106561476436,0.419373541863394,4.11008446384341));
#39169=CARTESIAN_POINT('Ctrl Pts',(21.034514065675,0.315353119032788,4.29756540021079));
#39170=CARTESIAN_POINT('Ctrl Pts',(21.0583719837064,0.134220268060588,4.41228349058099));
#39171=CARTESIAN_POINT('Ctrl Pts',(21.0822299017379,-0.079733094278782,
4.42618703719455));
#39172=CARTESIAN_POINT('Ctrl Pts',(21.1060878197692,-0.274189543318984,
4.33587624407661));
#39173=CARTESIAN_POINT('Ctrl Pts',(21.1299457378007,-0.401599180171465,
4.16343456021562));
#39174=CARTESIAN_POINT('Ctrl Pts',(21.1538036558321,-0.430806878168669,
3.95102867450389));
#39175=CARTESIAN_POINT('Ctrl Pts',(21.1776615738635,-0.354670559489406,
3.75059761183336));
#39176=CARTESIAN_POINT('Ctrl Pts',(21.2015194918949,-0.191807627993766,
3.61115222665144));
#39177=CARTESIAN_POINT('Ctrl Pts',(21.2253774099264,0.0179574932869785,
3.56679071405539));
#39178=CARTESIAN_POINT('Ctrl Pts',(21.2492353279577,0.223331518303719,3.62836067225603));
#39179=CARTESIAN_POINT('Ctrl Pts',(21.2730932459892,0.374094903668402,3.78080656934254));
#39180=CARTESIAN_POINT('Ctrl Pts',(21.2969511640206,0.433381894944723,3.98685123093373));
#39181=CARTESIAN_POINT('Ctrl Pts',(21.320809082052,0.386695207821707,4.19611112472705));
#39182=CARTESIAN_POINT('Ctrl Pts',(21.3446670000834,0.245451009020076,4.35741650656472));
#39183=CARTESIAN_POINT('Ctrl Pts',(21.3685249181149,0.0441873525619181,
4.43132381671722));
#39184=CARTESIAN_POINT('Ctrl Pts',(21.3923828361462,-0.167881315237013,
4.39976070465745));
#39185=CARTESIAN_POINT('Ctrl Pts',(21.4162407541777,-0.338898428465248,
4.27044521104599));
#39186=CARTESIAN_POINT('Ctrl Pts',(21.4400986722091,-0.427045644525908,
4.07499849655415));
#39187=CARTESIAN_POINT('Ctrl Pts',(21.4639565902406,-0.410768568010174,
3.86121260673678));
#39188=CARTESIAN_POINT('Ctrl Pts',(21.4878145082719,-0.294047387504818,
3.68136401506497));
#39189=CARTESIAN_POINT('Ctrl Pts',(21.5116724263034,-0.105423611064507,
3.57943060117972));
#39190=CARTESIAN_POINT('Ctrl Pts',(21.5355303443348,0.108979109962582,3.58033786138646));
#39191=CARTESIAN_POINT('Ctrl Pts',(21.5593882623662,0.296733470072461,3.68386394585134));
#39192=CARTESIAN_POINT('Ctrl Pts',(21.5832461803976,0.411928413892185,3.86469390692879));
#39193=CARTESIAN_POINT('Ctrl Pts',(21.6071040984291,0.426395639810567,4.07860989342611));
#39194=CARTESIAN_POINT('Ctrl Pts',(21.6309620164605,0.33659751701124,4.27330361969026));
#39195=CARTESIAN_POINT('Ctrl Pts',(21.6548199344919,0.164492132570386,4.401167166299));
#39196=CARTESIAN_POINT('Ctrl Pts',(21.6786778525233,-0.0478360589596606,
4.43093441317345));
#39197=CARTESIAN_POINT('Ctrl Pts',(21.7025357705547,-0.248467031045983,
4.35532645760922));
#39198=CARTESIAN_POINT('Ctrl Pts',(21.7263936885861,-0.388341045935521,
4.1928315042612));
#39199=CARTESIAN_POINT('Ctrl Pts',(21.7502516066176,-0.433255096896122,
3.98318399549658));
#39200=CARTESIAN_POINT('Ctrl Pts',(21.774109524649,-0.372226475033738,3.77764845789182));
#39201=CARTESIAN_POINT('Ctrl Pts',(21.7979674426804,-0.220178340780001,
3.62648392906691));
#39202=CARTESIAN_POINT('Ctrl Pts',(21.8218253607118,-0.0142906046679706,
3.56665425395863));
#39203=CARTESIAN_POINT('Ctrl Pts',(21.8456832787432,0.195091573553633,3.61278941785858));
#39204=CARTESIAN_POINT('Ctrl Pts',(21.8695411967747,0.356768547853618,3.75360811649661));
#39205=CARTESIAN_POINT('Ctrl Pts',(21.8933991148061,0.431205894023261,3.95467634223136));
#39206=CARTESIAN_POINT('Ctrl Pts',(21.9172570328375,0.400201653291494,4.16682743688221));
#39207=CARTESIAN_POINT('Ctrl Pts',(21.941114950869,0.271337207055788,4.33818467892719));
#39208=CARTESIAN_POINT('Ctrl Pts',(21.9649728689003,0.0761234226178432,
4.4268465550088));
#39209=CARTESIAN_POINT('Ctrl Pts',(21.9888307869318,-0.137704612210607,
4.41113282132402));
#39210=CARTESIAN_POINT('Ctrl Pts',(22.0126887049632,-0.317860118355158,
4.29488591379237));
#39211=CARTESIAN_POINT('Ctrl Pts',(22.0365466229946,-0.420290167226249,
4.10653136780738));
#39212=CARTESIAN_POINT('Ctrl Pts',(22.060404541026,-0.419947821735935,3.89212700053744));
#39213=CARTESIAN_POINT('Ctrl Pts',(22.0842624590574,-0.316916794682727,
3.70410052003731));
#39214=CARTESIAN_POINT('Ctrl Pts',(22.1081203770888,-0.136390978688423,
3.58842952252864));
#39215=CARTESIAN_POINT('Ctrl Pts',(22.1319782951203,0.0774861468089536,
3.57339871771534));
#39216=CARTESIAN_POINT('Ctrl Pts',(22.1558362131517,0.27241579873489,3.66268354680831));
#39217=CARTESIAN_POINT('Ctrl Pts',(22.1796941311831,0.400732367405962,3.83445143701846));
#39218=CARTESIAN_POINT('Ctrl Pts',(22.2035520492145,0.431058956528623,4.04670046033727));
#39219=CARTESIAN_POINT('Ctrl Pts',(22.227409967246,0.355979888945518,4.24752994899471));
#39220=CARTESIAN_POINT('Ctrl Pts',(22.2512678852773,0.193854041863619,4.38783162256878));
#39221=CARTESIAN_POINT('Ctrl Pts',(22.2751258033088,-0.0156743990186396,
4.43329790005389));
#39222=CARTESIAN_POINT('Ctrl Pts',(22.2989837213402,-0.221370022215225,
4.37281103827166));
#39223=CARTESIAN_POINT('Ctrl Pts',(22.3228416393716,-0.372934645290675,
4.22116172228637));
#39224=CARTESIAN_POINT('Ctrl Pts',(22.346699557403,-0.43330658847365,4.01543234121164));
#39225=CARTESIAN_POINT('Ctrl Pts',(22.3705574754345,-0.387723268841402,
3.80592933171158));
#39226=CARTESIAN_POINT('Ctrl Pts',(22.3944153934659,-0.247331046528593,
3.64388188817752));
#39227=CARTESIAN_POINT('Ctrl Pts',(22.4182733114973,-0.0464596501027702,
3.56891502119853));
#39228=CARTESIAN_POINT('Ctrl Pts',(22.4421312295287,0.165772403721094,3.59936017830047));
#39229=CARTESIAN_POINT('Ctrl Pts',(22.4659891475602,0.337468575289321,3.7277726770023));
#39230=CARTESIAN_POINT('Ctrl Pts',(22.4898470655915,0.426644514167594,3.92275218663495));
#39231=CARTESIAN_POINT('Ctrl Pts',(22.513704983623,0.411494197867752,4.13662086224655));
#39232=CARTESIAN_POINT('Ctrl Pts',(22.5375629016544,0.295722435535401,4.31708206952049));
#39233=CARTESIAN_POINT('Ctrl Pts',(22.5614208196858,0.107638304484935,4.42000797176855));
#39234=CARTESIAN_POINT('Ctrl Pts',(22.5852787377172,-0.106765988085903,
4.42023067651324));
#39235=CARTESIAN_POINT('Ctrl Pts',(22.6091366557487,-0.295063722636797,
4.31769517074077));
#39236=CARTESIAN_POINT('Ctrl Pts',(22.6329945737801,-0.411209141905604,
4.13747522778479));
#39237=CARTESIAN_POINT('Ctrl Pts',(22.6568524918115,-0.426804986482714,
3.92363755172126));
#39238=CARTESIAN_POINT('Ctrl Pts',(22.6807104098429,-0.33803111495158,3.72847502015617));
#39239=CARTESIAN_POINT('Ctrl Pts',(22.7045683278743,-0.16660749730952,3.59970312177549));
#39240=CARTESIAN_POINT('Ctrl Pts',(22.7284262459057,0.0455714674079685,
3.56882345794434));
#39241=CARTESIAN_POINT('Ctrl Pts',(22.7522841639372,0.246577802732478,3.64336153500176));
#39242=CARTESIAN_POINT('Ctrl Pts',(22.7761420819686,0.387346815298129,3.80514019809748));
#39243=CARTESIAN_POINT('Ctrl Pts',(22.7920473606562,0.417963038852713,3.94471011778788));
#39244=CARTESIAN_POINT('Ctrl Pts',(22.8,0.415641328671541,4.01393920819689));
#39245=CARTESIAN_POINT('Ctrl Pts',(3.96816317011929,0.203757107801821,4.42939176513376));
#39246=CARTESIAN_POINT('Ctrl Pts',(3.9761158094631,0.132237748973037,4.46332948562603));
#39247=CARTESIAN_POINT('Ctrl Pts',(3.99202108815071,-0.0280119004087947,
4.49474661085258));
#39248=CARTESIAN_POINT('Ctrl Pts',(4.01587900618213,-0.261670681609628,
4.42079217330492));
#39249=CARTESIAN_POINT('Ctrl Pts',(4.03973692421355,-0.431283260509235,
4.24398813071681));
#39250=CARTESIAN_POINT('Ctrl Pts',(4.06359484224497,-0.495466080430727,
4.00749935521381));
#39251=CARTESIAN_POINT('Ctrl Pts',(4.08745276027639,-0.438477829352452,
3.76918881818141));
#39252=CARTESIAN_POINT('Ctrl Pts',(4.11131067830781,-0.274278321106756,
3.5873115455631));
#39253=CARTESIAN_POINT('Ctrl Pts',(4.13516859633923,-0.0430057845205295,
3.50635120590702));
#39254=CARTESIAN_POINT('Ctrl Pts',(4.15902651437064,0.198780450874126,3.54609966156282));
#39255=CARTESIAN_POINT('Ctrl Pts',(4.18288443240206,0.391960715466274,3.69684005745713));
#39256=CARTESIAN_POINT('Ctrl Pts',(4.20674235043348,0.489295238859844,3.92171081754005));
#39257=CARTESIAN_POINT('Ctrl Pts',(4.2306002684649,0.466984102771714,4.16572567991789));
#39258=CARTESIAN_POINT('Ctrl Pts',(4.25445818649632,0.330482445391075,4.36921595913043));
#39259=CARTESIAN_POINT('Ctrl Pts',(4.27831610452774,0.113168927396708,4.48242295331799));
#39260=CARTESIAN_POINT('Ctrl Pts',(4.30217402255916,-0.131817528672551,
4.47766435517297));
#39261=CARTESIAN_POINT('Ctrl Pts',(4.32603194059057,-0.344570980451485,
4.35610383169054));
#39262=CARTESIAN_POINT('Ctrl Pts',(4.349889858622,-0.473067456356951,4.14746621026076));
#39263=CARTESIAN_POINT('Ctrl Pts',(4.37374777665341,-0.485886045261059,
3.9027690893624));
#39264=CARTESIAN_POINT('Ctrl Pts',(4.39760569468484,-0.379892264971952,
3.68184757153936));
#39265=CARTESIAN_POINT('Ctrl Pts',(4.42146361271625,-0.181004475645389,
3.53872299041084));
#39266=CARTESIAN_POINT('Ctrl Pts',(4.44532153074767,0.0621438372772935,
3.50839320219298));
#39267=CARTESIAN_POINT('Ctrl Pts',(4.46917944877909,0.290096289836991,3.5982746675986));
#39268=CARTESIAN_POINT('Ctrl Pts',(4.49303736681051,0.447112297141319,3.78638891931142));
#39269=CARTESIAN_POINT('Ctrl Pts',(4.51689528484194,0.494797168872773,4.02673689903048));
#39270=CARTESIAN_POINT('Ctrl Pts',(4.54075320287334,0.421490654719143,4.26054697856981));
#39271=CARTESIAN_POINT('Ctrl Pts',(4.56461112090478,0.245118194360182,4.43064622472778));
#39272=CARTESIAN_POINT('Ctrl Pts',(4.58846903893618,0.00880765856895839,
4.49544073835303));
#39273=CARTESIAN_POINT('Ctrl Pts',(4.61232695696761,-0.229656589644598,
4.43908649592634));
#39274=CARTESIAN_POINT('Ctrl Pts',(4.63618487499902,-0.411963545977342,
4.2753636447643));
#39275=CARTESIAN_POINT('Ctrl Pts',(4.66004279303045,-0.493534193653132,
4.04430688170513));
#39276=CARTESIAN_POINT('Ctrl Pts',(4.68390071106186,-0.454422287381232,
3.80241587917234));
#39277=CARTESIAN_POINT('Ctrl Pts',(4.70775862909328,-0.304191753628974,
3.60883957626609));
#39278=CARTESIAN_POINT('Ctrl Pts',(4.7316165471247,-0.0795780500979935,
3.51091265195837));
#39279=CARTESIAN_POINT('Ctrl Pts',(4.75547446515612,0.164494654344808,3.53258090671894));
#39280=CARTESIAN_POINT('Ctrl Pts',(4.77933238318754,0.368343935055725,3.66854586202706));
#39281=CARTESIAN_POINT('Ctrl Pts',(4.80319030121895,0.482123090158262,3.88556038269908));
#39282=CARTESIAN_POINT('Ctrl Pts',(4.82704821925038,0.478010016947761,4.13055850707372));
#39283=CARTESIAN_POINT('Ctrl Pts',(4.85090613728179,0.357010473862124,4.34363152012653));
#39284=CARTESIAN_POINT('Ctrl Pts',(4.87476405531322,0.14871214514713,4.47267726617372));
#39285=CARTESIAN_POINT('Ctrl Pts',(4.89862197334463,-0.0959503538938319,
4.48614054517122));
#39286=CARTESIAN_POINT('Ctrl Pts',(4.92247989137606,-0.317150377772593,
4.38072921867179));
#39287=CARTESIAN_POINT('Ctrl Pts',(4.94633780940747,-0.460798495283114,
4.1822192273514));
#39288=CARTESIAN_POINT('Ctrl Pts',(4.97019572743889,-0.49176882879792,3.93915167139151));
#39289=CARTESIAN_POINT('Ctrl Pts',(4.99405364547031,-0.40248828815769,3.71096318925158));
#39290=CARTESIAN_POINT('Ctrl Pts',(5.01791156350173,-0.214788397502062,
3.55345208054429));
#39291=CARTESIAN_POINT('Ctrl Pts',(5.04176948153314,0.0254331070612992,
3.50513410186502));
#39292=CARTESIAN_POINT('Ctrl Pts',(5.06562739956457,0.259435524164246,3.57782431515618));
#39293=CARTESIAN_POINT('Ctrl Pts',(5.08948531759598,0.429998888727244,3.75374798322641));
#39294=CARTESIAN_POINT('Ctrl Pts',(5.11334323562741,0.495415812061873,3.98988697716804));
#39295=CARTESIAN_POINT('Ctrl Pts',(5.13720115365882,0.439690074491602,4.2284988806653));
#39296=CARTESIAN_POINT('Ctrl Pts',(5.16105907169025,0.276448136790977,4.41123658365534));
#39297=CARTESIAN_POINT('Ctrl Pts',(5.18491698972166,0.0456070993489057,
4.49341574008204));
#39298=CARTESIAN_POINT('Ctrl Pts',(5.20877490775308,-0.196386116196418,
4.45494130768376));
#39299=CARTESIAN_POINT('Ctrl Pts',(5.2326328257845,-0.390357576881318,4.3052213332044));
#39300=CARTESIAN_POINT('Ctrl Pts',(5.25649074381592,-0.488875976891831,
4.08086642869437));
#39301=CARTESIAN_POINT('Ctrl Pts',(5.28034866184734,-0.467850883838054,
3.83673747961128));
#39302=CARTESIAN_POINT('Ctrl Pts',(5.30420657987876,-0.332423505683668,
3.632530663945));
#39303=CARTESIAN_POINT('Ctrl Pts',(5.32806449791017,-0.115709525355139,
3.5181801106079));
#39304=CARTESIAN_POINT('Ctrl Pts',(5.3519224159416,0.129298585786916,3.52164764473745));
#39305=CARTESIAN_POINT('Ctrl Pts',(5.37578033397301,0.342689670681295,3.64208535978523));
#39306=CARTESIAN_POINT('Ctrl Pts',(5.39963825200445,0.472283796414913,3.85004295376459));
#39307=CARTESIAN_POINT('Ctrl Pts',(5.42349617003584,0.48639166917272,4.09466913029638));
#39308=CARTESIAN_POINT('Ctrl Pts',(5.44735408806728,0.381563529774833,4.31614612573549));
#39309=CARTESIAN_POINT('Ctrl Pts',(5.47121200609869,0.183432713764955,4.46031678178449));
#39310=CARTESIAN_POINT('Ctrl Pts',(5.49506992413012,-0.059552397366927,
4.49192744591021));
#39311=CARTESIAN_POINT('Ctrl Pts',(5.51892784216153,-0.287975325168481,
4.40324844967551));
#39312=CARTESIAN_POINT('Ctrl Pts',(5.54278576019295,-0.445980441674811,
4.21596422322942));
#39313=CARTESIAN_POINT('Ctrl Pts',(5.56664367822437,-0.494931191930538,
3.97587086145358));
#39314=CARTESIAN_POINT('Ctrl Pts',(5.59050159625579,-0.422857784100094,
3.74167773132221));
#39315=CARTESIAN_POINT('Ctrl Pts',(5.61435951428721,-0.247384129650275,
3.57065143242979));
#39316=CARTESIAN_POINT('Ctrl Pts',(5.63821743231862,-0.0114183168777074,
3.50461255354752));
#39317=CARTESIAN_POINT('Ctrl Pts',(5.66207535035005,0.227339585372105,3.55970939936999));
#39318=CARTESIAN_POINT('Ctrl Pts',(5.68593326838146,0.410506766445453,3.72246929038963));
#39319=CARTESIAN_POINT('Ctrl Pts',(5.70979118641288,0.493293861043031,3.9530929995654));
#39320=CARTESIAN_POINT('Ctrl Pts',(5.73364910444431,0.455457169749513,4.19518674831082));
#39321=CARTESIAN_POINT('Ctrl Pts',(5.75750702247572,0.306248793691327,4.38955201985635));
#39322=CARTESIAN_POINT('Ctrl Pts',(5.78136494050715,0.0821542461994931,
4.48866121222712));
#39323=CARTESIAN_POINT('Ctrl Pts',(5.80522285853855,-0.162029253596618,
4.46827942571263));
#39324=CARTESIAN_POINT('Ctrl Pts',(5.82908077656998,-0.366592184898752,
4.33339056701663));
#39325=CARTESIAN_POINT('Ctrl Pts',(5.85293869460139,-0.481513345756758,
4.11697862749145));
#39326=CARTESIAN_POINT('Ctrl Pts',(5.87679661263282,-0.478691368855474,
3.87196223809426));
#39327=CARTESIAN_POINT('Ctrl Pts',(5.90065453066423,-0.358816329143926,
3.65825454842257));
#39328=CARTESIAN_POINT('Ctrl Pts',(5.92451244869565,-0.151200892471453,
3.52811296978032));
#39329=CARTESIAN_POINT('Ctrl Pts',(5.94837036672708,0.093387223403125,3.5133605500302));
#39330=CARTESIAN_POINT('Ctrl Pts',(5.97222828475848,0.315139728168714,3.61760487120619));
#39331=CARTESIAN_POINT('Ctrl Pts',(5.99608620278992,0.459831779670103,3.81535495398299));
#39332=CARTESIAN_POINT('Ctrl Pts',(6.01994412082132,0.492082823488737,4.05825627791571));
#39333=CARTESIAN_POINT('Ctrl Pts',(6.04380203885276,0.404005480250355,4.28691141512903));
#39334=CARTESIAN_POINT('Ctrl Pts',(6.06765995688416,0.21713917558903,4.44541067075535));
#39335=CARTESIAN_POINT('Ctrl Pts',(6.09151787491559,-0.0228261843714051,
4.49499153360272));
#39336=CARTESIAN_POINT('Ctrl Pts',(6.11537579294701,-0.257204988275768,
4.42353981062321));
#39337=CARTESIAN_POINT('Ctrl Pts',(6.13923371097843,-0.428699479426561,
4.24850911946619));
#39338=CARTESIAN_POINT('Ctrl Pts',(6.16309162900984,-0.49534768549136,4.01273373861842));
#39339=CARTESIAN_POINT('Ctrl Pts',(6.18694954704127,-0.440903093044182,
3.77380201544612));
#39340=CARTESIAN_POINT('Ctrl Pts',(6.21080746507268,-0.278582990390117,
3.59026229064107));
#39341=CARTESIAN_POINT('Ctrl Pts',(6.23466538310411,-0.048260127889517,
3.50676273730504));
#39342=CARTESIAN_POINT('Ctrl Pts',(6.25852330113552,0.194087080856728,3.5441598063702));
#39343=CARTESIAN_POINT('Ctrl Pts',(6.28238121916694,0.388553448942855,3.69248145192407));
#39344=CARTESIAN_POINT('Ctrl Pts',(6.30623913719837,0.488798280742691,3.9170164641697));
#39345=CARTESIAN_POINT('Ctrl Pts',(6.33009705522977,0.468067515948433,4.15995908608738));
#39346=CARTESIAN_POINT('Ctrl Pts',(6.36190761260502,0.291040001689194,4.43610431491443));
#39347=CARTESIAN_POINT('Ctrl Pts',(6.40167080932402,-0.143168317426403,
4.54352222151223));
#39348=CARTESIAN_POINT('Ctrl Pts',(6.44938664538688,-0.535165231989368,
4.17285582464912));
#39349=CARTESIAN_POINT('Ctrl Pts',(6.49710248144971,-0.434543251113388,
3.64369891234367));
#39350=CARTESIAN_POINT('Ctrl Pts',(6.54481831751255,0.0645215567551043,
3.4416075490323));
#39351=CARTESIAN_POINT('Ctrl Pts',(6.59253415357539,0.504653900644641,3.75236619672659));
#39352=CARTESIAN_POINT('Ctrl Pts',(6.64024998963822,0.481186238846835,4.29049388273239));
#39353=CARTESIAN_POINT('Ctrl Pts',(6.68796582570107,0.01592709648968,4.56187610740764));
#39354=CARTESIAN_POINT('Ctrl Pts',(6.7356816617639,-0.464005405879062,4.31726850783359));
#39355=CARTESIAN_POINT('Ctrl Pts',(6.78339749782674,-0.517809574500644,
3.78131383674221));
#39356=CARTESIAN_POINT('Ctrl Pts',(6.83111333388957,-0.0961144992151805,
3.44617913151078));
#39357=CARTESIAN_POINT('Ctrl Pts',(6.87882916995242,0.413851019972934,3.61962818876606));
#39358=CARTESIAN_POINT('Ctrl Pts',(6.92654500601525,0.543767061592725,4.14237771887731));
#39359=CARTESIAN_POINT('Ctrl Pts',(6.97426084207809,0.174335412693353,4.53438003016987));
#39360=CARTESIAN_POINT('Ctrl Pts',(7.02197667814094,-0.355192171006393,
4.43565270890428));
#39361=CARTESIAN_POINT('Ctrl Pts',(7.06969251420376,-0.558540766450571,
3.93685892261342));
#39362=CARTESIAN_POINT('Ctrl Pts',(7.11740835026661,-0.248973074301851,
3.49604849518665));
#39363=CARTESIAN_POINT('Ctrl Pts',(7.16512418632944,0.289230577826905,3.51802452284194));
#39364=CARTESIAN_POINT('Ctrl Pts',(7.21284002239229,0.561829257914175,3.98260602935256));
#39365=CARTESIAN_POINT('Ctrl Pts',(7.26055585845511,0.318491529052478,4.46316069626365));
#39366=CARTESIAN_POINT('Ctrl Pts',(7.30827169451797,-0.217321894570402,
4.51838776411367));
#39367=CARTESIAN_POINT('Ctrl Pts',(7.35598753058078,-0.553565266295818,
4.09757137442565));
#39368=CARTESIAN_POINT('Ctrl Pts',(7.40370336664365,-0.381461142739227,
3.58715368886071));
#39369=CARTESIAN_POINT('Ctrl Pts',(7.45141920270646,0.140944621146953,3.45585912402047));
#39370=CARTESIAN_POINT('Ctrl Pts',(7.49913503876933,0.533918768911932,3.82425749787944));
#39371=CARTESIAN_POINT('Ctrl Pts',(7.54685087483214,0.436587096747522,4.3540429157916));
#39372=CARTESIAN_POINT('Ctrl Pts',(7.594566710895,-0.0616692246238245,4.5587052763707));
#39373=CARTESIAN_POINT('Ctrl Pts',(7.64228254695782,-0.503293747851232,
4.25029998493175));
#39374=CARTESIAN_POINT('Ctrl Pts',(7.68999838302067,-0.482735878399531,
3.7120403659385));
#39375=CARTESIAN_POINT('Ctrl Pts',(7.7377142190835,-0.0188742238918736,
3.43821850974892));
#39376=CARTESIAN_POINT('Ctrl Pts',(7.78543005514633,0.462319920793015,3.6802892401675));
#39377=CARTESIAN_POINT('Ctrl Pts',(7.83314589120918,0.518958568528469,4.21595528072725));
#39378=CARTESIAN_POINT('Ctrl Pts',(7.88086172727202,0.099029577569048,4.55330626409362));
#39379=CARTESIAN_POINT('Ctrl Pts',(7.92857756333485,-0.411839798232008,
4.38254759143289));
#39380=CARTESIAN_POINT('Ctrl Pts',(7.9762933993977,-0.544510350349916,3.86048957930736));
#39381=CARTESIAN_POINT('Ctrl Pts',(8.02400923546053,-0.177148669371157,
3.466546133148));
#39382=CARTESIAN_POINT('Ctrl Pts',(8.07172507152338,0.352891360472903,3.56248158116143));
#39383=CARTESIAN_POINT('Ctrl Pts',(8.1194409075862,0.558865824063627,4.06019692528064));
#39384=CARTESIAN_POINT('Ctrl Pts',(8.16715674364906,0.251625202160443,4.50263250666582));
#39385=CARTESIAN_POINT('Ctrl Pts',(8.21487257971187,-0.286686714637947,
4.48349292318459));
#39386=CARTESIAN_POINT('Ctrl Pts',(8.26258841577472,-0.561729810142263,
4.02035434884804));
#39387=CARTESIAN_POINT('Ctrl Pts',(8.31030425183756,-0.32092777766878,3.53852406277244));
#39388=CARTESIAN_POINT('Ctrl Pts',(8.3580200879004,0.21458717114652,3.4804742305729));
#39389=CARTESIAN_POINT('Ctrl Pts',(8.40573592396324,0.553043418849938,3.89951290636976));
#39390=CARTESIAN_POINT('Ctrl Pts',(8.45345176002607,0.383631385356639,4.41083042643994));
#39391=CARTESIAN_POINT('Ctrl Pts',(8.50116759608892,-0.13807525223727,4.54487604447167));
#39392=CARTESIAN_POINT('Ctrl Pts',(8.54888343215175,-0.532985261140852,
4.17855360686946));
#39393=CARTESIAN_POINT('Ctrl Pts',(8.59659926821459,-0.43844670370641,3.64826264467864));
#39394=CARTESIAN_POINT('Ctrl Pts',(8.64431510427743,0.0587242081113278,
3.4409775080543));
#39395=CARTESIAN_POINT('Ctrl Pts',(8.69203094034026,0.501967776032349,3.74705132745037));
#39396=CARTESIAN_POINT('Ctrl Pts',(8.73974677640311,0.484246611455832,4.28541180496438));
#39397=CARTESIAN_POINT('Ctrl Pts',(8.78746261246592,0.021834332487559,4.56167423035448));
#39398=CARTESIAN_POINT('Ctrl Pts',(8.83517844852879,-0.460628749968427,
4.32214256754115));
#39399=CARTESIAN_POINT('Ctrl Pts',(8.88289428459161,-0.520089363644054,
3.78678242815423));
#39400=CARTESIAN_POINT('Ctrl Pts',(8.93061012065447,-0.101943912081849,
3.44722326576734));
#39401=CARTESIAN_POINT('Ctrl Pts',(8.97832595671729,0.409818202553832,3.61528748398963));
#39402=CARTESIAN_POINT('Ctrl Pts',(9.02604179278014,0.545237955920739,4.1366391252272));
#39403=CARTESIAN_POINT('Ctrl Pts',(9.07375762884296,0.179957304801303,4.53251295530543));
#39404=CARTESIAN_POINT('Ctrl Pts',(9.12147346490582,-0.350580908316224,
4.43937194476168));
#39405=CARTESIAN_POINT('Ctrl Pts',(9.16918930096864,-0.559175278946307,
3.94274891673689));
#39406=CARTESIAN_POINT('Ctrl Pts',(9.21690513703149,-0.254270386902387,
3.49870043939378));
#39407=CARTESIAN_POINT('Ctrl Pts',(9.26462097309432,0.284134913886797,3.51500306204057));
#39408=CARTESIAN_POINT('Ctrl Pts',(9.31233680915716,0.56161475127612,3.97668583545263));
#39409=CARTESIAN_POINT('Ctrl Pts',(9.36005264522,0.323355121014866,4.45977836490307));
#39410=CARTESIAN_POINT('Ctrl Pts',(9.40776848128284,-0.211846492332409,
4.52064934726353));
#39411=CARTESIAN_POINT('Ctrl Pts',(9.45548431734568,-0.552506212093558,
4.10340002281193));
#39412=CARTESIAN_POINT('Ctrl Pts',(9.50320015340851,-0.385790975888367,
3.59119686639829));
#39413=CARTESIAN_POINT('Ctrl Pts',(9.55091598947136,0.135202049632292,3.45440391781584));
#39414=CARTESIAN_POINT('Ctrl Pts',(9.59863182553417,0.532036952624682,3.81864024657791));
#39415=CARTESIAN_POINT('Ctrl Pts',(9.64634766159704,0.440294135581046,4.34942202748599));
#39416=CARTESIAN_POINT('Ctrl Pts',(9.69406349765985,-0.0557775609627595,
4.55932418400469));
#39417=CARTESIAN_POINT('Ctrl Pts',(9.74177933372271,-0.500627865026369,
4.25559033604309));
#39418=CARTESIAN_POINT('Ctrl Pts',(9.78949516978553,-0.485743897486414,
3.71714394973028));
#39419=CARTESIAN_POINT('Ctrl Pts',(9.83721100584839,-0.0247938347541151,
3.43844862667992));
#39420=CARTESIAN_POINT('Ctrl Pts',(9.88492684191122,0.458924787935076,3.67543457032792));
#39421=CARTESIAN_POINT('Ctrl Pts',(9.93264267797406,0.521205716397956,4.21047394212484));
#39422=CARTESIAN_POINT('Ctrl Pts',(9.98035851403688,0.104855415711801,4.55223185431066));
#39423=CARTESIAN_POINT('Ctrl Pts',(10.0280743500997,-0.407785226630454,
4.3868667575037));
#39424=CARTESIAN_POINT('Ctrl Pts',(10.0757901861625,-0.54595042077573,3.86623596457089));
#39425=CARTESIAN_POINT('Ctrl Pts',(10.1235060222254,-0.182760942995651,
3.46844274359687));
#39426=CARTESIAN_POINT('Ctrl Pts',(10.1712218582882,0.34826072087591,3.55878673023755));
#39427=CARTESIAN_POINT('Ctrl Pts',(10.2189376943511,0.559469206087141,4.05430365143988));
#39428=CARTESIAN_POINT('Ctrl Pts',(10.2666535304139,0.256908510808291,4.49995269395588));
#39429=CARTESIAN_POINT('Ctrl Pts',(10.3143693664768,-0.281575222991369,
4.4864874848512));
#39430=CARTESIAN_POINT('Ctrl Pts',(10.3620852025396,-0.561484096926345,
4.02627333283551));
#39431=CARTESIAN_POINT('Ctrl Pts',(10.4098010386024,-0.325773485110519,
3.5419319750098));
#39432=CARTESIAN_POINT('Ctrl Pts',(10.4575168746653,0.209099930751681,3.47824153281512));
#39433=CARTESIAN_POINT('Ctrl Pts',(10.5052327107281,0.55195366278862,3.89368991932227));
#39434=CARTESIAN_POINT('Ctrl Pts',(10.552948546791,0.387939853388008,4.40676448870664));
#39435=CARTESIAN_POINT('Ctrl Pts',(10.6006643828538,-0.13232509260073,4.54630096923553));
#39436=CARTESIAN_POINT('Ctrl Pts',(10.6483802189166,-0.531073869970951,
4.18416086379456));
#39437=CARTESIAN_POINT('Ctrl Pts',(10.6960960549795,-0.442129340924997,
3.6529030034519));
#39438=CARTESIAN_POINT('Ctrl Pts',(10.7438118910423,0.0528293649267388,
3.44038965581316));
#39439=CARTESIAN_POINT('Ctrl Pts',(10.7915277271051,0.499274052081986,3.74177509795313));
#39440=CARTESIAN_POINT('Ctrl Pts',(10.839243563168,0.487227694891584,4.28029244094358));
#39441=CARTESIAN_POINT('Ctrl Pts',(10.8869593992308,0.0277526485205102,
4.56141292256198));
#39442=CARTESIAN_POINT('Ctrl Pts',(10.9346752352937,-0.457208082016334,
4.32697927894352));
#39443=CARTESIAN_POINT('Ctrl Pts',(10.9823910713565,-0.522307595786967,
3.79227553224832));
#39444=CARTESIAN_POINT('Ctrl Pts',(11.0301069074193,-0.107764007611043,
3.44832836054127));
#39445=CARTESIAN_POINT('Ctrl Pts',(11.0778227434822,0.405740926916492,3.61098974390844));
#39446=CARTESIAN_POINT('Ctrl Pts',(11.125538579545,0.54664772512998,4.13088523113667));
#39447=CARTESIAN_POINT('Ctrl Pts',(11.1732544156078,0.185559506100192,4.53058679668394));
#39448=CARTESIAN_POINT('Ctrl Pts',(11.2209702516707,-0.345930862581405,
4.4430423427091));
#39449=CARTESIAN_POINT('Ctrl Pts',(11.2686860877335,-0.559747597323992,
3.94864528834179));
#39450=CARTESIAN_POINT('Ctrl Pts',(11.3164019237964,-0.259539500620097,
3.50140805588402));
#39451=CARTESIAN_POINT('Ctrl Pts',(11.3641177598592,0.279007713031768,3.51203547753114));
#39452=CARTESIAN_POINT('Ctrl Pts',(11.411833595922,0.561337850721073,3.97076822846069));
#39453=CARTESIAN_POINT('Ctrl Pts',(11.4595494319849,0.328182802800164,4.45634496498341));
#39454=CARTESIAN_POINT('Ctrl Pts',(11.5072652680477,-0.206347562673641,
4.52285309839201));
#39455=CARTESIAN_POINT('Ctrl Pts',(11.5549811041106,-0.551385786278872,
4.10921718641821));
#39456=CARTESIAN_POINT('Ctrl Pts',(11.6026969401734,-0.390077958183356,
3.59528545163414));
#39457=CARTESIAN_POINT('Ctrl Pts',(11.6504127762362,0.129444461032819,3.45300931394821));
#39458=CARTESIAN_POINT('Ctrl Pts',(11.6981286122991,0.530096039923511,3.8130431397972));
#39459=CARTESIAN_POINT('Ctrl Pts',(11.7458444483619,0.443952268776438,4.34476232707146));
#39460=CARTESIAN_POINT('Ctrl Pts',(11.7935602844247,-0.0498797018717475,
4.55988096454574));
#39461=CARTESIAN_POINT('Ctrl Pts',(11.8412761204876,-0.497906374793238,
4.26085229740167));
#39462=CARTESIAN_POINT('Ctrl Pts',(11.8889919565504,-0.48869796246776,3.72227895182515));
#39463=CARTESIAN_POINT('Ctrl Pts',(11.9367077926133,-0.0307106916234339,
3.43874111807518));
#39464=CARTESIAN_POINT('Ctrl Pts',(11.9844236286761,0.455478679883424,3.67061595167475));
#39465=CARTESIAN_POINT('Ctrl Pts',(12.0321394647389,0.523394971212992,4.20496922507643));
#39466=CARTESIAN_POINT('Ctrl Pts',(12.0798553008018,0.110669607010866,4.5510961052335));
#39467=CARTESIAN_POINT('Ctrl Pts',(12.1275711368646,-0.403685360180124,
4.39114295225112));
#39468=CARTESIAN_POINT('Ctrl Pts',(12.1752869729274,-0.547329849620031,
3.8719972077086));
#39469=CARTESIAN_POINT('Ctrl Pts',(12.2230028089903,-0.188352916401613,
3.4703983969034));
#39470=CARTESIAN_POINT('Ctrl Pts',(12.2707186450531,0.34359139813055,3.55514088718992));
#39471=CARTESIAN_POINT('Ctrl Pts',(12.318434481116,0.560010444926212,4.04840434580723));
#39472=CARTESIAN_POINT('Ctrl Pts',(12.3661503171788,0.262163283277844,4.49721734887317));
#39473=CARTESIAN_POINT('Ctrl Pts',(12.4138661532417,-0.276432455305192,
4.48942800979656));
#39474=CARTESIAN_POINT('Ctrl Pts',(12.4615819893045,-0.561176016721412,
4.03218939850585));
#39475=CARTESIAN_POINT('Ctrl Pts',(12.5092978253673,-0.330583007179444,
3.54539076726965));
#39476=CARTESIAN_POINT('Ctrl Pts',(12.5570136614301,0.203589464528802,3.47606678951191));
#39477=CARTESIAN_POINT('Ctrl Pts',(12.604729497493,0.550802598333678,3.88787874069406));
#39478=CARTESIAN_POINT('Ctrl Pts',(12.6524453335558,0.392205230901379,4.40265336950419));
#39479=CARTESIAN_POINT('Ctrl Pts',(12.7001611696187,-0.126560234920843,
4.54766521348015));
#39480=CARTESIAN_POINT('Ctrl Pts',(12.7478770056815,-0.529103489635726,
4.18974766500481));
#39481=CARTESIAN_POINT('Ctrl Pts',(12.7955928417443,-0.44576286851447,3.65758191611243));
#39482=CARTESIAN_POINT('Ctrl Pts',(12.8433086778072,0.0469286537069902,
3.43986396243348));
#39483=CARTESIAN_POINT('Ctrl Pts',(12.89102451387,0.496524871139168,3.73652755085263));
#39484=CARTESIAN_POINT('Ctrl Pts',(12.9387403499328,0.490154659387074,4.27514194336855));
#39485=CARTESIAN_POINT('Ctrl Pts',(12.9864561859957,0.0336678819209607,
4.56108925568614));
#39486=CARTESIAN_POINT('Ctrl Pts',(13.0341720220585,-0.45373662956012,4.33177967103923));
#39487=CARTESIAN_POINT('Ctrl Pts',(13.0818878581214,-0.524467812480695,
3.79779170939055));
#39488=CARTESIAN_POINT('Ctrl Pts',(13.1296036941842,-0.113572133225654,
3.44949473238301));
#39489=CARTESIAN_POINT('Ctrl Pts',(13.177319530247,0.401618583502394,3.60673521324049));
#39490=CARTESIAN_POINT('Ctrl Pts',(13.2250353663099,0.547996775303968,4.12511679893576));
#39491=CARTESIAN_POINT('Ctrl Pts',(13.2727512023727,0.191141096329688,4.52860170299893));
#39492=CARTESIAN_POINT('Ctrl Pts',(13.3204670384356,-0.341242392487953,
4.4466635296155));
#39493=CARTESIAN_POINT('Ctrl Pts',(13.3681828744984,-0.560257741594785,
3.95454736418435));
#39494=CARTESIAN_POINT('Ctrl Pts',(13.4158987105612,-0.264779785921688,
3.5041710536014));
#39495=CARTESIAN_POINT('Ctrl Pts',(13.4636145466241,0.273849521323983,3.50912209380529));
#39496=CARTESIAN_POINT('Ctrl Pts',(13.5113303826869,0.560998599421335,3.96485386839523));
#39497=CARTESIAN_POINT('Ctrl Pts',(13.5590462187498,0.332974031597074,4.45286087643057));
#39498=CARTESIAN_POINT('Ctrl Pts',(13.6067620548126,-0.200825712906817,
4.52499877347948));
#39499=CARTESIAN_POINT('Ctrl Pts',(13.6544778908754,-0.550204115147588,
4.11502221869768));
#39500=CARTESIAN_POINT('Ctrl Pts',(13.7021937269383,-0.394321612469819,
3.5994189906415));
#39501=CARTESIAN_POINT('Ctrl Pts',(13.7499095630011,0.123672494356884,3.45167546721031));
#39502=CARTESIAN_POINT('Ctrl Pts',(13.7976253990639,0.528096246669736,3.80746679929733));
#39503=CARTESIAN_POINT('Ctrl Pts',(13.8453412351268,0.44756108986054,4.34006433209368));
#39504=CARTESIAN_POINT('Ctrl Pts',(13.8930570711896,-0.0439763023801491,
4.56037555616609));
#39505=CARTESIAN_POINT('Ctrl Pts',(13.9407729072525,-0.495129579482757,
4.26608528452492));
#39506=CARTESIAN_POINT('Ctrl Pts',(13.9884887433153,-0.491597745198497,
3.72744480185615));
#39507=CARTESIAN_POINT('Ctrl Pts',(14.0362045793781,-0.0366241372948624,
3.43909595144367));
#39508=CARTESIAN_POINT('Ctrl Pts',(14.083920415441,0.451981979421435,3.66583391943861));
#39509=CARTESIAN_POINT('Ctrl Pts',(14.1316362515038,0.525526089798339,4.19944174101915));
#39510=CARTESIAN_POINT('Ctrl Pts',(14.1793520875667,0.11647150565515,4.54989914301615));
#39511=CARTESIAN_POINT('Ctrl Pts',(14.2270679236295,-0.399540654275635,
4.39537570069553));
#39512=CARTESIAN_POINT('Ctrl Pts',(14.2747837596924,-0.548648483661927,
3.87777266878906));
#39513=CARTESIAN_POINT('Ctrl Pts',(14.3224995957551,-0.193923968459428,
3.47241287584284));
#39514=CARTESIAN_POINT('Ctrl Pts',(14.370215431818,0.338883910883161,3.5515444569815));
#39515=CARTESIAN_POINT('Ctrl Pts',(14.4179312678808,0.560489480462528,4.04249966364955));
#39516=CARTESIAN_POINT('Ctrl Pts',(14.4656471039437,0.267388935893957,4.49442677524682));
#39517=CARTESIAN_POINT('Ctrl Pts',(14.5133629400065,-0.271258982813659,
4.49231417140114));
#39518=CARTESIAN_POINT('Ctrl Pts',(14.5610787760694,-0.560805603747543,
4.03810188873054));
#39519=CARTESIAN_POINT('Ctrl Pts',(14.6087946121322,-0.335355809656676,
3.54890005536578));
#39520=CARTESIAN_POINT('Ctrl Pts',(14.656510448195,0.198056384554314,3.47395024222346));
#39521=CARTESIAN_POINT('Ctrl Pts',(14.7042262842579,0.549590353339887,3.88208001596329));
#39522=CARTESIAN_POINT('Ctrl Pts',(14.7519421203207,0.396427044118869,4.3984975254762));
#39523=CARTESIAN_POINT('Ctrl Pts',(14.7996579563836,-0.120781319530639,
4.54896862567174));
#39524=CARTESIAN_POINT('Ctrl Pts',(14.8473737924464,-0.527074338995675,
4.19531338994486));
#39525=CARTESIAN_POINT('Ctrl Pts',(14.8950896285092,-0.449346882879826,
3.66229886294881));
#39526=CARTESIAN_POINT('Ctrl Pts',(14.9428054645721,0.041022729875082,3.43940048630678));
#39527=CARTESIAN_POINT('Ctrl Pts',(14.9905213006349,0.493720538569869,3.73130926902151));
#39528=CARTESIAN_POINT('Ctrl Pts',(15.0382371366977,0.493027179828974,4.2699608843321));
#39529=CARTESIAN_POINT('Ctrl Pts',(15.0859529727606,0.0395793756528551,
4.56070326567839));
#39530=CARTESIAN_POINT('Ctrl Pts',(15.1336688088234,-0.450214778192253,
4.33654321062351));
#39531=CARTESIAN_POINT('Ctrl Pts',(15.1813846448863,-0.526569773778615,
3.80333034687015));
#39532=CARTESIAN_POINT('Ctrl Pts',(15.2291004809491,-0.119367643786657,
3.45072225173751));
#39533=CARTESIAN_POINT('Ctrl Pts',(15.2768163170119,0.397451630201876,3.60252436455885));
#39534=CARTESIAN_POINT('Ctrl Pts',(15.3245321530748,0.549284956596614,4.11933446935456));
#39535=CARTESIAN_POINT('Ctrl Pts',(15.3722479891376,0.196701455513243,4.52655789474516));
#39536=CARTESIAN_POINT('Ctrl Pts',(15.4199638252005,-0.336516018808871,
4.45023510325662));
#39537=CARTESIAN_POINT('Ctrl Pts',(15.4676796612633,-0.560705655094284,
3.96045448869));
#39538=CARTESIAN_POINT('Ctrl Pts',(15.5153954973261,-0.269990660741143,
3.50698912564524));
#39539=CARTESIAN_POINT('Ctrl Pts',(15.5631113333889,0.268660911710894,3.50626323446785));
#39540=CARTESIAN_POINT('Ctrl Pts',(15.6108271694518,0.560597035059331,3.95894341219528));
#39541=CARTESIAN_POINT('Ctrl Pts',(15.6585430055146,0.337728275218647,4.44932648624059));
#39542=CARTESIAN_POINT('Ctrl Pts',(15.7062588415775,-0.1952815563728,4.52708613419449));
#39543=CARTESIAN_POINT('Ctrl Pts',(15.7539746776403,-0.548961329954127,
4.12081447485494));
#39544=CARTESIAN_POINT('Ctrl Pts',(15.8016905137031,-0.398521467382777,
3.60359702428645));
#39545=CARTESIAN_POINT('Ctrl Pts',(15.849406349766,0.117886790727162,3.4504025257595));
#39546=CARTESIAN_POINT('Ctrl Pts',(15.8971221858288,0.526037794990907,3.80191184447176));
#39547=CARTESIAN_POINT('Ctrl Pts',(15.9448380218916,0.451120197982628,4.33532856438364));
#39548=CARTESIAN_POINT('Ctrl Pts',(15.9925538579545,-0.0380680182095728,
4.56080790392885));
#39549=CARTESIAN_POINT('Ctrl Pts',(16.0402696940173,-0.492297787528177,
4.27128871615743));
#39550=CARTESIAN_POINT('Ctrl Pts',(16.0879855300802,-0.494442923584513,
3.73264092602517));
#39551=CARTESIAN_POINT('Ctrl Pts',(16.135701366143,-0.0425335149309099,
3.43951308737216));
#39552=CARTESIAN_POINT('Ctrl Pts',(16.1834172022058,0.448435074945997,3.66108900478495));
#39553=CARTESIAN_POINT('Ctrl Pts',(16.2311330382687,0.52759883543946,4.19389210391969));
#39554=CARTESIAN_POINT('Ctrl Pts',(16.2788488743315,0.122260467197297,4.54864110061148));
#39555=CARTESIAN_POINT('Ctrl Pts',(16.3265647103944,-0.395351569291248,
4.39956453268331));
#39556=CARTESIAN_POINT('Ctrl Pts',(16.3742805464572,-0.549906176433804,
3.88356170630145));
#39557=CARTESIAN_POINT('Ctrl Pts',(16.42199638252,-0.199473480363076,3.47448595665642));
#39558=CARTESIAN_POINT('Ctrl Pts',(16.4697122185829,0.334138782019088,3.54799783908671));
#39559=CARTESIAN_POINT('Ctrl Pts',(16.5174280546457,0.560906259487099,4.0365902608309));
#39560=CARTESIAN_POINT('Ctrl Pts',(16.5651438907085,0.272584888215931,4.49158128304055));
#39561=CARTESIAN_POINT('Ctrl Pts',(16.6128597267714,-0.26605538016154,4.49514564908375));
#39562=CARTESIAN_POINT('Ctrl Pts',(16.6605755628342,-0.560372899148451,
4.04401014677825));
#39563=CARTESIAN_POINT('Ctrl Pts',(16.7082913988971,-0.340091362401967,
3.55245944950311));
#39564=CARTESIAN_POINT('Ctrl Pts',(16.7560072349599,0.19250130541649,3.4718921260458));
#39565=CARTESIAN_POINT('Ctrl Pts',(16.8037230710227,0.548317062457662,3.87629438922476));
#39566=CARTESIAN_POINT('Ctrl Pts',(16.8514389070856,0.400604824101502,4.39429741823411));
#39567=CARTESIAN_POINT('Ctrl Pts',(16.8991547431484,-0.114988988324618,
4.55021106103346));
#39568=CARTESIAN_POINT('Ctrl Pts',(16.9468705792113,-0.524986643439221,
4.20085742040038));
#39569=CARTESIAN_POINT('Ctrl Pts',(16.9945864152741,-0.45288098592576,3.66705332002498));
#39570=CARTESIAN_POINT('Ctrl Pts',(17.0423022513369,0.0351122494330066,
3.4389992789138));
#39571=CARTESIAN_POINT('Ctrl Pts',(17.0900180873998,0.490861365866046,3.72612083208173));
#39572=CARTESIAN_POINT('Ctrl Pts',(17.1377339234626,0.49584493715134,4.26474983932169));
#39573=CARTESIAN_POINT('Ctrl Pts',(17.1854497595254,0.0454864730955262,
4.56025499541263));
#39574=CARTESIAN_POINT('Ctrl Pts',(17.2331655955883,-0.446642919103261,
4.34126936858499));
#39575=CARTESIAN_POINT('Ctrl Pts',(17.2808814316511,-0.528613246204851,
3.80889082948154));
#39576=CARTESIAN_POINT('Ctrl Pts',(17.328597267714,-0.125149895556227,3.45201078225777));
#39577=CARTESIAN_POINT('Ctrl Pts',(17.3763131037768,0.393240529860342,3.59835766558462));
#39578=CARTESIAN_POINT('Ctrl Pts',(17.4240289398397,0.55051212592285,4.1135388846668));
#39579=CARTESIAN_POINT('Ctrl Pts',(17.4717447759024,0.202239966032548,4.52445559893916));
#39580=CARTESIAN_POINT('Ctrl Pts',(17.5194606119653,-0.331752266527324,
4.45375666691904));
#39581=CARTESIAN_POINT('Ctrl Pts',(17.5671764480281,-0.561091288070378,
3.96636600572338));
#39582=CARTESIAN_POINT('Ctrl Pts',(17.614892284091,-0.275171546279217,3.50986195899749));
#39583=CARTESIAN_POINT('Ctrl Pts',(17.6626081201538,0.263442460518632,3.50345921706735));
#39584=CARTESIAN_POINT('Ctrl Pts',(17.7103239562167,0.560133202238927,3.95303751636628));
#39585=CARTESIAN_POINT('Ctrl Pts',(17.7580397922795,0.342445005586054,4.44574218699675));
#39586=CARTESIAN_POINT('Ctrl Pts',(17.8057556283423,-0.189715708890181,
4.52911494868296));
#39587=CARTESIAN_POINT('Ctrl Pts',(17.8534714644052,-0.547657568741173,
4.12659331151364));
#39588=CARTESIAN_POINT('Ctrl Pts',(17.901187300468,-0.402677056422281,3.60781908849286));
#39589=CARTESIAN_POINT('Ctrl Pts',(17.9489031365308,0.112087992792125,3.44919063098808));
#39590=CARTESIAN_POINT('Ctrl Pts',(17.9966189725937,0.523920913530056,3.79637889233847));
#39591=CARTESIAN_POINT('Ctrl Pts',(18.0443348086565,0.454629197813879,4.33055554996792));
#39592=CARTESIAN_POINT('Ctrl Pts',(18.0920506447194,-0.0321555056241734,
4.56117795981091));
#39593=CARTESIAN_POINT('Ctrl Pts',(18.1397664807822,-0.489411313471489,
4.27646201432672));
#39594=CARTESIAN_POINT('Ctrl Pts',(18.1874823168451,-0.497233181596917,
3.73786674717144));
#39595=CARTESIAN_POINT('Ctrl Pts',(18.2351981529079,-0.0484381681459794,
3.43999247952716));
#39596=CARTESIAN_POINT('Ctrl Pts',(18.2829139889707,0.444838360430441,3.65638173475637));
#39597=CARTESIAN_POINT('Ctrl Pts',(18.3306298250336,0.529612977905601,4.18832093020544));
#39598=CARTESIAN_POINT('Ctrl Pts',(18.3783456610964,0.128035848626906,4.54732211775687));
#39599=CARTESIAN_POINT('Ctrl Pts',(18.4260614971592,-0.391118570530631,
4.40370898293889));
#39600=CARTESIAN_POINT('Ctrl Pts',(18.4737773332221,-0.551102788237131,
3.88936367722697));
#39601=CARTESIAN_POINT('Ctrl Pts',(18.5214931692849,-0.205000835699102,
3.47661740907615));
#39602=CARTESIAN_POINT('Ctrl Pts',(18.5692090053478,0.329356538604741,3.54450142744705));
#39603=CARTESIAN_POINT('Ctrl Pts',(18.6169248414106,0.561260735706054,4.03067679373969));
#39604=CARTESIAN_POINT('Ctrl Pts',(18.6646406774734,0.2777505631021,4.48868118831814));
#39605=CARTESIAN_POINT('Ctrl Pts',(18.7123565135363,-0.260822225340423,
4.49792212833724));
#39606=CARTESIAN_POINT('Ctrl Pts',(18.7600723495991,-0.559877950986752,
4.04991351638789));
#39607=CARTESIAN_POINT('Ctrl Pts',(18.8077881856619,-0.344789139412875,
3.55606855432066));
#39608=CARTESIAN_POINT('Ctrl Pts',(18.8555040217248,0.186924844147682,3.46989266958543));
#39609=CARTESIAN_POINT('Ctrl Pts',(18.9032198577876,0.546982867117114,3.87052250311704));
#39610=CARTESIAN_POINT('Ctrl Pts',(18.9509356938504,0.404738106803207,4.39005351430856));
#39611=CARTESIAN_POINT('Ctrl Pts',(18.9986515299133,-0.109183884691052,
4.55139238155646));
#39612=CARTESIAN_POINT('Ctrl Pts',(19.0463673659761,-0.522840634850846,
4.20637914057629));
#39613=CARTESIAN_POINT('Ctrl Pts',(19.094083202039,-0.456364785113784,3.67184475922049));
#39614=CARTESIAN_POINT('Ctrl Pts',(19.1417990381018,0.029197868913272,3.43866038485254));
#39615=CARTESIAN_POINT('Ctrl Pts',(19.1895148741647,0.487947670564988,3.72096281627648));
#39616=CARTESIAN_POINT('Ctrl Pts',(19.2372307102275,0.498607618457993,4.25950938727589));
#39617=CARTESIAN_POINT('Ctrl Pts',(19.2849465462903,0.0513885179525073,
4.55974449445321));
#39618=CARTESIAN_POINT('Ctrl Pts',(19.3326623823531,-0.44302144872845,4.34595762039384));
#39619=CARTESIAN_POINT('Ctrl Pts',(19.380378218416,-0.530598003365269,3.81447253878192));
#39620=CARTESIAN_POINT('Ctrl Pts',(19.4280940544788,-0.130918245164485,
3.45336018235082));
#39621=CARTESIAN_POINT('Ctrl Pts',(19.4758098905417,0.38898574814073,3.59423557624425));
#39622=CARTESIAN_POINT('Ctrl Pts',(19.5235257266045,0.551678150913516,4.10773069407674));
#39623=CARTESIAN_POINT('Ctrl Pts',(19.5712415626673,0.207756005258534,4.52229503878775));
#39624=CARTESIAN_POINT('Ctrl Pts',(19.6189573987302,-0.326951650734615,
4.4572278489044));
#39625=CARTESIAN_POINT('Ctrl Pts',(19.666673234793,-0.561414624206118,3.9722812219163));
#39626=CARTESIAN_POINT('Ctrl Pts',(19.7143890708559,-0.280321816997631,
3.51278930393937));
#39627=CARTESIAN_POINT('Ctrl Pts',(19.7621049069187,0.258194652845487,3.5007102220535));
#39628=CARTESIAN_POINT('Ctrl Pts',(19.8098207429815,0.559607330995945,3.94713708427543));
#39629=CARTESIAN_POINT('Ctrl Pts',(19.8575365790444,0.347123361713752,4.44210790974427));
#39630=CARTESIAN_POINT('Ctrl Pts',(19.9052524151072,-0.184128152223511,
4.53108587353909));
#39631=CARTESIAN_POINT('Ctrl Pts',(19.9529682511701,-0.546294178096705,
4.13235642149579));
#39632=CARTESIAN_POINT('Ctrl Pts',(20.0006840872329,-0.406785648814185,
3.61208785870539));
#39633=CARTESIAN_POINT('Ctrl Pts',(20.0483999232957,0.106272459957556,3.44803398021027));
#39634=CARTESIAN_POINT('Ctrl Pts',(20.0961157593586,0.5217539278249,3.7908797683689));
#39635=CARTESIAN_POINT('Ctrl Pts',(20.1438315954214,0.458072423058868,4.32572464996293));
#39636=CARTESIAN_POINT('Ctrl Pts',(20.1915474314842,-0.0262105744965466,
4.56152565902554));
#39637=CARTESIAN_POINT('Ctrl Pts',(20.2392632675471,-0.486524960252488,
4.28152908133109));
#39638=CARTESIAN_POINT('Ctrl Pts',(20.2869791036099,-0.499865224545849,
3.74326461201656));
#39639=CARTESIAN_POINT('Ctrl Pts',(20.3346949396728,-0.0545328049175168,
3.440261547834));
#39640=CARTESIAN_POINT('Ctrl Pts',(20.3824107757356,0.441568512678419,3.6522489094147));
#39641=CARTESIAN_POINT('Ctrl Pts',(20.4221739724547,0.515928418030698,4.09332268501583));
#39642=CARTESIAN_POINT('Ctrl Pts',(20.4539845298298,0.333108474939506,4.36566768059473));
#39643=CARTESIAN_POINT('Ctrl Pts',(20.4778424478613,0.118510552090848,4.48142006140068));
#39644=CARTESIAN_POINT('Ctrl Pts',(20.5017003658927,-0.127372553428812,
4.47887124859312));
#39645=CARTESIAN_POINT('Ctrl Pts',(20.5255582839241,-0.340862259689409,
4.35954554232165));
#39646=CARTESIAN_POINT('Ctrl Pts',(20.5494162019555,-0.471665647836603,
4.15213005589169));
#39647=CARTESIAN_POINT('Ctrl Pts',(20.5732741199869,-0.486782001098211,
3.90760543082941));
#39648=CARTESIAN_POINT('Ctrl Pts',(20.5971320380184,-0.38305332993788,3.68562568155832));
#39649=CARTESIAN_POINT('Ctrl Pts',(20.6209899560498,-0.185558943137764,
3.54054450025879));
#39650=CARTESIAN_POINT('Ctrl Pts',(20.6448478740812,0.0572573647513246,
3.50779920733485));
#39651=CARTESIAN_POINT('Ctrl Pts',(20.6687057921126,0.28610038304352,3.59541756340761));
#39652=CARTESIAN_POINT('Ctrl Pts',(20.6925637101441,0.444969396676924,3.78196356026503));
#39653=CARTESIAN_POINT('Ctrl Pts',(20.7164216281754,0.495039040219165,4.02182741068269));
#39654=CARTESIAN_POINT('Ctrl Pts',(20.7402795462069,0.424054039808096,4.25635280284423));
#39655=CARTESIAN_POINT('Ctrl Pts',(20.7641374642383,0.249378454468877,4.42819351412177));
#39656=CARTESIAN_POINT('Ctrl Pts',(20.7879953822697,0.0137218901755031,
4.49532894963167));
#39657=CARTESIAN_POINT('Ctrl Pts',(20.8118533003011,-0.22528943893053,4.44134312218709));
#39658=CARTESIAN_POINT('Ctrl Pts',(20.8357112183326,-0.409211687104306,
4.27943679589328));
#39659=CARTESIAN_POINT('Ctrl Pts',(20.859569136364,-0.493070359673604,4.04920060553547));
#39660=CARTESIAN_POINT('Ctrl Pts',(20.8834270543954,-0.456359989112496,
3.80693350349834));
#39661=CARTESIAN_POINT('Ctrl Pts',(20.9072849724268,-0.308057122141145,
3.61187643128937));
#39662=CARTESIAN_POINT('Ctrl Pts',(20.9311428904583,-0.0844259229598539,
3.51172613733272));
#39663=CARTESIAN_POINT('Ctrl Pts',(20.9550008084896,0.159849727585384,3.53097210659131));
#39664=CARTESIAN_POINT('Ctrl Pts',(20.9788587265211,0.365037758375503,3.66490817000854));
#39665=CARTESIAN_POINT('Ctrl Pts',(21.0027166445525,0.480964117596,3.88078331455297));
#39666=CARTESIAN_POINT('Ctrl Pts',(21.026574562584,0.479281646861755,4.12581018556955));
#39667=CARTESIAN_POINT('Ctrl Pts',(21.0504324806153,0.360401759160676,4.34007303948752));
#39668=CARTESIAN_POINT('Ctrl Pts',(21.0742903986468,0.153393823636192,4.47117877170218));
#39669=CARTESIAN_POINT('Ctrl Pts',(21.0981483166782,-0.0911230798336762,
4.48706845966041));
#39670=CARTESIAN_POINT('Ctrl Pts',(21.1220062347096,-0.313357908298923,
4.38385664171252));
#39671=CARTESIAN_POINT('Ctrl Pts',(21.145864152741,-0.458968192403581,4.18678141884249));
#39672=CARTESIAN_POINT('Ctrl Pts',(21.1697220707724,-0.492348251467217,
3.94403305123036));
#39673=CARTESIAN_POINT('Ctrl Pts',(21.1935799888039,-0.405335751726616,
3.71497012710753));
#39674=CARTESIAN_POINT('Ctrl Pts',(21.2174379068353,-0.21920761957706,3.55560477096155));
#39675=CARTESIAN_POINT('Ctrl Pts',(21.2412958248667,0.0205227466613194,
3.50490615340017));
#39676=CARTESIAN_POINT('Ctrl Pts',(21.2651537428981,0.255234742309135,3.57527146741714));
#39677=CARTESIAN_POINT('Ctrl Pts',(21.2890116609295,0.427534891009427,3.74949447702405));
#39678=CARTESIAN_POINT('Ctrl Pts',(21.312869578961,0.495291113040325,3.98497291063177));
#39679=CARTESIAN_POINT('Ctrl Pts',(21.3367274969923,0.441935166474334,4.22412587691986));
#39680=CARTESIAN_POINT('Ctrl Pts',(21.3605854150238,0.280514033632862,4.40847396123464));
#39681=CARTESIAN_POINT('Ctrl Pts',(21.3844433330552,0.0504995785194436,
4.49293903542029));
#39682=CARTESIAN_POINT('Ctrl Pts',(21.4083012510867,-0.191863399122956,
4.45686708805594));
#39683=CARTESIAN_POINT('Ctrl Pts',(21.432159169118,-0.387310549425693,4.3090786928523));
#39684=CARTESIAN_POINT('Ctrl Pts',(21.4560170871495,-0.488049720266331,
4.08571213811173));
#39685=CARTESIAN_POINT('Ctrl Pts',(21.4798750051809,-0.469447440294381,
3.84138663085107));
#39686=CARTESIAN_POINT('Ctrl Pts',(21.5037329232123,-0.336052473678932,
3.63584641288874));
#39687=CARTESIAN_POINT('Ctrl Pts',(21.5275908412437,-0.120483523363382,
3.51935166631968));
#39688=CARTESIAN_POINT('Ctrl Pts',(21.5514487592752,0.124546930319796,3.5203885299332));
#39689=CARTESIAN_POINT('Ctrl Pts',(21.5753066773065,0.339122266949511,3.63870346233219));
#39690=CARTESIAN_POINT('Ctrl Pts',(21.599164595338,0.470772971804989,3.84536523971104));
#39691=CARTESIAN_POINT('Ctrl Pts',(21.6230225133694,0.487306861455871,4.08983942814686));
#39692=CARTESIAN_POINT('Ctrl Pts',(21.6468804314008,0.384680949508402,4.31234542922385));
#39693=CARTESIAN_POINT('Ctrl Pts',(21.6707383494323,0.187990066907445,4.45847446473699));
#39694=CARTESIAN_POINT('Ctrl Pts',(21.6945962674636,-0.0546695077989956,
4.49249400502822));
#39695=CARTESIAN_POINT('Ctrl Pts',(21.7184541854951,-0.283960898681086,
4.40608534582272));
#39696=CARTESIAN_POINT('Ctrl Pts',(21.7423121035264,-0.443816114896065,
4.22037775802082));
#39697=CARTESIAN_POINT('Ctrl Pts',(21.766170021558,-0.495146201710716,3.98078180541326));
#39698=CARTESIAN_POINT('Ctrl Pts',(21.7900279395893,-0.425399554695369,
3.74588522487523));
#39699=CARTESIAN_POINT('Ctrl Pts',(21.8138858576208,-0.25163112890579,3.57312662880273));
#39700=CARTESIAN_POINT('Ctrl Pts',(21.8377437756521,-0.0163320378044167,
3.50475019978512));
#39701=CARTESIAN_POINT('Ctrl Pts',(21.8616016936836,0.222960681415914,3.55747583725374));
#39702=CARTESIAN_POINT('Ctrl Pts',(21.885459611715,0.407733440703041,3.71841068663001));
#39703=CARTESIAN_POINT('Ctrl Pts',(21.9093175297464,0.492804267302335,3.94820179346412));
#39704=CARTESIAN_POINT('Ctrl Pts',(21.9331754477779,0.457371026827486,4.19065897275109));
#39705=CARTESIAN_POINT('Ctrl Pts',(21.9570333658092,0.310098111756678,4.38649483975425));
#39706=CARTESIAN_POINT('Ctrl Pts',(21.9808912838407,0.0869977614584207,
4.48782219052945));
#39707=CARTESIAN_POINT('Ctrl Pts',(22.0047492018721,-0.15737591128791,4.46986372771052));
#39708=CARTESIAN_POINT('Ctrl Pts',(22.0286071199035,-0.363266886890503,
4.33701078463543));
#39709=CARTESIAN_POINT('Ctrl Pts',(22.0524650379349,-0.480329213457224,
4.12174952472744));
#39710=CARTESIAN_POINT('Ctrl Pts',(22.0763229559664,-0.479937963428243,
3.87671718963328));
#39711=CARTESIAN_POINT('Ctrl Pts',(22.1001808739978,-0.362188808094022,
3.66183085982978));
#39712=CARTESIAN_POINT('Ctrl Pts',(22.1240387920292,-0.155874623354616,
3.529636096341));
#39713=CARTESIAN_POINT('Ctrl Pts',(22.1478967100606,0.0885551527323001,
3.51245811975107));
#39714=CARTESIAN_POINT('Ctrl Pts',(22.1717546280921,0.311330781786364,3.61449741325855));
#39715=CARTESIAN_POINT('Ctrl Pts',(22.1956125461234,0.457977554205651,3.81080259009947));
#39716=CARTESIAN_POINT('Ctrl Pts',(22.2194704641549,0.492636339578261,4.05337168730347));
#39717=CARTESIAN_POINT('Ctrl Pts',(22.2433283821863,0.406832120751761,4.28288995313029));
#39718=CARTESIAN_POINT('Ctrl Pts',(22.2671863002177,0.22154636656941,4.44323391967918));
#39719=CARTESIAN_POINT('Ctrl Pts',(22.2910442182491,-0.0179135091400202,
4.49519511936025));
#39720=CARTESIAN_POINT('Ctrl Pts',(22.3149021362805,-0.2529930437236,4.42606762362056));
#39721=CARTESIAN_POINT('Ctrl Pts',(22.338760054312,-0.426208888077552,4.25275498785448));
#39722=CARTESIAN_POINT('Ctrl Pts',(22.3626179723434,-0.495205048933098,
4.01763687303198));
#39723=CARTESIAN_POINT('Ctrl Pts',(22.3864758903748,-0.443110087468167,
3.77820606161377));
#39724=CARTESIAN_POINT('Ctrl Pts',(22.4103338084062,-0.282662637164788,
3.59300991103726));
#39725=CARTESIAN_POINT('Ctrl Pts',(22.4341917264377,-0.0530964769854286,
3.50733392083031));
#39726=CARTESIAN_POINT('Ctrl Pts',(22.458049644469,0.189453226607198,3.5421282117862));
#39727=CARTESIAN_POINT('Ctrl Pts',(22.4819075625005,0.385676439696491,3.6888846179772));
#39728=CARTESIAN_POINT('Ctrl Pts',(22.5057654805319,0.487591287867653,3.9117172269821));
#39729=CARTESIAN_POINT('Ctrl Pts',(22.5296233985634,0.470276727405835,4.15613734610506));
#39730=CARTESIAN_POINT('Ctrl Pts',(22.5534813165947,0.337966804695391,4.36237769267677));
#39731=CARTESIAN_POINT('Ctrl Pts',(22.5773392346262,0.123014588878675,4.48000670597833));
#39732=CARTESIAN_POINT('Ctrl Pts',(22.6011971526576,-0.122017660845505,
4.48026122441149));
#39733=CARTESIAN_POINT('Ctrl Pts',(22.625055070689,-0.337213993725473,4.36307837627545));
#39734=CARTESIAN_POINT('Ctrl Pts',(22.6489129887204,-0.469950950795418,
4.15711375897153));
#39735=CARTESIAN_POINT('Ctrl Pts',(22.6727709067518,-0.487774683880463,
3.912729067726));
#39736=CARTESIAN_POINT('Ctrl Pts',(22.6966288247832,-0.386319338946922,
3.6896872918462));
#39737=CARTESIAN_POINT('Ctrl Pts',(22.7204867428147,-0.190407614498503,
3.54252014522276));
#39738=CARTESIAN_POINT('Ctrl Pts',(22.7443446608461,0.0520814161336476,
3.50722927763546));
#39739=CARTESIAN_POINT('Ctrl Pts',(22.7682025788775,0.281801791424649,3.59241522467272));
#39740=CARTESIAN_POINT('Ctrl Pts',(22.7920604969089,0.442679857002608,3.77730419914427));
#39741=CARTESIAN_POINT('Ctrl Pts',(22.8079657755965,0.477669651496365,3.93681187972983));
#39742=CARTESIAN_POINT('Ctrl Pts',(22.8159184149403,0.475016281724327,4.01593044384941));
#39743=CARTESIAN_POINT('Ctrl Pts',(3.98408158505964,0.229225853138217,4.48306385360099));
#39744=CARTESIAN_POINT('Ctrl Pts',(3.99203422440344,0.148766887950233,4.52124364039387));
#39745=CARTESIAN_POINT('Ctrl Pts',(4.00793950309106,-0.0315132651739855,
4.55658776856145));
#39746=CARTESIAN_POINT('Ctrl Pts',(4.03179742112247,-0.29437836981663,4.47338935048851));
#39747=CARTESIAN_POINT('Ctrl Pts',(4.0556553391539,-0.485191777607318,4.27448557757091));
#39748=CARTESIAN_POINT('Ctrl Pts',(4.07951325718531,-0.557397168683185,
4.00843674174317));
#39749=CARTESIAN_POINT('Ctrl Pts',(4.10337117521674,-0.493285636019562,
3.74033843218029));
#39750=CARTESIAN_POINT('Ctrl Pts',(4.12722909324815,-0.308561908987092,
3.53572729771651));
#39751=CARTESIAN_POINT('Ctrl Pts',(4.15108701127957,-0.0483813190761145,
3.44464727048097));
#39752=CARTESIAN_POINT('Ctrl Pts',(4.17494492931099,0.223627135909104,3.48936410886239));
#39753=CARTESIAN_POINT('Ctrl Pts',(4.19880284734241,0.440954086798485,3.65894639349553));
#39754=CARTESIAN_POINT('Ctrl Pts',(4.22266076537383,0.55045499896491,3.91192501290154));
#39755=CARTESIAN_POINT('Ctrl Pts',(4.24651868340524,0.525355068663259,4.18644066347397));
#39756=CARTESIAN_POINT('Ctrl Pts',(4.27037660143667,0.371791302444591,4.41536633561891));
#39757=CARTESIAN_POINT('Ctrl Pts',(4.29423451946808,0.127314547262185,4.54272370785395));
#39758=CARTESIAN_POINT('Ctrl Pts',(4.31809243749951,-0.14829414195428,4.5373703057994));
#39759=CARTESIAN_POINT('Ctrl Pts',(4.34195035553092,-0.387640842632661,
4.40061524972397));
#39760=CARTESIAN_POINT('Ctrl Pts',(4.36580827356235,-0.53219881478122,4.16589884014724));
#39761=CARTESIAN_POINT('Ctrl Pts',(4.38966619159376,-0.546619671109945,
3.89061565172978));
#39762=CARTESIAN_POINT('Ctrl Pts',(4.41352410962518,-0.427377132892538,
3.64207991255526));
#39763=CARTESIAN_POINT('Ctrl Pts',(4.4373820276566,-0.203629241694984,3.48106538615089));
#39764=CARTESIAN_POINT('Ctrl Pts',(4.46123994568802,0.0699115445388116,
3.44694450735191));
#39765=CARTESIAN_POINT('Ctrl Pts',(4.48509786371944,0.326357054473012,3.54806076195131));
#39766=CARTESIAN_POINT('Ctrl Pts',(4.50895578175085,0.502999374434197,3.7596884705576));
#39767=CARTESIAN_POINT('Ctrl Pts',(4.53281369978229,0.556644646112557,4.03007889421215));
#39768=CARTESIAN_POINT('Ctrl Pts',(4.55667161781369,0.474175139017821,4.29311420882242));
#39769=CARTESIAN_POINT('Ctrl Pts',(4.58052953584512,0.275756894216243,4.48447511514554));
#39770=CARTESIAN_POINT('Ctrl Pts',(4.60438745387653,0.00990857728296194,
4.55736865895685));
#39771=CARTESIAN_POINT('Ctrl Pts',(4.62824537190795,-0.258362656684952,
4.49397038324719));
#39772=CARTESIAN_POINT('Ctrl Pts',(4.65210328993938,-0.463457183444019,
4.30978289334447));
#39773=CARTESIAN_POINT('Ctrl Pts',(4.67596120797079,-0.555223804526532,
4.04984504770563));
#39774=CARTESIAN_POINT('Ctrl Pts',(4.69981912600221,-0.511223081411799,
3.77771873014923));
#39775=CARTESIAN_POINT('Ctrl Pts',(4.72367704403363,-0.342214389453536,
3.55994623789246));
#39776=CARTESIAN_POINT('Ctrl Pts',(4.74753496206505,-0.0895249575417115,
3.44977887729433));
#39777=CARTESIAN_POINT('Ctrl Pts',(4.77139288009647,0.185055765100279,3.47415556892044));
#39778=CARTESIAN_POINT('Ctrl Pts',(4.79525079812788,0.414385312357242,3.62711554766008));
#39779=CARTESIAN_POINT('Ctrl Pts',(4.81910871615931,0.542386363113676,3.87125593216545));
#39780=CARTESIAN_POINT('Ctrl Pts',(4.84296663419071,0.537759173780872,4.14687774817434));
#39781=CARTESIAN_POINT('Ctrl Pts',(4.86682455222215,0.401635218192884,4.38658395388507));
#39782=CARTESIAN_POINT('Ctrl Pts',(4.89068247025356,0.167300511433038,4.53175985253543));
#39783=CARTESIAN_POINT('Ctrl Pts',(4.91454038828499,-0.107943727546613,
4.54690598239331));
#39784=CARTESIAN_POINT('Ctrl Pts',(4.9383983063164,-0.356792784813018,4.42831870213619));
#39785=CARTESIAN_POINT('Ctrl Pts',(4.96225622434782,-0.518396287352312,
4.20499583203957));
#39786=CARTESIAN_POINT('Ctrl Pts',(4.98611414237924,-0.553237776802617,
3.93154589703492));
#39787=CARTESIAN_POINT('Ctrl Pts',(5.00997206041066,-0.452797559930213,
3.67483485485756));
#39788=CARTESIAN_POINT('Ctrl Pts',(5.03382997844208,-0.241636005696979,
3.49763554798826));
#39789=CARTESIAN_POINT('Ctrl Pts',(5.05768789647349,0.0286121339618079,
3.44327803376872));
#39790=CARTESIAN_POINT('Ctrl Pts',(5.08154581450492,0.291863827488053,3.52505420509465));
#39791=CARTESIAN_POINT('Ctrl Pts',(5.10540373253633,0.48374686498243,3.72296756053861));
#39792=CARTESIAN_POINT('Ctrl Pts',(5.12926165056775,0.557340616988569,3.98862289364304));
#39793=CARTESIAN_POINT('Ctrl Pts',(5.15311956859917,0.49464940648741,4.25706023915787));
#39794=CARTESIAN_POINT('Ctrl Pts',(5.17697748663059,0.311002942120779,4.46263935401832));
#39795=CARTESIAN_POINT('Ctrl Pts',(5.20083540466201,0.0513077868555636,
4.55509054477827));
#39796=CARTESIAN_POINT('Ctrl Pts',(5.22469332269342,-0.22093351989189,4.5118069769771));
#39797=CARTESIAN_POINT('Ctrl Pts',(5.24855124072485,-0.439150562917527,
4.34337266196288));
#39798=CARTESIAN_POINT('Ctrl Pts',(5.27240915875626,-0.549983331088669,
4.09097437781523));
#39799=CARTESIAN_POINT('Ctrl Pts',(5.29626707678769,-0.526330193563486,
3.81633038019944));
#39800=CARTESIAN_POINT('Ctrl Pts',(5.32012499481911,-0.373974986765411,
3.5865986076849));
#39801=CARTESIAN_POINT('Ctrl Pts',(5.34398291285052,-0.130172708829089,
3.45795473641922));
#39802=CARTESIAN_POINT('Ctrl Pts',(5.36784083088195,0.145460342249349,3.46185569711558));
#39803=CARTESIAN_POINT('Ctrl Pts',(5.39169874891335,0.385524377387638,3.59734759862366));
#39804=CARTESIAN_POINT('Ctrl Pts',(5.41555666694479,0.531317200781484,3.83129898029949));
#39805=CARTESIAN_POINT('Ctrl Pts',(5.4394145849762,0.547188495794237,4.10650235661553));
#39806=CARTESIAN_POINT('Ctrl Pts',(5.46327250300762,0.42925729847004,4.35566300567327));
#39807=CARTESIAN_POINT('Ctrl Pts',(5.48713042103904,0.206360998935678,4.51785436177788));
#39808=CARTESIAN_POINT('Ctrl Pts',(5.51098833907045,-0.0669961859988386,
4.55341622035867));
#39809=CARTESIAN_POINT('Ctrl Pts',(5.53484625710188,-0.323970978517869,
4.45365273830571));
#39810=CARTESIAN_POINT('Ctrl Pts',(5.55870417513329,-0.501726041995696,
4.2429588044862));
#39811=CARTESIAN_POINT('Ctrl Pts',(5.58256209316472,-0.556795421465071,
3.97285482490167));
#39812=CARTESIAN_POINT('Ctrl Pts',(5.60642001119613,-0.475713153578786,
3.70938858005442));
#39813=CARTESIAN_POINT('Ctrl Pts',(5.63027792922756,-0.27830606148521,3.51698474346866));
#39814=CARTESIAN_POINT('Ctrl Pts',(5.65413584725897,-0.0128455564368745,
3.44269129419766));
#39815=CARTESIAN_POINT('Ctrl Pts',(5.67799376529039,0.255756037034639,3.5046750042392));
#39816=CARTESIAN_POINT('Ctrl Pts',(5.70185168332181,0.46181831285622,3.68777916820271));
#39817=CARTESIAN_POINT('Ctrl Pts',(5.72570960135323,0.554953431393631,3.94722983012095));
#39818=CARTESIAN_POINT('Ctrl Pts',(5.74956751938465,0.512387319539865,4.21958423627784));
#39819=CARTESIAN_POINT('Ctrl Pts',(5.77342543741606,0.344528550506956,4.43824431479549));
#39820=CARTESIAN_POINT('Ctrl Pts',(5.79728335544749,0.0924231668635294,
4.54974172178225));
#39821=CARTESIAN_POINT('Ctrl Pts',(5.82114127347891,-0.182282200065281,
4.52681230129395));
#39822=CARTESIAN_POINT('Ctrl Pts',(5.84499919151032,-0.412414601109181,
4.37506292652603));
#39823=CARTESIAN_POINT('Ctrl Pts',(5.86885710954175,-0.541700403334708,
4.13160044316952));
#39824=CARTESIAN_POINT('Ctrl Pts',(5.89271502757316,-0.538525691690445,
3.85595807909033));
#39825=CARTESIAN_POINT('Ctrl Pts',(5.91657294560459,-0.403666797469215,
3.61553786496538));
#39826=CARTESIAN_POINT('Ctrl Pts',(5.94043086363599,-0.170100341263849,
3.46912915944898));
#39827=CARTESIAN_POINT('Ctrl Pts',(5.96428878166742,0.105060216979666,3.45253275189516));
#39828=CARTESIAN_POINT('Ctrl Pts',(5.98814669969884,0.354530812822036,3.5698071562788));
#39829=CARTESIAN_POINT('Ctrl Pts',(6.01200461773026,0.517308736525128,3.79227513259484));
#39830=CARTESIAN_POINT('Ctrl Pts',(6.03586253576167,0.553591019453439,4.06553805729756));
#39831=CARTESIAN_POINT('Ctrl Pts',(6.0597204537931,0.454504394384077,4.32277408438697));
#39832=CARTESIAN_POINT('Ctrl Pts',(6.08357837182452,0.244280620740535,4.50108505220882));
#39833=CARTESIAN_POINT('Ctrl Pts',(6.10743628985593,-0.0256793573627324,
4.55686330558177));
#39834=CARTESIAN_POINT('Ctrl Pts',(6.13129420788736,-0.289354484390735,
4.47648043042773));
#39835=CARTESIAN_POINT('Ctrl Pts',(6.15515212591877,-0.482285035214929,
4.27957167009689));
#39836=CARTESIAN_POINT('Ctrl Pts',(6.17901004395019,-0.557263974895364,
4.01432540012922));
#39837=CARTESIAN_POINT('Ctrl Pts',(6.20286796198161,-0.496014047041978,
3.74552825888183));
#39838=CARTESIAN_POINT('Ctrl Pts',(6.22672588001303,-0.313404643062,3.53904687299508));
#39839=CARTESIAN_POINT('Ctrl Pts',(6.25058379804445,-0.0542924323345977,
3.44511024149985));
#39840=CARTESIAN_POINT('Ctrl Pts',(6.27444171607587,0.218347115212216,3.48718178027374));
#39841=CARTESIAN_POINT('Ctrl Pts',(6.29829963410728,0.437120926894882,3.65404298137615));
#39842=CARTESIAN_POINT('Ctrl Pts',(6.32215755213871,0.549895923261456,3.90664388593688));
#39843=CARTESIAN_POINT('Ctrl Pts',(6.34601547017011,0.526573903738089,4.17995327069166));
#39844=CARTESIAN_POINT('Ctrl Pts',(6.37782602754536,0.327418726170013,4.4906154426808));
#39845=CARTESIAN_POINT('Ctrl Pts',(6.41758922426438,-0.161063729547888,
4.61146011675295));
#39846=CARTESIAN_POINT('Ctrl Pts',(6.46530506032721,-0.60205854017139,4.19446204504257));
#39847=CARTESIAN_POINT('Ctrl Pts',(6.51302089639007,-0.488859252747234,
3.59916283817905));
#39848=CARTESIAN_POINT('Ctrl Pts',(6.56073673245289,0.0725864685289804,
3.37181094029106));
#39849=CARTESIAN_POINT('Ctrl Pts',(6.60845256851574,0.567733426150434,3.72141305678318));
#39850=CARTESIAN_POINT('Ctrl Pts',(6.65616840457857,0.541332409494817,4.32680434473755));
#39851=CARTESIAN_POINT('Ctrl Pts',(6.70388424064141,0.0179179137367747,
4.6321081579338));
#39852=CARTESIAN_POINT('Ctrl Pts',(6.75160007670425,-0.522004047715759,
4.35692568061372));
#39853=CARTESIAN_POINT('Ctrl Pts',(6.79931591276708,-0.582533501572452,
3.75397902491298));
#39854=CARTESIAN_POINT('Ctrl Pts',(6.84703174882993,-0.10812839031349,3.37695395054049));
#39855=CARTESIAN_POINT('Ctrl Pts',(6.89474758489276,0.465580583415614,3.57208337966475));
#39856=CARTESIAN_POINT('Ctrl Pts',(6.9424634209556,0.611735560770294,4.16017430964564));
#39857=CARTESIAN_POINT('Ctrl Pts',(6.99017925701844,0.196126575106773,4.60117519156627));
#39858=CARTESIAN_POINT('Ctrl Pts',(7.03789509308127,-0.399589635450545,
4.49010738789885));
#39859=CARTESIAN_POINT('Ctrl Pts',(7.08561092914412,-0.628355913977057,
3.92896656470948));
#39860=CARTESIAN_POINT('Ctrl Pts',(7.13332676520695,-0.280093617253323,
3.43305676608093));
#39861=CARTESIAN_POINT('Ctrl Pts',(7.1810426012698,0.325383132256395,3.45777970086456));
#39862=CARTESIAN_POINT('Ctrl Pts',(7.22875843733263,0.632055452459012,3.98043185926557));
#39863=CARTESIAN_POINT('Ctrl Pts',(7.27647427339546,0.358301574124045,4.52105375310108));
#39864=CARTESIAN_POINT('Ctrl Pts',(7.32419010945831,-0.244486178793781,
4.58318396235269));
#39865=CARTESIAN_POINT('Ctrl Pts',(7.37190594552114,-0.622758498112341,
4.10976736853928));
#39866=CARTESIAN_POINT('Ctrl Pts',(7.41962178158399,-0.42914211350377,3.53554970961824));
#39867=CARTESIAN_POINT('Ctrl Pts',(7.46733761764681,0.158562080980748,3.38784389968312));
#39868=CARTESIAN_POINT('Ctrl Pts',(7.51505345370967,0.600656274672958,3.80229045545538));
#39869=CARTESIAN_POINT('Ctrl Pts',(7.56276928977248,0.491158570126743,4.3982967283715));
#39870=CARTESIAN_POINT('Ctrl Pts',(7.61048512583535,-0.0693776073840611,
4.62854098691609));
#39871=CARTESIAN_POINT('Ctrl Pts',(7.65820096189817,-0.566203260219877,
4.28158638589565));
#39872=CARTESIAN_POINT('Ctrl Pts',(7.70591679796101,-0.543075747198986,
3.67604667390869));
#39873=CARTESIAN_POINT('Ctrl Pts',(7.75363263402386,-0.0212334191459514,
3.36799828595259));
#39874=CARTESIAN_POINT('Ctrl Pts',(7.80134847008666,0.520107884382028,3.64032679659274));
#39875=CARTESIAN_POINT('Ctrl Pts',(7.84906430614954,0.583826114817312,4.24294874421058));
#39876=CARTESIAN_POINT('Ctrl Pts',(7.89678014221235,0.111407840683781,4.62246712177016));
#39877=CARTESIAN_POINT('Ctrl Pts',(7.94449597827521,-0.463317967772962,
4.43036436352186));
#39878=CARTESIAN_POINT('Ctrl Pts',(7.99221181433803,-0.612571757364041,
3.84305138824375));
#39879=CARTESIAN_POINT('Ctrl Pts',(8.03992765040088,-0.199291476537812,
3.39986673810663));
#39880=CARTESIAN_POINT('Ctrl Pts',(8.08764348646372,0.397001233685627,3.50779369660314));
#39881=CARTESIAN_POINT('Ctrl Pts',(8.13535932252656,0.628721602366905,4.06772127707659));
#39882=CARTESIAN_POINT('Ctrl Pts',(8.18307515858938,0.283077249469033,4.56545936678474));
#39883=CARTESIAN_POINT('Ctrl Pts',(8.23079099465223,-0.32252129731946,4.54392741926377));
#39884=CARTESIAN_POINT('Ctrl Pts',(8.27850683071506,-0.631943574151527,
4.02289855323374));
#39885=CARTESIAN_POINT('Ctrl Pts',(8.32622266677791,-0.361042343138453,
3.48084159342964));
#39886=CARTESIAN_POINT('Ctrl Pts',(8.37393850284074,0.241409626929164,3.41553578665797));
#39887=CARTESIAN_POINT('Ctrl Pts',(8.42165433890358,0.622171422023167,3.88695246013618));
#39888=CARTESIAN_POINT('Ctrl Pts',(8.46937017496642,0.431583626935426,4.46218242893131));
#39889=CARTESIAN_POINT('Ctrl Pts',(8.51708601102927,-0.155334053534803,
4.61298316164806));
#39890=CARTESIAN_POINT('Ctrl Pts',(8.56480184709209,-0.599606082522386,
4.20087202506506));
#39891=CARTESIAN_POINT('Ctrl Pts',(8.61251768315494,-0.493250619804184,
3.60429701705146));
#39892=CARTESIAN_POINT('Ctrl Pts',(8.66023351921777,0.0660644767165412,
3.37110214695249));
#39893=CARTESIAN_POINT('Ctrl Pts',(8.70794935528061,0.564711547735832,3.71543385214437));
#39894=CARTESIAN_POINT('Ctrl Pts',(8.75566519134344,0.544775315265253,4.32108702952508));
#39895=CARTESIAN_POINT('Ctrl Pts',(8.80338102740629,0.0245635283409047,
4.6318810471339));
#39896=CARTESIAN_POINT('Ctrl Pts',(8.85109686346912,-0.518205324617361,
4.36240897642002));
#39897=CARTESIAN_POINT('Ctrl Pts',(8.89881269953197,-0.585098254365674,
3.76013116628075));
#39898=CARTESIAN_POINT('Ctrl Pts',(8.9465285355948,-0.114686454236133,3.3781285970023));
#39899=CARTESIAN_POINT('Ctrl Pts',(8.99424437165764,0.461043681496376,3.56720010581811));
#39900=CARTESIAN_POINT('Ctrl Pts',(9.04196020772047,0.613390310441866,4.15371841694351));
#39901=CARTESIAN_POINT('Ctrl Pts',(9.08967604378332,0.202451179085494,4.59907474052783));
#39902=CARTESIAN_POINT('Ctrl Pts',(9.13739187984615,-0.394401985136886,
4.49429151193569));
#39903=CARTESIAN_POINT('Ctrl Pts',(9.18510771590899,-0.629069737753471,
3.93559278228048));
#39904=CARTESIAN_POINT('Ctrl Pts',(9.23282355197184,-0.28605307070895,3.43604019168954));
#39905=CARTESIAN_POINT('Ctrl Pts',(9.28053938803466,0.319650532659854,3.45438057070715));
#39906=CARTESIAN_POINT('Ctrl Pts',(9.32825522409751,0.631814133431458,3.97377166707843));
#39907=CARTESIAN_POINT('Ctrl Pts',(9.37597106016033,0.363773093762905,4.51724864514637));
#39908=CARTESIAN_POINT('Ctrl Pts',(9.4236868962232,-0.238326375276645,4.58572823348297));
#39909=CARTESIAN_POINT('Ctrl Pts',(9.47140273228601,-0.621567066777005,
4.11632457242483));
#39910=CARTESIAN_POINT('Ctrl Pts',(9.51911856834886,-0.434013156817378,
3.54009826662536));
#39911=CARTESIAN_POINT('Ctrl Pts',(9.5668344044117,0.152101713198456,3.38620679908157));
#39912=CARTESIAN_POINT('Ctrl Pts',(9.61455024047453,0.598539239598464,3.79597107236355));
#39913=CARTESIAN_POINT('Ctrl Pts',(9.66226607653739,0.495328972565208,4.39309824928265));
#39914=CARTESIAN_POINT('Ctrl Pts',(9.7099819126002,-0.0627495115905886,
4.62923725529147));
#39915=CARTESIAN_POINT('Ctrl Pts',(9.75769774866305,-0.563204153727404,
4.28753800770644));
#39916=CARTESIAN_POINT('Ctrl Pts',(9.80541358472588,-0.54645975548653,3.68178818330365));
#39917=CARTESIAN_POINT('Ctrl Pts',(9.85312942078873,-0.027892955418244,
3.36825716649128));
#39918=CARTESIAN_POINT('Ctrl Pts',(9.90084525685157,0.516288374798902,3.63486531430293));
#39919=CARTESIAN_POINT('Ctrl Pts',(9.9485610929144,0.58635414632045,4.2367822623095));
#39920=CARTESIAN_POINT('Ctrl Pts',(9.99627692897723,0.117961883057689,4.62125841547385));
#39921=CARTESIAN_POINT('Ctrl Pts',(10.0439927650401,-0.458756592493822,
4.4352234064191));
#39922=CARTESIAN_POINT('Ctrl Pts',(10.0917086011029,-0.614191830280748,
3.8495160464768));
#39923=CARTESIAN_POINT('Ctrl Pts',(10.1394244371658,-0.205605259764808,
3.40200041654811));
#39924=CARTESIAN_POINT('Ctrl Pts',(10.1871402732286,0.391791784436726,3.5036370055096));
#39925=CARTESIAN_POINT('Ctrl Pts',(10.2348561092915,0.629400404498524,4.06109136983801));
#39926=CARTESIAN_POINT('Ctrl Pts',(10.2825719453542,0.289020948539269,4.56244458923262));
#39927=CARTESIAN_POINT('Ctrl Pts',(10.3302877814171,-0.316770891622519,
4.54729628801251));
#39928=CARTESIAN_POINT('Ctrl Pts',(10.3780036174799,-0.631667147860668,
4.02955738427466));
#39929=CARTESIAN_POINT('Ctrl Pts',(10.4257194535428,-0.366493742769977,
3.48467547975859));
#39930=CARTESIAN_POINT('Ctrl Pts',(10.4734352896056,0.235236505537468,3.41302401146715));
#39931=CARTESIAN_POINT('Ctrl Pts',(10.5211511256685,0.620945451230968,3.88040162523195));
#39932=CARTESIAN_POINT('Ctrl Pts',(10.5688669617313,0.436430634585191,4.45760826680378));
#39933=CARTESIAN_POINT('Ctrl Pts',(10.6165827977941,-0.148865149148659,
4.61458619576145));
#39934=CARTESIAN_POINT('Ctrl Pts',(10.664298633857,-0.597455775834545,4.20718016452724));
#39935=CARTESIAN_POINT('Ctrl Pts',(10.7120144699198,-0.497393570532806,
3.60951740033105));
#39936=CARTESIAN_POINT('Ctrl Pts',(10.7597303059826,0.059432803973042,3.37044081575797));
#39937=CARTESIAN_POINT('Ctrl Pts',(10.8074461420455,0.56168112009921,3.70949811708754));
#39938=CARTESIAN_POINT('Ctrl Pts',(10.8551619781083,0.548129021063343,4.31532776744164));
#39939=CARTESIAN_POINT('Ctrl Pts',(10.9028778141712,0.0312216079359222,
4.63158707701274));
#39940=CARTESIAN_POINT('Ctrl Pts',(10.950593650234,-0.514357088165242,4.36785025554668));
#39941=CARTESIAN_POINT('Ctrl Pts',(10.9983094862968,-0.587593755803164,
3.7663108843084));
#39942=CARTESIAN_POINT('Ctrl Pts',(11.0460253223597,-0.12123403619496,3.37937182377895));
#39943=CARTESIAN_POINT('Ctrl Pts',(11.0937411584225,0.456456764276497,3.56236516706526));
#39944=CARTESIAN_POINT('Ctrl Pts',(11.1414569944854,0.61497629462275,4.14724531131301));
#39945=CARTESIAN_POINT('Ctrl Pts',(11.1891728305482,0.208753630990335,4.59690782052167));
#39946=CARTESIAN_POINT('Ctrl Pts',(11.236888666611,-0.389170704067994,4.49842069353791));
#39947=CARTESIAN_POINT('Ctrl Pts',(11.2846045026739,-0.629713593419695,
3.94222617449013));
#39948=CARTESIAN_POINT('Ctrl Pts',(11.3323203387367,-0.291980800545002,
3.43908624837263));
#39949=CARTESIAN_POINT('Ctrl Pts',(11.3800361747996,0.313882454172263,3.45104205114199));
#39950=CARTESIAN_POINT('Ctrl Pts',(11.4277520108624,0.631502621520784,3.96711438515144));
#39951=CARTESIAN_POINT('Ctrl Pts',(11.4754678469252,0.369204214609944,4.51338608528654));
#39952=CARTESIAN_POINT('Ctrl Pts',(11.5231836829881,-0.232140103514266,
4.58820744384271));
#39953=CARTESIAN_POINT('Ctrl Pts',(11.5708995190509,-0.620306592646703,
4.12286885598323));
#39954=CARTESIAN_POINT('Ctrl Pts',(11.6186153551137,-0.438835993107895,
3.54469790709399));
#39955=CARTESIAN_POINT('Ctrl Pts',(11.6663311911766,0.145624451261577,3.38463787584353));
#39956=CARTESIAN_POINT('Ctrl Pts',(11.7140470272394,0.596355721317347,3.78967435176932));
#39957=CARTESIAN_POINT('Ctrl Pts',(11.7617628633022,0.499444356375145,4.38785610674141));
#39958=CARTESIAN_POINT('Ctrl Pts',(11.8094786993651,-0.0561144459655822,
4.62986363095956));
#39959=CARTESIAN_POINT('Ctrl Pts',(11.8571945354279,-0.560142489144378,
4.29345769116983));
#39960=CARTESIAN_POINT('Ctrl Pts',(11.9049103714908,-0.549783065641843,
3.68756503815187));
#39961=CARTESIAN_POINT('Ctrl Pts',(11.9526262075536,-0.0345493934605723,
3.36858621802886));
#39962=CARTESIAN_POINT('Ctrl Pts',(12.0003420436164,0.512411518346294,3.62944438943981));
#39963=CARTESIAN_POINT('Ctrl Pts',(12.0480578796793,0.588817048391095,4.23058947975914));
#39964=CARTESIAN_POINT('Ctrl Pts',(12.0957737157421,0.1245028227835,4.61998070274044));
#39965=CARTESIAN_POINT('Ctrl Pts',(12.1434895518049,-0.454144260708352,
4.44003410676589));
#39966=CARTESIAN_POINT('Ctrl Pts',(12.1912053878678,-0.615743681684068,
3.85599741975318));
#39967=CARTESIAN_POINT('Ctrl Pts',(12.2389212239306,-0.211896205334937,
3.40420051794564));
#39968=CARTESIAN_POINT('Ctrl Pts',(12.2866370599935,0.386538816815474,3.49953544806202));
#39969=CARTESIAN_POINT('Ctrl Pts',(12.3343528960563,0.63000929582004,4.05445467686));
#39970=CARTESIAN_POINT('Ctrl Pts',(12.3820687321191,0.294932544534008,4.55936733800455));
#39971=CARTESIAN_POINT('Ctrl Pts',(12.429784568182,-0.310985300518122,4.55060436568669));
#39972=CARTESIAN_POINT('Ctrl Pts',(12.4775004042448,-0.631320558980542,
4.0362129322216));
#39973=CARTESIAN_POINT('Ctrl Pts',(12.5252162403077,-0.371904434015698,
3.48856660588983));
#39974=CARTESIAN_POINT('Ctrl Pts',(12.5729320763705,0.229037255191033,3.41057743478371));
#39975=CARTESIAN_POINT('Ctrl Pts',(12.6206479124333,0.619650508764677,3.87386407474765));
#39976=CARTESIAN_POINT('Ctrl Pts',(12.6683637484962,0.44122916559109,4.4529832757215));
#39977=CARTESIAN_POINT('Ctrl Pts',(12.716079584559,-0.142379709528176,4.61612096455669));
#39978=CARTESIAN_POINT('Ctrl Pts',(12.7637954206218,-0.595239106594286,
4.21346529139986));
#39979=CARTESIAN_POINT('Ctrl Pts',(12.8115112566847,-0.501481273143938,
3.61478115656484));
#39980=CARTESIAN_POINT('Ctrl Pts',(12.8592270927475,0.0527945297157079,
3.36984941301012));
#39981=CARTESIAN_POINT('Ctrl Pts',(12.9069429288104,0.558588303589165,3.70359464960132));
#39982=CARTESIAN_POINT('Ctrl Pts',(12.9546587648732,0.551421843290858,4.30953348024615));
#39983=CARTESIAN_POINT('Ctrl Pts',(13.002374600936,0.0378762195828894,4.63122295319618));
#39984=CARTESIAN_POINT('Ctrl Pts',(13.0500904369989,-0.510451719368595,
4.37325067561256));
#39985=CARTESIAN_POINT('Ctrl Pts',(13.0978062730617,-0.590023990114621,
3.77251655941407));
#39986=CARTESIAN_POINT('Ctrl Pts',(13.1455221091246,-0.127768152052348,
3.38068398698829));
#39987=CARTESIAN_POINT('Ctrl Pts',(13.1932379451874,0.451819146005312,3.55757883871291));
#39988=CARTESIAN_POINT('Ctrl Pts',(13.2409537812502,0.616493970155128,4.14075585037205));
#39989=CARTESIAN_POINT('Ctrl Pts',(13.2886696173131,0.215032895532453,4.59467459882739));
#39990=CARTESIAN_POINT('Ctrl Pts',(13.3363854533759,-0.383896195764066,
4.50249451293469));
#39991=CARTESIAN_POINT('Ctrl Pts',(13.3841012894387,-0.630287503488198,
3.94886598394213));
#39992=CARTESIAN_POINT('Ctrl Pts',(13.4318171255016,-0.297876098539286,
3.4421946086935));
#39993=CARTESIAN_POINT('Ctrl Pts',(13.4795329615644,0.308079511111167,3.44776450722078));
#39994=CARTESIAN_POINT('Ctrl Pts',(13.5272487976272,0.631120965295637,3.96046075600252));
#39995=CARTESIAN_POINT('Ctrl Pts',(13.5749646336901,0.374594326004835,4.50946650093658));
#39996=CARTESIAN_POINT('Ctrl Pts',(13.6226804697529,-0.225928046730791,
4.59062131891086));
#39997=CARTESIAN_POINT('Ctrl Pts',(13.6703963058158,-0.618977217803688,
4.12939949185215));
#39998=CARTESIAN_POINT('Ctrl Pts',(13.7181121418786,-0.443610085578744,
3.54934812035851));
#39999=CARTESIAN_POINT('Ctrl Pts',(13.7658279779415,0.139131014051702,3.38313730411011));
#40000=CARTESIAN_POINT('Ctrl Pts',(13.8135438140043,0.594105962672646,3.78340099315002));
#40001=CARTESIAN_POINT('Ctrl Pts',(13.8612596500671,0.503504264276035,4.38257088298437));
#40002=CARTESIAN_POINT('Ctrl Pts',(13.90897548613,-0.0494731474142026,4.63042004436449));
#40003=CARTESIAN_POINT('Ctrl Pts',(13.9566913221928,-0.557018606591754,
4.29934477874546));
#40004=CARTESIAN_POINT('Ctrl Pts',(14.0044071582556,-0.553045308503159,
3.69337659679301));
#40005=CARTESIAN_POINT('Ctrl Pts',(14.0521229943185,-0.0412019939202257,
3.36898540401303));
#40006=CARTESIAN_POINT('Ctrl Pts',(14.0998388303813,0.50847774565382,3.62406462413548));
#40007=CARTESIAN_POINT('Ctrl Pts',(14.1475546664442,0.591214547458171,4.22437108442359));
#40008=CARTESIAN_POINT('Ctrl Pts',(14.195270502507,0.131029933326566,4.61863412549262));
#40009=CARTESIAN_POINT('Ctrl Pts',(14.2429863385698,-0.4494814847335,4.44479593021223));
#40010=CARTESIAN_POINT('Ctrl Pts',(14.2907021746327,-0.617227139201166,
3.86249478815283));
#40011=CARTESIAN_POINT('Ctrl Pts',(14.3384180106955,-0.218163614480107,
3.40646679792233));
#40012=CARTESIAN_POINT('Ctrl Pts',(14.3861338467583,0.381242914296727,3.49548947984197));
#40013=CARTESIAN_POINT('Ctrl Pts',(14.4338496828212,0.630548208698617,4.0478119353149));
#40014=CARTESIAN_POINT('Ctrl Pts',(14.481565518884,0.300811380821271,4.55622795490698));
#40015=CARTESIAN_POINT('Ctrl Pts',(14.5292813549469,-0.305165166642291,
4.55385128484077));
#40016=CARTESIAN_POINT('Ctrl Pts',(14.5769971910097,-0.630903846008588,
4.04286445780787));
#40017=CARTESIAN_POINT('Ctrl Pts',(14.6247130270726,-0.37727381588172,3.49251453961553));
#40018=CARTESIAN_POINT('Ctrl Pts',(14.6724288631354,0.222812564473163,3.40819632836178));
#40019=CARTESIAN_POINT('Ctrl Pts',(14.7201446991982,0.618286738460357,3.86734053484336));
#40020=CARTESIAN_POINT('Ctrl Pts',(14.7678605352611,0.44597868695508,4.44830796940654));
#40021=CARTESIAN_POINT('Ctrl Pts',(14.8155763713239,-0.135878455045208,
4.6175872975589));
#40022=CARTESIAN_POINT('Ctrl Pts',(14.8632922073867,-0.592956321018707,
4.2197267075609));
#40023=CARTESIAN_POINT('Ctrl Pts',(14.9110080434496,-0.505513273594975,
3.62008770107973));
#40024=CARTESIAN_POINT('Ctrl Pts',(14.9587238795124,0.0461503912925444,
3.36932800439917));
#40025=CARTESIAN_POINT('Ctrl Pts',(15.0064397155752,0.555433441741075,3.69772410541485));
#40026=CARTESIAN_POINT('Ctrl Pts',(15.0541555516381,0.554653416196733,4.30370481154056));
#40027=CARTESIAN_POINT('Ctrl Pts',(15.1018713877009,0.0445266241191229,
4.63078871612938));
#40028=CARTESIAN_POINT('Ctrl Pts',(15.1495872237638,-0.506489652017253,
4.37860963676461));
#40029=CARTESIAN_POINT('Ctrl Pts',(15.1973030598266,-0.592388687361149,
3.77874750230084));
#40030=CARTESIAN_POINT('Ctrl Pts',(15.2450188958894,-0.134288076029725,
3.38206494088146));
#40031=CARTESIAN_POINT('Ctrl Pts',(15.2927347319523,0.447131341807447,3.5528416524037));
#40032=CARTESIAN_POINT('Ctrl Pts',(15.3404505680151,0.617943168462805,4.13425075493917));
#40033=CARTESIAN_POINT('Ctrl Pts',(15.3881664040779,0.221288275240951,4.59237532350063));
#40034=CARTESIAN_POINT('Ctrl Pts',(15.4358822401408,-0.378579046092452,
4.50651251762549));
#40035=CARTESIAN_POINT('Ctrl Pts',(15.4835980762036,-0.630791404211772,
3.95551147311801));
#40036=CARTESIAN_POINT('Ctrl Pts',(15.5313139122665,-0.303738309870084,
3.44536492739022));
#40037=CARTESIAN_POINT('Ctrl Pts',(15.5790297483293,0.302242348039936,3.44454830299756));
#40038=CARTESIAN_POINT('Ctrl Pts',(15.6267455843921,0.630669207148581,3.95381151868517));
#40039=CARTESIAN_POINT('Ctrl Pts',(15.674461420455,0.379942829239589,4.50549032746533));
#40040=CARTESIAN_POINT('Ctrl Pts',(15.7221772565178,-0.219690894932002,
4.59296959056563));
#40041=CARTESIAN_POINT('Ctrl Pts',(15.7698930925806,-0.617579089908608,
4.13591575463957));
#40042=CARTESIAN_POINT('Ctrl Pts',(15.8176089286435,-0.448334903946386,
3.5540483898953));
#40043=CARTESIAN_POINT('Ctrl Pts',(15.8653247647063,0.13262212282903,3.3817052505577));
#40044=CARTESIAN_POINT('Ctrl Pts',(15.9130406007692,0.591790213556878,3.77715169332057));
#40045=CARTESIAN_POINT('Ctrl Pts',(15.960756436832,0.507508245312566,4.37724316506909));
#40046=CARTESIAN_POINT('Ctrl Pts',(16.0084722728949,-0.0428263536203826,
4.63090643370248));
#40047=CARTESIAN_POINT('Ctrl Pts',(16.0561881089577,-0.553832853055588,
4.30519861652357));
#40048=CARTESIAN_POINT('Ctrl Pts',(16.1039039450205,-0.556246121716014,
3.69922221370673));
#40049=CARTESIAN_POINT('Ctrl Pts',(16.1516197810833,-0.0478500178579074,
3.36945468010413));
#40050=CARTESIAN_POINT('Ctrl Pts',(16.1993356171462,0.504487493666278,3.61872661594874));
#40051=CARTESIAN_POINT('Ctrl Pts',(16.247051453209,0.593546377218863,4.21812776701271));
#40052=CARTESIAN_POINT('Ctrl Pts',(16.2947672892719,0.137542489686435,4.61721883330181));
#40053=CARTESIAN_POINT('Ctrl Pts',(16.3424831253347,-0.444768782488292,
4.44950834783736));
#40054=CARTESIAN_POINT('Ctrl Pts',(16.3901989613976,-0.618642038056621,
3.86900742997889));
#40055=CARTESIAN_POINT('Ctrl Pts',(16.4379147974604,-0.224406791046256,
3.40879900475058));
#40056=CARTESIAN_POINT('Ctrl Pts',(16.4856306335233,0.375904665124208,3.49149955025639));
#40057=CARTESIAN_POINT('Ctrl Pts',(16.533346469586,0.631017083274371,4.04116388304691));
#40058=CARTESIAN_POINT('Ctrl Pts',(16.5810623056489,0.306656804407812,4.55302678864769));
#40059=CARTESIAN_POINT('Ctrl Pts',(16.6287781417117,-0.29931113646787,4.55703668482238));
#40060=CARTESIAN_POINT('Ctrl Pts',(16.6764939777746,-0.630417055231307,
4.04951122221356));
#40061=CARTESIAN_POINT('Ctrl Pts',(16.7242098138374,-0.382601291962586,
3.49651884241796));
#40062=CARTESIAN_POINT('Ctrl Pts',(16.7719256499003,0.216563124792967,3.40588095668335));
#40063=CARTESIAN_POINT('Ctrl Pts',(16.8196414859631,0.616854291799135,3.86083173012294));
#40064=CARTESIAN_POINT('Ctrl Pts',(16.8673573220259,0.450678671122871,4.44358286716973));
#40065=CARTESIAN_POINT('Ctrl Pts',(16.9150731580887,-0.129362107828251,
4.61898503189482));
#40066=CARTESIAN_POINT('Ctrl Pts',(16.9627889941516,-0.590607672668797,
4.22596371752193));
#40067=CARTESIAN_POINT('Ctrl Pts',(17.0105048302144,-0.509489124030439,
3.62543644444997));
#40068=CARTESIAN_POINT('Ctrl Pts',(17.0582206662773,0.0395011267029154,
3.3688766478407));
#40069=CARTESIAN_POINT('Ctrl Pts',(17.1059365023401,0.552216884982031,3.69188713660034));
#40070=CARTESIAN_POINT('Ctrl Pts',(17.153652338403,0.557823380833178,4.29784240874569));
#40071=CARTESIAN_POINT('Ctrl Pts',(17.2013681744658,0.0511720828492506,
4.63028441404532));
#40072=CARTESIAN_POINT('Ctrl Pts',(17.2490840105287,-0.502471326198846,
4.38392654375487));
#40073=CARTESIAN_POINT('Ctrl Pts',(17.2967998465914,-0.594687584883411,
3.78500302086511));
#40074=CARTESIAN_POINT('Ctrl Pts',(17.3445156826543,-0.140793083924855,
3.38351453206865));
#40075=CARTESIAN_POINT('Ctrl Pts',(17.3922315187171,0.442393872381948,3.5481541343218));
#40076=CARTESIAN_POINT('Ctrl Pts',(17.43994735478,0.61932372857571,4.1277307475695));
#40077=CARTESIAN_POINT('Ctrl Pts',(17.4876631908428,0.227519075297936,4.590010249934));
#40078=CARTESIAN_POINT('Ctrl Pts',(17.5353790269057,-0.373219845656906,
4.51047426130944));
#40079=CARTESIAN_POINT('Ctrl Pts',(17.5830948629685,-0.631225239619516,
3.96216190386831));
#40080=CARTESIAN_POINT('Ctrl Pts',(17.6308106990313,-0.309566783390781,
3.44859685231885));
#40081=CARTESIAN_POINT('Ctrl Pts',(17.6785265350942,0.29637161332294,3.44139379571298));
#40082=CARTESIAN_POINT('Ctrl Pts',(17.726242371157,0.630147397258769,3.94716741176515));
#40083=CARTESIAN_POINT('Ctrl Pts',(17.7739582072198,0.385249130227842,4.50145800652724));
#40084=CARTESIAN_POINT('Ctrl Pts',(17.8216740432827,-0.213429340911116,
4.59525199797214));
#40085=CARTESIAN_POINT('Ctrl Pts',(17.8693898793456,-0.616112364258878,
4.14241692054995));
#40086=CARTESIAN_POINT('Ctrl Pts',(17.9171057154084,-0.453009923400427,
3.55879819362073));
#40087=CARTESIAN_POINT('Ctrl Pts',(17.9648215514712,0.126098500570276,3.38034187425201));
#40088=CARTESIAN_POINT('Ctrl Pts',(18.012537387534,0.589408731192455,3.77092714642348));
#40089=CARTESIAN_POINT('Ctrl Pts',(18.0602532235969,0.511455854741549,4.3718735447732));
#40090=CARTESIAN_POINT('Ctrl Pts',(18.1079690596597,-0.0361748028784226,
4.6313227449477));
#40091=CARTESIAN_POINT('Ctrl Pts',(18.1556848957226,-0.55058558239424,4.31101855428765));
#40092=CARTESIAN_POINT('Ctrl Pts',(18.2034007317854,-0.559385149749292,
3.70510123958967));
#40093=CARTESIAN_POINT('Ctrl Pts',(18.2511165678482,-0.0544927268426965,
3.36999399417717));
#40094=CARTESIAN_POINT('Ctrl Pts',(18.2988324039111,0.500441205601937,3.6134309578002));
#40095=CARTESIAN_POINT('Ctrl Pts',(18.3465482399739,0.595812278664582,4.21186022100458));
#40096=CARTESIAN_POINT('Ctrl Pts',(18.3942640760367,0.144039768479226,4.61573498337195));
#40097=CARTESIAN_POINT('Ctrl Pts',(18.4419799120996,-0.440006677437314,
4.4541708362083));
#40098=CARTESIAN_POINT('Ctrl Pts',(18.4896957481624,-0.619988221090196,
3.87553462183804));
#40099=CARTESIAN_POINT('Ctrl Pts',(18.5374115842252,-0.230625041570952,
3.41119687937986));
#40100=CARTESIAN_POINT('Ctrl Pts',(18.5851274202881,0.370524662245315,3.48756610248778));
#40101=CARTESIAN_POINT('Ctrl Pts',(18.6328432563509,0.631415867466904,4.03451125849008));
#40102=CARTESIAN_POINT('Ctrl Pts',(18.6805590924138,0.31246816601179,4.54976419479712));
#40103=CARTESIAN_POINT('Ctrl Pts',(18.7282749284766,-0.293423860232864,
4.56016021181225));
#40104=CARTESIAN_POINT('Ctrl Pts',(18.7759907645394,-0.629860240718928,
4.05615248714788));
#40105=CARTESIAN_POINT('Ctrl Pts',(18.8237066006023,-0.387886270507855,
3.50057906951772));
#40106=CARTESIAN_POINT('Ctrl Pts',(18.8714224366651,0.210289630309142,3.40363157692976));
#40107=CARTESIAN_POINT('Ctrl Pts',(18.919138272728,0.615353327889266,3.85433838355196));
#40108=CARTESIAN_POINT('Ctrl Pts',(18.9668541087908,0.455328596044662,4.43880849385601));
#40109=CARTESIAN_POINT('Ctrl Pts',(19.0145699448537,-0.122831391686292,
4.62031401230505));
#40110=CARTESIAN_POINT('Ctrl Pts',(19.0622857809165,-0.588193422413584,
4.2321756285162));
#40111=CARTESIAN_POINT('Ctrl Pts',(19.1100016169793,-0.513408382846255,
3.63082679254236));
#40112=CARTESIAN_POINT('Ctrl Pts',(19.1577174530421,0.0328474745430158,
3.36849539350727));
#40113=CARTESIAN_POINT('Ctrl Pts',(19.205433289105,0.548938990540088,3.68608439142882));
#40114=CARTESIAN_POINT('Ctrl Pts',(19.2531491251678,0.560931385193363,4.2919469231649));
#40115=CARTESIAN_POINT('Ctrl Pts',(19.3008649612307,0.0578118574426247,
4.62971010270368));
#40116=CARTESIAN_POINT('Ctrl Pts',(19.3485807972935,-0.498397187901359,
4.38920080648958));
#40117=CARTESIAN_POINT('Ctrl Pts',(19.3962966333563,-0.596920427988996,
3.79128241936144));
#40118=CARTESIAN_POINT('Ctrl Pts',(19.4440124694192,-0.147282451949449,
3.38503260125846));
#40119=CARTESIAN_POINT('Ctrl Pts',(19.491728305482,0.437607261597584,3.54351680188243));
#40120=CARTESIAN_POINT('Ctrl Pts',(19.5394441415449,0.620635501579114,4.12119655861503));
#40121=CARTESIAN_POINT('Ctrl Pts',(19.5871599776077,0.233724595248439,4.58757962923414));
#40122=CARTESIAN_POINT('Ctrl Pts',(19.6348758136705,-0.367819173932889,
4.51437932582758));
#40123=CARTESIAN_POINT('Ctrl Pts',(19.6825916497334,-0.631588991354928,
3.96881649615688));
#40124=CARTESIAN_POINT('Ctrl Pts',(19.7303074857962,-0.315360815373557,
3.4518901025469));
#40125=CARTESIAN_POINT('Ctrl Pts',(19.778023321859,0.290467852693633,3.43830118837221));
#40126=CARTESIAN_POINT('Ctrl Pts',(19.8257391579219,0.629555794415491,3.94052945152661));
#40127=CARTESIAN_POINT('Ctrl Pts',(19.8734549939847,0.390512260364629,4.49736946054851));
#40128=CARTESIAN_POINT('Ctrl Pts',(19.9211708300476,-0.207143364153331,
4.59746927979605));
#40129=CARTESIAN_POINT('Ctrl Pts',(19.9688866661104,-0.61457855576007,4.14890039401813));
#40130=CARTESIAN_POINT('Ctrl Pts',(20.0166025021732,-0.45763207183192,3.5636005413983));
#40131=CARTESIAN_POINT('Ctrl Pts',(20.0643183382361,0.119556051622903,3.37904064719698));
#40132=CARTESIAN_POINT('Ctrl Pts',(20.1120341742989,0.586970881772813,3.7647406560623));
#40133=CARTESIAN_POINT('Ctrl Pts',(20.1597500103618,0.515329468049299,4.36643880344312));
#40134=CARTESIAN_POINT('Ctrl Pts',(20.2074658464246,-0.029486781418557,
4.63171390504007));
#40135=CARTESIAN_POINT('Ctrl Pts',(20.2551816824874,-0.547338447674763,
4.31671898245684));
#40136=CARTESIAN_POINT('Ctrl Pts',(20.3028975185503,-0.562346186529673,
3.71117381387971));
#40137=CARTESIAN_POINT('Ctrl Pts',(20.3506133546131,-0.0613491664957494,
3.37029669484294));
#40138=CARTESIAN_POINT('Ctrl Pts',(20.398329190676,0.496762641213801,3.60878154740643));
#40139=CARTESIAN_POINT('Ctrl Pts',(20.4380923873949,0.580417208789547,4.10498761157686));
#40140=CARTESIAN_POINT('Ctrl Pts',(20.4699029447702,0.374745574175769,4.41137453781958));
#40141=CARTESIAN_POINT('Ctrl Pts',(20.4937608628016,0.13332385162888,4.54159545884303));
#40142=CARTESIAN_POINT('Ctrl Pts',(20.517618780833,-0.143293564288956,4.53872805560682));
#40143=CARTESIAN_POINT('Ctrl Pts',(20.5414766988645,-0.38346854803195,4.40448715909776));
#40144=CARTESIAN_POINT('Ctrl Pts',(20.5653346168959,-0.530621786340447,
4.17114564603877));
#40145=CARTESIAN_POINT('Ctrl Pts',(20.5891925349273,-0.547627617499454,
3.89605651468078));
#40146=CARTESIAN_POINT('Ctrl Pts',(20.6130504529587,-0.430933317123153,
3.64633026976583));
#40147=CARTESIAN_POINT('Ctrl Pts',(20.6369083709901,-0.208752997660079,
3.48311457674551));
#40148=CARTESIAN_POINT('Ctrl Pts',(20.6607662890215,0.0644142843662171,
3.4462762657402));
#40149=CARTESIAN_POINT('Ctrl Pts',(20.684624207053,0.321861676845817,3.54484653226013));
#40150=CARTESIAN_POINT('Ctrl Pts',(20.7084821250844,0.500588620804837,3.75470996102831));
#40151=CARTESIAN_POINT('Ctrl Pts',(20.7323400431158,0.556916750317041,4.02455574134091));
#40152=CARTESIAN_POINT('Ctrl Pts',(20.7561979611472,0.47705893600668,4.28839577951569));
#40153=CARTESIAN_POINT('Ctrl Pts',(20.7800558791787,0.280549668164313,4.48171582646486));
#40154=CARTESIAN_POINT('Ctrl Pts',(20.8039137972101,0.0154370662995263,
4.55724289713534));
#40155=CARTESIAN_POINT('Ctrl Pts',(20.8277717152415,-0.253449631274377,
4.49650907789895));
#40156=CARTESIAN_POINT('Ctrl Pts',(20.8516296332729,-0.460361354274216,
4.31436517051053));
#40157=CARTESIAN_POINT('Ctrl Pts',(20.8754875513043,-0.554701993332711,
4.05535046556385));
#40158=CARTESIAN_POINT('Ctrl Pts',(20.8993454693358,-0.513402987365846,
3.78280103771366));
#40159=CARTESIAN_POINT('Ctrl Pts',(20.9232033873672,-0.346562912086465,
3.56336268648205));
#40160=CARTESIAN_POINT('Ctrl Pts',(20.9470613053986,-0.0949787932613798,
3.45069404477467));
#40161=CARTESIAN_POINT('Ctrl Pts',(20.97091922343,0.179830242856268,3.47234567582879));
#40162=CARTESIAN_POINT('Ctrl Pts',(20.9947771414614,0.410665878084123,3.62302316008453));
#40163=CARTESIAN_POINT('Ctrl Pts',(21.0186350594928,0.541082524061315,3.86588175144064));
#40164=CARTESIAN_POINT('Ctrl Pts',(21.0424929775243,0.539189751860116,4.14153590729571));
#40165=CARTESIAN_POINT('Ctrl Pts',(21.0663508955557,0.405450399288564,4.38258067876424));
#40166=CARTESIAN_POINT('Ctrl Pts',(21.0902088135871,0.172567379211795,4.53007405282339));
#40167=CARTESIAN_POINT('Ctrl Pts',(21.1140667316185,-0.102513065388571,
4.54794988212627));
#40168=CARTESIAN_POINT('Ctrl Pts',(21.1379246496499,-0.352526273278862,
4.43183703934844));
#40169=CARTESIAN_POINT('Ctrl Pts',(21.1617825676814,-0.516337204635697,
4.21012827746935));
#40170=CARTESIAN_POINT('Ctrl Pts',(21.1856404857128,-0.553889624765765,
3.93703742795684));
#40171=CARTESIAN_POINT('Ctrl Pts',(21.2094984037442,-0.456000943963824,
3.67934264238169));
#40172=CARTESIAN_POINT('Ctrl Pts',(21.2333563217756,-0.246607611160355,
3.50005731527167));
#40173=CARTESIAN_POINT('Ctrl Pts',(21.257214239807,0.0230880000356606,3.44302159274494));
#40174=CARTESIAN_POINT('Ctrl Pts',(21.2810721578385,0.287137966314551,3.52218226257825));
#40175=CARTESIAN_POINT('Ctrl Pts',(21.3049300758698,0.480974878350452,3.71818238470557));
#40176=CARTESIAN_POINT('Ctrl Pts',(21.3287879939013,0.557200331135927,3.9830945903298));
#40177=CARTESIAN_POINT('Ctrl Pts',(21.3526459119327,0.497175125126959,4.25214062911267));
#40178=CARTESIAN_POINT('Ctrl Pts',(21.3765038299641,0.31557705824565,4.45953141590455));
#40179=CARTESIAN_POINT('Ctrl Pts',(21.4003617479955,0.0568118044769688,
4.55455425412338));
#40180=CARTESIAN_POINT('Ctrl Pts',(21.424219666027,-0.215845483008899,4.51397347145443));
#40181=CARTESIAN_POINT('Ctrl Pts',(21.4480775840584,-0.435722670386138,
4.34771217465862));
#40182=CARTESIAN_POINT('Ctrl Pts',(21.4719355020898,-0.549053796006754,
4.0964257796693));
#40183=CARTESIAN_POINT('Ctrl Pts',(21.4957934201212,-0.528126312578589,
3.82156065496534));
#40184=CARTESIAN_POINT('Ctrl Pts',(21.5196513381527,-0.378057559853047,
3.59032881071252));
#40185=CARTESIAN_POINT('Ctrl Pts',(21.543509256184,-0.135543435662257,3.45927273145963));
#40186=CARTESIAN_POINT('Ctrl Pts',(21.5673671742155,0.14011475067701,3.46043919847993));
#40187=CARTESIAN_POINT('Ctrl Pts',(21.5912250922469,0.381511063826562,3.59354297881304));
#40188=CARTESIAN_POINT('Ctrl Pts',(21.6150830102783,0.529617529717794,3.8260365724933));
#40189=CARTESIAN_POINT('Ctrl Pts',(21.6389409283097,0.548218083101175,4.10106896286759));
#40190=CARTESIAN_POINT('Ctrl Pts',(21.6627988463412,0.432764382005563,4.35138723875747));
#40191=CARTESIAN_POINT('Ctrl Pts',(21.6866567643726,0.211488001244504,4.51578176317496));
#40192=CARTESIAN_POINT('Ctrl Pts',(21.710514682404,-0.0615029566383307,
4.55405359688301));
#40193=CARTESIAN_POINT('Ctrl Pts',(21.7343726004354,-0.319454766316188,
4.4568442340362));
#40194=CARTESIAN_POINT('Ctrl Pts',(21.7582305184669,-0.499291183856609,
4.24792401178047));
#40195=CARTESIAN_POINT('Ctrl Pts',(21.7820884364982,-0.557037306525311,
3.97837961532992));
#40196=CARTESIAN_POINT('Ctrl Pts',(21.8059463545297,-0.478572634356998,
3.71412199185867));
#40197=CARTESIAN_POINT('Ctrl Pts',(21.8298042725611,-0.283083917031579,
3.51976932853855));
#40198=CARTESIAN_POINT('Ctrl Pts',(21.8536621905926,-0.018373470940863,
3.44284614561161));
#40199=CARTESIAN_POINT('Ctrl Pts',(21.8775201086239,0.250829789278194,3.5021622566489));
#40200=CARTESIAN_POINT('Ctrl Pts',(21.9013780266554,0.458698333552465,3.68321325676341));
#40201=CARTESIAN_POINT('Ctrl Pts',(21.9252359446868,0.55440264058141,3.94172724469688));
#40202=CARTESIAN_POINT('Ctrl Pts',(21.9490938627182,0.514540400363477,4.21449050861997));
#40203=CARTESIAN_POINT('Ctrl Pts',(21.9729517807496,0.348859016457567,4.4348050005813));
#40204=CARTESIAN_POINT('Ctrl Pts',(21.996809698781,0.0978721002989983,4.54879782605011));
#40205=CARTESIAN_POINT('Ctrl Pts',(22.0206676168125,-0.177047210365213,
4.52859463409701));
#40206=CARTESIAN_POINT('Ctrl Pts',(22.0445255348439,-0.408673655425848,
4.3791356554785));
#40207=CARTESIAN_POINT('Ctrl Pts',(22.0683834528753,-0.540368259688198,
4.13696768164748));
#40208=CARTESIAN_POINT('Ctrl Pts',(22.0922413709067,-0.53992810512055,3.86130737872913));
#40209=CARTESIAN_POINT('Ctrl Pts',(22.1160992889381,-0.407460821505317,
3.61956119962225));
#40210=CARTESIAN_POINT('Ctrl Pts',(22.1399572069695,-0.175358268020808,
3.47084267015335));
#40211=CARTESIAN_POINT('Ctrl Pts',(22.163815125001,0.0996241586556461,3.45151752178681));
#40212=CARTESIAN_POINT('Ctrl Pts',(22.1876730430324,0.350245764837839,3.56631127970877));
#40213=CARTESIAN_POINT('Ctrl Pts',(22.2115309610638,0.51522274100534,3.78715374318048));
#40214=CARTESIAN_POINT('Ctrl Pts',(22.2353888790952,0.554213722627899,4.06004291426965));
#40215=CARTESIAN_POINT('Ctrl Pts',(22.2592467971266,0.457684352558003,4.31824995726588));
#40216=CARTESIAN_POINT('Ctrl Pts',(22.2831047151581,0.249238691275201,4.49863621678958));
#40217=CARTESIAN_POINT('Ctrl Pts',(22.3069626331895,-0.0201526192614011,
4.55709233866662));
#40218=CARTESIAN_POINT('Ctrl Pts',(22.3308205512209,-0.284616065231974,
4.47932420896945));
#40219=CARTESIAN_POINT('Ctrl Pts',(22.3546784692523,-0.479483130864429,
4.28434825342259));
#40220=CARTESIAN_POINT('Ctrl Pts',(22.3785363872838,-0.557103509392546,
4.01984140485232));
#40221=CARTESIAN_POINT('Ctrl Pts',(22.4023943053151,-0.498496906094933,
3.75048279151596));
#40222=CARTESIAN_POINT('Ctrl Pts',(22.4262522233466,-0.317994227800984,
3.542137933897));
#40223=CARTESIAN_POINT('Ctrl Pts',(22.450110141378,-0.0597333038680864,
3.44575282046209));
#40224=CARTESIAN_POINT('Ctrl Pts',(22.4739680594094,0.213134049493302,3.48489624527193));
#40225=CARTESIAN_POINT('Ctrl Pts',(22.4978259774408,0.433884304103661,3.6499965589521));
#40226=CARTESIAN_POINT('Ctrl Pts',(22.5216838954723,0.548538061567711,3.90068226732924));
#40227=CARTESIAN_POINT('Ctrl Pts',(22.5455418135037,0.529059256943919,4.17565382996358));
#40228=CARTESIAN_POINT('Ctrl Pts',(22.5693997315351,0.380211173855379,4.40767331583304));
#40229=CARTESIAN_POINT('Ctrl Pts',(22.5932576495665,0.138390873272415,4.54000544018811));
#40230=CARTESIAN_POINT('Ctrl Pts',(22.6171155675979,-0.137269333605106,
4.54029177230974));
#40231=CARTESIAN_POINT('Ctrl Pts',(22.6409734856293,-0.379364264814148,
4.40846158181013));
#40232=CARTESIAN_POINT('Ctrl Pts',(22.6648314036608,-0.528692759685234,
4.17675229015827));
#40233=CARTESIAN_POINT('Ctrl Pts',(22.6886893216921,-0.54874438127821,3.90182058373076));
#40234=CARTESIAN_POINT('Ctrl Pts',(22.7125472397236,-0.434607562942265,
3.65089956353622));
#40235=CARTESIAN_POINT('Ctrl Pts',(22.736405157755,-0.214207731687487,3.48533716867003));
#40236=CARTESIAN_POINT('Ctrl Pts',(22.7602630757864,0.0585913648593265,
3.44563509732658));
#40237=CARTESIAN_POINT('Ctrl Pts',(22.7841209938179,0.31702578011682,3.5414689143437));
#40238=CARTESIAN_POINT('Ctrl Pts',(22.8079789118493,0.498012898707086,3.74946820019106));
#40239=CARTESIAN_POINT('Ctrl Pts',(22.8238841905369,0.537376264140017,3.92891364167179));
#40240=CARTESIAN_POINT('Ctrl Pts',(22.8318368298807,0.534391234777113,4.01792167950194));
#40241=CARTESIAN_POINT('Ctrl Pts',(3.99999999999998,0.254694598474614,4.53673594206822));
#40242=CARTESIAN_POINT('Ctrl Pts',(4.00795263934379,0.165296026927429,4.57915779516171));
#40243=CARTESIAN_POINT('Ctrl Pts',(4.0238579180314,-0.0350146299391769,
4.61842892627033));
#40244=CARTESIAN_POINT('Ctrl Pts',(4.04771583606282,-0.327086058023631,
4.5259865276721));
#40245=CARTESIAN_POINT('Ctrl Pts',(4.07157375409423,-0.539100294705402,
4.30498302442502));
#40246=CARTESIAN_POINT('Ctrl Pts',(4.09543167212566,-0.619328256935644,
4.00937412827253));
#40247=CARTESIAN_POINT('Ctrl Pts',(4.11928959015708,-0.548093442686671,
3.71148804617917));
#40248=CARTESIAN_POINT('Ctrl Pts',(4.1431475081885,-0.342845496867427,3.48414304986991));
#40249=CARTESIAN_POINT('Ctrl Pts',(4.16700542621991,-0.0537568536316998,
3.38294333505492));
#40250=CARTESIAN_POINT('Ctrl Pts',(4.19086334425134,0.248473820944083,3.43262855616194));
#40251=CARTESIAN_POINT('Ctrl Pts',(4.21472126228276,0.489947458130694,3.62105272953394));
#40252=CARTESIAN_POINT('Ctrl Pts',(4.23857918031417,0.611614759069978,3.90213920826301));
#40253=CARTESIAN_POINT('Ctrl Pts',(4.26243709834559,0.583726034554802,4.20715564703007));
#40254=CARTESIAN_POINT('Ctrl Pts',(4.28629501637702,0.413100159498109,4.46151671210738));
#40255=CARTESIAN_POINT('Ctrl Pts',(4.31015293440843,0.141460167127662,4.60302446238992));
#40256=CARTESIAN_POINT('Ctrl Pts',(4.33401085243986,-0.164770755236008,
4.59707625642582));
#40257=CARTESIAN_POINT('Ctrl Pts',(4.35786877047126,-0.430710704813839,
4.44512666775742));
#40258=CARTESIAN_POINT('Ctrl Pts',(4.38172668850269,-0.59133017320549,4.18433147003372));
#40259=CARTESIAN_POINT('Ctrl Pts',(4.40558460653411,-0.607353296958831,
3.87846221409715));
#40260=CARTESIAN_POINT('Ctrl Pts',(4.42944252456553,-0.474862000813124,
3.60231225357117));
#40261=CARTESIAN_POINT('Ctrl Pts',(4.45330044259694,-0.226254007744579,
3.42340778189093));
#40262=CARTESIAN_POINT('Ctrl Pts',(4.47715836062837,0.0776792518003291,
3.38549581251083));
#40263=CARTESIAN_POINT('Ctrl Pts',(4.50101627865978,0.362617819109035,3.49784685630402));
#40264=CARTESIAN_POINT('Ctrl Pts',(4.5248741966912,0.558886451727075,3.73298802180378));
#40265=CARTESIAN_POINT('Ctrl Pts',(4.54873211472262,0.618492123352341,4.03342088939383));
#40266=CARTESIAN_POINT('Ctrl Pts',(4.57259003275404,0.5268596233165,4.32568143907503));
#40267=CARTESIAN_POINT('Ctrl Pts',(4.59644795078546,0.306395594072305,4.5383040055633));
#40268=CARTESIAN_POINT('Ctrl Pts',(4.62030586881688,0.0110094959969652,
4.61929657956068));
#40269=CARTESIAN_POINT('Ctrl Pts',(4.6441637868483,-0.287068723725306,4.54885427056805));
#40270=CARTESIAN_POINT('Ctrl Pts',(4.66802170487971,-0.514950820910697,
4.34420214192463));
#40271=CARTESIAN_POINT('Ctrl Pts',(4.69187962291114,-0.616913415399932,
4.05538321370614));
#40272=CARTESIAN_POINT('Ctrl Pts',(4.71573754094255,-0.568023875442366,
3.75302158112612));
#40273=CARTESIAN_POINT('Ctrl Pts',(4.73959545897398,-0.380237025278099,
3.51105289951885));
#40274=CARTESIAN_POINT('Ctrl Pts',(4.76345337700539,-0.0994718649854296,
3.38864510263028));
#40275=CARTESIAN_POINT('Ctrl Pts',(4.78731129503681,0.205616875855751,3.41573023112194));
#40276=CARTESIAN_POINT('Ctrl Pts',(4.81116921306823,0.460426689658758,3.5856852332931));
#40277=CARTESIAN_POINT('Ctrl Pts',(4.83502713109965,0.60264963606909,3.85695148163183));
#40278=CARTESIAN_POINT('Ctrl Pts',(4.85888504913107,0.597508330613982,4.16319698927494));
#40279=CARTESIAN_POINT('Ctrl Pts',(4.88274296716248,0.446259962523644,4.42953638764361));
#40280=CARTESIAN_POINT('Ctrl Pts',(4.90660088519391,0.185888877718945,4.59084243889714));
#40281=CARTESIAN_POINT('Ctrl Pts',(4.93045880322533,-0.119937101199393,
4.60767141961541));
#40282=CARTESIAN_POINT('Ctrl Pts',(4.95431672125674,-0.396435191853442,
4.47590818560059));
#40283=CARTESIAN_POINT('Ctrl Pts',(4.97817463928816,-0.575994079421511,
4.22777243672773));
#40284=CARTESIAN_POINT('Ctrl Pts',(5.00203255731958,-0.614706724807315,
3.92394012267834));
#40285=CARTESIAN_POINT('Ctrl Pts',(5.025890475351,-0.503106831702736,3.63870652046354));
#40286=CARTESIAN_POINT('Ctrl Pts',(5.04974839338242,-0.268483613891896,
3.44181901543221));
#40287=CARTESIAN_POINT('Ctrl Pts',(5.07360631141384,0.0317911608623165,
3.38142196567243));
#40288=CARTESIAN_POINT('Ctrl Pts',(5.09746422944526,0.32429213081186,3.47228409503311));
#40289=CARTESIAN_POINT('Ctrl Pts',(5.12132214747667,0.537494841237617,3.69218713785082));
#40290=CARTESIAN_POINT('Ctrl Pts',(5.1451800655081,0.619265421915264,3.98735881011802));
#40291=CARTESIAN_POINT('Ctrl Pts',(5.16903798353952,0.549608738483219,4.28562159765047));
#40292=CARTESIAN_POINT('Ctrl Pts',(5.19289590157094,0.34555774745058,4.51404212438126));
#40293=CARTESIAN_POINT('Ctrl Pts',(5.21675381960235,0.0570084743622218,
4.61676534947452));
#40294=CARTESIAN_POINT('Ctrl Pts',(5.24061173763377,-0.245480923587363,
4.56867264627043));
#40295=CARTESIAN_POINT('Ctrl Pts',(5.26446965566519,-0.487943548953736,
4.38152399072137));
#40296=CARTESIAN_POINT('Ctrl Pts',(5.28832757369661,-0.611090685285508,
4.10108232693608));
#40297=CARTESIAN_POINT('Ctrl Pts',(5.31218549172803,-0.584809503288917,
3.79592328078761));
#40298=CARTESIAN_POINT('Ctrl Pts',(5.33604340975945,-0.415526467847156,
3.5406665514248));
#40299=CARTESIAN_POINT('Ctrl Pts',(5.35990132779088,-0.144635892303038,
3.39772936223054));
#40300=CARTESIAN_POINT('Ctrl Pts',(5.38375924582228,0.161622098711782,3.40206374949372));
#40301=CARTESIAN_POINT('Ctrl Pts',(5.40761716385371,0.428359084093981,3.55260983746209));
#40302=CARTESIAN_POINT('Ctrl Pts',(5.43147508188512,0.590350605148055,3.81255500683439));
#40303=CARTESIAN_POINT('Ctrl Pts',(5.45533299991655,0.607985322415754,4.11833558293467));
#40304=CARTESIAN_POINT('Ctrl Pts',(5.47919091794796,0.476951067165249,4.39517988561105));
#40305=CARTESIAN_POINT('Ctrl Pts',(5.50304883597938,0.2292892841064,4.57539194177126));
#40306=CARTESIAN_POINT('Ctrl Pts',(5.5269067540108,-0.0744399746307492,
4.61490499480714));
#40307=CARTESIAN_POINT('Ctrl Pts',(5.55076467204222,-0.359966631867259,
4.5040570269359));
#40308=CARTESIAN_POINT('Ctrl Pts',(5.57462259007364,-0.55747164231658,4.26995338574299));
#40309=CARTESIAN_POINT('Ctrl Pts',(5.59848050810506,-0.618659650999605,
3.96983878834977));
#40310=CARTESIAN_POINT('Ctrl Pts',(5.62233842613648,-0.528568523057477,
3.67709942878664));
#40311=CARTESIAN_POINT('Ctrl Pts',(5.6461963441679,-0.309227993320144,3.46331805450751));
#40312=CARTESIAN_POINT('Ctrl Pts',(5.67005426219932,-0.0142727959960426,
3.38077003484781));
#40313=CARTESIAN_POINT('Ctrl Pts',(5.69391218023074,0.284172488697173,3.4496406091084));
#40314=CARTESIAN_POINT('Ctrl Pts',(5.71777009826216,0.513129859266986,3.65308904601577));
#40315=CARTESIAN_POINT('Ctrl Pts',(5.74162801629357,0.616613001744231,3.94136666067651));
#40316=CARTESIAN_POINT('Ctrl Pts',(5.765485934325,0.569317469330215,4.24398172424487));
#40317=CARTESIAN_POINT('Ctrl Pts',(5.78934385235641,0.382808307322586,4.48693660973462));
#40318=CARTESIAN_POINT('Ctrl Pts',(5.81320177038783,0.102692087527565,4.61082223133738));
#40319=CARTESIAN_POINT('Ctrl Pts',(5.83705968841925,-0.202535146533943,
4.58534517687525));
#40320=CARTESIAN_POINT('Ctrl Pts',(5.86091760645067,-0.458237017319611,
4.41673528603543));
#40321=CARTESIAN_POINT('Ctrl Pts',(5.88477552448209,-0.601887460912657,
4.14622225884759));
#40322=CARTESIAN_POINT('Ctrl Pts',(5.9086334425135,-0.598360014525416,3.83995392008642));
#40323=CARTESIAN_POINT('Ctrl Pts',(5.93249136054493,-0.448517265794504,
3.57282118150817));
#40324=CARTESIAN_POINT('Ctrl Pts',(5.95634927857635,-0.188999790056246,
3.41014534911766));
#40325=CARTESIAN_POINT('Ctrl Pts',(5.98020719660777,0.116733210556207,3.39170495376011));
#40326=CARTESIAN_POINT('Ctrl Pts',(6.00406511463918,0.393921897475357,3.52200944135141));
#40327=CARTESIAN_POINT('Ctrl Pts',(6.02792303267061,0.574785693380153,3.76919531120668));
#40328=CARTESIAN_POINT('Ctrl Pts',(6.05178095070201,0.61509921541814,4.07281983667942));
#40329=CARTESIAN_POINT('Ctrl Pts',(6.07563886873346,0.505003308517799,4.35863675364492));
#40330=CARTESIAN_POINT('Ctrl Pts',(6.09949678676485,0.27142206589204,4.55675943366228));
#40331=CARTESIAN_POINT('Ctrl Pts',(6.12335470479629,-0.0285325303540597,
4.61873507756083));
#40332=CARTESIAN_POINT('Ctrl Pts',(6.14721262282769,-0.321503980505702,
4.52942105023226));
#40333=CARTESIAN_POINT('Ctrl Pts',(6.17107054085913,-0.535870591003297,
4.31063422072759));
#40334=CARTESIAN_POINT('Ctrl Pts',(6.19492845889052,-0.619180264299368,
4.01591706164003));
#40335=CARTESIAN_POINT('Ctrl Pts',(6.21878637692196,-0.551125001039776,
3.71725450231754));
#40336=CARTESIAN_POINT('Ctrl Pts',(6.24264429495337,-0.348226295733882,
3.48783145534908));
#40337=CARTESIAN_POINT('Ctrl Pts',(6.2665022129848,-0.0603247367796791,
3.38345774569467));
#40338=CARTESIAN_POINT('Ctrl Pts',(6.29036013101621,0.242607149567705,3.43020375417728));
#40339=CARTESIAN_POINT('Ctrl Pts',(6.31421804904763,0.485688404846908,3.61560451082823));
#40340=CARTESIAN_POINT('Ctrl Pts',(6.33807596707905,0.61099356578022,3.89627130770405));
#40341=CARTESIAN_POINT('Ctrl Pts',(6.36193388511046,0.585080291527744,4.19994745529594));
#40342=CARTESIAN_POINT('Ctrl Pts',(6.3937444424857,0.363797450650833,4.54512657044717));
#40343=CARTESIAN_POINT('Ctrl Pts',(6.43350763920472,-0.178959141669374,
4.67939801199369));
#40344=CARTESIAN_POINT('Ctrl Pts',(6.48122347526757,-0.668951848353412,
4.21606826543601));
#40345=CARTESIAN_POINT('Ctrl Pts',(6.5289393113304,-0.543175254381078,3.55462676401443));
#40346=CARTESIAN_POINT('Ctrl Pts',(6.57665514739324,0.0806513803028556,
3.30201433154981));
#40347=CARTESIAN_POINT('Ctrl Pts',(6.62437098345608,0.630812951656228,3.69045991683978));
#40348=CARTESIAN_POINT('Ctrl Pts',(6.67208681951892,0.601478580142798,4.36311480674272));
#40349=CARTESIAN_POINT('Ctrl Pts',(6.71980265558175,0.0199087309838695,
4.70234020845997));
#40350=CARTESIAN_POINT('Ctrl Pts',(6.76751849164459,-0.580002689552455,
4.39658285339385));
#40351=CARTESIAN_POINT('Ctrl Pts',(6.81523432770743,-0.64725742864426,3.72664421308375));
#40352=CARTESIAN_POINT('Ctrl Pts',(6.86295016377027,-0.120142281411799,
3.30772876957018));
#40353=CARTESIAN_POINT('Ctrl Pts',(6.91066599983311,0.517310146858294,3.52453857056345));
#40354=CARTESIAN_POINT('Ctrl Pts',(6.95838183589594,0.679704059947864,4.17797090041396));
#40355=CARTESIAN_POINT('Ctrl Pts',(7.00609767195879,0.217917737520193,4.66797035296266));
#40356=CARTESIAN_POINT('Ctrl Pts',(7.05381350802161,-0.443987099894697,
4.54456206689342));
#40357=CARTESIAN_POINT('Ctrl Pts',(7.10152934408447,-0.698171061503544,
3.92107420680554));
#40358=CARTESIAN_POINT('Ctrl Pts',(7.14924518014729,-0.311214160204793,
3.3700650369752));
#40359=CARTESIAN_POINT('Ctrl Pts',(7.19696101621015,0.361535686685884,3.39753487888718));
#40360=CARTESIAN_POINT('Ctrl Pts',(7.24467685227297,0.702281647003851,3.97825768917858));
#40361=CARTESIAN_POINT('Ctrl Pts',(7.29239268833582,0.398111619195611,4.5789468099385));
#40362=CARTESIAN_POINT('Ctrl Pts',(7.34010852439865,-0.271650463017158,
4.64798016059173));
#40363=CARTESIAN_POINT('Ctrl Pts',(7.38782436046149,-0.691951729928866,
4.1219633626529));
#40364=CARTESIAN_POINT('Ctrl Pts',(7.43554019652432,-0.476823084268312,
3.48394573037578));
#40365=CARTESIAN_POINT('Ctrl Pts',(7.48325603258717,0.17617954081454,3.31982867534575));
#40366=CARTESIAN_POINT('Ctrl Pts',(7.53097186865001,0.667393780433987,3.78032341303133));
#40367=CARTESIAN_POINT('Ctrl Pts',(7.57868770471284,0.545730043505963,4.44255054095139));
#40368=CARTESIAN_POINT('Ctrl Pts',(7.62640354077568,-0.077085990144297,
4.69837669746149));
#40369=CARTESIAN_POINT('Ctrl Pts',(7.67411937683852,-0.629112772588521,
4.31287278685955));
#40370=CARTESIAN_POINT('Ctrl Pts',(7.72183521290136,-0.603415615998442,
3.64005298187887));
#40371=CARTESIAN_POINT('Ctrl Pts',(7.76955104896419,-0.0235926144000291,
3.29777806215626));
#40372=CARTESIAN_POINT('Ctrl Pts',(7.81726688502703,0.577895847971041,3.60036435301798));
#40373=CARTESIAN_POINT('Ctrl Pts',(7.86498272108987,0.648693661106154,4.26994220769392));
#40374=CARTESIAN_POINT('Ctrl Pts',(7.9126985571527,0.123786103798515,4.6916279794467));
#40375=CARTESIAN_POINT('Ctrl Pts',(7.96041439321555,-0.514796137313916,
4.47818113561083));
#40376=CARTESIAN_POINT('Ctrl Pts',(8.00813022927838,-0.680633164378164,
3.82561319718015));
#40377=CARTESIAN_POINT('Ctrl Pts',(8.05584606534123,-0.221434283704469,
3.33318734306526));
#40378=CARTESIAN_POINT('Ctrl Pts',(8.10356190140405,0.441111106898351,3.45310581204486));
#40379=CARTESIAN_POINT('Ctrl Pts',(8.1512777374669,0.698577380670183,4.07524562887252));
#40380=CARTESIAN_POINT('Ctrl Pts',(8.19899357352974,0.314529296777622,4.62828622690367));
#40381=CARTESIAN_POINT('Ctrl Pts',(8.24670940959258,-0.358355880000973,
4.60436191534297));
#40382=CARTESIAN_POINT('Ctrl Pts',(8.29442524565541,-0.70215733816079,4.02544275761943));
#40383=CARTESIAN_POINT('Ctrl Pts',(8.34214108171825,-0.401156908608127,
3.42315912408683));
#40384=CARTESIAN_POINT('Ctrl Pts',(8.3898569177811,0.268232082711808,3.35059734274305));
#40385=CARTESIAN_POINT('Ctrl Pts',(8.43757275384392,0.691299425196396,3.8743920139026));
#40386=CARTESIAN_POINT('Ctrl Pts',(8.48528858990677,0.479535868514212,4.51353443142269));
#40387=CARTESIAN_POINT('Ctrl Pts',(8.53300442596961,-0.172592854832336,
4.68109027882443));
#40388=CARTESIAN_POINT('Ctrl Pts',(8.58072026203244,-0.66622690390392,4.22319044326068));
#40389=CARTESIAN_POINT('Ctrl Pts',(8.62843609809529,-0.548054535901959,
3.56033138942427));
#40390=CARTESIAN_POINT('Ctrl Pts',(8.67615193415812,0.0734047453217555,
3.30122678585069));
#40391=CARTESIAN_POINT('Ctrl Pts',(8.72386777022095,0.627455319439314,3.68381637683837));
#40392=CARTESIAN_POINT('Ctrl Pts',(8.7715836062838,0.605304019074675,4.35676225408577));
#40393=CARTESIAN_POINT('Ctrl Pts',(8.81929944234663,0.0272927241942496,
4.70208786391332));
#40394=CARTESIAN_POINT('Ctrl Pts',(8.86701527840948,-0.575781899266294,
4.40267538529889));
#40395=CARTESIAN_POINT('Ctrl Pts',(8.9147311144723,-0.650107145087294,3.73347990440727));
#40396=CARTESIAN_POINT('Ctrl Pts',(8.96244695053515,-0.127428996390418,
3.30903392823725));
#40397=CARTESIAN_POINT('Ctrl Pts',(9.01016278659798,0.512269160438921,3.51911272764658));
#40398=CARTESIAN_POINT('Ctrl Pts',(9.05787862266082,0.681542664962993,4.17079770865984));
#40399=CARTESIAN_POINT('Ctrl Pts',(9.10559445872366,0.224945053369686,4.66563652575022));
#40400=CARTESIAN_POINT('Ctrl Pts',(9.1533102947865,-0.438223061957547,4.54921107910972));
#40401=CARTESIAN_POINT('Ctrl Pts',(9.20102613084934,-0.698964196560635,
3.92843664782408));
#40402=CARTESIAN_POINT('Ctrl Pts',(9.24874196691217,-0.317835754515511,
3.3733799439853));
#40403=CARTESIAN_POINT('Ctrl Pts',(9.29645780297501,0.355166151432911,3.39375807937372));
#40404=CARTESIAN_POINT('Ctrl Pts',(9.34417363903786,0.702013515586798,3.97085749870423));
#40405=CARTESIAN_POINT('Ctrl Pts',(9.39188947510068,0.404191066510942,4.57471892538967));
#40406=CARTESIAN_POINT('Ctrl Pts',(9.43960531116354,-0.264806258220881,
4.65080711970243));
#40407=CARTESIAN_POINT('Ctrl Pts',(9.48732114722635,-0.690627921460452,
4.12924912203773));
#40408=CARTESIAN_POINT('Ctrl Pts',(9.53503698328922,-0.482235337746388,
3.48899966685243));
#40409=CARTESIAN_POINT('Ctrl Pts',(9.58275281935202,0.169001376764621,3.31800968034731));
#40410=CARTESIAN_POINT('Ctrl Pts',(9.63046865541491,0.665041526572246,3.77330189814918));
#40411=CARTESIAN_POINT('Ctrl Pts',(9.6781844914777,0.550363809549371,4.43677447107931));
#40412=CARTESIAN_POINT('Ctrl Pts',(9.72590032754056,-0.0697214622184181,
4.69915032657822));
#40413=CARTESIAN_POINT('Ctrl Pts',(9.7736161636034,-0.625780442428439,4.31948567936979));
#40414=CARTESIAN_POINT('Ctrl Pts',(9.82133199966623,-0.607175613486645,
3.64643241687702));
#40415=CARTESIAN_POINT('Ctrl Pts',(9.86904783572907,-0.030992076082374,
3.29806570630264));
#40416=CARTESIAN_POINT('Ctrl Pts',(9.91676367179191,0.573651961662729,3.59429605827795));
#40417=CARTESIAN_POINT('Ctrl Pts',(9.96447950785474,0.651502576242943,4.26309058249416));
#40418=CARTESIAN_POINT('Ctrl Pts',(10.0121953439176,0.131068350403577,4.69028497663703));
#40419=CARTESIAN_POINT('Ctrl Pts',(10.0599111799804,-0.50972795835719,4.48358005533451));
#40420=CARTESIAN_POINT('Ctrl Pts',(10.1076270160433,-0.682433239785766,
3.83279612838271));
#40421=CARTESIAN_POINT('Ctrl Pts',(10.1553428521061,-0.228449576533966,
3.33555808949935));
#40422=CARTESIAN_POINT('Ctrl Pts',(10.2030586881689,0.435322847997542,3.44848728078164));
#40423=CARTESIAN_POINT('Ctrl Pts',(10.2507745242318,0.699331602909907,4.06787908823615));
#40424=CARTESIAN_POINT('Ctrl Pts',(10.2984903602946,0.321133386270249,4.62493648450936));
#40425=CARTESIAN_POINT('Ctrl Pts',(10.3462061963575,-0.351966560253669,
4.60810509117381));
#40426=CARTESIAN_POINT('Ctrl Pts',(10.3939220324203,-0.701850198794989,
4.03284143571381));
#40427=CARTESIAN_POINT('Ctrl Pts',(10.4416378684831,-0.407214000429435,
3.42741898450738));
#40428=CARTESIAN_POINT('Ctrl Pts',(10.489353704546,0.261373080323254,3.34780649011919));
#40429=CARTESIAN_POINT('Ctrl Pts',(10.5370695406088,0.689937239673316,3.86711333114163));
#40430=CARTESIAN_POINT('Ctrl Pts',(10.5847853766716,0.484921415782374,4.50845204490092));
#40431=CARTESIAN_POINT('Ctrl Pts',(10.6325012127345,-0.165405205696588,
4.68287142228737));
#40432=CARTESIAN_POINT('Ctrl Pts',(10.6802170487973,-0.66383768169814,4.23019946525991));
#40433=CARTESIAN_POINT('Ctrl Pts',(10.7279328848602,-0.552657800140614,
3.5661317972102));
#40434=CARTESIAN_POINT('Ctrl Pts',(10.775648720923,0.0660362430193439,3.30049197570278));
#40435=CARTESIAN_POINT('Ctrl Pts',(10.8233645569858,0.624088188116435,3.67722113622194));
#40436=CARTESIAN_POINT('Ctrl Pts',(10.8710803930487,0.609030347235101,4.3503630939397));
#40437=CARTESIAN_POINT('Ctrl Pts',(10.9187962291115,0.0346905673513346,
4.70176123146349));
#40438=CARTESIAN_POINT('Ctrl Pts',(10.9665120651743,-0.57150609431415,4.40872123214985));
#40439=CARTESIAN_POINT('Ctrl Pts',(11.0142279012372,-0.65287991581936,3.74034623636848));
#40440=CARTESIAN_POINT('Ctrl Pts',(11.0619437373,-0.134704064778877,3.31041528701663));
#40441=CARTESIAN_POINT('Ctrl Pts',(11.1096595733629,0.507172601636502,3.51374059022208));
#40442=CARTESIAN_POINT('Ctrl Pts',(11.1573754094257,0.68330486411552,4.16360539148934));
#40443=CARTESIAN_POINT('Ctrl Pts',(11.2050912454885,0.231947755880478,4.66322884435941));
#40444=CARTESIAN_POINT('Ctrl Pts',(11.2528070815514,-0.432410545554582,
4.55379904436673));
#40445=CARTESIAN_POINT('Ctrl Pts',(11.3005229176142,-0.699679589515398,
3.93580706063847));
#40446=CARTESIAN_POINT('Ctrl Pts',(11.348238753677,-0.324422100469907,3.37676444086124));
#40447=CARTESIAN_POINT('Ctrl Pts',(11.3959545897399,0.348757195312759,3.39004862475285));
#40448=CARTESIAN_POINT('Ctrl Pts',(11.4436704258027,0.701667392320496,3.9634605418422));
#40449=CARTESIAN_POINT('Ctrl Pts',(11.4913862618656,0.410225626419724,4.57042720558968));
#40450=CARTESIAN_POINT('Ctrl Pts',(11.5391020979284,-0.257932644354891,
4.65356178929341));
#40451=CARTESIAN_POINT('Ctrl Pts',(11.5868179339912,-0.689227399014534,
4.13652052554825));
#40452=CARTESIAN_POINT('Ctrl Pts',(11.6345337700541,-0.487594028032435,
3.49411036255383));
#40453=CARTESIAN_POINT('Ctrl Pts',(11.6822496061169,0.161804441490335,3.31626643773886));
#40454=CARTESIAN_POINT('Ctrl Pts',(11.7299654421798,0.662615402711184,3.76630556374144));
#40455=CARTESIAN_POINT('Ctrl Pts',(11.7776812782426,0.554936443973853,4.43094988641136));
#40456=CARTESIAN_POINT('Ctrl Pts',(11.8253971143054,-0.062349190059417,
4.69984629737339));
#40457=CARTESIAN_POINT('Ctrl Pts',(11.8731129503683,-0.622378603495518,
4.32606308493799));
#40458=CARTESIAN_POINT('Ctrl Pts',(11.9208287864311,-0.610868168815925,
3.65285112447858));
#40459=CARTESIAN_POINT('Ctrl Pts',(11.9685446224939,-0.0383880952977111,
3.29843131798253));
#40460=CARTESIAN_POINT('Ctrl Pts',(12.0162604585568,0.569344356809164,3.58827282720487));
#40461=CARTESIAN_POINT('Ctrl Pts',(12.0639762946196,0.654239125569198,4.25620973444184));
#40462=CARTESIAN_POINT('Ctrl Pts',(12.1116921306825,0.138336038556134,4.68886530024737));
#40463=CARTESIAN_POINT('Ctrl Pts',(12.1594079667453,-0.50460316123658,4.48892526128066));
#40464=CARTESIAN_POINT('Ctrl Pts',(12.2071238028081,-0.684157513748105,
3.83999763179777));
#40465=CARTESIAN_POINT('Ctrl Pts',(12.254839638871,-0.235439494268261,3.33800263898788));
#40466=CARTESIAN_POINT('Ctrl Pts',(12.3025554749338,0.429486235500398,3.44393000893412));
#40467=CARTESIAN_POINT('Ctrl Pts',(12.3502713109967,0.700008146713868,4.06050500791278));
#40468=CARTESIAN_POINT('Ctrl Pts',(12.3979871470595,0.327701805790174,4.62151732713591));
#40469=CARTESIAN_POINT('Ctrl Pts',(12.4457029831223,-0.345538145731053,
4.61178072157682));
#40470=CARTESIAN_POINT('Ctrl Pts',(12.4934188191852,-0.701465101239671,
4.04023646593735));
#40471=CARTESIAN_POINT('Ctrl Pts',(12.541134655248,-0.413225860851952,3.43174244451));
#40472=CARTESIAN_POINT('Ctrl Pts',(12.5888504913108,0.254485045853264,3.34508808005552));
#40473=CARTESIAN_POINT('Ctrl Pts',(12.6365663273737,0.688498419195676,3.85984940880123));
#40474=CARTESIAN_POINT('Ctrl Pts',(12.6842821634365,0.490253100280801,4.50331318193882));
#40475=CARTESIAN_POINT('Ctrl Pts',(12.7319979994994,-0.158199184135511,
4.68457671563321));
#40476=CARTESIAN_POINT('Ctrl Pts',(12.7797138355622,-0.661374723552845,
4.23718291779492));
#40477=CARTESIAN_POINT('Ctrl Pts',(12.827429671625,-0.557199677773407,3.57198039701723));
#40478=CARTESIAN_POINT('Ctrl Pts',(12.8751455076879,0.058660405724426,3.29983486358678));
#40479=CARTESIAN_POINT('Ctrl Pts',(12.9228613437507,0.62065173603916,3.67066174834999));
#40480=CARTESIAN_POINT('Ctrl Pts',(12.9705771798135,0.612689027194643,4.34392501712378));
#40481=CARTESIAN_POINT('Ctrl Pts',(13.0182930158764,0.0420845572448178,
4.7013566507062));
#40482=CARTESIAN_POINT('Ctrl Pts',(13.0660088519392,-0.567166809177069,
4.4147216801859));
#40483=CARTESIAN_POINT('Ctrl Pts',(13.1137246880021,-0.655580167748548,
3.74724140943759));
#40484=CARTESIAN_POINT('Ctrl Pts',(13.1614405240649,-0.141964170879043,
3.31187324159358));
#40485=CARTESIAN_POINT('Ctrl Pts',(13.2091563601277,0.502019708508231,3.50842246418533));
#40486=CARTESIAN_POINT('Ctrl Pts',(13.2568721961906,0.684991165006287,4.15639490180834));
#40487=CARTESIAN_POINT('Ctrl Pts',(13.3045880322534,0.238924694735218,4.66074749465585));
#40488=CARTESIAN_POINT('Ctrl Pts',(13.3523038683163,-0.426549999040181,
4.55832549625387));
#40489=CARTESIAN_POINT('Ctrl Pts',(13.4000197043791,-0.700317265381609,
3.94318460369993));
#40490=CARTESIAN_POINT('Ctrl Pts',(13.4477355404419,-0.330972411156884,
3.38021816378559));
#40491=CARTESIAN_POINT('Ctrl Pts',(13.4954513765048,0.342309500898352,3.3864069206363));
#40492=CARTESIAN_POINT('Ctrl Pts',(13.5431672125676,0.70124333116994,3.95606764360979));
#40493=CARTESIAN_POINT('Ctrl Pts',(13.5908830486304,0.416214620412595,4.5660721254426));
#40494=CARTESIAN_POINT('Ctrl Pts',(13.6385988846933,-0.251030380554765,
4.65624386434224));
#40495=CARTESIAN_POINT('Ctrl Pts',(13.6863147207561,-0.687750320459788,
4.14377676500662));
#40496=CARTESIAN_POINT('Ctrl Pts',(13.734030556819,-0.492898558687668,3.49927725007553));
#40497=CARTESIAN_POINT('Ctrl Pts',(13.7817463928818,0.15458953374652,3.31459914100992));
#40498=CARTESIAN_POINT('Ctrl Pts',(13.8294622289446,0.660115678675556,3.75933518700271));
#40499=CARTESIAN_POINT('Ctrl Pts',(13.8771780650075,0.559447438691528,4.42507743387505));
#40500=CARTESIAN_POINT('Ctrl Pts',(13.9248939010703,-0.0549699924482557,
4.7004645325629));
#40501=CARTESIAN_POINT('Ctrl Pts',(13.9726097371331,-0.61890763370075,4.33260427296601));
#40502=CARTESIAN_POINT('Ctrl Pts',(14.020325573196,-0.614492871807821,3.65930839172987));
#40503=CARTESIAN_POINT('Ctrl Pts',(14.0680414092588,-0.0457798505455885,
3.29887485658241));
#40504=CARTESIAN_POINT('Ctrl Pts',(14.1157572453217,0.564973511886205,3.58229532883235));
#40505=CARTESIAN_POINT('Ctrl Pts',(14.1634730813845,0.656903005118004,4.24930042782804));
#40506=CARTESIAN_POINT('Ctrl Pts',(14.2111889174473,0.145588360997982,4.6873691079691));
#40507=CARTESIAN_POINT('Ctrl Pts',(14.2589047535102,-0.499422315191365,
4.49421615972892));
#40508=CARTESIAN_POINT('Ctrl Pts',(14.306620589573,-0.685805794740406,3.8472169075166));
#40509=CARTESIAN_POINT('Ctrl Pts',(14.3543364256359,-0.242403260500786,
3.34052072000184));
#40510=CARTESIAN_POINT('Ctrl Pts',(14.4020522616987,0.423601917710294,3.43943450270243));
#40511=CARTESIAN_POINT('Ctrl Pts',(14.4497680977615,0.700606936934704,4.05312420698026));
#40512=CARTESIAN_POINT('Ctrl Pts',(14.4974839338244,0.334233825748585,4.61802913456711));
#40513=CARTESIAN_POINT('Ctrl Pts',(14.5451997698872,-0.339071350470923,
4.61538839828042));
#40514=CARTESIAN_POINT('Ctrl Pts',(14.59291560595,-0.701002088269634,4.04762702688518));
#40515=CARTESIAN_POINT('Ctrl Pts',(14.6406314420129,-0.419191822106764,
3.43612902386528));
#40516=CARTESIAN_POINT('Ctrl Pts',(14.6883472780757,0.24756874439201,3.34244241450009));
#40517=CARTESIAN_POINT('Ctrl Pts',(14.7360631141386,0.686983123580828,3.85260105372344));
#40518=CARTESIAN_POINT('Ctrl Pts',(14.7837789502014,0.495530329791292,4.49811841333687));
#40519=CARTESIAN_POINT('Ctrl Pts',(14.8314947862642,-0.150975590559777,
4.68620596944608));
#40520=CARTESIAN_POINT('Ctrl Pts',(14.8792106223271,-0.658838303041738,
4.24414002517693));
#40521=CARTESIAN_POINT('Ctrl Pts',(14.9269264583899,-0.561679664310124,
3.57787653921065));
#40522=CARTESIAN_POINT('Ctrl Pts',(14.9746422944528,0.0512780527100071,
3.29925552249156));
#40523=CARTESIAN_POINT('Ctrl Pts',(15.0223581305156,0.617146344912281,3.6641389418082));
#40524=CARTESIAN_POINT('Ctrl Pts',(15.0700739665784,0.616279652564493,4.337448738749));
#40525=CARTESIAN_POINT('Ctrl Pts',(15.1177898026413,0.0494738725853903,
4.70087416658037));
#40526=CARTESIAN_POINT('Ctrl Pts',(15.1655056387041,-0.562764525842253,
4.42067606290572));
#40527=CARTESIAN_POINT('Ctrl Pts',(15.2132214747669,-0.658207600943685,
3.75416465773151));
#40528=CARTESIAN_POINT('Ctrl Pts',(15.2609373108298,-0.14920850827279,3.31340763002542));
#40529=CARTESIAN_POINT('Ctrl Pts',(15.3086531468926,0.496811053413015,3.50315894024854));
#40530=CARTESIAN_POINT('Ctrl Pts',(15.3563689829554,0.686601380328997,4.14916704052379));
#40531=CARTESIAN_POINT('Ctrl Pts',(15.4040848190183,0.245875094968658,4.6581927522561));
#40532=CARTESIAN_POINT('Ctrl Pts',(15.4518006550811,-0.420642073376032,
4.56278993199436));
#40533=CARTESIAN_POINT('Ctrl Pts',(15.499516491144,-0.700877153329261,3.95056845754601));
#40534=CARTESIAN_POINT('Ctrl Pts',(15.5472323272068,-0.337485958999024,
3.3837407291352));
#40535=CARTESIAN_POINT('Ctrl Pts',(15.5949481632696,0.335823784368978,3.38283337152726));
#40536=CARTESIAN_POINT('Ctrl Pts',(15.6426639993325,0.70074137923783,3.94867962517506));
#40537=CARTESIAN_POINT('Ctrl Pts',(15.6903798353953,0.422157383260532,4.56165416869007));
#40538=CARTESIAN_POINT('Ctrl Pts',(15.7380956714582,-0.244100233491204,
4.65885304693675));
#40539=CARTESIAN_POINT('Ctrl Pts',(15.785811507521,-0.686196849863089,4.15101703442422));
#40540=CARTESIAN_POINT('Ctrl Pts',(15.8335273435838,-0.498148340509996,
3.50449975550414));
#40541=CARTESIAN_POINT('Ctrl Pts',(15.8812431796467,0.147357454930898,3.3130079753559));
#40542=CARTESIAN_POINT('Ctrl Pts',(15.9289590157095,0.657542632122849,3.75239154216938));
#40543=CARTESIAN_POINT('Ctrl Pts',(15.9766748517723,0.563896292642505,4.41915776575455));
#40544=CARTESIAN_POINT('Ctrl Pts',(16.0243906878352,-0.0475846890311933,
4.70100496347609));
#40545=CARTESIAN_POINT('Ctrl Pts',(16.072106523898,-0.615367918582998,4.33910851688972));
#40546=CARTESIAN_POINT('Ctrl Pts',(16.1198223599609,-0.618049319847516,
3.66580350138828));
#40547=CARTESIAN_POINT('Ctrl Pts',(16.1675381960237,-0.0531665207849041,
3.29939627283611));
#40548=CARTESIAN_POINT('Ctrl Pts',(16.2152540320865,0.560539912386559,3.57636422711252));
#40549=CARTESIAN_POINT('Ctrl Pts',(16.2629698681494,0.659493918998266,4.24236343010572));
#40550=CARTESIAN_POINT('Ctrl Pts',(16.3106857042122,0.152824512175573,4.68579656599215));
#40551=CARTESIAN_POINT('Ctrl Pts',(16.358401540275,-0.494185995685336,4.49945216299141));
#40552=CARTESIAN_POINT('Ctrl Pts',(16.4061173763379,-0.687377899679438,
3.85445315365633));
#40553=CARTESIAN_POINT('Ctrl Pts',(16.4538332124007,-0.249340101729437,
3.34311205284473));
#40554=CARTESIAN_POINT('Ctrl Pts',(16.5015490484636,0.417670548229327,3.43500126142608));
#40555=CARTESIAN_POINT('Ctrl Pts',(16.5492648845264,0.701127907061643,4.04573750526291));
#40556=CARTESIAN_POINT('Ctrl Pts',(16.5969807205892,0.340728720599694,4.61447229425484));
#40557=CARTESIAN_POINT('Ctrl Pts',(16.6446965566521,-0.3325668927742,4.61892772056098));
#40558=CARTESIAN_POINT('Ctrl Pts',(16.6924123927149,-0.700461211314163,
4.05501229764889));
#40559=CARTESIAN_POINT('Ctrl Pts',(16.7401282287777,-0.425111221523205,
3.4405782353328));
#40560=CARTESIAN_POINT('Ctrl Pts',(16.7878440648406,0.240624944169445,3.3398697873209));
#40561=CARTESIAN_POINT('Ctrl Pts',(16.8355599009034,0.685391521140609,3.84536907102113));
#40562=CARTESIAN_POINT('Ctrl Pts',(16.8832757369663,0.500752518144239,4.49286831610534));
#40563=CARTESIAN_POINT('Ctrl Pts',(16.9309915730291,-0.143735227331884,
4.68775900275617));
#40564=CARTESIAN_POINT('Ctrl Pts',(16.978707409092,-0.656228701898373,4.25107001464348));
#40565=CARTESIAN_POINT('Ctrl Pts',(17.0264232451548,-0.566097262135119,
3.58381956887496));
#40566=CARTESIAN_POINT('Ctrl Pts',(17.0741390812176,0.0438900039728252,
3.29875401676759));
#40567=CARTESIAN_POINT('Ctrl Pts',(17.1218549172805,0.613572404098014,3.65765344111895));
#40568=CARTESIAN_POINT('Ctrl Pts',(17.1695707533433,0.619801824515016,4.33093497816967));
#40569=CARTESIAN_POINT('Ctrl Pts',(17.2172865894061,0.0568576926029748,
4.70031383267802));
#40570=CARTESIAN_POINT('Ctrl Pts',(17.265002425469,-0.558299733294432,4.42658371892475));
#40571=CARTESIAN_POINT('Ctrl Pts',(17.3127182615318,-0.66076192356197,3.76111521224867));
#40572=CARTESIAN_POINT('Ctrl Pts',(17.3604340975947,-0.156436272293483,
3.31501828187956));
#40573=CARTESIAN_POINT('Ctrl Pts',(17.4081499336575,0.491547214903555,3.49795060305896));
#40574=CARTESIAN_POINT('Ctrl Pts',(17.4558657697204,0.688135331228569,4.14192261047223));
#40575=CARTESIAN_POINT('Ctrl Pts',(17.5035816057831,0.252798184563325,4.65556490092881));
#40576=CARTESIAN_POINT('Ctrl Pts',(17.551297441846,-0.414687424786488,4.56719185569987));
#40577=CARTESIAN_POINT('Ctrl Pts',(17.5990132779088,-0.701359191168653,
3.95795780201324));
#40578=CARTESIAN_POINT('Ctrl Pts',(17.6467291139717,-0.343962020502345,
3.38733174564023));
#40579=CARTESIAN_POINT('Ctrl Pts',(17.6944449500345,0.329300766127249,3.37932837435862));
#40580=CARTESIAN_POINT('Ctrl Pts',(17.7421607860974,0.700161592278611,3.94129730716402));
#40581=CARTESIAN_POINT('Ctrl Pts',(17.7898766221602,0.428053254869629,4.55717382605774));
#40582=CARTESIAN_POINT('Ctrl Pts',(17.837592458223,-0.23714297293205,4.66138904726133));
#40583=CARTESIAN_POINT('Ctrl Pts',(17.8853082942859,-0.684567159776581,
4.15824052958626));
#40584=CARTESIAN_POINT('Ctrl Pts',(17.9330241303487,-0.503342790378573,
3.50977729874859));
#40585=CARTESIAN_POINT('Ctrl Pts',(17.9807399664116,0.140109008348428,3.31149311751593));
#40586=CARTESIAN_POINT('Ctrl Pts',(18.0284558024744,0.654896548854854,3.7454754005085));
#40587=CARTESIAN_POINT('Ctrl Pts',(18.0761716385372,0.568282511669218,4.41319153957849));
#40588=CARTESIAN_POINT('Ctrl Pts',(18.1238874746001,-0.040194100132671,
4.70146753008449));
#40589=CARTESIAN_POINT('Ctrl Pts',(18.1716033106629,-0.611759851316993,
4.34557509424858));
#40590=CARTESIAN_POINT('Ctrl Pts',(18.2193191467258,-0.621537117901666,
3.67233573200791));
#40591=CARTESIAN_POINT('Ctrl Pts',(18.2670349827885,-0.0605472855394143,
3.29999550882718));
#40592=CARTESIAN_POINT('Ctrl Pts',(18.3147508188514,0.556044050773433,3.57048018084402));
#40593=CARTESIAN_POINT('Ctrl Pts',(18.3624666549143,0.662011579423562,4.23539951180373));
#40594=CARTESIAN_POINT('Ctrl Pts',(18.4101824909771,0.160043688331546,4.684147848987));
#40595=CARTESIAN_POINT('Ctrl Pts',(18.4578983270399,-0.488894784343999,
4.50463268947774));
#40596=CARTESIAN_POINT('Ctrl Pts',(18.5056141631028,-0.68887365394326,3.86170556644909));
#40597=CARTESIAN_POINT('Ctrl Pts',(18.5533299991656,-0.256249247442801,
3.34577634968359));
#40598=CARTESIAN_POINT('Ctrl Pts',(18.6010458352284,0.41169278588589,3.4306307775285));
#40599=CARTESIAN_POINT('Ctrl Pts',(18.6487616712913,0.701570999227752,4.03834572324048));
#40600=CARTESIAN_POINT('Ctrl Pts',(18.6964775073541,0.347185768921481,4.6108472012761));
#40601=CARTESIAN_POINT('Ctrl Pts',(18.744193343417,-0.326025495125306,4.62239829528727));
#40602=CARTESIAN_POINT('Ctrl Pts',(18.7919091794798,-0.699842530451103,
4.06239145790787));
#40603=CARTESIAN_POINT('Ctrl Pts',(18.8396250155426,-0.430983401602837,
3.44508958471478));
#40604=CARTESIAN_POINT('Ctrl Pts',(18.8873408516055,0.233654416470602,3.33737048427408));
#40605=CARTESIAN_POINT('Ctrl Pts',(18.9350566876683,0.683723788661416,3.83815426398688));
#40606=CARTESIAN_POINT('Ctrl Pts',(18.9827725237312,0.505919085286118,4.48756347340344));
#40607=CARTESIAN_POINT('Ctrl Pts',(19.030488359794,-0.136478898681533,4.68923564305365));
#40608=CARTESIAN_POINT('Ctrl Pts',(19.0782041958568,-0.653546209976322,
4.2579721164561));
#40609=CARTESIAN_POINT('Ctrl Pts',(19.1259200319197,-0.570451980578726,
3.58980882586423));
#40610=CARTESIAN_POINT('Ctrl Pts',(19.1736358679825,0.0364970801727598,
3.29833040216201));
#40611=CARTESIAN_POINT('Ctrl Pts',(19.2213517040453,0.609930310515188,3.65120596658116));
#40612=CARTESIAN_POINT('Ctrl Pts',(19.2690675401082,0.623255151928734,4.32438445905389));
#40613=CARTESIAN_POINT('Ctrl Pts',(19.316783376171,0.0642351969327414,4.69967571095415));
#40614=CARTESIAN_POINT('Ctrl Pts',(19.3644992122339,-0.553772927074266,
4.43244399258532));
#40615=CARTESIAN_POINT('Ctrl Pts',(19.4122150482967,-0.663242852612724,
3.76809229994096));
#40616=CARTESIAN_POINT('Ctrl Pts',(19.4599308843595,-0.163646658734412,
3.3167050201661));
#40617=CARTESIAN_POINT('Ctrl Pts',(19.5076467204224,0.486228775054438,3.49279802752061));
#40618=CARTESIAN_POINT('Ctrl Pts',(19.5553625564852,0.689592852244711,4.13466242315333));
#40619=CARTESIAN_POINT('Ctrl Pts',(19.6030783925481,0.259693185238344,4.65286421968052));
#40620=CARTESIAN_POINT('Ctrl Pts',(19.6507942286109,-0.408686697131164,
4.57153080275077));
#40621=CARTESIAN_POINT('Ctrl Pts',(19.6985100646738,-0.701763358503738,
3.96535177039745));
#40622=CARTESIAN_POINT('Ctrl Pts',(19.7462259007365,-0.350399813749482,
3.39099090115443));
#40623=CARTESIAN_POINT('Ctrl Pts',(19.7939417367994,0.322741052541778,3.37589215469092));
#40624=CARTESIAN_POINT('Ctrl Pts',(19.8416575728622,0.699504257835039,3.93392181877779));
#40625=CARTESIAN_POINT('Ctrl Pts',(19.8893734089251,0.433901159015506,4.55263101135276));
#40626=CARTESIAN_POINT('Ctrl Pts',(19.9370892449879,-0.23015857608315,4.663852686053));
#40627=CARTESIAN_POINT('Ctrl Pts',(19.9848050810507,-0.682862933423436,
4.16544436654047));
#40628=CARTESIAN_POINT('Ctrl Pts',(20.0325209171136,-0.508478494849655,
3.51511322409123));
#40629=CARTESIAN_POINT('Ctrl Pts',(20.0802367531764,0.132839643288252,3.31004731418368));
#40630=CARTESIAN_POINT('Ctrl Pts',(20.1279525892393,0.652187835720725,3.73860154375571));
#40631=CARTESIAN_POINT('Ctrl Pts',(20.1756684253021,0.572586513039731,4.4071529569233));
#40632=CARTESIAN_POINT('Ctrl Pts',(20.2233842613649,-0.0327629883405684,
4.70190215105461));
#40633=CARTESIAN_POINT('Ctrl Pts',(20.2711000974278,-0.608151935097038,
4.35190888358257));
#40634=CARTESIAN_POINT('Ctrl Pts',(20.3188159334906,-0.624827148513498,
3.67908301574286));
#40635=CARTESIAN_POINT('Ctrl Pts',(20.3665317695535,-0.0681655280739813,
3.30033184185188));
#40636=CARTESIAN_POINT('Ctrl Pts',(20.4142476056163,0.551956769749184,3.56531418539817));
#40637=CARTESIAN_POINT('Ctrl Pts',(20.4540108023353,0.644905999548395,4.11665253813788));
#40638=CARTESIAN_POINT('Ctrl Pts',(20.4858213597105,0.416382673412033,4.45708139504444));
#40639=CARTESIAN_POINT('Ctrl Pts',(20.509679277742,0.148137151166912,4.60177085628536));
#40640=CARTESIAN_POINT('Ctrl Pts',(20.5335371957734,-0.159214575149101,
4.59858486262053));
#40641=CARTESIAN_POINT('Ctrl Pts',(20.5573951138048,-0.426074836374489,
4.44942877587387));
#40642=CARTESIAN_POINT('Ctrl Pts',(20.5812530318362,-0.589577924844292,
4.19016123618585));
#40643=CARTESIAN_POINT('Ctrl Pts',(20.6051109498677,-0.608473233900696,
3.88450759853215));
#40644=CARTESIAN_POINT('Ctrl Pts',(20.6289688678991,-0.478813304308425,
3.60703485797333));
#40645=CARTESIAN_POINT('Ctrl Pts',(20.6528267859305,-0.231947052182395,
3.42568465323223));
#40646=CARTESIAN_POINT('Ctrl Pts',(20.6766847039619,0.0715712039811096,
3.38475332414555));
#40647=CARTESIAN_POINT('Ctrl Pts',(20.7005426219933,0.357622970648114,3.49427550111266));
#40648=CARTESIAN_POINT('Ctrl Pts',(20.7244005400248,0.556207844932749,3.72745636179159));
#40649=CARTESIAN_POINT('Ctrl Pts',(20.7482584580561,0.618794460414918,4.02728407199912));
#40650=CARTESIAN_POINT('Ctrl Pts',(20.7721163760876,0.530063832205264,4.32043875618714));
#40651=CARTESIAN_POINT('Ctrl Pts',(20.7959742941189,0.311720881859749,4.53523813880796));
#40652=CARTESIAN_POINT('Ctrl Pts',(20.8198322121505,0.01715224242355,4.619156844639));
#40653=CARTESIAN_POINT('Ctrl Pts',(20.8436901301818,-0.281609823618225,
4.55167503361081));
#40654=CARTESIAN_POINT('Ctrl Pts',(20.8675480482133,-0.511511021444125,
4.34929354512778));
#40655=CARTESIAN_POINT('Ctrl Pts',(20.8914059662447,-0.616333626991818,
4.06150032559224));
#40656=CARTESIAN_POINT('Ctrl Pts',(20.9152638842761,-0.570445985619195,
3.75866857192897));
#40657=CARTESIAN_POINT('Ctrl Pts',(20.9391218023075,-0.385068702031786,
3.51484894167474));
#40658=CARTESIAN_POINT('Ctrl Pts',(20.9629797203389,-0.105531663562905,
3.38966195221662));
#40659=CARTESIAN_POINT('Ctrl Pts',(20.9868376383704,0.199810758127152,3.41371924506628));
#40660=CARTESIAN_POINT('Ctrl Pts',(21.0106955564018,0.456293997792742,3.58113815016051));
#40661=CARTESIAN_POINT('Ctrl Pts',(21.0345534744332,0.60120093052663,3.85098018832832));
#40662=CARTESIAN_POINT('Ctrl Pts',(21.0584113924646,0.599097856858477,4.15726162902184));
#40663=CARTESIAN_POINT('Ctrl Pts',(21.082269310496,0.450499039416452,4.42508831804098));
#40664=CARTESIAN_POINT('Ctrl Pts',(21.1061272285275,0.191740934787398,4.58896933394457));
#40665=CARTESIAN_POINT('Ctrl Pts',(21.1299851465589,-0.113903050943465,
4.60883130459215));
#40666=CARTESIAN_POINT('Ctrl Pts',(21.1538430645903,-0.391694638258801,
4.47981743698434));
#40667=CARTESIAN_POINT('Ctrl Pts',(21.1777009826217,-0.573706216867813,
4.23347513609622));
#40668=CARTESIAN_POINT('Ctrl Pts',(21.2015589006531,-0.615430998064313,
3.9300418046833));
#40669=CARTESIAN_POINT('Ctrl Pts',(21.2254168186846,-0.506666136201032,
3.64371515765586));
#40670=CARTESIAN_POINT('Ctrl Pts',(21.2492747367159,-0.27400760274365,3.44450985958179));
#40671=CARTESIAN_POINT('Ctrl Pts',(21.2731326547474,0.0256532534100022,
3.38113703208972));
#40672=CARTESIAN_POINT('Ctrl Pts',(21.2969905727788,0.319041190319967,3.46909305773936));
#40673=CARTESIAN_POINT('Ctrl Pts',(21.3208484908102,0.534414865691478,3.68687029238709));
#40674=CARTESIAN_POINT('Ctrl Pts',(21.3447064088416,0.619109549231529,3.98121627002784));
#40675=CARTESIAN_POINT('Ctrl Pts',(21.3685643268731,0.552415083779586,4.28015538130547));
#40676=CARTESIAN_POINT('Ctrl Pts',(21.3924222449044,0.350640082858436,4.51058887057447));
#40677=CARTESIAN_POINT('Ctrl Pts',(21.4162801629359,0.0631240304344945,
4.61616947282646));
#40678=CARTESIAN_POINT('Ctrl Pts',(21.4401380809673,-0.239827566894842,
4.57107985485291));
#40679=CARTESIAN_POINT('Ctrl Pts',(21.4639959989987,-0.484134791346583,
4.38634565646493));
#40680=CARTESIAN_POINT('Ctrl Pts',(21.4878539170302,-0.610057871747176,
4.10713942122688));
#40681=CARTESIAN_POINT('Ctrl Pts',(21.5117118350615,-0.586805184862796,
3.80173467907963));
#40682=CARTESIAN_POINT('Ctrl Pts',(21.535569753093,-0.420062646027161,3.5448112085363));
#40683=CARTESIAN_POINT('Ctrl Pts',(21.5594276711244,-0.150603347961132,
3.39919379659958));
#40684=CARTESIAN_POINT('Ctrl Pts',(21.5832855891558,0.155682571034224,3.40048986702667));
#40685=CARTESIAN_POINT('Ctrl Pts',(21.6071435071872,0.423899860703612,3.54838249529388));
#40686=CARTESIAN_POINT('Ctrl Pts',(21.6310014252187,0.588462087630599,3.80670790527556));
#40687=CARTESIAN_POINT('Ctrl Pts',(21.6548593432501,0.609129304746478,4.11229849758833));
#40688=CARTESIAN_POINT('Ctrl Pts',(21.6787172612815,0.480847814502724,4.39042904829107));
#40689=CARTESIAN_POINT('Ctrl Pts',(21.7025751793129,0.234985935581564,4.57308906161293));
#40690=CARTESIAN_POINT('Ctrl Pts',(21.7264330973443,-0.0683364054776661,
4.61561318873779));
#40691=CARTESIAN_POINT('Ctrl Pts',(21.7502910153758,-0.35494863395129,4.5076031222497));
#40692=CARTESIAN_POINT('Ctrl Pts',(21.7741489334072,-0.554766252817153,
4.2754702655401));
#40693=CARTESIAN_POINT('Ctrl Pts',(21.7980068514386,-0.618928411339905,
3.9759774252466));
#40694=CARTESIAN_POINT('Ctrl Pts',(21.82186476947,-0.531745714018629,3.68235875884208));
#40695=CARTESIAN_POINT('Ctrl Pts',(21.8457226875014,-0.314536705157368,
3.46641202827438));
#40696=CARTESIAN_POINT('Ctrl Pts',(21.8695806055329,-0.0204149040773093,
3.3809420914381));
#40697=CARTESIAN_POINT('Ctrl Pts',(21.8934385235643,0.278698897140474,3.44684867604406));
#40698=CARTESIAN_POINT('Ctrl Pts',(21.9172964415957,0.509663226401888,3.6480158268968));
#40699=CARTESIAN_POINT('Ctrl Pts',(21.9411543596271,0.616001013860485,3.93525269592965));
#40700=CARTESIAN_POINT('Ctrl Pts',(21.9650122776585,0.571709773899469,4.23832204448885));
#40701=CARTESIAN_POINT('Ctrl Pts',(21.98887019569,0.387619921158457,4.48311516140836));
#40702=CARTESIAN_POINT('Ctrl Pts',(22.0127281137213,0.108746439139576,4.60977346157076));
#40703=CARTESIAN_POINT('Ctrl Pts',(22.0365860317528,-0.196718509442517,
4.5873255404835));
#40704=CARTESIAN_POINT('Ctrl Pts',(22.0604439497842,-0.454080423961193,
4.42126052632156));
#40705=CARTESIAN_POINT('Ctrl Pts',(22.0843018678156,-0.600407305919173,
4.15218583856754));
#40706=CARTESIAN_POINT('Ctrl Pts',(22.1081597858471,-0.599918246812857,
3.84589756782496));
#40707=CARTESIAN_POINT('Ctrl Pts',(22.1320177038785,-0.452732834916613,
3.57729153941473));
#40708=CARTESIAN_POINT('Ctrl Pts',(22.1558756219099,-0.194841912687001,
3.41204924396571));
#40709=CARTESIAN_POINT('Ctrl Pts',(22.1797335399413,0.110693164578993,3.39057692382254));
#40710=CARTESIAN_POINT('Ctrl Pts',(22.2035914579728,0.389160747889314,3.51812514615901));
#40711=CARTESIAN_POINT('Ctrl Pts',(22.2274493760041,0.572467927805029,3.76350489626149));
#40712=CARTESIAN_POINT('Ctrl Pts',(22.2513072940356,0.615791105677536,4.06671414123586));
#40713=CARTESIAN_POINT('Ctrl Pts',(22.2751652120669,0.508536584364246,4.35360996140145));
#40714=CARTESIAN_POINT('Ctrl Pts',(22.2990231300984,0.276931015980992,4.55403851389998));
#40715=CARTESIAN_POINT('Ctrl Pts',(22.3228810481298,-0.0223917293827815,
4.61898955797298));
#40716=CARTESIAN_POINT('Ctrl Pts',(22.3467389661613,-0.31623908674035,4.53258079431836));
#40717=CARTESIAN_POINT('Ctrl Pts',(22.3705968841927,-0.532757373651304,
4.31594151899069));
#40718=CARTESIAN_POINT('Ctrl Pts',(22.3944548022241,-0.619001969851995,
4.02204593667267));
#40719=CARTESIAN_POINT('Ctrl Pts',(22.4183127202555,-0.553883724721699,
3.72275952141814));
#40720=CARTESIAN_POINT('Ctrl Pts',(22.4421706382869,-0.35332581843718,3.49126595675675));
#40721=CARTESIAN_POINT('Ctrl Pts',(22.4660285563184,-0.0663701307507445,
3.38417172009386));
#40722=CARTESIAN_POINT('Ctrl Pts',(22.4898864743497,0.236814872379406,3.42766427875767));
#40723=CARTESIAN_POINT('Ctrl Pts',(22.5137443923812,0.482092168510832,3.61110849992699));
#40724=CARTESIAN_POINT('Ctrl Pts',(22.5376023104126,0.609484835267769,3.88964730767638));
#40725=CARTESIAN_POINT('Ctrl Pts',(22.561460228444,0.587841786482003,4.19517031382209));
#40726=CARTESIAN_POINT('Ctrl Pts',(22.5853181464754,0.422455543015367,4.45296893898932));
#40727=CARTESIAN_POINT('Ctrl Pts',(22.6091760645069,0.153767157666155,4.60000417439789));
#40728=CARTESIAN_POINT('Ctrl Pts',(22.6330339825383,-0.152521006364708,
4.60032232020799));
#40729=CARTESIAN_POINT('Ctrl Pts',(22.6568919005697,-0.421514535902825,
4.45384478734481));
#40730=CARTESIAN_POINT('Ctrl Pts',(22.6807498186011,-0.587434568575047,
4.19639082134502));
#40731=CARTESIAN_POINT('Ctrl Pts',(22.7046077366325,-0.60971407867596,3.89091209973551));
#40732=CARTESIAN_POINT('Ctrl Pts',(22.728465654664,-0.482895786937606,3.61211183522625));
#40733=CARTESIAN_POINT('Ctrl Pts',(22.7523235726954,-0.23800784887647,3.4281541921173));
#40734=CARTESIAN_POINT('Ctrl Pts',(22.7761814907268,0.0651013135850054,
3.38404091701771));
#40735=CARTESIAN_POINT('Ctrl Pts',(22.8000394087582,0.352249768808992,3.49052260401466));
#40736=CARTESIAN_POINT('Ctrl Pts',(22.8238973267896,0.553345940411564,3.72163220123786));
#40737=CARTESIAN_POINT('Ctrl Pts',(22.8398026054772,0.597082876783669,3.92101540361374));
#40738=CARTESIAN_POINT('Ctrl Pts',(22.847755244821,0.593766187829899,4.01991291515446));
#40739=CARTESIAN_POINT('',(22.8,0.337479661717902,3.51106003648017));
#40740=CARTESIAN_POINT('Ctrl Pts',(22.8,0.337504360408405,3.51101527402275));
#40741=CARTESIAN_POINT('Ctrl Pts',(22.8,0.337610992569967,3.51114843896934));
#40742=CARTESIAN_POINT('Ctrl Pts',(22.8,0.337717562131928,3.51128164981369));
#40743=CARTESIAN_POINT('Ctrl Pts',(22.8,0.337824069051012,3.51141490653789));
#40744=CARTESIAN_POINT('Ctrl Pts',(22.8,0.354145371784291,3.53183539523119));
#40745=CARTESIAN_POINT('Ctrl Pts',(22.8,0.368999739942303,3.55333386321799));
#40746=CARTESIAN_POINT('Ctrl Pts',(22.8,0.382262544471458,3.57576050230915));
#40747=CARTESIAN_POINT('Ctrl Pts',(22.8,0.395177725624396,3.59759933027929));
#40748=CARTESIAN_POINT('Ctrl Pts',(22.8,0.406583379369087,3.62031953557487));
#40749=CARTESIAN_POINT('Ctrl Pts',(22.8,0.416319965152677,3.64376476659274));
#40750=CARTESIAN_POINT('Ctrl Pts',(22.8,0.420499854003763,3.65382973822867));
#40751=CARTESIAN_POINT('Ctrl Pts',(22.8,0.424371599987778,3.66402799385056));
#40752=CARTESIAN_POINT('Ctrl Pts',(22.8,0.42792023461967,3.67434527679585));
#40753=CARTESIAN_POINT('Ctrl Pts',(22.8,0.430015882150509,3.68043815216119));
#40754=CARTESIAN_POINT('Ctrl Pts',(22.8,0.431995626466768,3.68656321156818));
#40755=CARTESIAN_POINT('Ctrl Pts',(22.8,0.433857425300493,3.69271766785326));
#40756=CARTESIAN_POINT('Ctrl Pts',(22.8,0.440667704273582,3.71523007009016));
#40757=CARTESIAN_POINT('Ctrl Pts',(22.8,0.445903532435623,3.73813926926309));
#40758=CARTESIAN_POINT('Ctrl Pts',(22.8,0.449441836754149,3.76130640751661));
#40759=CARTESIAN_POINT('Ctrl Pts',(22.8,0.450038513826676,3.76521316594877));
#40760=CARTESIAN_POINT('Ctrl Pts',(22.8,0.450586822418701,3.76912718643627));
#40761=CARTESIAN_POINT('Ctrl Pts',(22.8,0.451086059471329,3.77304770583064));
#40762=CARTESIAN_POINT('Ctrl Pts',(22.8,0.453684096906641,3.79345015011803));
#40763=CARTESIAN_POINT('Ctrl Pts',(22.8,0.454954433743694,3.81403106227893));
#40764=CARTESIAN_POINT('Ctrl Pts',(22.8,0.45484641916779,3.83463783350426));
#40765=CARTESIAN_POINT('Ctrl Pts',(22.8,0.454808390965019,3.84189276616533));
#40766=CARTESIAN_POINT('Ctrl Pts',(22.8,0.454599381710613,3.84915061719132));
#40767=CARTESIAN_POINT('Ctrl Pts',(22.8,0.454216814112443,3.8564037154462));
#40768=CARTESIAN_POINT('Ctrl Pts',(22.8,0.453866695925276,3.86304160538904));
#40769=CARTESIAN_POINT('Ctrl Pts',(22.8,0.453371644107099,3.86966645154658));
#40770=CARTESIAN_POINT('Ctrl Pts',(22.8,0.452731182295137,3.87626933737115));
#40771=CARTESIAN_POINT('Ctrl Pts',(22.8,0.450713457978438,3.89707120727158));
#40772=CARTESIAN_POINT('Ctrl Pts',(22.8,0.447253508643,3.9176725514372));
#40773=CARTESIAN_POINT('Ctrl Pts',(22.8,0.442312061254715,3.9379035771693));
#40774=CARTESIAN_POINT('Ctrl Pts',(22.8,0.437564183511961,3.95734209977996));
#40775=CARTESIAN_POINT('Ctrl Pts',(22.8,0.431447509288203,3.97643919003209));
#40776=CARTESIAN_POINT('Ctrl Pts',(22.8,0.423915075143768,3.9949978423605));
#40777=CARTESIAN_POINT('Ctrl Pts',(22.8,0.421325190817866,4.00137888225459));
#40778=CARTESIAN_POINT('Ctrl Pts',(22.8,0.418567902041021,4.00769582483512));
#40779=CARTESIAN_POINT('Ctrl Pts',(22.8,0.415641328671541,4.01393920819689));
#40780=CARTESIAN_POINT('Ctrl Pts',(22.6211545887425,-1.51173456864708E-7,
4.59404872180247));
#40781=CARTESIAN_POINT('Ctrl Pts',(22.6251143866744,-0.0492822808754852,
4.59404929162283));
#40782=CARTESIAN_POINT('Ctrl Pts',(22.6290741846063,-0.0985642856931001,
4.58798571459226));
#40783=CARTESIAN_POINT('Ctrl Pts',(22.6330339825383,-0.14630523394925,4.57585637376244));
#40784=CARTESIAN_POINT('Ctrl Pts',(22.6409866218821,-0.242185516210759,
4.55149647592026));
#40785=CARTESIAN_POINT('Ctrl Pts',(22.6489392612259,-0.331850026056775,
4.50267063163255));
#40786=CARTESIAN_POINT('Ctrl Pts',(22.6568919005697,-0.404335619758509,
4.43534871515538));
#40787=CARTESIAN_POINT('Ctrl Pts',(22.6648445399135,-0.476821213460227,
4.36802679867822));
#40788=CARTESIAN_POINT('Ctrl Pts',(22.6727971792573,-0.532127891017642,
4.28220881001161));
#40789=CARTESIAN_POINT('Ctrl Pts',(22.6807498186011,-0.563494481479829,
4.18838669541007));
#40790=CARTESIAN_POINT('Ctrl Pts',(22.6887024579449,-0.594861071942019,
4.09456458080851));
#40791=CARTESIAN_POINT('Ctrl Pts',(22.6966550972887,-0.602287575308989,
3.99273834027202));
#40792=CARTESIAN_POINT('Ctrl Pts',(22.7046077366325,-0.584864445036083,
3.89535850925222));
#40793=CARTESIAN_POINT('Ctrl Pts',(22.7125603759763,-0.567441314763176,
3.79797867823242));
#40794=CARTESIAN_POINT('Ctrl Pts',(22.7205130153201,-0.525168550850394,
3.70504525672934));
#40795=CARTESIAN_POINT('Ctrl Pts',(22.7284656546639,-0.463217512550482,
3.62791893879298));
#40796=CARTESIAN_POINT('Ctrl Pts',(22.7364182940078,-0.401266474250563,
3.5507926208566));
#40797=CARTESIAN_POINT('Ctrl Pts',(22.7443709333516,-0.319637161563486,
3.48947340648693));
#40798=CARTESIAN_POINT('Ctrl Pts',(22.7523235726954,-0.228304311476372,
3.45146158678551));
#40799=CARTESIAN_POINT('Ctrl Pts',(22.7602762120392,-0.136971461389268,
3.41344976708409));
#40800=CARTESIAN_POINT('Ctrl Pts',(22.768228851383,-0.0359350739021178,
3.3987453420509));
#40801=CARTESIAN_POINT('Ctrl Pts',(22.7761814907268,0.062441195712126,3.40914007736714));
#40802=CARTESIAN_POINT('Ctrl Pts',(22.7841209938178,0.160654966376612,3.41951764255099));
#40803=CARTESIAN_POINT('Ctrl Pts',(22.7920604969089,0.256217399931083,3.45491151845628));
#40804=CARTESIAN_POINT('Ctrl Pts',(22.8,0.337504360408238,3.51101527402264));
#40805=CARTESIAN_POINT('Ctrl Pts',(4.,-0.219914231356244,4.35301468169996));
#40806=CARTESIAN_POINT('Ctrl Pts',(4.00793950309107,-0.278596966840389,
4.31645650682028));
#40807=CARTESIAN_POINT('Ctrl Pts',(4.02383164552594,-0.377405665439666,
4.21337674819164));
#40808=CARTESIAN_POINT('Ctrl Pts',(4.04767642730463,-0.433534992178268,
4.00656196868444));
#40809=CARTESIAN_POINT('Ctrl Pts',(4.07153434533603,-0.383670022685343,
3.79803920418254));
#40810=CARTESIAN_POINT('Ctrl Pts',(4.09539226336747,-0.239994733226421,
3.63889579340969));
#40811=CARTESIAN_POINT('Ctrl Pts',(4.11925018139887,-0.0376302499649443,
3.56805514133307));
#40812=CARTESIAN_POINT('Ctrl Pts',(4.1431080994303,0.173933765839147,3.60283521426327));
#40813=CARTESIAN_POINT('Ctrl Pts',(4.16696601746172,0.342967344134064,3.73473372141871));
#40814=CARTESIAN_POINT('Ctrl Pts',(4.19082393549313,0.428135478754777,3.93149662217858));
#40815=CARTESIAN_POINT('Ctrl Pts',(4.21468185352456,0.40861313688017,4.1450106963618));
#40816=CARTESIAN_POINT('Ctrl Pts',(4.23853977155597,0.289173588337559,4.32306558264197));
#40817=CARTESIAN_POINT('Ctrl Pts',(4.25811226835493,0.13317859508208,4.40432939198872));
#40818=CARTESIAN_POINT('Ctrl Pts',(4.26973212581007,0.0319512750557707,
4.41584666103033));
#40819=CARTESIAN_POINT('Ctrl Pts',(4.2733993439214,2.51014653359152E-6,
4.41583996132385));
#40820=CARTESIAN_POINT('Origin',(3.42660065607856,0.,4.));
#40821=CARTESIAN_POINT('Ctrl Pts',(4.,-0.219892372743211,3.64701365460636));
#40822=CARTESIAN_POINT('Ctrl Pts',(4.00795263934381,-0.161099076858729,
3.61038844940468));
#40823=CARTESIAN_POINT('Ctrl Pts',(4.02385791803142,-0.0249198690254346,
3.56711791692558));
#40824=CARTESIAN_POINT('Ctrl Pts',(4.04771583606284,0.185569069288609,3.60813812632505));
#40825=CARTESIAN_POINT('Ctrl Pts',(4.07157375409426,0.350624105231944,3.74494568050885));
#40826=CARTESIAN_POINT('Ctrl Pts',(4.09543167212568,0.429971014252744,3.94413788601839));
#40827=CARTESIAN_POINT('Ctrl Pts',(4.1192895901571,0.40416308778273,4.15698104289539));
#40828=CARTESIAN_POINT('Ctrl Pts',(4.14314750818851,0.279534313346206,4.3314427366163));
#40829=CARTESIAN_POINT('Ctrl Pts',(4.16225119682902,0.125004509401131,4.40624063703925));
#40830=CARTESIAN_POINT('Ctrl Pts',(4.1734022461257,0.0278694809177792,4.41585864517498));
#40831=CARTESIAN_POINT('Ctrl Pts',(4.17660065607858,5.88453344126799E-6,
4.41584444980552));
#40832=CARTESIAN_POINT('Ctrl Pts',(3.95224475517896,-0.314128184302177,
3.49573985500833));
#40833=CARTESIAN_POINT('Ctrl Pts',(3.96019739452277,-0.230138771413741,
3.44341876234755));
#40834=CARTESIAN_POINT('Ctrl Pts',(3.97610267321038,-0.0355993848822847,
3.38160445914153));
#40835=CARTESIAN_POINT('Ctrl Pts',(3.9999605912418,0.265095483172694,3.44020405374152));
#40836=CARTESIAN_POINT('Ctrl Pts',(4.02381850927322,0.500885556761892,3.63564106712445));
#40837=CARTESIAN_POINT('Ctrl Pts',(4.04767642730465,0.614236921112272,3.92019793948569));
#40838=CARTESIAN_POINT('Ctrl Pts',(4.07153434533605,0.577368897990231,4.22425593648149));
#40839=CARTESIAN_POINT('Ctrl Pts',(4.09539226336749,0.399329932212592,4.47348393104611));
#40840=CARTESIAN_POINT('Ctrl Pts',(4.11925018139889,0.123637843932736,4.60692867011962));
#40841=CARTESIAN_POINT('Ctrl Pts',(4.14310809943032,-0.182283847264271,
4.59196468982869));
#40842=CARTESIAN_POINT('Ctrl Pts',(4.16696601746173,-0.443633876576525,
4.43224822622665));
#40843=CARTESIAN_POINT('Ctrl Pts',(4.19082393549315,-0.596502436238336,
4.16683582239239));
#40844=CARTESIAN_POINT('Ctrl Pts',(4.21468185352458,-0.603510379797736,
3.86062723727387));
#40845=CARTESIAN_POINT('Ctrl Pts',(4.23853977155598,-0.462943343075553,
3.58849923641164));
#40846=CARTESIAN_POINT('Ctrl Pts',(4.26239768958742,-0.209174182705692,
3.41699430327496));
#40847=CARTESIAN_POINT('Ctrl Pts',(4.28625560761882,0.0957438341235747,
3.38805018506757));
#40848=CARTESIAN_POINT('Ctrl Pts',(4.31011352565025,0.377249837899377,3.50874444390425));
#40849=CARTESIAN_POINT('Ctrl Pts',(4.33397144368167,0.566508000142931,3.7495640793295));
#40850=CARTESIAN_POINT('Ctrl Pts',(4.35782936171309,0.617239514437223,4.05162211295782));
#40851=CARTESIAN_POINT('Ctrl Pts',(4.3816872797445,0.517039159770137,4.34105713706075));
#40852=CARTESIAN_POINT('Ctrl Pts',(4.40554519777592,0.290408643717306,4.54709439922074));
#40853=CARTESIAN_POINT('Ctrl Pts',(4.42940311580735,-0.00723469473045889,
4.61935217913086));
#40854=CARTESIAN_POINT('Ctrl Pts',(4.45326103383876,-0.303108954077165,
4.54016147994594));
#40855=CARTESIAN_POINT('Ctrl Pts',(4.47711895187019,-0.524864817190473,
4.3288865854667));
#40856=CARTESIAN_POINT('Ctrl Pts',(4.5009768699016,-0.618276935702851,4.03718996201469));
#40857=CARTESIAN_POINT('Ctrl Pts',(4.52483478793302,-0.560503501787052,
3.7363993798876));
#40858=CARTESIAN_POINT('Ctrl Pts',(4.54869270596444,-0.365671693940747,
3.50006632967672));
#40859=CARTESIAN_POINT('Ctrl Pts',(4.57255062399586,-0.0814231961944085,
3.38598067979976));
#40860=CARTESIAN_POINT('Ctrl Pts',(4.59640854202727,0.222735490926488,3.42203947925158));
#40861=CARTESIAN_POINT('Ctrl Pts',(4.6202664600587,0.472429283332598,3.59942536936051));
#40862=CARTESIAN_POINT('Ctrl Pts',(4.64412437809011,0.606601247243452,3.87476266809168));
#40863=CARTESIAN_POINT('Ctrl Pts',(4.66798229612153,0.592442682719785,4.18072390587243));
#40864=CARTESIAN_POINT('Ctrl Pts',(4.69184021415295,0.433415744455024,4.44249322584619));
#40865=CARTESIAN_POINT('Ctrl Pts',(4.71569813218437,0.168406850663934,4.59606089882753));
#40866=CARTESIAN_POINT('Ctrl Pts',(4.7395560502158,-0.1377821054254,4.60387544567241));
#40867=CARTESIAN_POINT('Ctrl Pts',(4.7634139682472,-0.410279583628813,4.46402599681362));
#40868=CARTESIAN_POINT('Ctrl Pts',(4.78727188627863,-0.582452527843622,
4.21070955191949));
#40869=CARTESIAN_POINT('Ctrl Pts',(4.81112980431005,-0.612199963312297,
3.9058688819681));
#40870=CARTESIAN_POINT('Ctrl Pts',(4.83498772234147,-0.492247831758966,
3.62404583445569));
#40871=CARTESIAN_POINT('Ctrl Pts',(4.85884564037289,-0.251927696778831,
3.4341538212047));
#40872=CARTESIAN_POINT('Ctrl Pts',(4.88270355840431,0.0499956224363984,
3.38262661200963));
#40873=CARTESIAN_POINT('Ctrl Pts',(4.90656147643572,0.339693650112522,3.48206401309162));
#40874=CARTESIAN_POINT('Ctrl Pts',(4.93041939446714,0.546327327266884,3.70815087126575));
#40875=CARTESIAN_POINT('Ctrl Pts',(4.95427731249857,0.619369091246891,4.00560279122603));
#40876=CARTESIAN_POINT('Ctrl Pts',(4.97813523052998,0.540958241141728,4.3016846761146));
#40877=CARTESIAN_POINT('Ctrl Pts',(5.00199314856141,0.330268365670778,4.52399643996756));
#40878=CARTESIAN_POINT('Ctrl Pts',(5.02585106659282,0.0388188784636707,
4.61817680087201));
#40879=CARTESIAN_POINT('Ctrl Pts',(5.04970898462424,-0.262122881932824,
4.56119609516527));
#40880=CARTESIAN_POINT('Ctrl Pts',(5.07356690265566,-0.498968457612796,
4.36698765751594));
#40881=CARTESIAN_POINT('Ctrl Pts',(5.09742482068708,-0.613802653778546,
4.08304074106085));
#40882=CARTESIAN_POINT('Ctrl Pts',(5.12128273871849,-0.578545381446849,
3.77878810143205));
#40883=CARTESIAN_POINT('Ctrl Pts',(5.14514065674992,-0.40181800409162,3.52862779669421));
#40884=CARTESIAN_POINT('Ctrl Pts',(5.16899857478133,-0.126835179433317,
3.39373083558568));
#40885=CARTESIAN_POINT('Ctrl Pts',(5.19285649281276,0.179162301517353,3.4070831996169));
#40886=CARTESIAN_POINT('Ctrl Pts',(5.21671441084417,0.441349719463922,3.56541987207117));
#40887=CARTESIAN_POINT('Ctrl Pts',(5.24057232887559,0.595615108876583,3.83002322352904));
#40888=CARTESIAN_POINT('Ctrl Pts',(5.26443024690701,0.604236379939102,4.13619052690848));
#40889=CARTESIAN_POINT('Ctrl Pts',(5.28828816493843,0.465105397037983,4.40905553670335));
#40890=CARTESIAN_POINT('Ctrl Pts',(5.31214608296985,0.21224347534444,4.58189532532512));
#40891=CARTESIAN_POINT('Ctrl Pts',(5.33600400100126,-0.0925177574670201,
4.61244585639451));
#40892=CARTESIAN_POINT('Ctrl Pts',(5.35986191903269,-0.37465587844466,4.49323669288525));
#40893=CARTESIAN_POINT('Ctrl Pts',(5.3837198370641,-0.565180431721392,4.25341772246777));
#40894=CARTESIAN_POINT('Ctrl Pts',(5.40757775509553,-0.617502974236318,
3.95163121594683));
#40895=CARTESIAN_POINT('Ctrl Pts',(5.43143567312694,-0.518829219107294,
3.66167219466597));
#40896=CARTESIAN_POINT('Ctrl Pts',(5.45529359115837,-0.293287587282116,
3.45444353765392));
#40897=CARTESIAN_POINT('Ctrl Pts',(5.47915150918978,0.00397084862654925,
3.38061829634467));
#40898=CARTESIAN_POINT('Ctrl Pts',(5.50300942722121,0.300258303883157,3.45824875319892));
#40899=CARTESIAN_POINT('Ctrl Pts',(5.52686734525262,0.523124424966688,3.66835214690199));
#40900=CARTESIAN_POINT('Ctrl Pts',(5.55072526328404,0.618072374525773,3.95955247459688));
#40901=CARTESIAN_POINT('Ctrl Pts',(5.57458318131546,0.561884792553919,4.26064332401524));
#40902=CARTESIAN_POINT('Ctrl Pts',(5.59844109934688,0.368301073379394,4.49799978094171));
#40903=CARTESIAN_POINT('Ctrl Pts',(5.62229901737829,0.0846577094226282,
4.61358172616469));
#40904=CARTESIAN_POINT('Ctrl Pts',(5.64615693540972,-0.219686770477705,
4.57912622575047));
#40905=CARTESIAN_POINT('Ctrl Pts',(5.67001485344113,-0.470311850924231,
4.40305858798173));
#40906=CARTESIAN_POINT('Ctrl Pts',(5.69387277147256,-0.605932872639677,
4.12843214650112));
#40907=CARTESIAN_POINT('Ctrl Pts',(5.71773068950397,-0.593386801983745,
3.82240054650545));
#40908=CARTESIAN_POINT('Ctrl Pts',(5.74158860753539,-0.435741494202748,
3.55979685111874));
#40909=CARTESIAN_POINT('Ctrl Pts',(5.76544652556682,-0.171545522688555,
3.40483481554927));
#40910=CARTESIAN_POINT('Ctrl Pts',(5.78930444359822,0.134598003740687,3.39540688139736));
#40911=CARTESIAN_POINT('Ctrl Pts',(5.81316236162965,0.407828648458881,3.53381843004554));
#40912=CARTESIAN_POINT('Ctrl Pts',(5.83702027966106,0.58133408605803,3.78622407765735));
#40913=CARTESIAN_POINT('Ctrl Pts',(5.86087819769249,0.612687492198482,4.09090374899912));
#40914=CARTESIAN_POINT('Ctrl Pts',(5.8847361157239,0.494222140250734,4.3733550009975));
#40915=CARTESIAN_POINT('Ctrl Pts',(5.90859403375532,0.254905969192102,4.56451074097759));
#40916=CARTESIAN_POINT('Ctrl Pts',(5.93245195178675,-0.0467415727364197,
4.61762831145024));
#40917=CARTESIAN_POINT('Ctrl Pts',(5.95630986981815,-0.336959681931401,
4.51971877801409));
#40918=CARTESIAN_POINT('Ctrl Pts',(5.98016778784959,-0.544781677596122,
4.29472414464893));
#40919=CARTESIAN_POINT('Ctrl Pts',(6.00402570588099,-0.61939026621187,3.99766086682344));
#40920=CARTESIAN_POINT('Ctrl Pts',(6.02788362391242,-0.542540019317823,
3.70117063377655));
#40921=CARTESIAN_POINT('Ctrl Pts',(6.05174154194384,-0.333025929677459,
3.47775031355921));
#40922=CARTESIAN_POINT('Ctrl Pts',(6.07559945997526,-0.042074208138152,
3.38203805739984));
#40923=CARTESIAN_POINT('Ctrl Pts',(6.09945737800668,0.259158778028439,3.43742717299816));
#40924=CARTESIAN_POINT('Ctrl Pts',(6.12331529603809,0.497033648893269,3.63039418124561));
#40925=CARTESIAN_POINT('Ctrl Pts',(6.14717321406952,0.613345206175343,3.91371436613889));
#40926=CARTESIAN_POINT('Ctrl Pts',(6.17103113210093,0.579724447951105,4.21818191418763));
#40927=CARTESIAN_POINT('Ctrl Pts',(6.19488905013236,0.40425597056565,4.46920707734689));
#40928=CARTESIAN_POINT('Ctrl Pts',(6.21874696816377,0.13010450107023,4.60567007851858));
#40929=CARTESIAN_POINT('Ctrl Pts',(6.24260488619519,-0.176179318911185,
4.59370602015056));
#40930=CARTESIAN_POINT('Ctrl Pts',(6.26646280422661,-0.438782409775579,
4.43717629804221));
#40931=CARTESIAN_POINT('Ctrl Pts',(6.29032072225803,-0.595217424383659,
4.17259489198797));
#40932=CARTESIAN_POINT('Ctrl Pts',(6.31417864028945,-0.604035436411749,
3.86794272465182));
#40933=CARTESIAN_POINT('Ctrl Pts',(6.34598919766468,-0.423477061217623,
3.4998212904071));
#40934=CARTESIAN_POINT('Ctrl Pts',(6.3857523943837,0.100470573235224,3.30464850830547));
#40935=CARTESIAN_POINT('Ctrl Pts',(6.43346823044655,0.640013163212275,3.70919899990029));
#40936=CARTESIAN_POINT('Ctrl Pts',(6.48118406650937,0.590335835129396,4.3806576914582));
#40937=CARTESIAN_POINT('Ctrl Pts',(6.52889990257223,-0.000686065451295705,
4.70262946694599));
#40938=CARTESIAN_POINT('Ctrl Pts',(6.57661573863505,-0.591483599613884,
4.37932465573422));
#40939=CARTESIAN_POINT('Ctrl Pts',(6.6243315746979,-0.638898060441451,3.70770201230499));
#40940=CARTESIAN_POINT('Ctrl Pts',(6.67204741076074,-0.0997162142428727,
3.30448953810453));
#40941=CARTESIAN_POINT('Ctrl Pts',(6.71976324682356,0.531096731682035,3.53998115137447));
#40942=CARTESIAN_POINT('Ctrl Pts',(6.76747908288643,0.674163513320998,4.19791190586338));
#40943=CARTESIAN_POINT('Ctrl Pts',(6.81519491894923,0.19815244237474,4.67409883091767));
#40944=CARTESIAN_POINT('Ctrl Pts',(6.86291075501209,-0.459834002450772,
4.53124951681343));
#40945=CARTESIAN_POINT('Ctrl Pts',(6.91062659107492,-0.695543074258338,
3.90054607923755));
#40946=CARTESIAN_POINT('Ctrl Pts',(6.95834242713776,-0.292526745343327,
3.36117245204842));
#40947=CARTESIAN_POINT('Ctrl Pts',(7.00605826320061,0.379122722467859,3.40844412700009));
#40948=CARTESIAN_POINT('Ctrl Pts',(7.05377409926343,0.702617257610868,3.99895059076549));
#40949=CARTESIAN_POINT('Ctrl Pts',(7.10148993532628,0.380887926283931,4.59042078110798));
#40950=CARTESIAN_POINT('Ctrl Pts',(7.14920577138911,-0.290616845661789,
4.63969846327979));
#40951=CARTESIAN_POINT('Ctrl Pts',(7.19692160745196,-0.695243592084394,
4.10153121423426));
#40952=CARTESIAN_POINT('Ctrl Pts',(7.24463744351478,-0.461417505508394,
3.47012628326466));
#40953=CARTESIAN_POINT('Ctrl Pts',(7.29235327957764,0.196135405489393,3.32531254251214));
#40954=CARTESIAN_POINT('Ctrl Pts',(7.34006911564046,0.673574140181709,3.80007467379138));
#40955=CARTESIAN_POINT('Ctrl Pts',(7.38778495170331,0.532459385890787,4.45843130921146));
#40956=CARTESIAN_POINT('Ctrl Pts',(7.43550078776614,-0.0976210197556089,
4.69580341906706));
#40957=CARTESIAN_POINT('Ctrl Pts',(7.48321662382899,-0.638054538563543,
4.29420854311633));
#40958=CARTESIAN_POINT('Ctrl Pts',(7.53093245989182,-0.592552758097988,
3.62243743491725));
#40959=CARTESIAN_POINT('Ctrl Pts',(7.57864829595465,-0.00290066162856385,
3.29738783984629));
#40960=CARTESIAN_POINT('Ctrl Pts',(7.6263641320175,0.589415156704478,3.61755780248734));
#40961=CARTESIAN_POINT('Ctrl Pts',(7.67407996808033,0.64046196749915,4.28893031975233));
#40962=CARTESIAN_POINT('Ctrl Pts',(7.72179580414318,0.103362698669259,4.69497367861456));
#40963=CARTESIAN_POINT('Ctrl Pts',(7.769511640206,-0.528656126737314,4.46281201486565));
#40964=CARTESIAN_POINT('Ctrl Pts',(7.81722747626886,-0.675201896567852,
3.80564295658466));
#40965=CARTESIAN_POINT('Ctrl Pts',(7.86494331233168,-0.201699375449268,
3.32695496184095));
#40966=CARTESIAN_POINT('Ctrl Pts',(7.91265914839452,0.457026785680635,3.46633458176699));
#40967=CARTESIAN_POINT('Ctrl Pts',(7.96037498445737,0.696058217263005,4.09578736675475));
#40968=CARTESIAN_POINT('Ctrl Pts',(8.0080908205202,0.295888677698302,4.63727713897333));
#40969=CARTESIAN_POINT('Ctrl Pts',(8.05580665658303,-0.375999987428149,
4.59354550870361));
#40970=CARTESIAN_POINT('Ctrl Pts',(8.10352249264589,-0.702602078596463,
4.00475190491975));
#40971=CARTESIAN_POINT('Ctrl Pts',(8.1512383287087,-0.383993870066737,3.41159455373064));
#40972=CARTESIAN_POINT('Ctrl Pts',(8.19895416477156,0.287241817850264,3.35877897763223));
#40973=CARTESIAN_POINT('Ctrl Pts',(8.24667000083438,0.694698924651979,3.89480653282778));
#40974=CARTESIAN_POINT('Ctrl Pts',(8.29438583689724,0.464203319628796,4.52743486753713));
#40975=CARTESIAN_POINT('Ctrl Pts',(8.34210167296006,-0.192577336495663,
4.67571164775853));
#40976=CARTESIAN_POINT('Ctrl Pts',(8.3898175090229,-0.672511261332963,4.20347202468314));
#40977=CARTESIAN_POINT('Ctrl Pts',(8.43753334508575,-0.534867746972347,
3.54438091052171));
#40978=CARTESIAN_POINT('Ctrl Pts',(8.48524918114857,0.0939530494311211,
3.303691816829));
#40979=CARTESIAN_POINT('Ctrl Pts',(8.53296501721143,0.636495314888509,3.70243324182078));
#40980=CARTESIAN_POINT('Ctrl Pts',(8.58068085327425,0.594534138944492,4.37443479950165));
#40981=CARTESIAN_POINT('Ctrl Pts',(8.6283966893371,0.00660311512414562,
4.7025871193802));
#40982=CARTESIAN_POINT('Ctrl Pts',(8.67611252539993,-0.58739165091669,4.3855428768395));
#40983=CARTESIAN_POINT('Ctrl Pts',(8.72382836146277,-0.64197562573843,3.71444867815739));
#40984=CARTESIAN_POINT('Ctrl Pts',(8.77154419752561,-0.107023505379864,
3.30558065209521));
#40985=CARTESIAN_POINT('Ctrl Pts',(8.81926003358845,0.526209946737336,3.53440859822909));
#40986=CARTESIAN_POINT('Ctrl Pts',(8.86697586965128,0.676216707984864,4.19079629265377));
#40987=CARTESIAN_POINT('Ctrl Pts',(8.91469170571413,0.20524326135842,4.67197281575615));
#40988=CARTESIAN_POINT('Ctrl Pts',(8.96240754177695,-0.45420823024697,4.53606636251889));
#40989=CARTESIAN_POINT('Ctrl Pts',(9.0101233778398,-0.69655331512461,3.90788192013928));
#40990=CARTESIAN_POINT('Ctrl Pts',(9.05783921390263,-0.299242772872918,
3.36429092791464));
#40991=CARTESIAN_POINT('Ctrl Pts',(9.10555504996548,0.37286701214988,3.40448135822736));
#40992=CARTESIAN_POINT('Ctrl Pts',(9.15327088602831,0.702567282619003,3.99154572051203));
#40993=CARTESIAN_POINT('Ctrl Pts',(9.20098672209116,0.387089207071907,4.58637377773631));
#40994=CARTESIAN_POINT('Ctrl Pts',(9.24870255815397,-0.28385884346236,4.64272577234503));
#40995=CARTESIAN_POINT('Ctrl Pts',(9.29641839421684,-0.694134950315416,
4.10885280060212));
#40996=CARTESIAN_POINT('Ctrl Pts',(9.34413423027966,-0.46697625165475,3.47501862715065));
#40997=CARTESIAN_POINT('Ctrl Pts',(9.39185006634251,0.189013924253689,3.32328292626348));
#40998=CARTESIAN_POINT('Ctrl Pts',(9.43956590240535,0.671429705166911,3.79298692681914));
#40999=CARTESIAN_POINT('Ctrl Pts',(9.48728173846818,0.537261256551386,4.45279421778236));
#41000=CARTESIAN_POINT('Ctrl Pts',(9.53499757453101,-0.090282470782305,
4.69679361142145));
#41001=CARTESIAN_POINT('Ctrl Pts',(9.58271341059386,-0.634918416022234,
4.30091671014441));
#41002=CARTESIAN_POINT('Ctrl Pts',(9.63042924665669,-0.596499010353368,
3.62870336374299));
#41003=CARTESIAN_POINT('Ctrl Pts',(9.67814508271953,-0.0103053851599677,
3.29745743154951));
#41004=CARTESIAN_POINT('Ctrl Pts',(9.72586091878236,0.585351833794561,3.61136714997101));
#41005=CARTESIAN_POINT('Ctrl Pts',(9.77357675484522,0.643471456979869,4.28216439445919));
#41006=CARTESIAN_POINT('Ctrl Pts',(9.82129259090803,0.110681340139534,4.69384573385819));
#41007=CARTESIAN_POINT('Ctrl Pts',(9.8690084269709,-0.523749154402255,4.46835785966634));
#41008=CARTESIAN_POINT('Ctrl Pts',(9.91672426303372,-0.677212741539845,
3.81276975633088));
#41009=CARTESIAN_POINT('Ctrl Pts',(9.96444009909655,-0.208781447863971,
3.32911806666439));
#41010=CARTESIAN_POINT('Ctrl Pts',(10.0121559351594,0.451377061900895,3.4615475792254));
#41011=CARTESIAN_POINT('Ctrl Pts',(10.0598717712222,0.697029070393332,4.08844623493918));
#41012=CARTESIAN_POINT('Ctrl Pts',(10.1075876072851,0.302588558372737,4.63412335218805));
#41013=CARTESIAN_POINT('Ctrl Pts',(10.1553034433479,-0.369723682724971,
4.5974752378807));
#41014=CARTESIAN_POINT('Ctrl Pts',(10.2030192794108,-0.702512977046242,
4.01215641928927));
#41015=CARTESIAN_POINT('Ctrl Pts',(10.2507351154736,-0.390173794994359,
3.41567417381395));
#41016=CARTESIAN_POINT('Ctrl Pts',(10.2984509515364,0.280467986596366,3.3557873255338));
#41017=CARTESIAN_POINT('Ctrl Pts',(10.3461667875993,0.693551700540965,3.8874908887021));
#41018=CARTESIAN_POINT('Ctrl Pts',(10.3938826236621,0.469736216214169,4.52251329995044));
#41019=CARTESIAN_POINT('Ctrl Pts',(10.441598459725,-0.185445263282835,4.67770370795377));
#41020=CARTESIAN_POINT('Ctrl Pts',(10.4893142957878,-0.670329504065059,
4.21054837313121));
#41021=CARTESIAN_POINT('Ctrl Pts',(10.5370301318506,-0.539639846919137,
3.55004322755915));
#41022=CARTESIAN_POINT('Ctrl Pts',(10.5847459679134,0.0866093850789692,
3.30274030959437));
#41023=CARTESIAN_POINT('Ctrl Pts',(10.6324618039763,0.633323886102378,3.69574169404847));
#41024=CARTESIAN_POINT('Ctrl Pts',(10.6801776400391,0.598447317577389,4.36814816247366));
#41025=CARTESIAN_POINT('Ctrl Pts',(10.727893476102,0.0140073690254923,4.70247850861168));
#41026=CARTESIAN_POINT('Ctrl Pts',(10.7756093121648,-0.583295762033595,
4.39171203127037));
#41027=CARTESIAN_POINT('Ctrl Pts',(10.8233251482277,-0.644949419658282,
3.72123036834915));
#41028=CARTESIAN_POINT('Ctrl Pts',(10.8710409842905,-0.114336101388361,
3.30674714759503));
#41029=CARTESIAN_POINT('Ctrl Pts',(10.9187568203533,0.521273818073547,3.52888868827067));
#41030=CARTESIAN_POINT('Ctrl Pts',(10.9664726564162,0.678189969569843,4.18365899548663));
#41031=CARTESIAN_POINT('Ctrl Pts',(11.014188492479,0.212313836716152,4.66977242119035));
#41032=CARTESIAN_POINT('Ctrl Pts',(11.0619043285418,-0.44853335926228,4.54082352674158));
#41033=CARTESIAN_POINT('Ctrl Pts',(11.1096201646047,-0.697485469857315,
3.91522806604643));
#41034=CARTESIAN_POINT('Ctrl Pts',(11.1573360006675,-0.305925941288932,
3.36747997668469));
#41035=CARTESIAN_POINT('Ctrl Pts',(11.2050518367303,0.36657008644075,3.40058475730499));
#41036=CARTESIAN_POINT('Ctrl Pts',(11.2527676727932,0.702439163386103,3.98414177848112));
#41037=CARTESIAN_POINT('Ctrl Pts',(11.300483508856,0.393247548178179,4.58226164848818));
#41038=CARTESIAN_POINT('Ctrl Pts',(11.3481993449189,-0.277069341413063,
4.64568168744144));
#41039=CARTESIAN_POINT('Ctrl Pts',(11.3959151809817,-0.692949191524882,
4.11616229772746));
#41040=CARTESIAN_POINT('Ctrl Pts',(11.4436310170446,-0.47248313666557,3.47996928262364));
#41041=CARTESIAN_POINT('Ctrl Pts',(11.4913468531074,0.181871452681271,3.32132847698764));
#41042=CARTESIAN_POINT('Ctrl Pts',(11.5390626891702,0.669210688578896,3.78592217363756));
#41043=CARTESIAN_POINT('Ctrl Pts',(11.586778525233,0.54200345202451,4.44710683224685));
#41044=CARTESIAN_POINT('Ctrl Pts',(11.6344943612959,-0.082933894319074,
4.69770640718098));
#41045=CARTESIAN_POINT('Ctrl Pts',(11.6822101973587,-0.631711769407458,
4.30759145280778));
#41046=CARTESIAN_POINT('Ctrl Pts',(11.7299260334216,-0.600379006513997,
3.63501053441836));
#41047=CARTESIAN_POINT('Ctrl Pts',(11.7776418694844,-0.0177089639202829,
3.29760505835735));
#41048=CARTESIAN_POINT('Ctrl Pts',(11.8253577055473,0.581223492728864,3.60521966494218));
#41049=CARTESIAN_POINT('Ctrl Pts',(11.8730735416101,0.646409472732109,4.27536712768685));
#41050=CARTESIAN_POINT('Ctrl Pts',(11.9207893776729,0.11798768763725,4.69264072000881));
#41051=CARTESIAN_POINT('Ctrl Pts',(11.9685052137358,-0.518784006488825,
4.4738516814993));
#41052=CARTESIAN_POINT('Ctrl Pts',(12.0162210497986,-0.679148364938221,
3.81991735272367));
#41053=CARTESIAN_POINT('Ctrl Pts',(12.0639368858614,-0.215840329824027,
3.33135568986959));
#41054=CARTESIAN_POINT('Ctrl Pts',(12.1116527219243,0.445677201297934,3.45682038542343));
#41055=CARTESIAN_POINT('Ctrl Pts',(12.1593685579871,0.697922500842799,4.08109527893561));
#41056=CARTESIAN_POINT('Ctrl Pts',(12.2070843940499,0.309254828945687,4.63089912998995));
#41057=CARTESIAN_POINT('Ctrl Pts',(12.2548002301128,-0.36340631086944,4.60133860234362));
#41058=CARTESIAN_POINT('Ctrl Pts',(12.3025160661756,-0.702345843688318,
4.0195595833814));
#41059=CARTESIAN_POINT('Ctrl Pts',(12.3502319022385,-0.396310381268302,
3.41981869803717));
#41060=CARTESIAN_POINT('Ctrl Pts',(12.3979477383013,0.273663002289436,3.35286722952223));
#41061=CARTESIAN_POINT('Ctrl Pts',(12.4456635743641,0.69232743999824,3.88018774155459));
#41062=CARTESIAN_POINT('Ctrl Pts',(12.493379410427,0.475216936729713,4.51753369406595));
#41063=CARTESIAN_POINT('Ctrl Pts',(12.5410952464898,-0.178292591690169,
4.67962049203707));
#41064=CARTESIAN_POINT('Ctrl Pts',(12.5888110825527,-0.66807328977682,4.21760133486514));
#41065=CARTESIAN_POINT('Ctrl Pts',(12.6365269186155,-0.544352006232531,
3.55575552365962));
#41066=CARTESIAN_POINT('Ctrl Pts',(12.6842427546784,0.0792561005673328,
3.3018662506574));
#41067=CARTESIAN_POINT('Ctrl Pts',(12.7319585907411,0.630082110704352,3.68908394184497));
#41068=CARTESIAN_POINT('Ctrl Pts',(12.779674426804,0.60229402352211,4.36182063329482));
#41069=CARTESIAN_POINT('Ctrl Pts',(12.8273902628668,0.0214100670547408,
4.70229186986395));
#41070=CARTESIAN_POINT('Ctrl Pts',(12.8751060989297,-0.579135083425219,
4.39783767618763));
#41071=CARTESIAN_POINT('Ctrl Pts',(12.9228219349925,-0.647851575657132,
3.7280430229487));
#41072=CARTESIAN_POINT('Ctrl Pts',(12.9705377710554,-0.121635997485283,
3.30799064633195));
#41073=CARTESIAN_POINT('Ctrl Pts',(13.0182536071182,0.516279788787698,3.52342110712114));
#41074=CARTESIAN_POINT('Ctrl Pts',(13.065969443181,0.68008790103128,4.17650129834983));
#41075=CARTESIAN_POINT('Ctrl Pts',(13.1136852792439,0.219360829260397,4.66749763148232));
#41076=CARTESIAN_POINT('Ctrl Pts',(13.1614011153067,-0.44280866732052,4.54552061885334));
#41077=CARTESIAN_POINT('Ctrl Pts',(13.2091169513696,-0.698340151213866,
3.92258362801769));
#41078=CARTESIAN_POINT('Ctrl Pts',(13.2568327874324,-0.31257512890311,3.37073928277739));
#41079=CARTESIAN_POINT('Ctrl Pts',(13.3045486234952,0.36023244386594,3.39675473658331));
#41080=CARTESIAN_POINT('Ctrl Pts',(13.3522644595581,0.702233020544282,3.97673959790624));
#41081=CARTESIAN_POINT('Ctrl Pts',(13.3999802956209,0.39936220921291,4.57808484437918));
#41082=CARTESIAN_POINT('Ctrl Pts',(13.4476961316837,-0.270249063816132,
4.64856588328003));
#41083=CARTESIAN_POINT('Ctrl Pts',(13.4954119677466,-0.691686463226468,
4.123458892096));
#41084=CARTESIAN_POINT('Ctrl Pts',(13.5431278038094,-0.47793754049168,3.48497770064095));
#41085=CARTESIAN_POINT('Ctrl Pts',(13.5908436398723,0.174708779690948,3.31944941132403));
#41086=CARTESIAN_POINT('Ctrl Pts',(13.6385594759351,0.666917339243262,3.77888119920505));
#41087=CARTESIAN_POINT('Ctrl Pts',(13.6862753119979,0.54668544432619,4.44136978420615));
#41088=CARTESIAN_POINT('Ctrl Pts',(13.7339911480608,-0.075576105952426,
4.69854170502367));
#41089=CARTESIAN_POINT('Ctrl Pts',(13.7817069841236,-0.62843495524706,4.31423202967224));
#41090=CARTESIAN_POINT('Ctrl Pts',(13.8294228201864,-0.604192315423611,
3.64135824639153));
#41091=CARTESIAN_POINT('Ctrl Pts',(13.8771386562493,-0.025110575652917,
3.29783070386218));
#41092=CARTESIAN_POINT('Ctrl Pts',(13.9248544923121,0.577030592115723,3.59911603023956));
#41093=CARTESIAN_POINT('Ctrl Pts',(13.972570328375,0.649275688387581,4.26853927444071));
#41094=CARTESIAN_POINT('Ctrl Pts',(14.0202861644378,0.125280929622514,4.69135877091509));
#41095=CARTESIAN_POINT('Ctrl Pts',(14.0680020005006,-0.513761234509794,
4.47929287013608));
#41096=CARTESIAN_POINT('Ctrl Pts',(14.1157178365635,-0.681008551759042,
3.82708495184235));
#41097=CARTESIAN_POINT('Ctrl Pts',(14.1634336726263,-0.222875237264486,
3.33366758291179));
#41098=CARTESIAN_POINT('Ctrl Pts',(14.2111495086891,0.439927836986373,3.45215352543546));
#41099=CARTESIAN_POINT('Ctrl Pts',(14.258865344752,0.698738409372782,4.07373531525328));
#41100=CARTESIAN_POINT('Ctrl Pts',(14.3065811808148,0.315886748959774,4.62760483051036));
#41101=CARTESIAN_POINT('Ctrl Pts',(14.3542970168777,-0.357048573565392,
4.60513517296818));
#41102=CARTESIAN_POINT('Ctrl Pts',(14.4020128529405,-0.702100697086982,
4.02696057488784));
#41103=CARTESIAN_POINT('Ctrl Pts',(14.4497286890033,-0.402402947265751,
3.42402766604624));
#41104=CARTESIAN_POINT('Ctrl Pts',(14.4974445250662,0.266827620794843,3.35001901394789));
#41105=CARTESIAN_POINT('Ctrl Pts',(14.545160361129,0.691026279008849,3.87289790258421));
#41106=CARTESIAN_POINT('Ctrl Pts',(14.5928761971919,0.480644872403009,4.51249660299459));
#41107=CARTESIAN_POINT('Ctrl Pts',(14.6405920332547,-0.171120116202498,
4.6814617871012));
#41108=CARTESIAN_POINT('Ctrl Pts',(14.6883078693176,-0.665742869077823,
4.22463012647536));
#41109=CARTESIAN_POINT('Ctrl Pts',(14.7360237053803,-0.549003701508229,
3.56151716432844));
#41110=CARTESIAN_POINT('Ctrl Pts',(14.7837395414432,0.0718940126641393,
3.30106973710437));
#41111=CARTESIAN_POINT('Ctrl Pts',(14.831455377506,0.626770348775451,3.68246072472179));
#41112=CARTESIAN_POINT('Ctrl Pts',(14.8791712135689,0.606073829504824,4.35545291479698));
#41113=CARTESIAN_POINT('Ctrl Pts',(14.9268870496317,0.0288103869553486,
4.70202722386799));
#41114=CARTESIAN_POINT('Ctrl Pts',(14.9746028856946,-0.574910077240004,
4.4039191311837));
#41115=CARTESIAN_POINT('Ctrl Pts',(15.0223187217574,-0.650681771377263,
3.73488588523872));
#41116=CARTESIAN_POINT('Ctrl Pts',(15.0700345578202,-0.128922382832804,
3.30931101018402));
#41117=CARTESIAN_POINT('Ctrl Pts',(15.1177503938831,0.511228413592865,3.51800646209349));
#41118=CARTESIAN_POINT('Ctrl Pts',(15.1654662299459,0.681910291555949,4.16932399628639));
#41119=CARTESIAN_POINT('Ctrl Pts',(15.2131820660088,0.226383456244684,4.6651486993049));
#41120=CARTESIAN_POINT('Ctrl Pts',(15.2608979020716,-0.437034790293287,
4.55015711712348));
#41121=CARTESIAN_POINT('Ctrl Pts',(15.3086137381344,-0.699117264260319,
3.92994778903219));
#41122=CARTESIAN_POINT('Ctrl Pts',(15.3563295741972,-0.319189597155267,
3.37406848416447));
#41123=CARTESIAN_POINT('Ctrl Pts',(15.4040454102601,0.353854788380711,3.39299172148285));
#41124=CARTESIAN_POINT('Ctrl Pts',(15.4517612463229,0.70194887699091,3.96934000098645));
#41125=CARTESIAN_POINT('Ctrl Pts',(15.4994770823858,0.40543251098856,4.57384382934891));
#41126=CARTESIAN_POINT('Ctrl Pts',(15.5471929184486,-0.263398768235635,
4.65137803949801));
#41127=CARTESIAN_POINT('Ctrl Pts',(15.5949087545115,-0.690346905678043,
4.13074177323664));
#41128=CARTESIAN_POINT('Ctrl Pts',(15.6426245905743,-0.483338857283784,
3.4900433248913));
#41129=CARTESIAN_POINT('Ctrl Pts',(15.6903404266371,0.167526700878456,3.31764593799033));
#41130=CARTESIAN_POINT('Ctrl Pts',(15.7380562627,0.664549911894371,3.77186478559966));
#41131=CARTESIAN_POINT('Ctrl Pts',(15.7857720987628,0.551306713402943,4.43558371090429));
#41132=CARTESIAN_POINT('Ctrl Pts',(15.8334879348256,-0.0682099229505586,
4.69929941216862));
#41133=CARTESIAN_POINT('Ctrl Pts',(15.8812037708885,-0.625088337514006,
4.32083770313399));
#41134=CARTESIAN_POINT('Ctrl Pts',(15.9289196069513,-0.607938513517956,
3.64774579458877));
#41135=CARTESIAN_POINT('Ctrl Pts',(15.9766354430142,-0.0325093982219456,
3.29813434300035));
#41136=CARTESIAN_POINT('Ctrl Pts',(16.024351279077,0.572773597682653,3.59305692382598));
#41137=CARTESIAN_POINT('Ctrl Pts',(16.0720671151399,0.652069785580651,4.2616815931263));
#41138=CARTESIAN_POINT('Ctrl Pts',(16.1197829512026,0.132560255996602,4.69000002896988));
#41139=CARTESIAN_POINT('Ctrl Pts',(16.1674987872655,-0.508681396370837,
4.48468082119526));
#41140=CARTESIAN_POINT('Ctrl Pts',(16.2152146233283,-0.682793095381579,
3.83427175754402));
#41141=CARTESIAN_POINT('Ctrl Pts',(16.2629304593912,-0.229885388781225,
3.33605348899688));
#41142=CARTESIAN_POINT('Ctrl Pts',(16.310646295454,0.434129607578297,3.44754751763412));
#41143=CARTESIAN_POINT('Ctrl Pts',(16.3583621315168,0.699476705356048,4.06636716140204));
#41144=CARTESIAN_POINT('Ctrl Pts',(16.4060779675797,0.322483581772784,4.62424081966442));
#41145=CARTESIAN_POINT('Ctrl Pts',(16.4537938036425,-0.350651177000141,
4.60886452804932));
#41146=CARTESIAN_POINT('Ctrl Pts',(16.5015096397054,-0.701777564471952,
4.03435857174156));
#41147=CARTESIAN_POINT('Ctrl Pts',(16.5492254757682,-0.408450816253369,
3.42830061032894));
#41148=CARTESIAN_POINT('Ctrl Pts',(16.596941311831,0.259962601354342,3.34724299517707));
#41149=CARTESIAN_POINT('Ctrl Pts',(16.6446571478939,0.689648362099571,3.86562218151166));
#41150=CARTESIAN_POINT('Ctrl Pts',(16.6923729839567,0.486019420324727,4.50740258623259));
#41151=CARTESIAN_POINT('Ctrl Pts',(16.7400888200196,-0.163928633504336,
4.6832273886238));
#41152=CARTESIAN_POINT('Ctrl Pts',(16.7878046560824,-0.663338500820136,
4.23163396723712));
#41153=CARTESIAN_POINT('Ctrl Pts',(16.8355204921452,-0.553594416058007,
3.56732750958986));
#41154=CARTESIAN_POINT('Ctrl Pts',(16.8832363282081,0.064523939115192,3.30035085740826));
#41155=CARTESIAN_POINT('Ctrl Pts',(16.9309521642709,0.623388968170475,3.67587277835446));
#41156=CARTESIAN_POINT('Ctrl Pts',(16.9786680003338,0.609786315682611,4.34904571427615));
#41157=CARTESIAN_POINT('Ctrl Pts',(17.0263838363966,0.0362075067348799,
4.70168460001938));
#41158=CARTESIAN_POINT('Ctrl Pts',(17.0740996724594,-0.570621212771584,
4.40995572075944));
#41159=CARTESIAN_POINT('Ctrl Pts',(17.1218155085223,-0.653439692453966,
3.74175819514654));
#41160=CARTESIAN_POINT('Ctrl Pts',(17.1695313445851,-0.136194448093839,
3.31070809249149));
#41161=CARTESIAN_POINT('Ctrl Pts',(17.2172471806479,0.50612025357182,3.51264535462077));
#41162=CARTESIAN_POINT('Ctrl Pts',(17.2649630167108,0.683656938721366,4.16212788651693));
#41163=CARTESIAN_POINT('Ctrl Pts',(17.3126788527736,0.233380937628925,4.66272588556639));
#41164=CARTESIAN_POINT('Ctrl Pts',(17.3603946888365,-0.431212369515449,
4.55473250655174));
#41165=CARTESIAN_POINT('Ctrl Pts',(17.4081105248993,-0.699816722678643,
3.93731973111387));
#41166=CARTESIAN_POINT('Ctrl Pts',(17.4558263609621,-0.325768611341644,
3.37746721105403));
#41167=CARTESIAN_POINT('Ctrl Pts',(17.503542197025,0.347437828384778,3.38929612998149));
#41168=CARTESIAN_POINT('Ctrl Pts',(17.5512580330878,0.701586764287296,3.96194380963385));
#41169=CARTESIAN_POINT('Ctrl Pts',(17.5989738691507,0.411457779244836,4.56953907446917));
#41170=CARTESIAN_POINT('Ctrl Pts',(17.6466897052135,-0.256519215569882,
4.65411784373439));
#41171=CARTESIAN_POINT('Ctrl Pts',(17.6944055412764,-0.688930667671302,
4.13801013220155));
#41172=CARTESIAN_POINT('Ctrl Pts',(17.7421213773391,-0.488686487089258,
3.49516559270919));
#41173=CARTESIAN_POINT('Ctrl Pts',(17.789837213402,0.160326013994967,3.3159182573078));
#41174=CARTESIAN_POINT('Ctrl Pts',(17.8375530494648,0.662108669494809,3.76487371217125));
#41175=CARTESIAN_POINT('Ctrl Pts',(17.8852688855277,0.555866745946156,4.42974925503083));
#41176=CARTESIAN_POINT('Ctrl Pts',(17.9329847215905,-0.060836163514142,
4.69997944445332));
#41177=CARTESIAN_POINT('Ctrl Pts',(17.9807005576534,-0.621672287934692,
4.32740773946617));
#41178=CARTESIAN_POINT('Ctrl Pts',(18.0284163937162,-0.611617184687133,
3.65417246951162));
#41179=CARTESIAN_POINT('Ctrl Pts',(18.0761322297791,-0.0399046098013318,
3.29851594204507));
#41180=CARTESIAN_POINT('Ctrl Pts',(18.1238480658419,0.568452982276385,3.58704301871817));
#41181=CARTESIAN_POINT('Ctrl Pts',(18.1715639019047,0.65479145395626,4.25479484546229));
#41182=CARTESIAN_POINT('Ctrl Pts',(18.2192797379675,0.139824858206545,4.68856464509573));
#41183=CARTESIAN_POINT('Ctrl Pts',(18.2669955740304,-0.503545056316242,
4.49001493620888));
#41184=CARTESIAN_POINT('Ctrl Pts',(18.3147114100932,-0.684501797587214,
3.84147697155243));
#41185=CARTESIAN_POINT('Ctrl Pts',(18.3624272461561,-0.236870005719869,
3.33851314310973));
#41186=CARTESIAN_POINT('Ctrl Pts',(18.4101430822189,0.42828315711354,3.44300287363294));
#41187=CARTESIAN_POINT('Ctrl Pts',(18.4578589182817,0.70013730678616,4.05899163580144));
#41188=CARTESIAN_POINT('Ctrl Pts',(18.5055747543446,0.32904459463985,4.62080747111051));
#41189=CARTESIAN_POINT('Ctrl Pts',(18.5532905904074,-0.34421483176614,4.61252625334797));
#41190=CARTESIAN_POINT('Ctrl Pts',(18.6010064264702,-0.701376481735239,
4.0417527522082));
#41191=CARTESIAN_POINT('Ctrl Pts',(18.6487222625331,-0.414453316462639,
3.43263705626685));
#41192=CARTESIAN_POINT('Ctrl Pts',(18.6964380985959,0.253068706501803,3.34453948155689));
#41193=CARTESIAN_POINT('Ctrl Pts',(18.7441539346588,0.68819384232267,3.85836138648927));
#41194=CARTESIAN_POINT('Ctrl Pts',(18.7918697707216,0.491339983515996,4.50225220959958));
#41195=CARTESIAN_POINT('Ctrl Pts',(18.8395856067844,-0.156718942392259,
4.68491710048942));
#41196=CARTESIAN_POINT('Ctrl Pts',(18.8873014428473,-0.660860452068119,
4.23861207919858));
#41197=CARTESIAN_POINT('Ctrl Pts',(18.9350172789101,-0.558123639969822,
3.57318591405529));
#41198=CARTESIAN_POINT('Ctrl Pts',(18.9827331149729,0.0571466985584877,
3.29970969142451));
#41199=CARTESIAN_POINT('Ctrl Pts',(19.0304489510358,0.619938344467307,3.66932083449001));
#41200=CARTESIAN_POINT('Ctrl Pts',(19.0781647870986,0.613431069708698,4.3425997434341));
#41201=CARTESIAN_POINT('Ctrl Pts',(19.1258806231615,0.0436006047213211,
4.70126403633668));
#41202=CARTESIAN_POINT('Ctrl Pts',(19.1735964592243,-0.566268966340429,
4.41594677447179));
#41203=CARTESIAN_POINT('Ctrl Pts',(19.2213122952871,-0.656125032675529,
3.74865918919138));
#41204=CARTESIAN_POINT('Ctrl Pts',(19.26902813135,-0.143451385285705,3.31218173833215));
#41205=CARTESIAN_POINT('Ctrl Pts',(19.3167439674128,0.500955875668841,3.50733837970023));
#41206=CARTESIAN_POINT('Ctrl Pts',(19.3644598034757,0.68532764936022,4.15491376927485));
#41207=CARTESIAN_POINT('Ctrl Pts',(19.4121756395385,0.240352494576274,4.66022945763735));
#41208=CARTESIAN_POINT('Ctrl Pts',(19.4598914756013,-0.425342048711971,
4.55924628221868));
#41209=CARTESIAN_POINT('Ctrl Pts',(19.5076073116642,-0.700438454444525,
3.94469862920436));
#41210=CARTESIAN_POINT('Ctrl Pts',(19.555323147727,-0.332311429993836,3.3809350976725));
#41211=CARTESIAN_POINT('Ctrl Pts',(19.6030389837899,0.340982256434611,3.38566835039883));
#41212=CARTESIAN_POINT('Ctrl Pts',(19.6507548198527,0.701146760813864,3.95455188724214));
#41213=CARTESIAN_POINT('Ctrl Pts',(19.6984706559155,0.417437272672218,4.56517097885182));
#41214=CARTESIAN_POINT('Ctrl Pts',(19.7461864919784,-0.249611033919464,
4.6567851409082));
#41215=CARTESIAN_POINT('Ctrl Pts',(19.7939023280412,-0.687438163400574,
4.14526287985386));
#41216=CARTESIAN_POINT('Ctrl Pts',(19.841618164104,-0.493979350866992,3.5003444672369));
#41217=CARTESIAN_POINT('Ctrl Pts',(19.8893340001669,0.153106602982307,3.31426555646693));
#41218=CARTESIAN_POINT('Ctrl Pts',(19.9370498362297,0.659595612567133,3.75791065255607));
#41219=CARTESIAN_POINT('Ctrl Pts',(19.9847656722925,0.560361770063263,4.42386348253578));
#41220=CARTESIAN_POINT('Ctrl Pts',(20.0324815083554,-0.0534494809679074,
4.70058849011268));
#41221=CARTESIAN_POINT('Ctrl Pts',(20.0801973444182,-0.618198828117398,
4.33392863744107));
#41222=CARTESIAN_POINT('Ctrl Pts',(20.1279131804811,-0.615205937201001,
3.66066167313574));
#41223=CARTESIAN_POINT('Ctrl Pts',(20.1756290165439,-0.0473369003220797,
3.29892991724937));
#41224=CARTESIAN_POINT('Ctrl Pts',(20.2233448526068,0.564147630203746,3.58116102158214));
#41225=CARTESIAN_POINT('Ctrl Pts',(20.2710606886696,0.657292163719816,4.24771695100806));
#41226=CARTESIAN_POINT('Ctrl Pts',(20.3187765247324,0.147355317357748,4.68736342730055));
#41227=CARTESIAN_POINT('Ctrl Pts',(20.3664923607953,-0.498896366832293,
4.49468216892218));
#41228=CARTESIAN_POINT('Ctrl Pts',(20.4062555575143,-0.653992183610565,
3.9575054511282));
#41229=CARTESIAN_POINT('Ctrl Pts',(20.4380661148895,-0.465699721472375,
3.59327933193152));
#41230=CARTESIAN_POINT('Ctrl Pts',(20.461924032921,-0.215665100260693,3.41899970433759));
#41231=CARTESIAN_POINT('Ctrl Pts',(20.4857819509523,0.0900520562992202,
3.38718375849312));
#41232=CARTESIAN_POINT('Ctrl Pts',(20.5096398689838,0.372154449079436,3.50499792242313));
#41233=CARTESIAN_POINT('Ctrl Pts',(20.5334977870152,0.564103623124681,3.74397162737493));
#41234=CARTESIAN_POINT('Ctrl Pts',(20.5573557050466,0.61766411855396,4.04548854604559));
#41235=CARTESIAN_POINT('Ctrl Pts',(20.581213623078,0.520427284318709,4.33591550271974));
#41236=CARTESIAN_POINT('Ctrl Pts',(20.6050715411094,0.295805552416038,4.5441843692251));
#41237=CARTESIAN_POINT('Ctrl Pts',(20.6289294591409,-0.00108183093298003,
4.61939465531364));
#41238=CARTESIAN_POINT('Ctrl Pts',(20.6527873771723,-0.297740088546312,
4.543141139652));
#41239=CARTESIAN_POINT('Ctrl Pts',(20.6766452952037,-0.521574030203058,
4.33407743490148));
#41240=CARTESIAN_POINT('Ctrl Pts',(20.7005032132351,-0.617878846294169,
4.04332131262121));
#41241=CARTESIAN_POINT('Ctrl Pts',(20.7243611312665,-0.563090193646282,
3.74197268265107));
#41242=CARTESIAN_POINT('Ctrl Pts',(20.748219049298,-0.370613436173077,3.50371837193987));
#41243=CARTESIAN_POINT('Ctrl Pts',(20.7720769673294,-0.0875101228827464,
3.38681864340431));
#41244=CARTESIAN_POINT('Ctrl Pts',(20.7959348853608,0.216991017820888,3.41985835035499));
#41245=CARTESIAN_POINT('Ctrl Pts',(20.8197928033922,0.468432357761717,3.59475855107288));
#41246=CARTESIAN_POINT('Ctrl Pts',(20.8436507214236,0.605329007232586,3.86875129405724));
#41247=CARTESIAN_POINT('Ctrl Pts',(20.8675086394551,0.594206341669864,4.17483793696784));
#41248=CARTESIAN_POINT('Ctrl Pts',(20.8913665574864,0.437783978244149,4.43817193323088));
#41249=CARTESIAN_POINT('Ctrl Pts',(20.9152244755179,0.174311539695801,4.5943609607934));
#41250=CARTESIAN_POINT('Ctrl Pts',(20.9390823935493,-0.13178483570001,4.60521254097096));
#41251=CARTESIAN_POINT('Ctrl Pts',(20.9629403115808,-0.405656219889506,
4.46807317049539));
#41252=CARTESIAN_POINT('Ctrl Pts',(20.9867982296121,-0.580333613298163,
4.21647715910241));
#41253=CARTESIAN_POINT('Ctrl Pts',(21.0106561476436,-0.613103627724174,
3.91194658594648));
#41254=CARTESIAN_POINT('Ctrl Pts',(21.034514065675,-0.495953105920446,3.62894747086441));
#41255=CARTESIAN_POINT('Ctrl Pts',(21.0583719837064,-0.257528539509485,
3.43668080652407));
#41256=CARTESIAN_POINT('Ctrl Pts',(21.0822299017379,0.0438687693677006,
3.38216102944232));
#41257=CARTESIAN_POINT('Ctrl Pts',(21.1060878197692,0.334538969374667,3.47871971028568));
#41258=CARTESIAN_POINT('Ctrl Pts',(21.1299457378007,0.543405278604256,3.7027456213393));
#41259=CARTESIAN_POINT('Ctrl Pts',(21.153803655832,0.619394195209021,3.99945832503004));
#41260=CARTESIAN_POINT('Ctrl Pts',(21.1776615738635,0.543924359096133,4.29630348300169));
#41261=CARTESIAN_POINT('Ctrl Pts',(21.2015194918949,0.33545020099803,4.52069436823682));
#41262=CARTESIAN_POINT('Ctrl Pts',(21.2253774099264,0.0449493312674926,
4.61776129700707));
#41263=CARTESIAN_POINT('Ctrl Pts',(21.2492353279577,-0.256542874348706,
4.56376876117982));
#41264=CARTESIAN_POINT('Ctrl Pts',(21.2730932459892,-0.495303359101402,
4.37191940649105));
#41265=CARTESIAN_POINT('Ctrl Pts',(21.2969511640206,-0.612948680759938,
4.08912562603418));
#41266=CARTESIAN_POINT('Ctrl Pts',(21.320809082052,-0.580711353586496,3.78453820227854));
#41267=CARTESIAN_POINT('Ctrl Pts',(21.3446670000834,-0.406474282201139,
3.53263705712739));
#41268=CARTESIAN_POINT('Ctrl Pts',(21.3685249181149,-0.132843176680646,
3.39501888221951));
#41269=CARTESIAN_POINT('Ctrl Pts',(21.3923828361463,0.17327170411384,3.40533506996376));
#41270=CARTESIAN_POINT('Ctrl Pts',(21.4162407541777,0.437016933425986,3.56106303144932));
#41271=CARTESIAN_POINT('Ctrl Pts',(21.4400986722091,0.593899618413251,3.82412303814848));
#41272=CARTESIAN_POINT('Ctrl Pts',(21.4639565902405,0.605557669197671,4.13018975281259));
#41273=CARTESIAN_POINT('Ctrl Pts',(21.4878145082719,0.469140374803543,4.40442152661638));
#41274=CARTESIAN_POINT('Ctrl Pts',(21.5116724263034,0.218005479642704,4.57976122094124));
#41275=CARTESIAN_POINT('Ctrl Pts',(21.5355303443348,-0.0864376936408111,
4.61333350436739));
#41276=CARTESIAN_POINT('Ctrl Pts',(21.5593882623662,-0.369744496313637,
4.49692903910649));
#41277=CARTESIAN_POINT('Ctrl Pts',(21.5832461803976,-0.562638697999917,
4.2590118877088));
#41278=CARTESIAN_POINT('Ctrl Pts',(21.607104098429,-0.617952412054802,3.95775927442416));
#41279=CARTESIAN_POINT('Ctrl Pts',(21.6309620164605,-0.522159928676552,
3.66683566915707));
#41280=CARTESIAN_POINT('Ctrl Pts',(21.6548199344919,-0.298685119385998,
3.45737981799522));
#41281=CARTESIAN_POINT('Ctrl Pts',(21.6786778525233,-0.00217366238626178,
3.38060938201055));
#41282=CARTESIAN_POINT('Ctrl Pts',(21.7025357705547,0.294869314276287,3.45529682398599));
#41283=CARTESIAN_POINT('Ctrl Pts',(21.7263936885862,0.519808711519421,3.66317902991346));
#41284=CARTESIAN_POINT('Ctrl Pts',(21.7502516066175,0.617640719491047,3.95342313784609));
#41285=CARTESIAN_POINT('Ctrl Pts',(21.774109524649,0.564442747351711,4.25505655730362));
#41286=CARTESIAN_POINT('Ctrl Pts',(21.7979674426804,0.373223148373148,4.49432170089927));
#41287=CARTESIAN_POINT('Ctrl Pts',(21.8218253607118,0.0907403232229101,
4.61271172357229));
#41288=CARTESIAN_POINT('Ctrl Pts',(21.8456832787432,-0.213930982672105,
4.58127703989962));
#41289=CARTESIAN_POINT('Ctrl Pts',(21.8695411967746,-0.466290335940828,
4.40770428630285));
#41290=CARTESIAN_POINT('Ctrl Pts',(21.8933991148061,-0.604629000578284,
4.13443672906324));
#41291=CARTESIAN_POINT('Ctrl Pts',(21.9172570328375,-0.595119404811066,
3.82829572958469));
#41292=CARTESIAN_POINT('Ctrl Pts',(21.9411149508689,-0.440086903840403,
3.56414110135311));
#41293=CARTESIAN_POINT('Ctrl Pts',(21.9649728689003,-0.177441167154219,
3.40656584639871));
#41294=CARTESIAN_POINT('Ctrl Pts',(21.9888307869318,0.128593768301574,3.39410140682164));
#41295=CARTESIAN_POINT('Ctrl Pts',(22.0126887049631,0.403184024583593,3.52979567762293));
#41296=CARTESIAN_POINT('Ctrl Pts',(22.0365466229946,0.579184804342829,3.7804677133541));
#41297=CARTESIAN_POINT('Ctrl Pts',(22.060404541026,0.613559122762511,4.08482137310942));
#41298=CARTESIAN_POINT('Ctrl Pts',(22.0842624590574,0.497901522652627,4.36843389665204));
#41299=CARTESIAN_POINT('Ctrl Pts',(22.1081203770888,0.260493437687466,4.56195429652472));
#41300=CARTESIAN_POINT('Ctrl Pts',(22.1319782951203,-0.0406123884881684,
4.61806156357065));
#41301=CARTESIAN_POINT('Ctrl Pts',(22.1558362131517,-0.33178737942464,4.52303594266224));
#41302=CARTESIAN_POINT('Ctrl Pts',(22.1796941311831,-0.541831318374727,
4.30011378656432));
#41303=CARTESIAN_POINT('Ctrl Pts',(22.2035520492145,-0.619382740812877,
4.00380563470766));
#41304=CARTESIAN_POINT('Ctrl Pts',(22.2274099672459,-0.545478211438426,
3.70656690151735));
#41305=CARTESIAN_POINT('Ctrl Pts',(22.2512678852774,-0.338189400908512,
3.48108055383335));
#41306=CARTESIAN_POINT('Ctrl Pts',(22.2751258033088,-0.0482040696311437,
3.38248414587532));
#41307=CARTESIAN_POINT('Ctrl Pts',(22.2989837213402,0.253568469476171,3.43488718493857));
#41308=CARTESIAN_POINT('Ctrl Pts',(22.3228416393716,0.493336611197201,3.62547570084914));
#41309=CARTESIAN_POINT('Ctrl Pts',(22.346699557403,0.612470512379129,3.90764560936005));
#41310=CARTESIAN_POINT('Ctrl Pts',(22.3705574754344,0.581838691587799,4.21239868278141));
#41311=CARTESIAN_POINT('Ctrl Pts',(22.3944153934659,0.408931458591185,4.46521449128699));
#41312=CARTESIAN_POINT('Ctrl Pts',(22.4182733114973,0.13602935083686,4.60427268703701));
#41313=CARTESIAN_POINT('Ctrl Pts',(22.4421312295287,-0.170135649772668,
4.59556974592947));
#41314=CARTESIAN_POINT('Ctrl Pts',(22.4659891475601,-0.434697828443077,
4.44123378804823));
#41315=CARTESIAN_POINT('Ctrl Pts',(22.4898470655916,-0.592964587096883,
4.17900413283907));
#41316=CARTESIAN_POINT('Ctrl Pts',(22.513704983623,-0.606235276705168,3.87300312362118));
#41317=CARTESIAN_POINT('Ctrl Pts',(22.5375629016543,-0.471265070143009,
3.59805624874041));
#41318=CARTESIAN_POINT('Ctrl Pts',(22.5614208196858,-0.22105744785653,3.4213956854475));
#41319=CARTESIAN_POINT('Ctrl Pts',(22.5852787377172,0.0832042338527798,
3.38621941950615));
#41320=CARTESIAN_POINT('Ctrl Pts',(22.6091366557487,0.36712117327337,3.50112963696785));
#41321=CARTESIAN_POINT('Ctrl Pts',(22.63299457378,0.561265174232679,3.7380264683998));
#41322=CARTESIAN_POINT('Ctrl Pts',(22.6568524918115,0.618167971965146,4.03898443479498));
#41323=CARTESIAN_POINT('Ctrl Pts',(22.6807104098429,0.523905402647805,4.33040686810369));
#41324=CARTESIAN_POINT('Ctrl Pts',(22.7045683278744,0.301545895245711,4.54104106792393));
#41325=CARTESIAN_POINT('Ctrl Pts',(22.7284262459057,0.00542710047790416,
4.61936606261506));
#41326=CARTESIAN_POINT('Ctrl Pts',(22.7522841639372,-0.291974666000346,
4.54625809930836));
#41327=CARTESIAN_POINT('Ctrl Pts',(22.7761420819686,-0.518067845615496,
4.33953802216683));
#41328=CARTESIAN_POINT('Ctrl Pts',(22.7920473606562,-0.584213376873476,
4.14642833911731));
#41329=CARTESIAN_POINT('Ctrl Pts',(22.8,-0.592174260192535,4.04779597854866));
#41330=CARTESIAN_POINT('Ctrl Pts',(3.96816317011931,-0.282716247115855,
3.54616445487434));
#41331=CARTESIAN_POINT('Ctrl Pts',(3.97611580946312,-0.207125539895404,
3.49907532469992));
#41332=CARTESIAN_POINT('Ctrl Pts',(3.99202108815073,-0.0320395462633344,
3.44344227840288));
#41333=CARTESIAN_POINT('Ctrl Pts',(4.01587900618214,0.238586678544665,3.49618207793602));
#41334=CARTESIAN_POINT('Ctrl Pts',(4.03973692421357,0.450798406251909,3.67207593825259));
#41335=CARTESIAN_POINT('Ctrl Pts',(4.06359484224498,0.552814952159096,3.92817792166325));
#41336=CARTESIAN_POINT('Ctrl Pts',(4.0874527602764,0.519633627921064,4.20183097195279));
#41337=CARTESIAN_POINT('Ctrl Pts',(4.11131067830782,0.359398059257131,4.42613686623617));
#41338=CARTESIAN_POINT('Ctrl Pts',(4.13516859633924,0.11127440638865,4.54623750576341));
#41339=CARTESIAN_POINT('Ctrl Pts',(4.15902651437066,-0.164055973910312,
4.53276988152218));
#41340=CARTESIAN_POINT('Ctrl Pts',(4.18288443240208,-0.399271733473279,
4.38902461621758));
#41341=CARTESIAN_POINT('Ctrl Pts',(4.2067423504335,-0.536853866020863,4.15015270818839));
#41342=CARTESIAN_POINT('Ctrl Pts',(4.23060026846491,-0.543161034884179,
3.87456412255522));
#41343=CARTESIAN_POINT('Ctrl Pts',(4.25445818649634,-0.416650307492554,
3.62964815836115));
#41344=CARTESIAN_POINT('Ctrl Pts',(4.27831610452775,-0.188257351244862,
3.47529323740438));
#41345=CARTESIAN_POINT('Ctrl Pts',(4.30217402255918,0.0861697193074588,
3.44924344981891));
#41346=CARTESIAN_POINT('Ctrl Pts',(4.32603194059059,0.339525912432458,3.55786862136322));
#41347=CARTESIAN_POINT('Ctrl Pts',(4.34988985862202,0.509858789389686,3.77460696883261));
#41348=CARTESIAN_POINT('Ctrl Pts',(4.37374777665342,0.555517294574929,4.0464600464808));
#41349=CARTESIAN_POINT('Ctrl Pts',(4.39760569468486,0.465336694276122,4.30695238014399));
#41350=CARTESIAN_POINT('Ctrl Pts',(4.42146361271626,0.261368594047533,4.4923864940975));
#41351=CARTESIAN_POINT('Ctrl Pts',(4.4453215307477,-0.00651124555331369,
4.55741869872598));
#41352=CARTESIAN_POINT('Ctrl Pts',(4.4691794487791,-0.272798909000308,4.48614684730087));
#41353=CARTESIAN_POINT('Ctrl Pts',(4.49303736681053,-0.472379807908186,
4.29599884956661));
#41354=CARTESIAN_POINT('Ctrl Pts',(4.51689528484195,-0.55645097662433,4.03347107014466));
#41355=CARTESIAN_POINT('Ctrl Pts',(4.54075320287336,-0.504454724024634,
3.76275870240323));
#41356=CARTESIAN_POINT('Ctrl Pts',(4.56461112090479,-0.329105550388866,
3.55005829421323));
#41357=CARTESIAN_POINT('Ctrl Pts',(4.5884690389362,-0.0732811049967102,
3.44738088927219));
#41358=CARTESIAN_POINT('Ctrl Pts',(4.61232695696762,0.200462566687888,3.47983390993684));
#41359=CARTESIAN_POINT('Ctrl Pts',(4.63618487499904,0.425187680335341,3.63948170866684));
#41360=CARTESIAN_POINT('Ctrl Pts',(4.66004279303046,0.54594282425631,3.88728604994618));
#41361=CARTESIAN_POINT('Ctrl Pts',(4.68390071106188,0.533200076465109,4.16265202228146));
#41362=CARTESIAN_POINT('Ctrl Pts',(4.7077586290933,0.390075385898422,4.39824514461603));
#41363=CARTESIAN_POINT('Ctrl Pts',(4.73161654712472,0.151566638040082,4.53645648111246));
#41364=CARTESIAN_POINT('Ctrl Pts',(4.75547446515614,-0.124004281411749,
4.54348959519552));
#41365=CARTESIAN_POINT('Ctrl Pts',(4.77933238318755,-0.369252776249408,
4.41762469889406));
#41366=CARTESIAN_POINT('Ctrl Pts',(4.80319030121898,-0.524208909050512,
4.18963918784455));
#41367=CARTESIAN_POINT('Ctrl Pts',(4.82704821925039,-0.550981684424725,
3.91528172969931));
#41368=CARTESIAN_POINT('Ctrl Pts',(4.85090613728181,-0.443024429517375,
3.66164019632193));
#41369=CARTESIAN_POINT('Ctrl Pts',(4.87476405531323,-0.226735633849849,
3.49073685167984));
#41370=CARTESIAN_POINT('Ctrl Pts',(4.89862197334465,0.0449962004486201,
3.44436221885167));
#41371=CARTESIAN_POINT('Ctrl Pts',(4.92247989137607,0.305725238065515,3.53385615878353));
#41372=CARTESIAN_POINT('Ctrl Pts',(4.94633780940749,0.491696127187109,3.73733496539613));
#41373=CARTESIAN_POINT('Ctrl Pts',(4.9701957274389,0.557433919677865,4.00504252782125));
#41374=CARTESIAN_POINT('Ctrl Pts',(4.99405364547033,0.486863934612277,4.27151705483839));
#41375=CARTESIAN_POINT('Ctrl Pts',(5.01791156350174,0.297242455626679,4.47159826597145));
#41376=CARTESIAN_POINT('Ctrl Pts',(5.04176948153317,0.0349370995184326,
4.55636085499566));
#41377=CARTESIAN_POINT('Ctrl Pts',(5.06562739956458,-0.235911329089554,
4.505078060008));
#41378=CARTESIAN_POINT('Ctrl Pts',(5.08948531759601,-0.449073011639563,
4.33028992129829));
#41379=CARTESIAN_POINT('Ctrl Pts',(5.11334323562741,-0.552424110340463,
4.07473689991432));
#41380=CARTESIAN_POINT('Ctrl Pts',(5.13720115365885,-0.520692466332485,
3.80090867070902));
#41381=CARTESIAN_POINT('Ctrl Pts',(5.16105907169026,-0.361637330928202,
3.57576369465428));
#41382=CARTESIAN_POINT('Ctrl Pts',(5.18491698972168,-0.114152017308863,
3.45435605122152));
#41383=CARTESIAN_POINT('Ctrl Pts',(5.2087749077531,0.161246573981014,3.46637321630784));
#41384=CARTESIAN_POINT('Ctrl Pts',(5.23263282578452,0.397215985664045,3.60887666570863));
#41385=CARTESIAN_POINT('Ctrl Pts',(5.25649074381594,0.536055268906009,3.84702042432939));
#41386=CARTESIAN_POINT('Ctrl Pts',(5.28034866184735,0.543814437048104,4.12257185628156));
#41387=CARTESIAN_POINT('Ctrl Pts',(5.30420657987878,0.418596162124088,4.3681511305826));
#41388=CARTESIAN_POINT('Ctrl Pts',(5.32806449791019,0.191019723230217,4.5237074252207));
#41389=CARTESIAN_POINT('Ctrl Pts',(5.35192241594161,-0.0832662412662402,
4.55120298888854));
#41390=CARTESIAN_POINT('Ctrl Pts',(5.37578033397303,-0.337191341646214,
4.44391440730515));
#41391=CARTESIAN_POINT('Ctrl Pts',(5.39963825200445,-0.508663974085987,
4.22807666114996));
#41392=CARTESIAN_POINT('Ctrl Pts',(5.42349617003587,-0.555754409133215,
3.95646795866016));
#41393=CARTESIAN_POINT('Ctrl Pts',(5.4473540880673,-0.466947752701331,3.69550402606682));
#41394=CARTESIAN_POINT('Ctrl Pts',(5.47121200609871,-0.263959651332346,
3.50899765340418));
#41395=CARTESIAN_POINT('Ctrl Pts',(5.49506992413013,0.00357377490351851,
3.44255472911916));
#41396=CARTESIAN_POINT('Ctrl Pts',(5.51892784216155,0.270233315828591,3.51242235806964));
#41397=CARTESIAN_POINT('Ctrl Pts',(5.54278576019296,0.470813450024345,3.70151600181885));
#41398=CARTESIAN_POINT('Ctrl Pts',(5.56664367822439,0.556266870991092,3.96359711366712));
#41399=CARTESIAN_POINT('Ctrl Pts',(5.5905015962558,0.505697889589837,4.23457972281303));
#41400=CARTESIAN_POINT('Ctrl Pts',(5.61435951428722,0.331471999260015,4.4482011999181));
#41401=CARTESIAN_POINT('Ctrl Pts',(5.63821743231864,0.0761921759760934,
4.55222527486821));
#41402=CARTESIAN_POINT('Ctrl Pts',(5.66207535035006,-0.197718709731212,
4.52121522783523));
#41403=CARTESIAN_POINT('Ctrl Pts',(5.68593326838148,-0.423281985227643,
4.3627538599096));
#41404=CARTESIAN_POINT('Ctrl Pts',(5.70979118641289,-0.545341285237878,
4.11558929214995));
#41405=CARTESIAN_POINT('Ctrl Pts',(5.73364910444432,-0.534049786451273,
3.84015999362387));
#41406=CARTESIAN_POINT('Ctrl Pts',(5.75750702247573,-0.392168567195948,
3.6038159310769));
#41407=CARTESIAN_POINT('Ctrl Pts',(5.78136494050716,-0.154391451667357,
3.46434966433946));
#41408=CARTESIAN_POINT('Ctrl Pts',(5.80522285853857,0.121138580962943,3.45586449715393));
#41409=CARTESIAN_POINT('Ctrl Pts',(5.82908077656999,0.367046927720705,3.58043527923202));
#41410=CARTESIAN_POINT('Ctrl Pts',(5.85293869460141,0.523202308305842,3.80760107017232));
#41411=CARTESIAN_POINT('Ctrl Pts',(5.87679661263283,0.551420461789987,4.08181362911724));
#41412=CARTESIAN_POINT('Ctrl Pts',(5.90065453066425,0.44480131269862,4.33602054829434));
#41413=CARTESIAN_POINT('Ctrl Pts',(5.92451244869567,0.229416087376931,4.50806125053784));
#41414=CARTESIAN_POINT('Ctrl Pts',(5.94837036672709,-0.042067546589846,
4.55586721297736));
#41415=CARTESIAN_POINT('Ctrl Pts',(5.97222828475851,-0.30326465903273,4.46774835821298));
#41416=CARTESIAN_POINT('Ctrl Pts',(5.99608620278993,-0.490305038147314,
4.26525255699254));
#41417=CARTESIAN_POINT('Ctrl Pts',(6.01994412082133,-0.557452977205748,
3.99789477357902));
#41418=CARTESIAN_POINT('Ctrl Pts',(6.04380203885278,-0.488287539408226,
3.73105273207384));
#41419=CARTESIAN_POINT('Ctrl Pts',(6.06765995688417,-0.299724270968661,
3.52997381710292));
#41420=CARTESIAN_POINT('Ctrl Pts',(6.09151787491561,-0.0378669053578504,
3.44383251805177));
#41421=CARTESIAN_POINT('Ctrl Pts',(6.11537579294702,0.233243627260218,3.49368287747685));
#41422=CARTESIAN_POINT('Ctrl Pts',(6.13923371097844,0.447331678364145,3.6673537262422));
#41423=CARTESIAN_POINT('Ctrl Pts',(6.16309162900986,0.552012406214274,3.92234268746235));
#41424=CARTESIAN_POINT('Ctrl Pts',(6.18694954704127,0.521753629494025,4.19636433484848));
#41425=CARTESIAN_POINT('Ctrl Pts',(6.2108074650727,0.363831507594212,4.42228768590875));
#41426=CARTESIAN_POINT('Ctrl Pts',(6.23466538310411,0.117094415953721,4.54510476979165));
#41427=CARTESIAN_POINT('Ctrl Pts',(6.25852330113554,-0.158561881267111,
4.53433708369694));
#41428=CARTESIAN_POINT('Ctrl Pts',(6.28238121916695,-0.394905399742298,
4.39345989467659));
#41429=CARTESIAN_POINT('Ctrl Pts',(6.30623913719837,-0.535697351746728,
4.1553358869807));
#41430=CARTESIAN_POINT('Ctrl Pts',(6.33009705522979,-0.543633587309765,
3.88114808171798));
#41431=CARTESIAN_POINT('Ctrl Pts',(6.36190761260502,-0.381130543103143,
3.54983775818315));
#41432=CARTESIAN_POINT('Ctrl Pts',(6.40167080932404,0.0904237977681596,
3.37418170676098));
#41433=CARTESIAN_POINT('Ctrl Pts',(6.4493866453869,0.576013642360818,3.73827828410759));
#41434=CARTESIAN_POINT('Ctrl Pts',(6.49710248144972,0.531303907723303,4.34259299019566));
#41435=CARTESIAN_POINT('Ctrl Pts',(6.54481831751257,-0.000617460830772086,
4.63236849138271));
#41436=CARTESIAN_POINT('Ctrl Pts',(6.5925341535754,-0.532336898979176,4.34139325430452));
#41437=CARTESIAN_POINT('Ctrl Pts',(6.64024998963824,-0.575010046738857,
3.73693099107234));
#41438=CARTESIAN_POINT('Ctrl Pts',(6.68796582570108,-0.0897448725589052,
3.37403863313417));
#41439=CARTESIAN_POINT('Ctrl Pts',(6.73568166176391,0.477988548433368,3.58598174571673));
#41440=CARTESIAN_POINT('Ctrl Pts',(6.78339749782676,0.606749053262868,4.17812127049189));
#41441=CARTESIAN_POINT('Ctrl Pts',(6.83111333388958,0.178337754027021,4.60669083891839));
#41442=CARTESIAN_POINT('Ctrl Pts',(6.87882916995244,-0.413851892207341,
4.47812605548031));
#41443=CARTESIAN_POINT('Ctrl Pts',(6.92654500601527,-0.625990718083913,
3.91049119230943));
#41444=CARTESIAN_POINT('Ctrl Pts',(6.97426084207811,-0.263274891453005,
3.42505341469988));
#41445=CARTESIAN_POINT('Ctrl Pts',(7.02197667814094,0.341211513798207,3.46759805477058));
#41446=CARTESIAN_POINT('Ctrl Pts',(7.06969251420378,0.63235750294684,3.99905552874491));
#41447=CARTESIAN_POINT('Ctrl Pts',(7.11740835026662,0.342800202184808,4.53138035934227));
#41448=CARTESIAN_POINT('Ctrl Pts',(7.16512418632946,-0.261555976381552,
4.57573041153878));
#41449=CARTESIAN_POINT('Ctrl Pts',(7.2128400223923,-0.625721183287191,4.0913783776429));
#41450=CARTESIAN_POINT('Ctrl Pts',(7.26055585845514,-0.41527704940159,3.52311216844965));
#41451=CARTESIAN_POINT('Ctrl Pts',(7.30827169451797,0.176522415171576,3.39277939551711));
#41452=CARTESIAN_POINT('Ctrl Pts',(7.35598753058081,0.606218615784068,3.8200666455489));
#41453=CARTESIAN_POINT('Ctrl Pts',(7.40370336664364,0.479214941044062,4.4125894643569));
#41454=CARTESIAN_POINT('Ctrl Pts',(7.4514192027065,-0.0878591916424711,
4.62622502914213));
#41455=CARTESIAN_POINT('Ctrl Pts',(7.49913503876932,-0.574250874682306,
4.26478851416677));
#41456=CARTESIAN_POINT('Ctrl Pts',(7.54685087483217,-0.53329914461431,3.6601926322252));
#41457=CARTESIAN_POINT('Ctrl Pts',(7.594566710895,-0.00261060360317682,
3.36764708477891));
#41458=CARTESIAN_POINT('Ctrl Pts',(7.64228254695784,0.530475294557976,3.65580094934904));
#41459=CARTESIAN_POINT('Ctrl Pts',(7.68999838302067,0.576417567478113,4.26003809833172));
#41460=CARTESIAN_POINT('Ctrl Pts',(7.73771421908353,0.093026718772369,4.62547826040714));
#41461=CARTESIAN_POINT('Ctrl Pts',(7.78543005514634,-0.475791997136335,
4.41653211173522));
#41462=CARTESIAN_POINT('Ctrl Pts',(7.8331458912092,-0.607683601098078,3.82507811568403));
#41463=CARTESIAN_POINT('Ctrl Pts',(7.88086172727203,-0.181530003744534,
3.39425757752065));
#41464=CARTESIAN_POINT('Ctrl Pts',(7.92857756333487,0.411325389238953,3.51969962646458));
#41465=CARTESIAN_POINT('Ctrl Pts',(7.97629339939771,0.626454348233276,4.08620889879763));
#41466=CARTESIAN_POINT('Ctrl Pts',(8.02400923546054,0.266300640003926,4.57355121287022));
#41467=CARTESIAN_POINT('Ctrl Pts',(8.07172507152339,-0.338401043502061,
4.5341926229444));
#41468=CARTESIAN_POINT('Ctrl Pts',(8.11944090758622,-0.632343841791292,
4.00427672775865));
#41469=CARTESIAN_POINT('Ctrl Pts',(8.16715674364906,-0.345595560302635,
3.47043344766624));
#41470=CARTESIAN_POINT('Ctrl Pts',(8.2148725797119,0.258518441882999,3.42289928101069));
#41471=CARTESIAN_POINT('Ctrl Pts',(8.26258841577473,0.625230981070026,3.90532558443901));
#41472=CARTESIAN_POINT('Ctrl Pts',(8.31030425183758,0.417784289925175,4.47469286043008));
#41473=CARTESIAN_POINT('Ctrl Pts',(8.35802008790041,-0.173320143095541,
4.60814237859973));
#41474=CARTESIAN_POINT('Ctrl Pts',(8.40573592396325,-0.605262021838435,
4.18312539302794));
#41475=CARTESIAN_POINT('Ctrl Pts',(8.45345176002609,-0.481382472773795,
3.58994154129225));
#41476=CARTESIAN_POINT('Ctrl Pts',(8.50116759608892,0.0845580080604409,
3.37332068174828));
#41477=CARTESIAN_POINT('Ctrl Pts',(8.54888343215178,0.572847569000584,3.73218908285563));
#41478=CARTESIAN_POINT('Ctrl Pts',(8.59659926821459,0.535082392934658,4.33699236997728));
#41479=CARTESIAN_POINT('Ctrl Pts',(8.64431510427745,0.00594282213592907,
4.6323303784547));
#41480=CARTESIAN_POINT('Ctrl Pts',(8.69203094034027,-0.528654133672296,
4.34698967074364));
#41481=CARTESIAN_POINT('Ctrl Pts',(8.73974677640312,-0.577779864139828,
3.74300300926635));
#41482=CARTESIAN_POINT('Ctrl Pts',(8.78746261246595,-0.0963214550818077,
3.37502063878676));
#41483=CARTESIAN_POINT('Ctrl Pts',(8.8351784485288,0.473590428273928,3.58096643225285));
#41484=CARTESIAN_POINT('Ctrl Pts',(8.88289428459164,0.608596934220305,4.17171719864135));
#41485=CARTESIAN_POINT('Ctrl Pts',(8.93061012065447,0.184719511004659,4.60477741930878));
#41486=CARTESIAN_POINT('Ctrl Pts',(8.97832595671731,-0.408788681441581,
4.48246123012823));
#41487=CARTESIAN_POINT('Ctrl Pts',(9.02604179278014,-0.626899937697651,
3.91709346970068));
#41488=CARTESIAN_POINT('Ctrl Pts',(9.07375762884299,-0.269319335070538,
3.42786005172794));
#41489=CARTESIAN_POINT('Ctrl Pts',(9.12147346490582,0.335581356962483,3.46403155175812));
#41490=CARTESIAN_POINT('Ctrl Pts',(9.16918930096866,0.632312525313962,3.99239112474344));
#41491=CARTESIAN_POINT('Ctrl Pts',(9.21690513703149,0.348381372290835,4.52773804495445));
#41492=CARTESIAN_POINT('Ctrl Pts',(9.26462097309434,-0.255473755443411,
4.5784549981902));
#41493=CARTESIAN_POINT('Ctrl Pts',(9.31233680915717,-0.624723402584967,
4.09796782591368));
#41494=CARTESIAN_POINT('Ctrl Pts',(9.36005264522002,-0.420279936527615,
3.52751529167185));
#41495=CARTESIAN_POINT('Ctrl Pts',(9.40776848128285,0.170113062081096,3.39095273519949));
#41496=CARTESIAN_POINT('Ctrl Pts',(9.45548431734569,0.604288618254829,3.81368765339017));
#41497=CARTESIAN_POINT('Ctrl Pts',(9.50320015340853,0.483536638109595,4.40751606625661));
#41498=CARTESIAN_POINT('Ctrl Pts',(9.55091598947137,-0.0812544769791981,
4.62711620503893));
#41499=CARTESIAN_POINT('Ctrl Pts',(9.5986318255342,-0.571428355597161,4.27082588331087));
#41500=CARTESIAN_POINT('Ctrl Pts',(9.64634766159704,-0.536850782714826,
3.66583198574659));
#41501=CARTESIAN_POINT('Ctrl Pts',(9.69406349765987,-0.0092748755543832,
3.36770971750703));
#41502=CARTESIAN_POINT('Ctrl Pts',(9.74177933372272,0.52681829253995,3.65022934471732));
#41503=CARTESIAN_POINT('Ctrl Pts',(9.78949516978555,0.579126116453474,4.253948746587));
#41504=CARTESIAN_POINT('Ctrl Pts',(9.83721100584839,0.099613516627068,4.62446310696212));
#41505=CARTESIAN_POINT('Ctrl Pts',(9.88492684191123,-0.471375708268938,
4.42152338761395));
#41506=CARTESIAN_POINT('Ctrl Pts',(9.93264267797408,-0.609493367214024,
3.83149225544889));
#41507=CARTESIAN_POINT('Ctrl Pts',(9.9803585140369,-0.187903888785556,3.39620437793004));
#41508=CARTESIAN_POINT('Ctrl Pts',(10.0280743500997,0.406240621987656,3.51539131074786));
#41509=CARTESIAN_POINT('Ctrl Pts',(10.0757901861626,0.627328118774167,4.07960185956908));
#41510=CARTESIAN_POINT('Ctrl Pts',(10.1235060222254,0.27233055140652,4.57071279591595));
#41511=CARTESIAN_POINT('Ctrl Pts',(10.1712218582883,-0.332752351661881,
4.5377293902281));
#41512=CARTESIAN_POINT('Ctrl Pts',(10.2189376943511,-0.632263650146131,
4.01094081146358));
#41513=CARTESIAN_POINT('Ctrl Pts',(10.2666535304139,-0.351157510074434,
3.47410511718603));
#41514=CARTESIAN_POINT('Ctrl Pts',(10.3143693664768,0.252421974751429,3.42020678572945));
#41515=CARTESIAN_POINT('Ctrl Pts',(10.3620852025396,0.624198476151732,3.89874148420283));
#41516=CARTESIAN_POINT('Ctrl Pts',(10.4098010386024,0.422763912373798,4.47026343579529));
#41517=CARTESIAN_POINT('Ctrl Pts',(10.4575168746653,-0.166901257195935,
4.60993523836389));
#41518=CARTESIAN_POINT('Ctrl Pts',(10.5052327107281,-0.603298434176698,
4.18949412648294));
#41519=CARTESIAN_POINT('Ctrl Pts',(10.552948546791,-0.485677376113382,3.5950376425108));
#41520=CARTESIAN_POINT('Ctrl Pts',(10.6006643828538,0.0779486895418537,
3.3724643225678));
#41521=CARTESIAN_POINT('Ctrl Pts',(10.6483802189166,0.569993274196054,3.72616667108832));
#41522=CARTESIAN_POINT('Ctrl Pts',(10.6960960549795,0.538604264682155,4.3313343790158));
#41523=CARTESIAN_POINT('Ctrl Pts',(10.7438118910423,0.0126066714187673,
4.63223262845832));
#41524=CARTESIAN_POINT('Ctrl Pts',(10.7915277271052,-0.524967822187051,
4.35254192703816));
#41525=CARTESIAN_POINT('Ctrl Pts',(10.839243563168,-0.580456287010268,3.74910654946403));
#41526=CARTESIAN_POINT('Ctrl Pts',(10.8869593992308,-0.102902812003948,
3.37607048800905));
#41527=CARTESIAN_POINT('Ctrl Pts',(10.9346752352937,0.469147898628881,3.5759984978049));
#41528=CARTESIAN_POINT('Ctrl Pts',(10.9823910713565,0.610372875182502,4.16529361116822));
#41529=CARTESIAN_POINT('Ctrl Pts',(11.0301069074193,0.191083048662156,4.60279705802663));
#41530=CARTESIAN_POINT('Ctrl Pts',(11.0778227434822,-0.403681281635282,
4.48674269127424));
#41531=CARTESIAN_POINT('Ctrl Pts',(11.125538579545,-0.627738879572117,3.92370502162571));
#41532=CARTESIAN_POINT('Ctrl Pts',(11.1732544156079,-0.275334205393669,
3.43073020456744));
#41533=CARTESIAN_POINT('Ctrl Pts',(11.2209702516707,0.329914106159097,3.46052459999659));
#41534=CARTESIAN_POINT('Ctrl Pts',(11.2686860877335,0.632197217644931,3.98572755614488));
#41535=CARTESIAN_POINT('Ctrl Pts',(11.3164019237964,0.353923896562866,4.52403711709511));
#41536=CARTESIAN_POINT('Ctrl Pts',(11.3641177598592,-0.24936318455202,4.58111533006939));
#41537=CARTESIAN_POINT('Ctrl Pts',(11.411833595922,-0.623656216347001,4.10454639383227));
#41538=CARTESIAN_POINT('Ctrl Pts',(11.4595494319849,-0.425236148486169,
3.53197089548594));
#41539=CARTESIAN_POINT('Ctrl Pts',(11.5072652680477,0.163684817628688,3.3891937253683));
#41540=CARTESIAN_POINT('Ctrl Pts',(11.5549811041106,0.602291497100466,3.80732935570755));
#41541=CARTESIAN_POINT('Ctrl Pts',(11.6026969401734,0.487804627338989,4.40239740331947));
#41542=CARTESIAN_POINT('Ctrl Pts',(11.6504127762363,-0.0746407375468588,
4.62793772378323));
#41543=CARTESIAN_POINT('Ctrl Pts',(11.6981286122991,-0.568542364648052,
4.276833170433));
#41544=CARTESIAN_POINT('Ctrl Pts',(11.7458444483619,-0.540342790144192,
3.67150845704832));
#41545=CARTESIAN_POINT('Ctrl Pts',(11.7935602844247,-0.0159381172083995,
3.36784258204823));
#41546=CARTESIAN_POINT('Ctrl Pts',(11.8412761204876,0.523102773999324,3.64469659094542));
#41547=CARTESIAN_POINT('Ctrl Pts',(11.8889919565504,0.581770338872691,4.24783118742311));
#41548=CARTESIAN_POINT('Ctrl Pts',(11.9367077926133,0.106189249871976,4.62337859111715));
#41549=CARTESIAN_POINT('Ctrl Pts',(11.9844236286761,-0.466907061217805,
4.4264678426758));
#41550=CARTESIAN_POINT('Ctrl Pts',(12.0321394647389,-0.611235433702689,
3.83792511225401));
#41551=CARTESIAN_POINT('Ctrl Pts',(12.0798553008018,-0.19425690235234,3.39821824509208));
#41552=CARTESIAN_POINT('Ctrl Pts',(12.1275711368646,0.401110731454808,3.51113682306459));
#41553=CARTESIAN_POINT('Ctrl Pts',(12.1752869729275,0.628132208685083,4.07298597854376));
#41554=CARTESIAN_POINT('Ctrl Pts',(12.2230028089903,0.27833021362349,4.56781098689255));
#41555=CARTESIAN_POINT('Ctrl Pts',(12.2707186450531,-0.327066699269377,
4.54120642908287));
#41556=CARTESIAN_POINT('Ctrl Pts',(12.3184344811159,-0.632113229655128,
4.01760367991507));
#41557=CARTESIAN_POINT('Ctrl Pts',(12.3661503171788,-0.356680454936339,
3.47783520061383));
#41558=CARTESIAN_POINT('Ctrl Pts',(12.4138661532416,0.246297469784735,3.4175786911271));
#41559=CARTESIAN_POINT('Ctrl Pts',(12.4615819893045,0.623096638228782,3.89216863128209));
#41560=CARTESIAN_POINT('Ctrl Pts',(12.5092978253673,0.427696576213203,4.46578177652963));
#41561=CARTESIAN_POINT('Ctrl Pts',(12.5570136614302,-0.16046383269669,4.61166034941614));
#41562=CARTESIAN_POINT('Ctrl Pts',(12.604729497493,-0.601267834987779,4.1958418118296));
#41563=CARTESIAN_POINT('Ctrl Pts',(12.6524453335558,-0.489918332714758,
3.60017872502631));
#41564=CARTESIAN_POINT('Ctrl Pts',(12.7001611696187,0.0713307128527425,
3.37167766707246));
#41565=CARTESIAN_POINT('Ctrl Pts',(12.7478770056815,0.56707566724347,3.72017467542775));
#41566=CARTESIAN_POINT('Ctrl Pts',(12.7955928417444,0.542066310823814,4.32563958500381));
#41567=CARTESIAN_POINT('Ctrl Pts',(12.8433086778072,0.0192691204123526,
4.63206465306178));
#41568=CARTESIAN_POINT('Ctrl Pts',(12.89102451387,-0.521223199767296,4.35805502464836));
#41569=CARTESIAN_POINT('Ctrl Pts',(12.9387403499329,-0.583068235550835,
3.7552379577156));
#41570=CARTESIAN_POINT('Ctrl Pts',(12.9864561859957,-0.109472738970043,
3.37718964036075));
#41571=CARTESIAN_POINT('Ctrl Pts',(13.0341720220585,0.464653258261548,3.57107765943178));
#41572=CARTESIAN_POINT('Ctrl Pts',(13.0818878581214,0.612081018822183,4.15885166366515));
#41573=CARTESIAN_POINT('Ctrl Pts',(13.1296036941842,0.197425361721354,4.6007497409078));
#41574=CARTESIAN_POINT('Ctrl Pts',(13.177319530247,-0.398529042827853,4.49097008735187));
#41575=CARTESIAN_POINT('Ctrl Pts',(13.2250353663099,-0.628508095190705,
3.93032504803489));
#41576=CARTESIAN_POINT('Ctrl Pts',(13.2727512023727,-0.281318492899819,
3.4336635891944));
#41577=CARTESIAN_POINT('Ctrl Pts',(13.3204670384356,0.324210210062374,3.45707757060249));
#41578=CARTESIAN_POINT('Ctrl Pts',(13.3681828744984,0.632011688508986,3.97906557286167));
#41579=CARTESIAN_POINT('Ctrl Pts',(13.4158987105612,0.359427108647973,4.52027798167956));
#41580=CARTESIAN_POINT('Ctrl Pts',(13.4636145466241,-0.243224915581421,
4.58371111441534));
#41581=CARTESIAN_POINT('Ctrl Pts',(13.5113303826869,-0.622519757336015,
4.11111334923356));
#41582=CARTESIAN_POINT('Ctrl Pts',(13.5590462187498,-0.430145127231255,
3.53647848575196));
#41583=CARTESIAN_POINT('Ctrl Pts',(13.6067620548126,0.157238391843492,3.38750256099959));
#41584=CARTESIAN_POINT('Ctrl Pts',(13.6544778908755,0.600227476264717,3.8009924589658));
#41585=CARTESIAN_POINT('Ctrl Pts',(13.7021937269383,0.492018433545193,4.39723404398833));
#41586=CARTESIAN_POINT('Ctrl Pts',(13.7499095630011,-0.0680187073756014,
4.62868949418496));
#41587=CARTESIAN_POINT('Ctrl Pts',(13.797625399064,-0.565593222711038,4.28280970824024));
#41588=CARTESIAN_POINT('Ctrl Pts',(13.8453412351268,-0.543774778860562,
3.67722141563181));
#41589=CARTESIAN_POINT('Ctrl Pts',(13.8930570711896,-0.0225995885319848,
3.36804566363559));
#41590=CARTESIAN_POINT('Ctrl Pts',(13.9407729072525,0.519329151684885,3.63920330259016));
#41591=CARTESIAN_POINT('Ctrl Pts',(13.9884887433153,0.584349941003394,4.24168610034696));
#41592=CARTESIAN_POINT('Ctrl Pts',(14.0362045793781,0.112753188118911,4.62222483333648));
#41593=CARTESIAN_POINT('Ctrl Pts',(14.083920415441,-0.462386552345973,4.43136492771341));
#41594=CARTESIAN_POINT('Ctrl Pts',(14.1316362515038,-0.612909607059929,
3.84437597156854));
#41595=CARTESIAN_POINT('Ctrl Pts',(14.1793520875667,-0.200588338784227,
3.40029895531576));
#41596=CARTESIAN_POINT('Ctrl Pts',(14.2270679236295,0.395936287445344,3.50693663598317));
#41597=CARTESIAN_POINT('Ctrl Pts',(14.2747837596923,0.628866528650988,4.06636199058228));
#41598=CARTESIAN_POINT('Ctrl Pts',(14.3224995957552,0.284298960241116,4.5648461081192));
#41599=CARTESIAN_POINT('Ctrl Pts',(14.370215431818,-0.321344717859966,4.54462335329573));
#41600=CARTESIAN_POINT('Ctrl Pts',(14.4179312678809,-0.631892597026201,
4.02426459303334));
#41601=CARTESIAN_POINT('Ctrl Pts',(14.4656471039437,-0.362163781425906,
3.48162328362967));
#41602=CARTESIAN_POINT('Ctrl Pts',(14.5133629400065,0.240145607263868,3.41501528911991));
#41603=CARTESIAN_POINT('Ctrl Pts',(14.5610787760693,0.6219255896881,3.8856077557581));
#41604=CARTESIAN_POINT('Ctrl Pts',(14.6087946121322,0.432581733546503,4.46124838043455));
#41605=CARTESIAN_POINT('Ctrl Pts',(14.656510448195,-0.154008584636381,4.61331752013935));
#41606=CARTESIAN_POINT('Ctrl Pts',(14.7042262842579,-0.599170449821005,
4.20216774399712));
#41607=CARTESIAN_POINT('Ctrl Pts',(14.7519421203207,-0.494104871512583,
3.60536421779174));
#41608=CARTESIAN_POINT('Ctrl Pts',(14.7996579563836,0.0647048130865326,
3.37096080264023));
#41609=CARTESIAN_POINT('Ctrl Pts',(14.8473737924464,0.564095072216763,3.71421376143635));
#41610=CARTESIAN_POINT('Ctrl Pts',(14.8950896285093,0.545468146811986,4.319908620492));
#41611=CARTESIAN_POINT('Ctrl Pts',(14.942805464572,0.0259294290834894,4.63182647092298));
#41612=CARTESIAN_POINT('Ctrl Pts',(14.9905213006349,-0.517420682347921,
4.36352835120552));
#41613=CARTESIAN_POINT('Ctrl Pts',(15.0382371366977,-0.585615419638682,
3.76139655297334));
#41614=CARTESIAN_POINT('Ctrl Pts',(15.0859529727606,-0.116030506223773,
3.3783779715317));
#41615=CARTESIAN_POINT('Ctrl Pts',(15.1336688088234,0.460107006415252,3.56620446371685));
#41616=CARTESIAN_POINT('Ctrl Pts',(15.1813846448862,0.613721175406852,4.15239207167311));
#41617=CARTESIAN_POINT('Ctrl Pts',(15.2291004809491,0.203745745708236,4.59863569535852));
#41618=CARTESIAN_POINT('Ctrl Pts',(15.2768163170119,-0.393332537305518,
4.49514294880206));
#41619=CARTESIAN_POINT('Ctrl Pts',(15.3245321530748,-0.629207499112597,
3.93695281360709));
#41620=CARTESIAN_POINT('Ctrl Pts',(15.3722479891376,-0.287271532882751,
3.43665987978239));
#41621=CARTESIAN_POINT('Ctrl Pts',(15.4199638252004,0.318470302234025,3.45369084645546));
#41622=CARTESIAN_POINT('Ctrl Pts',(15.4676796612633,0.631755958513824,3.97240591487529));
#41623=CARTESIAN_POINT('Ctrl Pts',(15.5153954973261,0.364890397275464,4.51646105625472));
#41624=CARTESIAN_POINT('Ctrl Pts',(15.563111333389,-0.237059630341402,4.58624206290064));
#41625=CARTESIAN_POINT('Ctrl Pts',(15.6108271694518,-0.621314151784485,
4.11766796269128));
#41626=CARTESIAN_POINT('Ctrl Pts',(15.6585430055147,-0.435006327496808,
3.54103756178819));
#41627=CARTESIAN_POINT('Ctrl Pts',(15.7062588415774,0.150774500763906,3.38587942993986));
#41628=CARTESIAN_POINT('Ctrl Pts',(15.7539746776403,0.598096785009218,3.79467766703735));
#41629=CARTESIAN_POINT('Ctrl Pts',(15.8016905137032,0.496177588678611,4.39202656178461));
#41630=CARTESIAN_POINT('Ctrl Pts',(15.849406349766,-0.0613891220090978,
4.62937143274106));
#41631=CARTESIAN_POINT('Ctrl Pts',(15.8971221858288,-0.562581257362808,
4.28875483288714));
#41632=CARTESIAN_POINT('Ctrl Pts',(15.9448380218917,-0.547146367654922,
3.68297022692873));
#41633=CARTESIAN_POINT('Ctrl Pts',(15.9925538579545,-0.0292585496004989,
3.36831893971177));
#41634=CARTESIAN_POINT('Ctrl Pts',(16.0402696940173,0.515497844752703,3.63375008981994));
#41635=CARTESIAN_POINT('Ctrl Pts',(16.0879855300802,0.586864636315616,4.23551416792571));
#41636=CARTESIAN_POINT('Ctrl Pts',(16.135701366143,0.119304602276749,4.62100196177401));
#41637=CARTESIAN_POINT('Ctrl Pts',(16.1834172022059,-0.457814683770117,
4.43621409878185));
#41638=CARTESIAN_POINT('Ctrl Pts',(16.2311330382687,-0.614515701326505,
3.85084411686165));
#41639=CARTESIAN_POINT('Ctrl Pts',(16.2788488743316,-0.206897494815317,
3.40244627748567));
#41640=CARTESIAN_POINT('Ctrl Pts',(16.3265647103943,0.390717864711932,3.50279121604045));
#41641=CARTESIAN_POINT('Ctrl Pts',(16.3742805464572,0.629530997107116,4.05973063144581));
#41642=CARTESIAN_POINT('Ctrl Pts',(16.42199638252,0.290236128279341,4.56181848892059));
#41643=CARTESIAN_POINT('Ctrl Pts',(16.4697122185829,-0.315587043004215,
4.54797978333095));
#41644=CARTESIAN_POINT('Ctrl Pts',(16.5174280546457,-0.631601776766168,
4.03092281095576));
#41645=CARTESIAN_POINT('Ctrl Pts',(16.5651438907086,-0.367606880481235,
3.48546894547127));
#41646=CARTESIAN_POINT('Ctrl Pts',(16.6128597267714,0.233967070508539,3.41251686443844));
#41647=CARTESIAN_POINT('Ctrl Pts',(16.6605755628343,0.620685460604191,3.87905958638177));
#41648=CARTESIAN_POINT('Ctrl Pts',(16.7082913988971,0.437418841753611,4.45666375105816));
#41649=CARTESIAN_POINT('Ctrl Pts',(16.7560072349599,-0.147536230033309,
4.61490656646286));
#41650=CARTESIAN_POINT('Ctrl Pts',(16.8037230710227,-0.597006511643959,
4.20847122033102));
#41651=CARTESIAN_POINT('Ctrl Pts',(16.8514389070856,-0.498236527486006,
3.61059354482716));
#41652=CARTESIAN_POINT('Ctrl Pts',(16.8991547431484,0.058071726216741,3.37031380889701));
#41653=CARTESIAN_POINT('Ctrl Pts',(16.9468705792113,0.561051820186282,3.70828459122417));
#41654=CARTESIAN_POINT('Ctrl Pts',(16.9945864152741,0.548809394786867,4.31414212204871));
#41655=CARTESIAN_POINT('Ctrl Pts',(17.0423022513369,0.0325868576366809,
4.63151810849805));
#41656=CARTESIAN_POINT('Ctrl Pts',(17.0900180873998,-0.513560692294518,
4.3689612987585));
#41657=CARTESIAN_POINT('Ctrl Pts',(17.1377339234626,-0.588097556344686,
3.76758165116972));
#41658=CARTESIAN_POINT('Ctrl Pts',(17.1854497595255,-0.122575385359494,
3.37963534952775));
#41659=CARTESIAN_POINT('Ctrl Pts',(17.2331655955883,0.455509648066065,3.56137945195155));
#41660=CARTESIAN_POINT('Ctrl Pts',(17.2808814316511,0.615293162755707,4.14591555269289));
#41661=CARTESIAN_POINT('Ctrl Pts',(17.328597267714,0.210043498584534,4.59645515619697));
#41662=CARTESIAN_POINT('Ctrl Pts',(17.3763131037768,-0.388092342271454,
4.49926081212312));
#41663=CARTESIAN_POINT('Ctrl Pts',(17.4240289398397,-0.629837013651323,
3.94358758216158));
#41664=CARTESIAN_POINT('Ctrl Pts',(17.4717447759025,-0.293192664107019,
3.43971874351766));
#41665=CARTESIAN_POINT('Ctrl Pts',(17.5194606119653,0.312695020235776,3.45036480373676));
#41666=CARTESIAN_POINT('Ctrl Pts',(17.5671764480282,0.631430056064715,3.96574932190893));
#41667=CARTESIAN_POINT('Ctrl Pts',(17.614892284091,0.370313155609181,4.51258676478657));
#41668=CARTESIAN_POINT('Ctrl Pts',(17.6626081201539,-0.230868013642575,
4.58870789439952));
#41669=CARTESIAN_POINT('Ctrl Pts',(17.7103239562166,-0.620039533605355,
4.12420950615009));
#41670=CARTESIAN_POINT('Ctrl Pts',(17.7580397922796,-0.43981920932378,3.54564761719411));
#41671=CARTESIAN_POINT('Ctrl Pts',(17.8057556283423,0.144293862368219,3.38432451247882));
#41672=CARTESIAN_POINT('Ctrl Pts',(17.8534714644052,0.595899660001039,3.78838568133928));
#41673=CARTESIAN_POINT('Ctrl Pts',(17.901187300468,0.500281630760053,4.38677553513073));
#41674=CARTESIAN_POINT('Ctrl Pts',(17.9489031365309,-0.0547527178302441,
4.62998346370502));
#41675=CARTESIAN_POINT('Ctrl Pts',(17.9966189725937,-0.559506803158163,
4.29466788401745));
#41676=CARTESIAN_POINT('Ctrl Pts',(18.0443348086565,-0.550457182027191,
3.68875425238845));
#41677=CARTESIAN_POINT('Ctrl Pts',(18.0920506447194,-0.0359142607682062,
3.36866237992255));
#41678=CARTESIAN_POINT('Ctrl Pts',(18.1397664807822,0.511609278766163,3.62833755835171));
#41679=CARTESIAN_POINT('Ctrl Pts',(18.187482316845,0.589314145488933,4.22931607570827));
#41680=CARTESIAN_POINT('Ctrl Pts',(18.2351981529079,0.12584276464555,4.61971011226051));
#41681=CARTESIAN_POINT('Ctrl Pts',(18.2829139889707,-0.453191963311679,
4.44101481725822));
#41682=CARTESIAN_POINT('Ctrl Pts',(18.3306298250336,-0.616053538105107,
3.85732882968247));
#41683=CARTESIAN_POINT('Ctrl Pts',(18.3783456610964,-0.213183669654489,
3.40465997308746));
#41684=CARTESIAN_POINT('Ctrl Pts',(18.4260614971592,0.385456042892229,3.49870102369));
#41685=CARTESIAN_POINT('Ctrl Pts',(18.4737773332221,0.630125540247444,4.05309263771424));
#41686=CARTESIAN_POINT('Ctrl Pts',(18.5214931692849,0.296141058265729,4.55872846559028));
#41687=CARTESIAN_POINT('Ctrl Pts',(18.5692090053478,-0.309794314237323,
4.55127534637221));
#41688=CARTESIAN_POINT('Ctrl Pts',(18.6169248414106,-0.631240801177943,
4.0375775941191));
#41689=CARTESIAN_POINT('Ctrl Pts',(18.6646406774734,-0.373009147508776,
3.4893717589807));
#41690=CARTESIAN_POINT('Ctrl Pts',(18.7123565135363,0.227762545801372,3.41008369459593));
#41691=CARTESIAN_POINT('Ctrl Pts',(18.7600723495991,0.619376388724522,3.87252485049244));
#41692=CARTESIAN_POINT('Ctrl Pts',(18.8077881856619,0.442207363551868,4.45202839763978));
#41693=CARTESIAN_POINT('Ctrl Pts',(18.8555040217248,-0.141047487806633,
4.61642731188217));
#41694=CARTESIAN_POINT('Ctrl Pts',(18.9032198577876,-0.594776260815313,
4.21475154067248));
#41695=CARTESIAN_POINT('Ctrl Pts',(18.9509356938505,-0.502312841712761,
3.615866125281));
#41696=CARTESIAN_POINT('Ctrl Pts',(18.9986515299133,0.0514321890198641,
3.36973675771293));
#41697=CARTESIAN_POINT('Ctrl Pts',(19.0463673659762,0.557946249173174,3.70238782336559));
#41698=CARTESIAN_POINT('Ctrl Pts',(19.0940832020389,0.552089683635207,4.30834073020757));
#41699=CARTESIAN_POINT('Ctrl Pts',(19.1417990381018,0.0392406665648073,
4.63113960000379));
#41700=CARTESIAN_POINT('Ctrl Pts',(19.1895148741646,-0.509643658296843,
4.3743532639067));
#41701=CARTESIAN_POINT('Ctrl Pts',(19.2372307102275,-0.590514370077448,
3.77379256516987));
#41702=CARTESIAN_POINT('Ctrl Pts',(19.2849465462903,-0.129106649190522,
3.38096163491845));
#41703=CARTESIAN_POINT('Ctrl Pts',(19.3326623823532,0.450861693465423,3.55660315963506));
#41704=CARTESIAN_POINT('Ctrl Pts',(19.380378218416,0.616796807017627,4.1394228269368));
#41705=CARTESIAN_POINT('Ctrl Pts',(19.4280940544789,0.216317919394901,4.59420836405745));
#41706=CARTESIAN_POINT('Ctrl Pts',(19.4758098905416,-0.382809037079938,
4.50332322288615));
#41707=CARTESIAN_POINT('Ctrl Pts',(19.5235257266046,-0.630396573984801,
3.95022861114352));
#41708=CARTESIAN_POINT('Ctrl Pts',(19.5712415626673,-0.299081219248977,
3.44283985120298));
#41709=CARTESIAN_POINT('Ctrl Pts',(19.6189573987302,0.306884987370396,3.44709979193512));
#41710=CARTESIAN_POINT('Ctrl Pts',(19.666673234793,0.631034051704256,3.95909657101937));
#41711=CARTESIAN_POINT('Ctrl Pts',(19.7143890708559,0.375694716468479,4.50865546647685));
#41712=CARTESIAN_POINT('Ctrl Pts',(19.7621049069187,-0.224650630777236,
4.59110846933868));
#41713=CARTESIAN_POINT('Ctrl Pts',(19.8098207429815,-0.618696275574682,
4.13073699938377));
#41714=CARTESIAN_POINT('Ctrl Pts',(19.8575365790444,-0.44458280157215,3.55030861879767));
#41715=CARTESIAN_POINT('Ctrl Pts',(19.9052524151072,0.13779637220375,3.3828370770856));
#41716=CARTESIAN_POINT('Ctrl Pts',(19.9529682511701,0.593637901716091,3.7821189081517));
#41717=CARTESIAN_POINT('Ctrl Pts',(20.0006840872329,0.504327165075627,4.38147832337345));
#41718=CARTESIAN_POINT('Ctrl Pts',(20.0483999232957,-0.0481046828163007,
4.63053160650705));
#41719=CARTESIAN_POINT('Ctrl Pts',(20.0961157593586,-0.556380679578279,
4.30053671048834));
#41720=CARTESIAN_POINT('Ctrl Pts',(20.1438315954214,-0.553687069357429,
3.69459455385474));
#41721=CARTESIAN_POINT('Ctrl Pts',(20.1915474314843,-0.0426033430871586,
3.36903495876776));
#41722=CARTESIAN_POINT('Ctrl Pts',(20.2392632675471,0.507734449822709,3.62304374442814));
#41723=CARTESIAN_POINT('Ctrl Pts',(20.2869791036099,0.591564791291533,4.22294595084339));
#41724=CARTESIAN_POINT('Ctrl Pts',(20.3346949396728,0.132620199007312,4.618629012875));
#41725=CARTESIAN_POINT('Ctrl Pts',(20.3824107757356,-0.449008129734859,
4.44521533979349));
#41726=CARTESIAN_POINT('Ctrl Pts',(20.4221739724547,-0.588594799935545,
3.96175478680276));
#41727=CARTESIAN_POINT('Ctrl Pts',(20.4539845298298,-0.419131055782338,
3.63395025773895));
#41728=CARTESIAN_POINT('Ctrl Pts',(20.4778424478613,-0.194099195253748,
3.47709810398663));
#41729=CARTESIAN_POINT('Ctrl Pts',(20.5017003658927,0.0810471032980313,
3.44846366347126));
#41730=CARTESIAN_POINT('Ctrl Pts',(20.5255582839241,0.334940048200093,3.55449674151986));
#41731=CARTESIAN_POINT('Ctrl Pts',(20.5494162019556,0.507694843328107,3.76957374638464));
#41732=CARTESIAN_POINT('Ctrl Pts',(20.5732741199869,0.555899439471162,4.04093981905292));
#41733=CARTESIAN_POINT('Ctrl Pts',(20.5971320380184,0.468386015874758,4.30232489481291));
#41734=CARTESIAN_POINT('Ctrl Pts',(20.6209899560498,0.266225827016684,4.48976745893774));
#41735=CARTESIAN_POINT('Ctrl Pts',(20.6448478740812,-0.000973650874560818,
4.55745692740964));
#41736=CARTESIAN_POINT('Ctrl Pts',(20.6687057921126,-0.267966914960919,
4.48882854939535));
#41737=CARTESIAN_POINT('Ctrl Pts',(20.6925637101441,-0.469418090387657,
4.30067062862012));
#41738=CARTESIAN_POINT('Ctrl Pts',(20.7164216281755,-0.556092695039732,
4.03898930289119));
#41739=CARTESIAN_POINT('Ctrl Pts',(20.7402795462069,-0.506782753954552,
3.7677746905255));
#41740=CARTESIAN_POINT('Ctrl Pts',(20.7641374642383,-0.333553132261349,
3.55334514249538));
#41741=CARTESIAN_POINT('Ctrl Pts',(20.7879953822697,-0.0787593560922578,
3.44813505886707));
#41742=CARTESIAN_POINT('Ctrl Pts',(20.8118533003012,0.19529252477751,3.47787088781106));
#41743=CARTESIAN_POINT('Ctrl Pts',(20.8357112183325,0.421590436108717,3.63528155911584));
#41744=CARTESIAN_POINT('Ctrl Pts',(20.859569136364,0.544797804677434,3.8818757964511));
#41745=CARTESIAN_POINT('Ctrl Pts',(20.8834270543954,0.534787374467886,4.15735463375504));
#41746=CARTESIAN_POINT('Ctrl Pts',(20.9072849724269,0.394006808563119,4.39435596913946));
#41747=CARTESIAN_POINT('Ctrl Pts',(20.9311428904582,0.156880874733563,4.53492653211281));
#41748=CARTESIAN_POINT('Ctrl Pts',(20.9550008084897,-0.118606721834374,
4.54469298471526));
#41749=CARTESIAN_POINT('Ctrl Pts',(20.9788587265211,-0.365091735913813,
4.42126716656144));
#41750=CARTESIAN_POINT('Ctrl Pts',(21.0027166445525,-0.522301880015273,
4.19483005048941));
#41751=CARTESIAN_POINT('Ctrl Pts',(21.0265745625839,-0.55179498493052,3.92075168033001));
#41752=CARTESIAN_POINT('Ctrl Pts',(21.0504324806153,-0.446359186657349,
3.66605168284066));
#41753=CARTESIAN_POINT('Ctrl Pts',(21.0742903986468,-0.231776408019839,
3.49301114555638));
#41754=CARTESIAN_POINT('Ctrl Pts',(21.0981483166782,0.0394820154987394,
3.44394319323497));
#41755=CARTESIAN_POINT('Ctrl Pts',(21.1220062347096,0.301086010940692,3.5308462768762));
#41756=CARTESIAN_POINT('Ctrl Pts',(21.145864152741,0.489066275193333,3.73247022529863));
#41757=CARTESIAN_POINT('Ctrl Pts',(21.1697220707724,0.557456513314207,3.9995124910074));
#41758=CARTESIAN_POINT('Ctrl Pts',(21.1935799888039,0.489533449092281,4.26667396594056));
#41759=CARTESIAN_POINT('Ctrl Pts',(21.2174379068352,0.30190612195814,4.46862639215028));
#41760=CARTESIAN_POINT('Ctrl Pts',(21.2412958248667,0.0404545242400231,
4.55598690035157));
#41761=CARTESIAN_POINT('Ctrl Pts',(21.2651537428981,-0.230889306609896,
4.50739346663836));
#41762=CARTESIAN_POINT('Ctrl Pts',(21.2890116609295,-0.445774412697373,
4.33472850921124));
#41763=CARTESIAN_POINT('Ctrl Pts',(21.312869578961,-0.551655532228011,4.08021331346062));
#41764=CARTESIAN_POINT('Ctrl Pts',(21.3367274969923,-0.522641847334507,
3.80608377760199));
#41765=CARTESIAN_POINT('Ctrl Pts',(21.3605854150238,-0.365827994289322,
3.57937204029158));
#41766=CARTESIAN_POINT('Ctrl Pts',(21.3844433330552,-0.119559231686077,
3.45551529680541));
#41767=CARTESIAN_POINT('Ctrl Pts',(21.4083012510867,0.155945019792583,3.46479989471587));
#41768=CARTESIAN_POINT('Ctrl Pts',(21.432159169118,0.393316466074861,3.60495549692644));
#41769=CARTESIAN_POINT('Ctrl Pts',(21.4560170871495,0.534511322676435,3.84171024093472));
#41770=CARTESIAN_POINT('Ctrl Pts',(21.4798750051809,0.545003601087511,4.11717114276091));
#41771=CARTESIAN_POINT('Ctrl Pts',(21.5037329232123,0.422227653432673,4.36398050850424));
#41772=CARTESIAN_POINT('Ctrl Pts',(21.5275908412437,0.196205543263173,4.52178672528827));
#41773=CARTESIAN_POINT('Ctrl Pts',(21.5514487592751,-0.0777941667658609,
4.5520018745543));
#41774=CARTESIAN_POINT('Ctrl Pts',(21.5753066773066,-0.332771083950078,
4.44723752926263));
#41775=CARTESIAN_POINT('Ctrl Pts',(21.5991645953379,-0.506376406606172,
4.23311142556056));
#41776=CARTESIAN_POINT('Ctrl Pts',(21.6230225133694,-0.556158904430687,
3.96198322848119));
#41777=CARTESIAN_POINT('Ctrl Pts',(21.6468804314008,-0.469945400657515,
3.70015116759423));
#41778=CARTESIAN_POINT('Ctrl Pts',(21.6707383494323,-0.268817445367881,
3.51164031394868));
#41779=CARTESIAN_POINT('Ctrl Pts',(21.6945962674636,-0.00195630224560004,
3.44254670619344));
#41780=CARTESIAN_POINT('Ctrl Pts',(21.7184541854951,0.26538321006433,3.50976561349676));
#41781=CARTESIAN_POINT('Ctrl Pts',(21.7423121035264,0.467829298620023,3.6968601820167));
#41782=CARTESIAN_POINT('Ctrl Pts',(21.766170021558,0.555878380248887,3.95808069339639));
#41783=CARTESIAN_POINT('Ctrl Pts',(21.7900279395893,0.508000056083844,4.22955161709966));
#41784=CARTESIAN_POINT('Ctrl Pts',(21.8138858576208,0.335901880562604,4.44489091756156));
#41785=CARTESIAN_POINT('Ctrl Pts',(21.8377437756521,0.0816665454602928,
4.55144227009437));
#41786=CARTESIAN_POINT('Ctrl Pts',(21.8616016936836,-0.192538484559094,
4.52315096660328));
#41787=CARTESIAN_POINT('Ctrl Pts',(21.885459611715,-0.419662610460766,4.36693500143146));
#41788=CARTESIAN_POINT('Ctrl Pts',(21.9093175297464,-0.544167796724789,
4.12099343330092));
#41789=CARTESIAN_POINT('Ctrl Pts',(21.9331754477779,-0.535609133856441,
3.84546567493331));
#41790=CARTESIAN_POINT('Ctrl Pts',(21.9570333658092,-0.396079448060293,
3.60772576847503));
#41791=CARTESIAN_POINT('Ctrl Pts',(21.9808912838407,-0.159697548225882,
3.46590759696012));
#41792=CARTESIAN_POINT('Ctrl Pts',(22.0047492018721,0.115734752223676,3.45468956637345));
#41793=CARTESIAN_POINT('Ctrl Pts',(22.0286071199035,0.362866753203085,3.5768147907664));
#41794=CARTESIAN_POINT('Ctrl Pts',(22.0524650379349,0.521267948732644,3.80242032615069));
#41795=CARTESIAN_POINT('Ctrl Pts',(22.0763229559664,0.552204931742854,4.07633947375325));
#41796=CARTESIAN_POINT('Ctrl Pts',(22.1001808739978,0.448112767182329,4.33159154057792));
#41797=CARTESIAN_POINT('Ctrl Pts',(22.1240387920292,0.23444482469764,4.5057604433585));
#41798=CARTESIAN_POINT('Ctrl Pts',(22.1478967100606,-0.0365512635718279,
4.55625714110116));
#41799=CARTESIAN_POINT('Ctrl Pts',(22.171754628092,-0.298609572266455,4.47073381570218));
#41800=CARTESIAN_POINT('Ctrl Pts',(22.1956125461234,-0.487649706571227,
4.2701032498363));
#41801=CARTESIAN_POINT('Ctrl Pts',(22.2194704641549,-0.557446204325542,
4.00342508191314));
#41802=CARTESIAN_POINT('Ctrl Pts',(22.2433283821863,-0.490931920559466,
3.73590938817905));
#41803=CARTESIAN_POINT('Ctrl Pts',(22.2671863002177,-0.304371409562025,
3.53297104269219));
#41804=CARTESIAN_POINT('Ctrl Pts',(22.2910442182491,-0.0433837978980346,
3.44423399893113));
#41805=CARTESIAN_POINT('Ctrl Pts',(22.3149021362806,0.228212333880327,3.49139688109763));
#41806=CARTESIAN_POINT('Ctrl Pts',(22.3387600543119,0.444004334066149,3.66292708008725));
#41807=CARTESIAN_POINT('Ctrl Pts',(22.3626179723434,0.551225179343846,3.91688078933633));
#41808=CARTESIAN_POINT('Ctrl Pts',(22.3864758903748,0.523656454698273,4.19115941035881));
#41809=CARTESIAN_POINT('Ctrl Pts',(22.4103338084062,0.368039459933637,4.41869434725418));
#41810=CARTESIAN_POINT('Ctrl Pts',(22.4341917264376,0.122426797365049,4.54384711353805));
#41811=CARTESIAN_POINT('Ctrl Pts',(22.458049644469,-0.153122562087755,4.53601444212637));
#41812=CARTESIAN_POINT('Ctrl Pts',(22.4819075625005,-0.391229265084309,
4.39711164706476));
#41813=CARTESIAN_POINT('Ctrl Pts',(22.5057654805319,-0.533669791868601,
4.16110422172694));
#41814=CARTESIAN_POINT('Ctrl Pts',(22.5296233985633,-0.545613449745194,
3.88570245498666));
#41815=CARTESIAN_POINT('Ctrl Pts',(22.5534813165947,-0.424139885198736,
3.63824949626794));
#41816=CARTESIAN_POINT('Ctrl Pts',(22.5773392346261,-0.198952323217499,
3.47925449370713));
#41817=CARTESIAN_POINT('Ctrl Pts',(22.6011971526576,0.0748840438856019,
3.44759575567767));
#41818=CARTESIAN_POINT('Ctrl Pts',(22.625055070689,0.330410085854462,3.55101527375816));
#41819=CARTESIAN_POINT('Ctrl Pts',(22.6489129887204,0.505140231362423,3.7642230866287));
#41820=CARTESIAN_POINT('Ctrl Pts',(22.6727709067518,0.556352908954721,4.03508610068096));
#41821=CARTESIAN_POINT('Ctrl Pts',(22.6966288247833,0.471516332128332,4.29736710820476));
#41822=CARTESIAN_POINT('Ctrl Pts',(22.7204867428146,0.27139215166714,4.48693847894857));
#41823=CARTESIAN_POINT('Ctrl Pts',(22.7443446608461,0.00488440565515616,
4.55743119390072));
#41824=CARTESIAN_POINT('Ctrl Pts',(22.7682025788775,-0.262778018495442,
4.49163382183027));
#41825=CARTESIAN_POINT('Ctrl Pts',(22.7920604969089,-0.466262514422727,
4.30558517247789));
#41826=CARTESIAN_POINT('Ctrl Pts',(22.8079657755965,-0.525793678117208,
4.1317859159904));
#41827=CARTESIAN_POINT('Ctrl Pts',(22.8159184149403,-0.532958495437544,
4.04301651477895));
#41828=CARTESIAN_POINT('Ctrl Pts',(3.98408158505965,-0.251304309929533,
3.59658905474035));
#41829=CARTESIAN_POINT('Ctrl Pts',(3.99203422440346,-0.184112308377066,
3.5547318870523));
#41830=CARTESIAN_POINT('Ctrl Pts',(4.00793950309107,-0.0284797076443847,
3.50528009766423));
#41831=CARTESIAN_POINT('Ctrl Pts',(4.03179742112249,0.212077873916637,3.55216010213054));
#41832=CARTESIAN_POINT('Ctrl Pts',(4.05565533915392,0.400711255741927,3.70851080938071));
#41833=CARTESIAN_POINT('Ctrl Pts',(4.07951325718533,0.49139298320592,3.93615790384083));
#41834=CARTESIAN_POINT('Ctrl Pts',(4.10337117521676,0.461898357851897,4.17940600742409));
#41835=CARTESIAN_POINT('Ctrl Pts',(4.12722909324816,0.319466186301668,4.37878980142624));
#41836=CARTESIAN_POINT('Ctrl Pts',(4.15108701127959,0.0989109688445654,
4.48554634140719));
#41837=CARTESIAN_POINT('Ctrl Pts',(4.174944929311,-0.145828100556353,4.47357507321567));
#41838=CARTESIAN_POINT('Ctrl Pts',(4.19880284734243,-0.354909590370033,
4.34580100620849));
#41839=CARTESIAN_POINT('Ctrl Pts',(4.22266076537384,-0.477205295803391,
4.13346959398438));
#41840=CARTESIAN_POINT('Ctrl Pts',(4.24651868340526,-0.482811689970624,
3.88850100783657));
#41841=CARTESIAN_POINT('Ctrl Pts',(4.27037660143669,-0.370357271909554,
3.67079708031066));
#41842=CARTESIAN_POINT('Ctrl Pts',(4.2942345194681,-0.167340519784032,3.53359217153378));
#41843=CARTESIAN_POINT('Ctrl Pts',(4.31809243749953,0.0765956044913427,
3.51043671457025));
#41844=CARTESIAN_POINT('Ctrl Pts',(4.34195035553093,0.301801986965541,3.60699279882218));
#41845=CARTESIAN_POINT('Ctrl Pts',(4.36580827356237,0.453209578636439,3.79964985833574));
#41846=CARTESIAN_POINT('Ctrl Pts',(4.38966619159377,0.493795074712635,4.04129798000377));
#41847=CARTESIAN_POINT('Ctrl Pts',(4.4135241096252,0.413634228782107,4.27284762322724));
#41848=CARTESIAN_POINT('Ctrl Pts',(4.43738202765661,0.23232854437776,4.43767858897425));
#41849=CARTESIAN_POINT('Ctrl Pts',(4.46123994568804,-0.00578779637616802,
4.49548521832112));
#41850=CARTESIAN_POINT('Ctrl Pts',(4.48509786371945,-0.242488863923451,
4.43213221465579));
#41851=CARTESIAN_POINT('Ctrl Pts',(4.50895578175088,-0.419894798625899,
4.26311111366653));
#41852=CARTESIAN_POINT('Ctrl Pts',(4.53281369978229,-0.494625017545811,
4.02975217827461));
#41853=CARTESIAN_POINT('Ctrl Pts',(4.55667161781372,-0.448405946262215,
3.78911802491887));
#41854=CARTESIAN_POINT('Ctrl Pts',(4.58052953584513,-0.292539406836986,
3.60005025874973));
#41855=CARTESIAN_POINT('Ctrl Pts',(4.60438745387655,-0.0651390137990107,
3.50878109874461));
#41856=CARTESIAN_POINT('Ctrl Pts',(4.62824537190797,0.178189642449287,3.53762834062211));
#41857=CARTESIAN_POINT('Ctrl Pts',(4.65210328993938,0.377946077338085,3.67953804797316));
#41858=CARTESIAN_POINT('Ctrl Pts',(4.67596120797081,0.485284401269169,3.89980943180067));
#41859=CARTESIAN_POINT('Ctrl Pts',(4.69981912600222,0.473957470210434,4.14458013869048));
#41860=CARTESIAN_POINT('Ctrl Pts',(4.72367704403364,0.34673502734182,4.35399706338589));
#41861=CARTESIAN_POINT('Ctrl Pts',(4.74753496206506,0.134726425416229,4.47685206339739));
#41862=CARTESIAN_POINT('Ctrl Pts',(4.77139288009648,-0.110226457398098,
4.48310374471865));
#41863=CARTESIAN_POINT('Ctrl Pts',(4.7952507981279,-0.328225968870003,4.37122340097448));
#41864=CARTESIAN_POINT('Ctrl Pts',(4.81910871615932,-0.465965290257402,
4.16856882376961));
#41865=CARTESIAN_POINT('Ctrl Pts',(4.84296663419074,-0.489763405537152,
3.92469457743051));
#41866=CARTESIAN_POINT('Ctrl Pts',(4.86682455222216,-0.393801027275785,
3.69923455818817));
#41867=CARTESIAN_POINT('Ctrl Pts',(4.89068247025357,-0.201543570920867,
3.54731988215497));
#41868=CARTESIAN_POINT('Ctrl Pts',(4.914540388285,0.039996778460842,3.50609782569371));
#41869=CARTESIAN_POINT('Ctrl Pts',(4.93839830631641,0.271756826018508,3.58564830447545));
#41870=CARTESIAN_POINT('Ctrl Pts',(4.96225622434784,0.437064927107334,3.76651905952651));
#41871=CARTESIAN_POINT('Ctrl Pts',(4.98611414237925,0.495498748108838,4.00448226441646));
#41872=CARTESIAN_POINT('Ctrl Pts',(5.00997206041068,0.432769628082826,4.24134943356216));
#41873=CARTESIAN_POINT('Ctrl Pts',(5.03382997844209,0.26421654558258,4.41920009197534));
#41874=CARTESIAN_POINT('Ctrl Pts',(5.05768789647352,0.031055320573195,4.49454490911931));
#41875=CARTESIAN_POINT('Ctrl Pts',(5.08154581450493,-0.209699776246285,
4.44896002485074));
#41876=CARTESIAN_POINT('Ctrl Pts',(5.10540373253635,-0.399177565666329,
4.29359218508065));
#41877=CARTESIAN_POINT('Ctrl Pts',(5.12926165056777,-0.491045566902382,
4.06643305876778));
#41878=CARTESIAN_POINT('Ctrl Pts',(5.15311956859918,-0.462839551218119,
3.823029239986));
#41879=CARTESIAN_POINT('Ctrl Pts',(5.17697748663061,-0.321456657764784,
3.62289959261435));
#41880=CARTESIAN_POINT('Ctrl Pts',(5.20083540466202,-0.101468855184408,
3.51498126685736));
#41881=CARTESIAN_POINT('Ctrl Pts',(5.22469332269345,0.143330846444675,3.52566323299877));
#41882=CARTESIAN_POINT('Ctrl Pts',(5.24855124072486,0.353082251864168,3.6523334593461));
#41883=CARTESIAN_POINT('Ctrl Pts',(5.27240915875629,0.476495428935435,3.86401762512973));
#41884=CARTESIAN_POINT('Ctrl Pts',(5.2962670767877,0.483392494157105,4.10895318565465));
#41885=CARTESIAN_POINT('Ctrl Pts',(5.32012499481913,0.372086927210194,4.32724672446184));
#41886=CARTESIAN_POINT('Ctrl Pts',(5.34398291285054,0.169795971115995,4.46551952511629));
#41887=CARTESIAN_POINT('Ctrl Pts',(5.36784083088196,-0.0740147250654609,
4.48996012138256));
#41888=CARTESIAN_POINT('Ctrl Pts',(5.39169874891337,-0.299726804847767,
4.39459212172504));
#41889=CARTESIAN_POINT('Ctrl Pts',(5.4155566669448,-0.452147516450583,4.20273559983216));
#41890=CARTESIAN_POINT('Ctrl Pts',(5.43941458497621,-0.494005844030112,
3.96130470137348));
#41891=CARTESIAN_POINT('Ctrl Pts',(5.46327250300764,-0.415066286295368,
3.72933585746768));
#41892=CARTESIAN_POINT('Ctrl Pts',(5.48713042103905,-0.234631715382576,
3.56355176915442));
#41893=CARTESIAN_POINT('Ctrl Pts',(5.51098833907048,0.00317670118048804,
3.50449116189365));
#41894=CARTESIAN_POINT('Ctrl Pts',(5.53484625710188,0.240208327774024,3.56659596294035));
#41895=CARTESIAN_POINT('Ctrl Pts',(5.55870417513332,0.418502475082003,3.73467985673571));
#41896=CARTESIAN_POINT('Ctrl Pts',(5.58256209316472,0.494461367456411,3.96764175273735));
#41897=CARTESIAN_POINT('Ctrl Pts',(5.60642001119615,0.449510986625754,4.20851612161082));
#41898=CARTESIAN_POINT('Ctrl Pts',(5.63027792922757,0.294642925140636,4.39840261889448));
#41899=CARTESIAN_POINT('Ctrl Pts',(5.65413584725899,0.0677266425295592,
4.49086882357174));
#41900=CARTESIAN_POINT('Ctrl Pts',(5.6779937652904,-0.17575064898472,4.46330422991997));
#41901=CARTESIAN_POINT('Ctrl Pts',(5.70185168332183,-0.376252119531055,
4.32244913183746));
#41902=CARTESIAN_POINT('Ctrl Pts',(5.72570960135325,-0.48474969783608,4.10274643779879));
#41903=CARTESIAN_POINT('Ctrl Pts',(5.74956751938466,-0.474712770918799,
3.85791944074229));
#41904=CARTESIAN_POINT('Ctrl Pts',(5.77342543741608,-0.348595640189148,
3.64783501103505));
#41905=CARTESIAN_POINT('Ctrl Pts',(5.7972833554475,-0.13723738064616,3.52386451312966));
#41906=CARTESIAN_POINT('Ctrl Pts',(5.82114127347893,0.1076791581852,3.5163221129105));
#41907=CARTESIAN_POINT('Ctrl Pts',(5.84499919151033,0.326265206982528,3.62705212841851));
#41908=CARTESIAN_POINT('Ctrl Pts',(5.86885710954176,0.465070530553655,3.82897806268729));
#41909=CARTESIAN_POINT('Ctrl Pts',(5.89271502757317,0.490153431381492,4.07272350923538));
#41910=CARTESIAN_POINT('Ctrl Pts',(5.9165729456046,0.395380485146506,4.29868609559117));
#41911=CARTESIAN_POINT('Ctrl Pts',(5.94043086363601,0.203926205561759,4.45161176009809));
#41912=CARTESIAN_POINT('Ctrl Pts',(5.96428878166744,-0.0373935204432717,
4.49410611450448));
#41913=CARTESIAN_POINT('Ctrl Pts',(5.98814669969885,-0.26956963613406,4.41577793841189));
#41914=CARTESIAN_POINT('Ctrl Pts',(6.01200461773027,-0.435828398698505,
4.23578096933615));
#41915=CARTESIAN_POINT('Ctrl Pts',(6.0358625357617,-0.495515688199628,3.99812868033461));
#41916=CARTESIAN_POINT('Ctrl Pts',(6.0597204537931,-0.434035059498629,3.76093483037113));
#41917=CARTESIAN_POINT('Ctrl Pts',(6.08357837182454,-0.266422612259865,
3.58219732064663));
#41918=CARTESIAN_POINT('Ctrl Pts',(6.10743628985594,-0.0336596025775484,
3.50562697870369));
#41919=CARTESIAN_POINT('Ctrl Pts',(6.13129420788738,0.207328476491996,3.54993858195554));
#41920=CARTESIAN_POINT('Ctrl Pts',(6.15515212591877,0.397629707835022,3.70431327123879));
#41921=CARTESIAN_POINT('Ctrl Pts',(6.17901004395022,0.490679606253205,3.93097100878581));
#41922=CARTESIAN_POINT('Ctrl Pts',(6.20286796198161,0.463782811036945,4.17454675550933));
#41923=CARTESIAN_POINT('Ctrl Pts',(6.22672588001306,0.323407044622774,4.3753682944706));
#41924=CARTESIAN_POINT('Ctrl Pts',(6.25058379804445,0.104084330837213,4.48453946106473));
#41925=CARTESIAN_POINT('Ctrl Pts',(6.27444171607588,-0.140944443623038,
4.4749681472433));
#41926=CARTESIAN_POINT('Ctrl Pts',(6.29829963410731,-0.351028389709017,
4.349743491311));
#41927=CARTESIAN_POINT('Ctrl Pts',(6.32215755213872,-0.476177279109797,
4.13807688197341));
#41928=CARTESIAN_POINT('Ctrl Pts',(6.34601547017014,-0.483231738207782,
3.89435343878414));
#41929=CARTESIAN_POINT('Ctrl Pts',(6.37782602754537,-0.338784024988664,
3.5998542259592));
#41930=CARTESIAN_POINT('Ctrl Pts',(6.41758922426439,0.0803770223010952,
3.44371490521648));
#41931=CARTESIAN_POINT('Ctrl Pts',(6.46530506032724,0.512014121509362,3.7673575683149));
#41932=CARTESIAN_POINT('Ctrl Pts',(6.51302089639006,0.472271980317209,4.30452828893312));
#41933=CARTESIAN_POINT('Ctrl Pts',(6.56073673245292,-0.000548856210248058,
4.56210751581942));
#41934=CARTESIAN_POINT('Ctrl Pts',(6.60845256851575,-0.473190198344468,
4.30346185287483));
#41935=CARTESIAN_POINT('Ctrl Pts',(6.65616840457859,-0.511122033036262,
3.76615996983968));
#41936=CARTESIAN_POINT('Ctrl Pts',(6.70388424064142,-0.0797735308749388,
3.44358772816382));
#41937=CARTESIAN_POINT('Ctrl Pts',(6.75160007670426,0.424880365184703,3.63198234005898));
#41938=CARTESIAN_POINT('Ctrl Pts',(6.7993159127671,0.539334593204737,4.15833063512042));
#41939=CARTESIAN_POINT('Ctrl Pts',(6.84703174882994,0.158523065679302,4.53928284691909));
#41940=CARTESIAN_POINT('Ctrl Pts',(6.89474758489278,-0.367869781963911,
4.42500259414721));
#41941=CARTESIAN_POINT('Ctrl Pts',(6.94246342095561,-0.556438361909488,
3.92043630538129));
#41942=CARTESIAN_POINT('Ctrl Pts',(6.99017925701846,-0.234023037562683,
3.48893437735136));
#41943=CARTESIAN_POINT('Ctrl Pts',(7.03789509308128,0.303300305128555,3.52675198254107));
#41944=CARTESIAN_POINT('Ctrl Pts',(7.08561092914413,0.562097748282813,3.99916046672433));
#41945=CARTESIAN_POINT('Ctrl Pts',(7.13332676520696,0.304712478085684,4.47233993757656));
#41946=CARTESIAN_POINT('Ctrl Pts',(7.18104260126981,-0.232495107101315,
4.51176235979777));
#41947=CARTESIAN_POINT('Ctrl Pts',(7.22875843733264,-0.556198774489988,
4.08122554105153));
#41948=CARTESIAN_POINT('Ctrl Pts',(7.27647427339549,-0.369136593294786,
3.57609805363465));
#41949=CARTESIAN_POINT('Ctrl Pts',(7.32419010945832,0.156909424853758,3.46024624852207));
#41950=CARTESIAN_POINT('Ctrl Pts',(7.37190594552116,0.538863091386428,3.84005861730642));
#41951=CARTESIAN_POINT('Ctrl Pts',(7.41962178158399,0.425970496197337,4.36674761950234));
#41952=CARTESIAN_POINT('Ctrl Pts',(7.46733761764684,-0.0780973635293338,
4.55664663921719));
#41953=CARTESIAN_POINT('Ctrl Pts',(7.51505345370967,-0.510447210801067,
4.2353684852172));
#41954=CARTESIAN_POINT('Ctrl Pts',(7.56276928977251,-0.474045531130633,
3.69794782953315));
#41955=CARTESIAN_POINT('Ctrl Pts',(7.61048512583535,-0.00232054557778912,
3.43790632971152));
#41956=CARTESIAN_POINT('Ctrl Pts',(7.65820096189818,0.471535432411473,3.69404409621074));
#41957=CARTESIAN_POINT('Ctrl Pts',(7.70591679796103,0.512373167457076,4.23114587691112));
#41958=CARTESIAN_POINT('Ctrl Pts',(7.75363263402387,0.0826907388754792,
4.55598284219971));
#41959=CARTESIAN_POINT('Ctrl Pts',(7.80134847008669,-0.422927867535356,
4.3702522086048));
#41960=CARTESIAN_POINT('Ctrl Pts',(7.84906430614955,-0.540165305628305,
3.84451327478339));
#41961=CARTESIAN_POINT('Ctrl Pts',(7.89678014221237,-0.161360632039799,
3.46156019320034));
#41962=CARTESIAN_POINT('Ctrl Pts',(7.94449597827521,0.365623992797271,3.57306467116217));
#41963=CARTESIAN_POINT('Ctrl Pts',(7.99221181433806,0.556850479203549,4.07663043084052));
#41964=CARTESIAN_POINT('Ctrl Pts',(8.03992765040089,0.236712602309549,4.50982528676712));
#41965=CARTESIAN_POINT('Ctrl Pts',(8.08764348646373,-0.300802099575971,
4.47483973718518));
#41966=CARTESIAN_POINT('Ctrl Pts',(8.13535932252656,-0.562085604986122,
4.00380155059756));
#41967=CARTESIAN_POINT('Ctrl Pts',(8.18307515858941,-0.307197250538534,
3.52927234160183));
#41968=CARTESIAN_POINT('Ctrl Pts',(8.23079099465223,0.229795065915734,3.48701958438918));
#41969=CARTESIAN_POINT('Ctrl Pts',(8.27850683071509,0.555763037488074,3.91584463605021));
#41970=CARTESIAN_POINT('Ctrl Pts',(8.32622266677791,0.371365260221553,4.42195085332305));
#41971=CARTESIAN_POINT('Ctrl Pts',(8.37393850284076,-0.154062949695418,
4.54057310944092));
#41972=CARTESIAN_POINT('Ctrl Pts',(8.4216543389036,-0.538012782343907,4.16277876137275));
#41973=CARTESIAN_POINT('Ctrl Pts',(8.46937017496643,-0.427897198575242,
3.6355021720628));
#41974=CARTESIAN_POINT('Ctrl Pts',(8.51708601102927,0.0751629666897603,
3.44294954666756));
#41975=CARTESIAN_POINT('Ctrl Pts',(8.56480184709211,0.50919982311266,3.76194492389047));
#41976=CARTESIAN_POINT('Ctrl Pts',(8.61251768315494,0.475630646924824,4.29954994045293));
#41977=CARTESIAN_POINT('Ctrl Pts',(8.66023351921779,0.00528252914771292,
4.56207363752918));
#41978=CARTESIAN_POINT('Ctrl Pts',(8.70794935528062,-0.469916616427902,
4.30843646464781));
#41979=CARTESIAN_POINT('Ctrl Pts',(8.75566519134346,-0.513584102541225,
3.7715573403753));
#41980=CARTESIAN_POINT('Ctrl Pts',(8.8033810274063,-0.0856194047837525,
3.44446062547832));
#41981=CARTESIAN_POINT('Ctrl Pts',(8.85109686346913,0.420970909810523,3.6275242662766));
#41982=CARTESIAN_POINT('Ctrl Pts',(8.89881269953199,0.540977160455745,4.15263810462895));
#41983=CARTESIAN_POINT('Ctrl Pts',(8.9465285355948,0.1641957606509,4.5375820228614));
#41984=CARTESIAN_POINT('Ctrl Pts',(8.99424437165766,-0.363369132636193,
4.42885609773758));
#41985=CARTESIAN_POINT('Ctrl Pts',(9.04196020772048,-0.557246560270691,
3.92630501926208));
#41986=CARTESIAN_POINT('Ctrl Pts',(9.08967604378333,-0.239395897268157,
3.49142917554125));
#41987=CARTESIAN_POINT('Ctrl Pts',(9.13739187984617,0.298295701775085,3.52358174528888));
#41988=CARTESIAN_POINT('Ctrl Pts',(9.18510771590899,0.562057768008922,3.99323652897485));
#41989=CARTESIAN_POINT('Ctrl Pts',(9.23282355197185,0.309673537509763,4.46910231217259));
#41990=CARTESIAN_POINT('Ctrl Pts',(9.28053938803466,-0.227088667424462,
4.51418422403538));
#41991=CARTESIAN_POINT('Ctrl Pts',(9.32825522409753,-0.555311854854516,
4.08708285122523));
#41992=CARTESIAN_POINT('Ctrl Pts',(9.37597106016035,-0.373583621400482,
3.58001195619306));
#41993=CARTESIAN_POINT('Ctrl Pts',(9.4236868962232,0.151212199908504,3.45862254413551));
#41994=CARTESIAN_POINT('Ctrl Pts',(9.47140273228603,0.537147531342748,3.83438837996121));
#41995=CARTESIAN_POINT('Ctrl Pts',(9.51911856834887,0.429812019667804,4.36223791473086));
#41996=CARTESIAN_POINT('Ctrl Pts',(9.5668344044117,-0.0722264831760907,
4.5574387986564));
#41997=CARTESIAN_POINT('Ctrl Pts',(9.61455024047456,-0.507938295172089,
4.24073505647735));
#41998=CARTESIAN_POINT('Ctrl Pts',(9.66226607653738,-0.477202555076283,
3.70296060775017));
#41999=CARTESIAN_POINT('Ctrl Pts',(9.70998191260023,-0.00824436594879979,
3.43796200346455));
#42000=CARTESIAN_POINT('Ctrl Pts',(9.75769774866306,0.46828475128534,3.68909153946361));
#42001=CARTESIAN_POINT('Ctrl Pts',(9.80541358472589,0.514780775927077,4.22573309871483));
#42002=CARTESIAN_POINT('Ctrl Pts',(9.85312942078874,0.0885456931146035,
4.55508048006603));
#42003=CARTESIAN_POINT('Ctrl Pts',(9.90084525685159,-0.419002262135622,
4.37468891556157));
#42004=CARTESIAN_POINT('Ctrl Pts',(9.9485610929144,-0.541773992888202,3.8502147545669));
#42005=CARTESIAN_POINT('Ctrl Pts',(9.99627692897727,-0.167026329707142,
3.46329068919569));
#42006=CARTESIAN_POINT('Ctrl Pts',(10.0439927650401,0.361104182074418,3.56923504227033));
#42007=CARTESIAN_POINT('Ctrl Pts',(10.0917086011029,0.557627167155001,4.07075748419897));
#42008=CARTESIAN_POINT('Ctrl Pts',(10.1394244371657,0.242072544440304,4.50730223964386));
#42009=CARTESIAN_POINT('Ctrl Pts',(10.1871402732286,-0.295781020598791,
4.47798354257549));
#42010=CARTESIAN_POINT('Ctrl Pts',(10.2348561092914,-0.56201432324602,4.00972520363789));
#42011=CARTESIAN_POINT('Ctrl Pts',(10.2825719453543,-0.312141225154507,
3.53253606055812));
#42012=CARTESIAN_POINT('Ctrl Pts',(10.3302877814171,0.224375962906492,3.48462624592509));
#42013=CARTESIAN_POINT('Ctrl Pts',(10.37800361748,0.554845251762499,3.90999207970357));
#42014=CARTESIAN_POINT('Ctrl Pts',(10.4257194535428,0.375791608533427,4.41801357164013));
#42015=CARTESIAN_POINT('Ctrl Pts',(10.4734352896056,-0.148357251109035,
4.54216676877402));
#42016=CARTESIAN_POINT('Ctrl Pts',(10.5211511256685,-0.536267364288337,
4.16843987983467));
#42017=CARTESIAN_POINT('Ctrl Pts',(10.5688669617313,-0.431714905307627,
3.64003205746247));
#42018=CARTESIAN_POINT('Ctrl Pts',(10.6165827977942,0.0692879940047382,
3.44218833554121));
#42019=CARTESIAN_POINT('Ctrl Pts',(10.664298633857,0.50666266228973,3.75659164812817));
#42020=CARTESIAN_POINT('Ctrl Pts',(10.7120144699198,0.478761211786921,4.29452059555793));
#42021=CARTESIAN_POINT('Ctrl Pts',(10.7597303059827,0.0112059738120427,
4.56198674830498));
#42022=CARTESIAN_POINT('Ctrl Pts',(10.8074461420455,-0.466639882340508,
4.31337182280594));
#42023=CARTESIAN_POINT('Ctrl Pts',(10.8551619781083,-0.515963154362253,
3.77698273057893));
#42024=CARTESIAN_POINT('Ctrl Pts',(10.9028778141712,-0.0914695226195351,
3.44539382842306));
#42025=CARTESIAN_POINT('Ctrl Pts',(10.950593650234,0.417021979184216,3.62310830733915));
#42026=CARTESIAN_POINT('Ctrl Pts',(10.9983094862969,0.542555780795161,4.14692822684982));
#42027=CARTESIAN_POINT('Ctrl Pts',(11.0460253223597,0.169852260608159,4.53582169486292));
#42028=CARTESIAN_POINT('Ctrl Pts',(11.0937411584225,-0.358829204008283,
4.43266185580689));
#42029=CARTESIAN_POINT('Ctrl Pts',(11.1414569944853,-0.55799228928692,3.93218197720501));
#42030=CARTESIAN_POINT('Ctrl Pts',(11.1891728305482,-0.244742469498405,
3.49398043245019));
#42031=CARTESIAN_POINT('Ctrl Pts',(11.236888666611,0.293258125877444,3.5204644426882));
#42032=CARTESIAN_POINT('Ctrl Pts',(11.2846045026739,0.561955271903759,3.98731333380864));
#42033=CARTESIAN_POINT('Ctrl Pts',(11.3323203387367,0.314600244947554,4.46581258570203));
#42034=CARTESIAN_POINT('Ctrl Pts',(11.3800361747996,-0.221657027690976,
4.51654897269734));
#42035=CARTESIAN_POINT('Ctrl Pts',(11.4277520108624,-0.554363241169119,
4.0929304899371));
#42036=CARTESIAN_POINT('Ctrl Pts',(11.4754678469252,-0.377989160306769,
3.58397250834823));
#42037=CARTESIAN_POINT('Ctrl Pts',(11.5231836829881,0.145498182576105,3.45705897374896));
#42038=CARTESIAN_POINT('Ctrl Pts',(11.5708995190509,0.535372305622036,3.82873653777755));
#42039=CARTESIAN_POINT('Ctrl Pts',(11.6186153551137,0.43360580265347,4.35768797439208));
#42040=CARTESIAN_POINT('Ctrl Pts',(11.6663311911766,-0.0663475807746441,
4.55816904038548));
#42041=CARTESIAN_POINT('Ctrl Pts',(11.7140470272394,-0.505372959888646,
4.24607488805821));
#42042=CARTESIAN_POINT('Ctrl Pts',(11.7617628633023,-0.480306573774387,
3.70800637967828));
#42043=CARTESIAN_POINT('Ctrl Pts',(11.8094786993651,-0.0141672704965164,
3.43808010573911));
#42044=CARTESIAN_POINT('Ctrl Pts',(11.8571945354279,0.464982055269784,3.68417351694868));
#42045=CARTESIAN_POINT('Ctrl Pts',(11.9049103714908,0.517131205013274,4.22029524715934));
#42046=CARTESIAN_POINT('Ctrl Pts',(11.9526262075536,0.0943908121067024,
4.55411646222552));
#42047=CARTESIAN_POINT('Ctrl Pts',(12.0003420436165,-0.415030115946784,
4.37908400385228));
#42048=CARTESIAN_POINT('Ctrl Pts',(12.0480578796793,-0.543322502467158,
3.85593287178435));
#42049=CARTESIAN_POINT('Ctrl Pts',(12.0957737157421,-0.172673474880652,
3.46508080031456));
#42050=CARTESIAN_POINT('Ctrl Pts',(12.143489551805,0.356544261611682,3.56545326070575));
#42051=CARTESIAN_POINT('Ctrl Pts',(12.1912053878678,0.558341916527368,4.06487667815191));
#42052=CARTESIAN_POINT('Ctrl Pts',(12.2389212239306,0.247405598301292,4.50472284379514));
#42053=CARTESIAN_POINT('Ctrl Pts',(12.2866370599935,-0.290727087669313,
4.48107425582212));
#42054=CARTESIAN_POINT('Ctrl Pts',(12.3343528960563,-0.56188061562194,4.01564777644873));
#42055=CARTESIAN_POINT('Ctrl Pts',(12.3820687321191,-0.317050528604376,
3.5358517031905));
#42056=CARTESIAN_POINT('Ctrl Pts',(12.429784568182,0.218931937280033,3.48229015273196));
#42057=CARTESIAN_POINT('Ctrl Pts',(12.4775004042448,0.553865836459325,3.90414952100961));
#42058=CARTESIAN_POINT('Ctrl Pts',(12.5252162403077,0.380176215696692,4.4140298589933));
#42059=CARTESIAN_POINT('Ctrl Pts',(12.5729320763705,-0.142635073703209,
4.54370020679522));
#42060=CARTESIAN_POINT('Ctrl Pts',(12.6206479124333,-0.53446238019874,4.17408228879405));
#42061=CARTESIAN_POINT('Ctrl Pts',(12.6683637484962,-0.435484659196984,
3.644601926393));
#42062=CARTESIAN_POINT('Ctrl Pts',(12.716079584559,0.0634053251381518,3.44148908348752));
#42063=CARTESIAN_POINT('Ctrl Pts',(12.7637954206219,0.504069223782589,3.75126540901054));
#42064=CARTESIAN_POINT('Ctrl Pts',(12.8115112566847,0.481838598125516,4.2894585367128));
#42065=CARTESIAN_POINT('Ctrl Pts',(12.8592270927475,0.0171281737699642,
4.56183743625962));
#42066=CARTESIAN_POINT('Ctrl Pts',(12.9069429288104,-0.463311316109371,
4.31827237310907));
#42067=CARTESIAN_POINT('Ctrl Pts',(12.9546587648732,-0.518284895444539,
3.78243289248252));
#42068=CARTESIAN_POINT('Ctrl Pts',(13.0023746009361,-0.0973094804548018,
3.44638863438952));
#42069=CARTESIAN_POINT('Ctrl Pts',(13.0500904369989,0.413026727735397,3.61873421174243));
#42070=CARTESIAN_POINT('Ctrl Pts',(13.0978062730617,0.544074136613086,4.14120202898048));
#42071=CARTESIAN_POINT('Ctrl Pts',(13.1455221091246,0.17548989418231,4.53400185033327));
#42072=CARTESIAN_POINT('Ctrl Pts',(13.1932379451874,-0.354249418335187,
4.4364195558504));
#42073=CARTESIAN_POINT('Ctrl Pts',(13.2409537812502,-0.558676039167545,
3.93806646805208));
#42074=CARTESIAN_POINT('Ctrl Pts',(13.2886696173131,-0.250061856896528,
3.49658789561142));
#42075=CARTESIAN_POINT('Ctrl Pts',(13.3363854533759,0.288187976258808,3.51740040462167));
#42076=CARTESIAN_POINT('Ctrl Pts',(13.3841012894388,0.56179035647369,3.9813915478171));
#42077=CARTESIAN_POINT('Ctrl Pts',(13.4318171255016,0.319492008083037,4.46247111897993));
#42078=CARTESIAN_POINT('Ctrl Pts',(13.4795329615644,-0.21620076734671,4.51885634555065));
#42079=CARTESIAN_POINT('Ctrl Pts',(13.5272487976273,-0.553353051445561,
4.09876780637113));
#42080=CARTESIAN_POINT('Ctrl Pts',(13.5749646336901,-0.382352713970831,
3.58797927086295));
#42081=CARTESIAN_POINT('Ctrl Pts',(13.6226804697529,0.139768003996038,3.45555571067516));
#42082=CARTESIAN_POINT('Ctrl Pts',(13.6703963058158,0.53353761328617,3.82310371872654));
#42083=CARTESIAN_POINT('Ctrl Pts',(13.7181121418786,0.437351422764197,4.35309830377052));
#42084=CARTESIAN_POINT('Ctrl Pts',(13.7658279779415,-0.0604613087987784,
4.55883728334624));
#42085=CARTESIAN_POINT('Ctrl Pts',(13.8135438140043,-0.502751490175015,
4.25138738680826));
#42086=CARTESIAN_POINT('Ctrl Pts',(13.8612596500671,-0.483357242297515,
3.71308458487209));
#42087=CARTESIAN_POINT('Ctrl Pts',(13.90897548613,-0.0200886014110514,3.43826062340902));
#42088=CARTESIAN_POINT('Ctrl Pts',(13.9566913221928,0.461627711254046,3.67929057494076));
#42089=CARTESIAN_POINT('Ctrl Pts',(14.0044071582557,0.519424193619207,4.21483292625321));
#42090=CARTESIAN_POINT('Ctrl Pts',(14.0521229943185,0.100225446615308,4.55309089575788));
#42091=CARTESIAN_POINT('Ctrl Pts',(14.0998388303813,-0.411011870182152,
4.38343698529073));
#42092=CARTESIAN_POINT('Ctrl Pts',(14.1475546664441,-0.544810662360815,
3.86166699129474));
#42093=CARTESIAN_POINT('Ctrl Pts',(14.195270502507,-0.178301440303968,3.46693032771971));
#42094=CARTESIAN_POINT('Ctrl Pts',(14.2429863385698,0.351944737904315,3.5617197465309));
#42095=CARTESIAN_POINT('Ctrl Pts',(14.2907021746327,0.558994647929194,4.05898866591129));
#42096=CARTESIAN_POINT('Ctrl Pts',(14.3384180106955,0.252711171522458,4.50208738572805));
#42097=CARTESIAN_POINT('Ctrl Pts',(14.3861338467583,-0.28564086215454,4.48411153362329));
#42098=CARTESIAN_POINT('Ctrl Pts',(14.4338496828212,-0.561684496965419,
4.02156861117883));
#42099=CARTESIAN_POINT('Ctrl Pts',(14.481565518884,-0.321924615586062,3.53921890121312));
#42100=CARTESIAN_POINT('Ctrl Pts',(14.5292813549469,0.213463593732893,3.48001156429194));
#42101=CARTESIAN_POINT('Ctrl Pts',(14.5769971910097,0.552824900367352,3.89831760893199));
#42102=CARTESIAN_POINT('Ctrl Pts',(14.6247130270725,0.384518594689996,4.4100001578745));
#42103=CARTESIAN_POINT('Ctrl Pts',(14.6724288631354,-0.136897053070264,
4.54517325317752));
#42104=CARTESIAN_POINT('Ctrl Pts',(14.7201446991982,-0.532598030564186,
4.17970536151887));
#42105=CARTESIAN_POINT('Ctrl Pts',(14.7678605352611,-0.439206041516937,
3.64921127125505));
#42106=CARTESIAN_POINT('Ctrl Pts',(14.8155763713239,0.0575156135089261,
3.44085186817608));
#42107=CARTESIAN_POINT('Ctrl Pts',(14.8632922073868,0.501419795658073,3.74596679815093));
#42108=CARTESIAN_POINT('Ctrl Pts',(14.9110080434496,0.484862464119148,4.284364326187));
#42109=CARTESIAN_POINT('Ctrl Pts',(14.9587238795124,0.0230484712116303,
4.56162571797798));
#42110=CARTESIAN_POINT('Ctrl Pts',(15.0064397155752,-0.459931287455839,
4.32313757122732));
#42111=CARTESIAN_POINT('Ctrl Pts',(15.0541555516381,-0.5205490679001,3.78790722070797));
#42112=CARTESIAN_POINT('Ctrl Pts',(15.1018713877009,-0.103138629614742,
3.44744493287938));
#42113=CARTESIAN_POINT('Ctrl Pts',(15.1495872237638,0.40898559923764,3.61440246534021));
#42114=CARTESIAN_POINT('Ctrl Pts',(15.1973030598266,0.545532059257757,4.13546014705983));
#42115=CARTESIAN_POINT('Ctrl Pts',(15.2450188958894,0.181108035171788,4.53212269141213));
#42116=CARTESIAN_POINT('Ctrl Pts',(15.2927347319523,-0.349630284317748,
4.44012878048063));
#42117=CARTESIAN_POINT('Ctrl Pts',(15.3404505680151,-0.559297733964875,
3.94395783818199));
#42118=CARTESIAN_POINT('Ctrl Pts',(15.3881664040779,-0.255353468610234,
3.49925127540033));
#42119=CARTESIAN_POINT('Ctrl Pts',(15.4358822401408,0.283085816087337,3.51438997142805));
#42120=CARTESIAN_POINT('Ctrl Pts',(15.4835980762036,0.561563040036739,3.97547182876414));
#42121=CARTESIAN_POINT('Ctrl Pts',(15.5313139122665,0.324348283562367,4.45907828316053));
#42122=CARTESIAN_POINT('Ctrl Pts',(15.5790297483293,-0.210720492447169,
4.52110608630326));
#42123=CARTESIAN_POINT('Ctrl Pts',(15.6267455843921,-0.552281397890927,
4.10459415214592));
#42124=CARTESIAN_POINT('Ctrl Pts',(15.674461420455,-0.386673797709831,3.59203179868507));
#42125=CARTESIAN_POINT('Ctrl Pts',(15.7221772565178,0.134022300649356,3.45411292188939));
#42126=CARTESIAN_POINT('Ctrl Pts',(15.7698930925807,0.531643658124066,3.81749054847505));
#42127=CARTESIAN_POINT('Ctrl Pts',(15.8176089286435,0.441048463954279,4.34846941266494));
#42128=CARTESIAN_POINT('Ctrl Pts',(15.8653247647064,-0.054568321067637,
4.5594434533135));
#42129=CARTESIAN_POINT('Ctrl Pts',(15.9130406007692,-0.500074177211609,
4.25667196264028));
#42130=CARTESIAN_POINT('Ctrl Pts',(15.960756436832,-0.486354221791887,3.71819465926869));
#42131=CARTESIAN_POINT('Ctrl Pts',(16.0084722728949,-0.0260077009790528,
3.4385035364232));
#42132=CARTESIAN_POINT('Ctrl Pts',(16.0561881089577,0.458222091822753,3.6744432558139));
#42133=CARTESIAN_POINT('Ctrl Pts',(16.1039039450206,0.52165948705058,4.2093467427251));
#42134=CARTESIAN_POINT('Ctrl Pts',(16.1516197810833,0.106048948556897,4.55200389457816));
#42135=CARTESIAN_POINT('Ctrl Pts',(16.1993356171462,-0.406947971169398,
4.38774737636841));
#42136=CARTESIAN_POINT('Ctrl Pts',(16.247051453209,-0.546238307271431,3.86741647617928));
#42137=CARTESIAN_POINT('Ctrl Pts',(16.2947672892719,-0.183909600849411,
3.46883906597446));
#42138=CARTESIAN_POINT('Ctrl Pts',(16.3424831253347,0.347306121845567,3.55803491444678));
#42139=CARTESIAN_POINT('Ctrl Pts',(16.3901989613975,0.559585288858183,4.05309410148958));
#42140=CARTESIAN_POINT('Ctrl Pts',(16.4379147974604,0.257988674785898,4.49939615817675));
#42141=CARTESIAN_POINT('Ctrl Pts',(16.4856306335232,-0.280522909008289,
4.4870950386126));
#42142=CARTESIAN_POINT('Ctrl Pts',(16.5333464695861,-0.561425989060384,
4.02748705016995));
#42143=CARTESIAN_POINT('Ctrl Pts',(16.5810623056489,-0.326762944709103,
3.54263728061361));
#42144=CARTESIAN_POINT('Ctrl Pts',(16.6287781417117,0.207971539662738,3.4777907336998));
#42145=CARTESIAN_POINT('Ctrl Pts',(16.6764939777746,0.551722559108811,3.89249699125187));
#42146=CARTESIAN_POINT('Ctrl Pts',(16.7242098138374,0.388818263182495,4.40592491588375));
#42147=CARTESIAN_POINT('Ctrl Pts',(16.7719256499003,-0.131143826562283,
4.54658574430191));
#42148=CARTESIAN_POINT('Ctrl Pts',(16.8196414859631,-0.53067452246778,4.18530847342493));
#42149=CARTESIAN_POINT('Ctrl Pts',(16.8673573220259,-0.442878638914007,
3.65385958006445));
#42150=CARTESIAN_POINT('Ctrl Pts',(16.9150731580888,0.0516195133182915,
3.44027676038576));
#42151=CARTESIAN_POINT('Ctrl Pts',(16.9627889941516,0.498714672202087,3.74069640409388));
#42152=CARTESIAN_POINT('Ctrl Pts',(17.0105048302145,0.487832473891125,4.27923852982128));
#42153=CARTESIAN_POINT('Ctrl Pts',(17.0582206662773,0.0289662085384809,
4.56135161697672));
#42154=CARTESIAN_POINT('Ctrl Pts',(17.1059365023401,-0.456500171817451,
4.32796687675757));
#42155=CARTESIAN_POINT('Ctrl Pts',(17.1536523384029,-0.522755420235406,
3.79340510719289));
#42156=CARTESIAN_POINT('Ctrl Pts',(17.2013681744658,-0.108956322625149,
3.44856260656401));
#42157=CARTESIAN_POINT('Ctrl Pts',(17.2490840105286,0.404899042560309,3.61011354928233));
#42158=CARTESIAN_POINT('Ctrl Pts',(17.2967998465915,0.54692938679005,4.12970321886885));
#42159=CARTESIAN_POINT('Ctrl Pts',(17.3445156826543,0.186706059540143,4.53018442682757));
#42160=CARTESIAN_POINT('Ctrl Pts',(17.3922315187172,-0.344972315027459,
4.4437891176945));
#42161=CARTESIAN_POINT('Ctrl Pts',(17.43994735478,-0.559857304624004,3.94985543320929));
#42162=CARTESIAN_POINT('Ctrl Pts',(17.4876631908428,-0.260616716872392,
3.5019702759813));
#42163=CARTESIAN_POINT('Ctrl Pts',(17.5353790269057,0.277952212086773,3.51143347749201));
#42164=CARTESIAN_POINT('Ctrl Pts',(17.5830948629685,0.561273347842132,3.96955483418404));
#42165=CARTESIAN_POINT('Ctrl Pts',(17.6308106990313,0.329168531973526,4.45563445510394));
#42166=CARTESIAN_POINT('Ctrl Pts',(17.6785265350942,-0.205216811715269,
4.52329794506467));
#42167=CARTESIAN_POINT('Ctrl Pts',(17.726242371157,-0.551148399539408,4.11040888009862));
#42168=CARTESIAN_POINT('Ctrl Pts',(17.7739582072198,-0.390951931558304,
3.59612964167903));
#42169=CARTESIAN_POINT('Ctrl Pts',(17.8216740432827,0.128261710741471,3.45273076764982));
#42170=CARTESIAN_POINT('Ctrl Pts',(17.8693898793456,0.529690650507269,3.81189765050732));
#42171=CARTESIAN_POINT('Ctrl Pts',(17.9171057154083,0.44469651557395,4.34380181523062));
#42172=CARTESIAN_POINT('Ctrl Pts',(17.9648215514712,-0.0486692721463468,
4.55998748295674));
#42173=CARTESIAN_POINT('Ctrl Pts',(18.012537387534,-0.497341318381634,4.26192802856871));
#42174=CARTESIAN_POINT('Ctrl Pts',(18.0602532235969,-0.489297179367249,
3.72333603526529));
#42175=CARTESIAN_POINT('Ctrl Pts',(18.1079690596597,-0.0319239117350811,
3.43880881780002));
#42176=CARTESIAN_POINT('Ctrl Pts',(18.1556848957225,0.454765575255941,3.66963209798526));
#42177=CARTESIAN_POINT('Ctrl Pts',(18.2034007317854,0.523836837021606,4.20383730595423));
#42178=CARTESIAN_POINT('Ctrl Pts',(18.2511165678483,0.111860671084556,4.5508555794253));
#42179=CARTESIAN_POINT('Ctrl Pts',(18.298832403911,-0.402838870307115,4.39201469830757));
#42180=CARTESIAN_POINT('Ctrl Pts',(18.346548239974,-0.547605278623001,3.87318068781251));
#42181=CARTESIAN_POINT('Ctrl Pts',(18.3942640760367,-0.189497333589109,
3.47080680306518));
#42182=CARTESIAN_POINT('Ctrl Pts',(18.4419799120997,0.342628928670919,3.55439917374707));
#42183=CARTESIAN_POINT('Ctrl Pts',(18.4896957481624,0.560113773708727,4.04719363962704));
#42184=CARTESIAN_POINT('Ctrl Pts',(18.5374115842253,0.263237521891608,4.49664946007004));
#42185=CARTESIAN_POINT('Ctrl Pts',(18.5851274202881,-0.275373796708506,
4.49002443939646));
#42186=CARTESIAN_POINT('Ctrl Pts',(18.632843256351,-0.561105120620647,4.03340243603));
#42187=CARTESIAN_POINT('Ctrl Pts',(18.6805590924138,-0.331564978554912,
3.54610646169455));
#42188=CARTESIAN_POINT('Ctrl Pts',(18.7282749284766,0.202456385100939,3.47562790763498));
#42189=CARTESIAN_POINT('Ctrl Pts',(18.7759907645394,0.550558935126376,3.8866883144956));
#42190=CARTESIAN_POINT('Ctrl Pts',(18.8237066006023,0.393074743587739,4.40180458567998));
#42191=CARTESIAN_POINT('Ctrl Pts',(18.8714224366651,-0.125376033221007,
4.54793752327491));
#42192=CARTESIAN_POINT('Ctrl Pts',(18.919138272728,-0.528692069562509,4.19089100214638));
#42193=CARTESIAN_POINT('Ctrl Pts',(18.9668541087908,-0.4465020434557,3.6585463365067));
#42194=CARTESIAN_POINT('Ctrl Pts',(19.0145699448537,0.0457176794812401,
3.43976382400136));
#42195=CARTESIAN_POINT('Ctrl Pts',(19.0622857809165,0.495954153879041,3.73545481224116));
#42196=CARTESIAN_POINT('Ctrl Pts',(19.1100016169793,0.490748297561716,4.27408171698104));
#42197=CARTESIAN_POINT('Ctrl Pts',(19.1577174530421,0.0348807284082936,
4.5610151636709));
#42198=CARTESIAN_POINT('Ctrl Pts',(19.205433289105,-0.453018350253257,4.33275975334162));
#42199=CARTESIAN_POINT('Ctrl Pts',(19.2531491251678,-0.524903707479367,
3.79892594114836));
#42200=CARTESIAN_POINT('Ctrl Pts',(19.3008649612307,-0.11476191309534,3.44974153150476));
#42201=CARTESIAN_POINT('Ctrl Pts',(19.3485807972935,0.400767511262006,3.60586793956989));
#42202=CARTESIAN_POINT('Ctrl Pts',(19.3962966333564,0.548265964675035,4.12393188459875));
#42203=CARTESIAN_POINT('Ctrl Pts',(19.4440124694192,0.192283344213529,4.52818727047755));
#42204=CARTESIAN_POINT('Ctrl Pts',(19.491728305482,-0.340276025447905,4.44740016355363));
#42205=CARTESIAN_POINT('Ctrl Pts',(19.5394441415448,-0.560354693525076,
3.95575859308266));
#42206=CARTESIAN_POINT('Ctrl Pts',(19.5871599776077,-0.265851008504119,
3.50474460473346));
#42207=CARTESIAN_POINT('Ctrl Pts',(19.6348758136705,0.272787718306182,3.5085312334714));
#42208=CARTESIAN_POINT('Ctrl Pts',(19.6825916497334,0.560921342594646,3.96364125479661));
#42209=CARTESIAN_POINT('Ctrl Pts',(19.7303074857962,0.33395216026474,4.45213995410186));
#42210=CARTESIAN_POINT('Ctrl Pts',(19.7780233218591,-0.199690227635008,
4.52543179776919));
#42211=CARTESIAN_POINT('Ctrl Pts',(19.8257391579219,-0.549954387748789,
4.11621111891367));
#42212=CARTESIAN_POINT('Ctrl Pts',(19.8734549939848,-0.395186252277308,
3.60027277035845));
#42213=CARTESIAN_POINT('Ctrl Pts',(19.9211708300475,0.122486141425193,3.45140859770427));
#42214=CARTESIAN_POINT('Ctrl Pts',(19.9688866661104,0.527680190865048,3.80632716374734));
#42215=CARTESIAN_POINT('Ctrl Pts',(20.0166025021732,0.448292560087992,4.33909316421112));
#42216=CARTESIAN_POINT('Ctrl Pts',(20.0643183382361,-0.0427598846646947,
4.56047472290141));
#42217=CARTESIAN_POINT('Ctrl Pts',(20.1120341742989,-0.49456253103916,4.26714478353561));
#42218=CARTESIAN_POINT('Ctrl Pts',(20.1597500103618,-0.492168201513856,
3.72852743457374));
#42219=CARTESIAN_POINT('Ctrl Pts',(20.2074658464246,-0.0378697858522375,
3.43914000028616));
#42220=CARTESIAN_POINT('Ctrl Pts',(20.2551816824874,0.451321269441671,3.66492646727415));
#42221=CARTESIAN_POINT('Ctrl Pts',(20.3028975185503,0.52583741886325,4.1981749506787));
#42222=CARTESIAN_POINT('Ctrl Pts',(20.3506133546131,0.117885080656874,4.54989459844945));
#42223=CARTESIAN_POINT('Ctrl Pts',(20.398329190676,-0.399119892637424,4.39574851066478));
#42224=CARTESIAN_POINT('Ctrl Pts',(20.438092387395,-0.523197416260526,3.96600412247733));
#42225=CARTESIAN_POINT('Ctrl Pts',(20.4699029447702,-0.3725623900923,3.67462118354637));
#42226=CARTESIAN_POINT('Ctrl Pts',(20.4937608628016,-0.172533290246804,
3.53519650363565));
#42227=CARTESIAN_POINT('Ctrl Pts',(20.5176187808331,0.0720421502968434,
3.50974356844941));
#42228=CARTESIAN_POINT('Ctrl Pts',(20.5414766988645,0.297725647320748,3.60399556061657));
#42229=CARTESIAN_POINT('Ctrl Pts',(20.5653346168959,0.451286063531533,3.79517586539437));
#42230=CARTESIAN_POINT('Ctrl Pts',(20.5891925349273,0.494134760388362,4.03639109206021));
#42231=CARTESIAN_POINT('Ctrl Pts',(20.6130504529587,0.416344747430809,4.26873428690612));
#42232=CARTESIAN_POINT('Ctrl Pts',(20.6369083709901,0.23664610161733,4.43535054865035));
#42233=CARTESIAN_POINT('Ctrl Pts',(20.6607662890216,-0.000865470816140784,
4.49551919950567));
#42234=CARTESIAN_POINT('Ctrl Pts',(20.684624207053,-0.238193741375527,4.43451595913869));
#42235=CARTESIAN_POINT('Ctrl Pts',(20.7084821250844,-0.417262150572256,
4.26726382233879));
#42236=CARTESIAN_POINT('Ctrl Pts',(20.7323400431158,-0.494306543785295,
4.03465729316116));
#42237=CARTESIAN_POINT('Ctrl Pts',(20.7561979611472,-0.45047531426282,3.79357669839993));
#42238=CARTESIAN_POINT('Ctrl Pts',(20.7800558791787,-0.296492828349621,
3.60297191305088));
#42239=CARTESIAN_POINT('Ctrl Pts',(20.80391379721,-0.0700085893017688,3.50945147432983));
#42240=CARTESIAN_POINT('Ctrl Pts',(20.8277717152415,0.173594031734132,3.53588342526713));
#42241=CARTESIAN_POINT('Ctrl Pts',(20.8516296332729,0.374748514455718,3.6758045671588));
#42242=CARTESIAN_POINT('Ctrl Pts',(20.8754875513043,0.484266602122282,3.89500029884494));
#42243=CARTESIAN_POINT('Ctrl Pts',(20.8993454693358,0.475368407265908,4.13987133054223));
#42244=CARTESIAN_POINT('Ctrl Pts',(20.9232033873671,0.350229638882089,4.35054000504804));
#42245=CARTESIAN_POINT('Ctrl Pts',(20.9470613053986,0.139450209771325,4.47549210343221));
#42246=CARTESIAN_POINT('Ctrl Pts',(20.97091922343,-0.105428607968738,4.48417342845956));
#42247=CARTESIAN_POINT('Ctrl Pts',(20.9947771414615,-0.324527251938122,
4.37446116262749));
#42248=CARTESIAN_POINT('Ctrl Pts',(21.0186350594928,-0.464270146732381,
4.17318294187641));
#42249=CARTESIAN_POINT('Ctrl Pts',(21.0424929775243,-0.490486342136868,
3.92955677471355));
#42250=CARTESIAN_POINT('Ctrl Pts',(21.0663508955557,-0.396765267394252,
3.7031558948169));
#42251=CARTESIAN_POINT('Ctrl Pts',(21.0902088135871,-0.206024276530194,
3.54934148458869));
#42252=CARTESIAN_POINT('Ctrl Pts',(21.1140667316185,0.0350952616297792,
3.50572535702762));
#42253=CARTESIAN_POINT('Ctrl Pts',(21.1379246496499,0.267633052506714,3.58297284346672));
#42254=CARTESIAN_POINT('Ctrl Pts',(21.1617825676814,0.434727271782411,3.76219482925797));
#42255=CARTESIAN_POINT('Ctrl Pts',(21.1856404857128,0.495518831419392,3.99956665698474));
#42256=CARTESIAN_POINT('Ctrl Pts',(21.2094984037442,0.43514253908843,4.23704444887943));
#42257=CARTESIAN_POINT('Ctrl Pts',(21.2333563217756,0.268362042918248,4.41655841606373));
#42258=CARTESIAN_POINT('Ctrl Pts',(21.257214239807,0.0359597172125542,4.49421250369607));
#42259=CARTESIAN_POINT('Ctrl Pts',(21.2810721578384,-0.205235738871087,
4.45101817209691));
#42260=CARTESIAN_POINT('Ctrl Pts',(21.3049300758699,-0.396245466293343,
4.29753761193144));
#42261=CARTESIAN_POINT('Ctrl Pts',(21.3287879939013,-0.490362383696085,
4.07130100088706));
#42262=CARTESIAN_POINT('Ctrl Pts',(21.3526459119327,-0.464572341082516,
3.82762935292545));
#42263=CARTESIAN_POINT('Ctrl Pts',(21.3765038299641,-0.325181706377507,
3.62610702345576));
#42264=CARTESIAN_POINT('Ctrl Pts',(21.4003617479955,-0.106275286691508,
3.51601171139131));
#42265=CARTESIAN_POINT('Ctrl Pts',(21.424219666027,0.138618335471326,3.52426471946798));
#42266=CARTESIAN_POINT('Ctrl Pts',(21.4480775840584,0.349615998723735,3.64884796240357));
#42267=CARTESIAN_POINT('Ctrl Pts',(21.4719355020898,0.475123026939619,3.85929744372095));
#42268=CARTESIAN_POINT('Ctrl Pts',(21.4957934201212,0.484449532977353,4.10415253270923));
#42269=CARTESIAN_POINT('Ctrl Pts',(21.5196513381527,0.375314932061802,4.32353949039209));
#42270=CARTESIAN_POINT('Ctrl Pts',(21.543509256184,0.174405606883644,4.4638122296353));
#42271=CARTESIAN_POINT('Ctrl Pts',(21.5673671742155,-0.069150639890911,
4.49067024474121));
#42272=CARTESIAN_POINT('Ctrl Pts',(21.5912250922469,-0.29579767158652,4.39754601941878));
#42273=CARTESIAN_POINT('Ctrl Pts',(21.6150830102783,-0.450114115212426,
4.20721096341231));
#42274=CARTESIAN_POINT('Ctrl Pts',(21.6389409283097,-0.494365396806572,
3.96620718253823));
#42275=CARTESIAN_POINT('Ctrl Pts',(21.6627988463412,-0.417730872638478,
3.73346666603139));
#42276=CARTESIAN_POINT('Ctrl Pts',(21.6866567643726,-0.238949771349764,
3.56590080990214));
#42277=CARTESIAN_POINT('Ctrl Pts',(21.710514682404,-0.00173894210493873,
3.50448403037633));
#42278=CARTESIAN_POINT('Ctrl Pts',(21.7343726004354,0.235897105852373,3.56423440300754));
#42279=CARTESIAN_POINT('Ctrl Pts',(21.7582305184669,0.415849885720624,3.73054133411992));
#42280=CARTESIAN_POINT('Ctrl Pts',(21.7820884364982,0.49411604100673,3.96273824894669));
#42281=CARTESIAN_POINT('Ctrl Pts',(21.8059463545297,0.451557364815975,4.20404667689569));
#42282=CARTESIAN_POINT('Ctrl Pts',(21.8298042725611,0.29858061275206,4.39546013422383));
#42283=CARTESIAN_POINT('Ctrl Pts',(21.8536621905925,0.0725927676976751,
4.49017281661646));
#42284=CARTESIAN_POINT('Ctrl Pts',(21.8775201086239,-0.171145986446082,
4.46502489330693));
#42285=CARTESIAN_POINT('Ctrl Pts',(21.9013780266554,-0.373034884980705,
4.32616571656009));
#42286=CARTESIAN_POINT('Ctrl Pts',(21.9252359446868,-0.483706592871294,
4.10755013753858));
#42287=CARTESIAN_POINT('Ctrl Pts',(21.9490938627182,-0.476098862901817,
3.86263562028194));
#42288=CARTESIAN_POINT('Ctrl Pts',(21.9729517807496,-0.352071992280181,
3.65131043559696));
#42289=CARTESIAN_POINT('Ctrl Pts',(21.996809698781,-0.141953929297546,3.52524934752154));
#42290=CARTESIAN_POINT('Ctrl Pts',(22.0206676168125,0.102875736145779,3.51527772592526));
#42291=CARTESIAN_POINT('Ctrl Pts',(22.0445255348438,0.322549481822576,3.62383390390986));
#42292=CARTESIAN_POINT('Ctrl Pts',(22.0683834528753,0.46335109312246,3.82437293894729));
#42293=CARTESIAN_POINT('Ctrl Pts',(22.0922413709067,0.490850740723195,4.06785757439707));
#42294=CARTESIAN_POINT('Ctrl Pts',(22.1160992889381,0.398324011712033,4.29474918450382));
#42295=CARTESIAN_POINT('Ctrl Pts',(22.1399572069695,0.208396211707814,4.44956659019228));
#42296=CARTESIAN_POINT('Ctrl Pts',(22.163815125001,-0.0324901386554863,
4.49445271863166));
#42297=CARTESIAN_POINT('Ctrl Pts',(22.1876730430324,-0.265431765108271,
4.41843168874211));
#42298=CARTESIAN_POINT('Ctrl Pts',(22.2115309610638,-0.433468094767725,
4.24009271310828));
#42299=CARTESIAN_POINT('Ctrl Pts',(22.2353888790952,-0.495509667838209,
4.00304452911861));
#42300=CARTESIAN_POINT('Ctrl Pts',(22.2592467971266,-0.436385629680506,
3.76525187484075));
#42301=CARTESIAN_POINT('Ctrl Pts',(22.2831047151581,-0.270553418215538,
3.58486153155103));
#42302=CARTESIAN_POINT('Ctrl Pts',(22.3069626331895,-0.0385635261649252,
3.50598385198694));
#42303=CARTESIAN_POINT('Ctrl Pts',(22.3308205512209,0.202856198284482,3.54790657725669));
#42304=CARTESIAN_POINT('Ctrl Pts',(22.3546784692523,0.394672056935096,3.70037845932536));
#42305=CARTESIAN_POINT('Ctrl Pts',(22.3785363872837,0.489979846308564,3.9261159693126));
#42306=CARTESIAN_POINT('Ctrl Pts',(22.4023943053151,0.465474217808745,4.1699201379362));
#42307=CARTESIAN_POINT('Ctrl Pts',(22.4262522233466,0.327147461276091,4.37217420322137));
#42308=CARTESIAN_POINT('Ctrl Pts',(22.450110141378,0.108824243893236,4.4834215400391));
#42309=CARTESIAN_POINT('Ctrl Pts',(22.4739680594094,-0.136109474402841,
4.47645913832327));
#42310=CARTESIAN_POINT('Ctrl Pts',(22.4978259774408,-0.347760701725541,
4.3529895060813));
#42311=CARTESIAN_POINT('Ctrl Pts',(22.5216838954723,-0.474374996640319,
4.1432043106148));
#42312=CARTESIAN_POINT('Ctrl Pts',(22.5455418135036,-0.484991622785221,
3.89840178635216));
#42313=CARTESIAN_POINT('Ctrl Pts',(22.5693997315351,-0.377014700254462,
3.67844274379546));
#42314=CARTESIAN_POINT('Ctrl Pts',(22.5932576495665,-0.176847198578467,
3.53711330196678));
#42315=CARTESIAN_POINT('Ctrl Pts',(22.6171155675979,0.0665638539184235,
3.50897209184919));
#42316=CARTESIAN_POINT('Ctrl Pts',(22.6409734856293,0.293698998435555,3.60090091054846));
#42317=CARTESIAN_POINT('Ctrl Pts',(22.6648314036608,0.449015288492166,3.79041970485759));
#42318=CARTESIAN_POINT('Ctrl Pts',(22.6886893216922,0.494537845944295,4.03118776656693));
#42319=CARTESIAN_POINT('Ctrl Pts',(22.7125472397236,0.419127261608858,4.26432734830583));
#42320=CARTESIAN_POINT('Ctrl Pts',(22.736405157755,0.241238408088568,4.43283588997321));
#42321=CARTESIAN_POINT('Ctrl Pts',(22.7602630757865,0.00434171083240793,
4.49549632518638));
#42322=CARTESIAN_POINT('Ctrl Pts',(22.7841209938178,-0.233581370990537,
4.43700954435219));
#42323=CARTESIAN_POINT('Ctrl Pts',(22.8079789118493,-0.414457183229959,
4.27163232278894));
#42324=CARTESIAN_POINT('Ctrl Pts',(22.8238841905369,-0.46737397936094,4.11714349286348));
#42325=CARTESIAN_POINT('Ctrl Pts',(22.8318368298807,-0.473742730682552,
4.03823705100924));
#42326=CARTESIAN_POINT('Ctrl Pts',(4.,-0.219892372743211,3.64701365460636));
#42327=CARTESIAN_POINT('Ctrl Pts',(4.00795263934381,-0.161099076858729,
3.61038844940468));
#42328=CARTESIAN_POINT('Ctrl Pts',(4.02385791803142,-0.0249198690254346,
3.56711791692558));
#42329=CARTESIAN_POINT('Ctrl Pts',(4.04771583606284,0.185569069288609,3.60813812632505));
#42330=CARTESIAN_POINT('Ctrl Pts',(4.07157375409426,0.350624105231944,3.74494568050885));
#42331=CARTESIAN_POINT('Ctrl Pts',(4.09543167212568,0.429971014252744,3.94413788601839));
#42332=CARTESIAN_POINT('Ctrl Pts',(4.1192895901571,0.40416308778273,4.15698104289539));
#42333=CARTESIAN_POINT('Ctrl Pts',(4.14314750818851,0.279534313346206,4.3314427366163));
#42334=CARTESIAN_POINT('Ctrl Pts',(4.16700542621994,0.0865475313004802,
4.42485517705098));
#42335=CARTESIAN_POINT('Ctrl Pts',(4.19086334425134,-0.127600227202394,
4.41438026490915));
#42336=CARTESIAN_POINT('Ctrl Pts',(4.21472126228278,-0.310547447266788,
4.30257739619942));
#42337=CARTESIAN_POINT('Ctrl Pts',(4.23857918031418,-0.417556725585918,
4.11678647978038));
#42338=CARTESIAN_POINT('Ctrl Pts',(4.26243709834561,-0.422462345057068,
3.90243789311793));
#42339=CARTESIAN_POINT('Ctrl Pts',(4.28629501637703,-0.324064236326554,
3.71194600226016));
#42340=CARTESIAN_POINT('Ctrl Pts',(4.31015293440845,-0.146423688323203,
3.59189110566319));
#42341=CARTESIAN_POINT('Ctrl Pts',(4.33401085243986,0.0670214896752265,
3.5716299793216));
#42342=CARTESIAN_POINT('Ctrl Pts',(4.35786877047129,0.264078061498623,3.65611697628114));
#42343=CARTESIAN_POINT('Ctrl Pts',(4.38172668850271,0.396560367883193,3.82469274783887));
#42344=CARTESIAN_POINT('Ctrl Pts',(4.40558460653412,0.432072854850341,4.03613591352675));
#42345=CARTESIAN_POINT('Ctrl Pts',(4.42944252456555,0.361931763288092,4.23874286631049));
#42346=CARTESIAN_POINT('Ctrl Pts',(4.45330044259696,0.203288494707987,4.382970683851));
#42347=CARTESIAN_POINT('Ctrl Pts',(4.47715836062838,-0.00506434719902249,
4.43355173791626));
#42348=CARTESIAN_POINT('Ctrl Pts',(4.5010162786598,-0.212178818846594,4.37811758201071));
#42349=CARTESIAN_POINT('Ctrl Pts',(4.52487419669122,-0.367409789343613,
4.23022337776645));
#42350=CARTESIAN_POINT('Ctrl Pts',(4.54873211472264,-0.432799058467291,
4.02603328640456));
#42351=CARTESIAN_POINT('Ctrl Pts',(4.57259003275406,-0.392357168499796,
3.8154773474345));
#42352=CARTESIAN_POINT('Ctrl Pts',(4.59644795078547,-0.255973263285106,
3.65004222328625));
#42353=CARTESIAN_POINT('Ctrl Pts',(4.6203058688169,-0.0569969226013119,
3.57018130821703));
#42354=CARTESIAN_POINT('Ctrl Pts',(4.64416378684831,0.155916718210686,3.59542277130738));
#42355=CARTESIAN_POINT('Ctrl Pts',(4.66802170487973,0.330704474340828,3.71959438727947));
#42356=CARTESIAN_POINT('Ctrl Pts',(4.69187962291115,0.424625978282027,3.91233281365517));
#42357=CARTESIAN_POINT('Ctrl Pts',(4.71573754094257,0.41471486395576,4.1265082550995));
#42358=CARTESIAN_POINT('Ctrl Pts',(4.73959545897399,0.303394668785218,4.30974898215573));
#42359=CARTESIAN_POINT('Ctrl Pts',(4.76345337700541,0.117886212792376,4.41724764568232));
#42360=CARTESIAN_POINT('Ctrl Pts',(4.78731129503683,-0.0964486333844469,
4.42271789424177));
#42361=CARTESIAN_POINT('Ctrl Pts',(4.81116921306824,-0.287199161490599,
4.32482210305491));
#42362=CARTESIAN_POINT('Ctrl Pts',(4.83502713109967,-0.407721671464292,
4.14749845969467));
#42363=CARTESIAN_POINT('Ctrl Pts',(4.85888504913109,-0.42854512664958,3.93410742516172));
#42364=CARTESIAN_POINT('Ctrl Pts',(4.8827429671625,-0.344577625034195,3.73682892005441));
#42365=CARTESIAN_POINT('Ctrl Pts',(4.90660088519393,-0.176351507991885,
3.60390291263011));
#42366=CARTESIAN_POINT('Ctrl Pts',(4.93045880322534,0.0349973564730633,
3.56783343253575));
#42367=CARTESIAN_POINT('Ctrl Pts',(4.95431672125677,0.237788413971502,3.63744045016736));
#42368=CARTESIAN_POINT('Ctrl Pts',(4.97817463928818,0.382433727027559,3.79570315365689));
#42369=CARTESIAN_POINT('Ctrl Pts',(5.0020325573196,0.433563576539811,4.00392200101168));
#42370=CARTESIAN_POINT('Ctrl Pts',(5.02589047535102,0.378675321553375,4.21118181228595));
#42371=CARTESIAN_POINT('Ctrl Pts',(5.04974839338244,0.231190635538481,4.36680191797922));
#42372=CARTESIAN_POINT('Ctrl Pts',(5.07360631141386,0.0271735416279573,
4.43272896324296));
#42373=CARTESIAN_POINT('Ctrl Pts',(5.09746422944527,-0.183488223403015,
4.39284198969348));
#42374=CARTESIAN_POINT('Ctrl Pts',(5.1213221474767,-0.349282119693095,4.256894448863));
#42375=CARTESIAN_POINT('Ctrl Pts',(5.1451800655081,-0.4296670234643,4.05812921762123));
#42376=CARTESIAN_POINT('Ctrl Pts',(5.16903798353954,-0.404986636103755,
3.84514980926298));
#42377=CARTESIAN_POINT('Ctrl Pts',(5.19289590157095,-0.281275984601366,
3.67003549057442));
#42378=CARTESIAN_POINT('Ctrl Pts',(5.21675381960238,-0.0887856930599551,
3.5756064824932));
#42379=CARTESIAN_POINT('Ctrl Pts',(5.24061173763379,0.125415118908336,3.58495324968971));
#42380=CARTESIAN_POINT('Ctrl Pts',(5.26446965566521,0.308948518064291,3.69579025298356));
#42381=CARTESIAN_POINT('Ctrl Pts',(5.28832757369662,0.416935588964862,3.88101482593007));
#42382=CARTESIAN_POINT('Ctrl Pts',(5.31218549172805,0.422970551266107,4.09533451502773));
#42383=CARTESIAN_POINT('Ctrl Pts',(5.33604340975946,0.325577692296299,4.28634231834109));
#42384=CARTESIAN_POINT('Ctrl Pts',(5.35990132779089,0.148572219001774,4.40733162501188));
#42385=CARTESIAN_POINT('Ctrl Pts',(5.3837592458223,-0.0647632088646815,
4.42871725387658));
#42386=CARTESIAN_POINT('Ctrl Pts',(5.40761716385372,-0.26226226804932,4.34526983614494));
#42387=CARTESIAN_POINT('Ctrl Pts',(5.43147508188515,-0.395631058815178,
4.17739453851434));
#42388=CARTESIAN_POINT('Ctrl Pts',(5.45533299991656,-0.432257278927009,
3.96614144408682));
#42389=CARTESIAN_POINT('Ctrl Pts',(5.47919091794798,-0.363184819889405,
3.76316768886851));
#42390=CARTESIAN_POINT('Ctrl Pts',(5.5030488359794,-0.205303779432806,3.61810588490468));
#42391=CARTESIAN_POINT('Ctrl Pts',(5.52690675401082,0.00277962745745752,
3.56642759466814));
#42392=CARTESIAN_POINT('Ctrl Pts',(5.55076467204224,0.210183339719457,3.62076956781107));
#42393=CARTESIAN_POINT('Ctrl Pts',(5.57462259007365,0.36619150013966,3.76784371165257));
#42394=CARTESIAN_POINT('Ctrl Pts',(5.59848050810508,0.432655863921731,3.97168639180759));
#42395=CARTESIAN_POINT('Ctrl Pts',(5.62233842613649,0.393324083661671,4.18245252040861));
#42396=CARTESIAN_POINT('Ctrl Pts',(5.64619634416792,0.257813851021257,4.34860403787086));
#42397=CARTESIAN_POINT('Ctrl Pts',(5.67005426219933,0.0592611090830247,
4.42951237227525));
#42398=CARTESIAN_POINT('Ctrl Pts',(5.69391218023075,-0.153782588238227,
4.40539323200473));
#42399=CARTESIAN_POINT('Ctrl Pts',(5.71777009826218,-0.329222253834466,
4.28214440376531));
#42400=CARTESIAN_POINT('Ctrl Pts',(5.74162801629359,-0.424158110434281,
4.08990358344764));
#42401=CARTESIAN_POINT('Ctrl Pts',(5.76548593432501,-0.415375755386326,
3.8756788878607));
#42402=CARTESIAN_POINT('Ctrl Pts',(5.78934385235642,-0.305022713182347,
3.69185409099321));
#42403=CARTESIAN_POINT('Ctrl Pts',(5.81320177038785,-0.120083309624962,
3.58337936191985));
#42404=CARTESIAN_POINT('Ctrl Pts',(5.83705968841926,0.0942197354074567,
3.57677972866706));
#42405=CARTESIAN_POINT('Ctrl Pts',(5.86091760645069,0.285483486244351,3.673668977605));
#42406=CARTESIAN_POINT('Ctrl Pts',(5.8847755244821,0.406938752801468,3.85035505520226));
#42407=CARTESIAN_POINT('Ctrl Pts',(5.90863344251353,0.428886400972996,4.06363338935351));
#42408=CARTESIAN_POINT('Ctrl Pts',(5.93249136054494,0.345959657594393,4.261351642888));
#42409=CARTESIAN_POINT('Ctrl Pts',(5.95634927857636,0.178436323746589,4.39516226965834));
#42410=CARTESIAN_POINT('Ctrl Pts',(5.98020719660778,-0.0327194942966983,
4.4323450160316));
#42411=CARTESIAN_POINT('Ctrl Pts',(6.0040651146392,-0.23587461323539,4.36380751861078));
#42412=CARTESIAN_POINT('Ctrl Pts',(6.02792303267061,-0.381351759249696,
4.20630938167977));
#42413=CARTESIAN_POINT('Ctrl Pts',(6.05178095070204,-0.433578399193506,
3.9983625870902));
#42414=CARTESIAN_POINT('Ctrl Pts',(6.07563886873346,-0.379782579589031,
3.79081692866841));
#42415=CARTESIAN_POINT('Ctrl Pts',(6.09949678676487,-0.233120953551068,
3.63442082419035));
#42416=CARTESIAN_POINT('Ctrl Pts',(6.12335470479629,-0.0294522997972467,
3.5674214393556));
#42417=CARTESIAN_POINT('Ctrl Pts',(6.14721262282771,0.181413325723775,3.60619428643423));
#42418=CARTESIAN_POINT('Ctrl Pts',(6.17107054085913,0.347927737305898,3.74127281623538));
#42419=CARTESIAN_POINT('Ctrl Pts',(6.19492845889055,0.429346806292137,3.93959933010928));
#42420=CARTESIAN_POINT('Ctrl Pts',(6.21878637692197,0.405811992579865,4.15272917617017));
#42421=CARTESIAN_POINT('Ctrl Pts',(6.24264429495339,0.282982581651336,4.32844890303245));
#42422=CARTESIAN_POINT('Ctrl Pts',(6.26650221298481,0.0910742457207041,
4.42397415233781));
#42423=CARTESIAN_POINT('Ctrl Pts',(6.29036013101623,-0.123327005978964,
4.41559921078967));
#42424=CARTESIAN_POINT('Ctrl Pts',(6.31421804904765,-0.307151379675736,
4.3060270879454));
#42425=CARTESIAN_POINT('Ctrl Pts',(6.33807596707907,-0.416657206472865,
4.12081787696614));
#42426=CARTESIAN_POINT('Ctrl Pts',(6.36193388511048,-0.422829889105799,
3.9075587958503));
#42427=CARTESIAN_POINT('Ctrl Pts',(6.39374444248571,-0.296437506874183,
3.64987069373525));
#42428=CARTESIAN_POINT('Ctrl Pts',(6.43350763920474,0.0703302468340302,
3.51324810367198));
#42429=CARTESIAN_POINT('Ctrl Pts',(6.48122347526758,0.448014600657906,3.7964368525222));
#42430=CARTESIAN_POINT('Ctrl Pts',(6.52893931133042,0.413240052911115,4.26646358767058));
#42431=CARTESIAN_POINT('Ctrl Pts',(6.57665514739325,-0.000480251589724132,
4.49184654025612));
#42432=CARTESIAN_POINT('Ctrl Pts',(6.62437098345609,-0.41404349770976,4.26553045144514));
#42433=CARTESIAN_POINT('Ctrl Pts',(6.67208681951894,-0.447234019333667,
3.79538894860702));
#42434=CARTESIAN_POINT('Ctrl Pts',(6.71980265558177,-0.0698021891909718,
3.51313682319347));
#42435=CARTESIAN_POINT('Ctrl Pts',(6.76751849164461,0.371772181936036,3.67798293440124));
#42436=CARTESIAN_POINT('Ctrl Pts',(6.81523432770745,0.471920133146607,4.13853999974893));
#42437=CARTESIAN_POINT('Ctrl Pts',(6.86295016377028,0.138708377331583,4.4718748549198));
#42438=CARTESIAN_POINT('Ctrl Pts',(6.91066599983312,-0.32188767172048,4.37187913281409));
#42439=CARTESIAN_POINT('Ctrl Pts',(6.95838183589596,-0.486886005735063,
3.93038141845316));
#42440=CARTESIAN_POINT('Ctrl Pts',(7.0060976719588,-0.204771183672361,3.55281534000283));
#42441=CARTESIAN_POINT('Ctrl Pts',(7.05381350802163,0.265389096458903,3.58590591031157));
#42442=CARTESIAN_POINT('Ctrl Pts',(7.10152934408448,0.491837993618785,3.99926540470374));
#42443=CARTESIAN_POINT('Ctrl Pts',(7.14924518014731,0.266624753986561,4.41329951581085));
#42444=CARTESIAN_POINT('Ctrl Pts',(7.19696101621015,-0.203434237821079,
4.44779430805676));
#42445=CARTESIAN_POINT('Ctrl Pts',(7.24467685227299,-0.486676365692783,
4.07107270446015));
#42446=CARTESIAN_POINT('Ctrl Pts',(7.29239268833582,-0.322996137187983,
3.62908393881966));
#42447=CARTESIAN_POINT('Ctrl Pts',(7.34010852439867,0.137296434535941,3.52771310152703));
#42448=CARTESIAN_POINT('Ctrl Pts',(7.3878243604615,0.471507566988788,3.86005058906394));
#42449=CARTESIAN_POINT('Ctrl Pts',(7.43554019652434,0.372726051350611,4.32090577464778));
#42450=CARTESIAN_POINT('Ctrl Pts',(7.48325603258718,-0.0683355354161961,
4.48706824929225));
#42451=CARTESIAN_POINT('Ctrl Pts',(7.53097186865002,-0.44664354691983,4.20594845626764));
#42452=CARTESIAN_POINT('Ctrl Pts',(7.57868770471286,-0.414791917646955,
3.73570302684109));
#42453=CARTESIAN_POINT('Ctrl Pts',(7.62640354077569,-0.00203048755240202,
3.50816557464413));
#42454=CARTESIAN_POINT('Ctrl Pts',(7.67411937683853,0.412595570264971,3.73228724307244));
#42455=CARTESIAN_POINT('Ctrl Pts',(7.72183521290137,0.448328767436039,4.20225365549051));
#42456=CARTESIAN_POINT('Ctrl Pts',(7.7695510489642,0.0723547589785895,4.48648742399228));
#42457=CARTESIAN_POINT('Ctrl Pts',(7.81726688502705,-0.370063737934377,
4.32397230547438));
#42458=CARTESIAN_POINT('Ctrl Pts',(7.86498272108989,-0.472647010158531,
3.86394843388276));
#42459=CARTESIAN_POINT('Ctrl Pts',(7.91269855715272,-0.141191260335066,
3.52886280888004));
#42460=CARTESIAN_POINT('Ctrl Pts',(7.96041439321556,0.31992259635559,3.62642971585976));
#42461=CARTESIAN_POINT('Ctrl Pts',(8.0081302292784,0.48724661017382,4.0670519628834));
#42462=CARTESIAN_POINT('Ctrl Pts',(8.05584606534124,0.207124564615173,4.44609936066402));
#42463=CARTESIAN_POINT('Ctrl Pts',(8.10356190140407,-0.263203155649882,
4.41548685142597));
#42464=CARTESIAN_POINT('Ctrl Pts',(8.15127773746691,-0.491827368180951,
4.00332637343646));
#42465=CARTESIAN_POINT('Ctrl Pts',(8.19899357352975,-0.268798940774433,
3.58811123553743));
#42466=CARTESIAN_POINT('Ctrl Pts',(8.24670940959259,0.201071689948468,3.55113988776764));
#42467=CARTESIAN_POINT('Ctrl Pts',(8.29442524565542,0.486295093906121,3.92636368766143));
#42468=CARTESIAN_POINT('Ctrl Pts',(8.34214108171827,0.324946230517931,4.36920884621601));
#42469=CARTESIAN_POINT('Ctrl Pts',(8.3898569177811,-0.134805756295296,4.47300384028212));
#42470=CARTESIAN_POINT('Ctrl Pts',(8.43757275384394,-0.470763542849379,
4.14243212971755));
#42471=CARTESIAN_POINT('Ctrl Pts',(8.48528858990678,-0.37441192437669,3.68106280283335));
#42472=CARTESIAN_POINT('Ctrl Pts',(8.53300442596962,0.0657679253190804,
3.51257841158684));
#42473=CARTESIAN_POINT('Ctrl Pts',(8.58072026203246,0.445552077224736,3.79170076492532));
#42474=CARTESIAN_POINT('Ctrl Pts',(8.62843609809529,0.41617890091499,4.26210751092856));
#42475=CARTESIAN_POINT('Ctrl Pts',(8.67615193415813,0.0046222361594965,
4.49181689660367));
#42476=CARTESIAN_POINT('Ctrl Pts',(8.72386777022097,-0.411179099183508,
4.26988325855195));
#42477=CARTESIAN_POINT('Ctrl Pts',(8.7715836062838,-0.449388340942622,3.80011167148426));
#42478=CARTESIAN_POINT('Ctrl Pts',(8.81929944234665,-0.0749173544856965,
3.51390061216986));
#42479=CARTESIAN_POINT('Ctrl Pts',(8.86701527840948,0.368351391347115,3.67408210030036));
#42480=CARTESIAN_POINT('Ctrl Pts',(8.91473111447233,0.473357386691186,4.13355901061654));
#42481=CARTESIAN_POINT('Ctrl Pts',(8.96244695053515,0.14367201029714,4.47038662641401));
#42482=CARTESIAN_POINT('Ctrl Pts',(9.01016278659801,-0.317949583830803,
4.37525096534692));
#42483=CARTESIAN_POINT('Ctrl Pts',(9.05787862266083,-0.487593182843731,
3.93551656882348));
#42484=CARTESIAN_POINT('Ctrl Pts',(9.10559445872368,-0.209472459465777,
3.55499829935456));
#42485=CARTESIAN_POINT('Ctrl Pts',(9.15331029478651,0.261010046587687,3.58313193881964));
#42486=CARTESIAN_POINT('Ctrl Pts',(9.20102613084934,0.491803010703882,3.99408193320625));
#42487=CARTESIAN_POINT('Ctrl Pts',(9.2487419669122,0.270965702728691,4.41046657939073));
#42488=CARTESIAN_POINT('Ctrl Pts',(9.29645780297501,-0.198703579405513,
4.44991344988054));
#42489=CARTESIAN_POINT('Ctrl Pts',(9.34417363903789,-0.485900307124067,
4.07619787653679));
#42490=CARTESIAN_POINT('Ctrl Pts',(9.39188947510068,-0.326887306273347,
3.63250862071426));
#42491=CARTESIAN_POINT('Ctrl Pts',(9.43960531116356,0.13231133773591,3.52629235307153));
#42492=CARTESIAN_POINT('Ctrl Pts',(9.48732114722637,0.470006444430667,3.85508910653225));
#42493=CARTESIAN_POINT('Ctrl Pts',(9.53503698328922,0.376087401226012,4.31695976320512));
#42494=CARTESIAN_POINT('Ctrl Pts',(9.58275281935206,-0.0631984893729827,
4.48776139227388));
#42495=CARTESIAN_POINT('Ctrl Pts',(9.63046865541489,-0.444448234747017,
4.21064422964382));
#42496=CARTESIAN_POINT('Ctrl Pts',(9.67818449147773,-0.41755432743774,3.74008922975375));
#42497=CARTESIAN_POINT('Ctrl Pts',(9.72590032754057,-0.00721385634321597,
3.50821428942208));
#42498=CARTESIAN_POINT('Ctrl Pts',(9.77361616360341,0.40975121003073,3.72795373420991));
#42499=CARTESIAN_POINT('Ctrl Pts',(9.82133199966624,0.450435435400681,4.19751745084266));
#42500=CARTESIAN_POINT('Ctrl Pts',(9.86904783572909,0.077477869602138,4.48569785316993));
#42501=CARTESIAN_POINT('Ctrl Pts',(9.91676367179192,-0.366628816002305,
4.3278544435092));
#42502=CARTESIAN_POINT('Ctrl Pts',(9.96447950785476,-0.474054618562381,
3.8689372536849));
#42503=CARTESIAN_POINT('Ctrl Pts',(10.0121953439176,-0.146148770628728,
3.53037700046135));
#42504=CARTESIAN_POINT('Ctrl Pts',(10.0599111799804,0.315967742161179,3.62307877379278));
#42505=CARTESIAN_POINT('Ctrl Pts',(10.1076270160433,0.487926215535836,4.06191310882887));
#42506=CARTESIAN_POINT('Ctrl Pts',(10.1553428521061,0.211814537474087,4.44389168337175));
#42507=CARTESIAN_POINT('Ctrl Pts',(10.203058688169,-0.258809689535701,4.4182376949229));
#42508=CARTESIAN_POINT('Ctrl Pts',(10.2507745242318,-0.491764996345908,
4.00850959581219));
#42509=CARTESIAN_POINT('Ctrl Pts',(10.2984903602946,-0.273124940234581,
3.59096700393021));
#42510=CARTESIAN_POINT('Ctrl Pts',(10.3462061963575,0.196329951061554,3.54904570612073));
#42511=CARTESIAN_POINT('Ctrl Pts',(10.3939220324203,0.485492027373267,3.92124267520431));
#42512=CARTESIAN_POINT('Ctrl Pts',(10.4416378684831,0.328819304693055,4.36576370748498));
#42513=CARTESIAN_POINT('Ctrl Pts',(10.489353704546,-0.129813245022134,4.47439829918413));
#42514=CARTESIAN_POINT('Ctrl Pts',(10.5370695406088,-0.469236294399976,
4.14738563318641));
#42515=CARTESIAN_POINT('Ctrl Pts',(10.5847853766716,-0.377752434501872,
3.68502647241413));
#42516=CARTESIAN_POINT('Ctrl Pts',(10.6325012127345,0.0606272984676223,
3.51191234851464));
#42517=CARTESIAN_POINT('Ctrl Pts',(10.6802170487973,0.443332050383407,3.78701662516801));
#42518=CARTESIAN_POINT('Ctrl Pts',(10.7279328848602,0.418918158891686,4.25770681210006));
#42519=CARTESIAN_POINT('Ctrl Pts',(10.775648720923,0.00980527620531799,
4.49174086815163));
#42520=CARTESIAN_POINT('Ctrl Pts',(10.8233645569858,-0.408311942493964,
4.27420171857372));
#42521=CARTESIAN_POINT('Ctrl Pts',(10.8710803930487,-0.451470021714238,
3.80485891169382));
#42522=CARTESIAN_POINT('Ctrl Pts',(10.9187962291115,-0.080036233235122,
3.51471716883706));
#42523=CARTESIAN_POINT('Ctrl Pts',(10.9665120651743,0.364896059739551,3.6702181168734));
#42524=CARTESIAN_POINT('Ctrl Pts',(11.0142279012372,0.47473868640782,4.1285628425314));
#42525=CARTESIAN_POINT('Ctrl Pts',(11.0619437373,0.148621472554162,4.46884633169921));
#42526=CARTESIAN_POINT('Ctrl Pts',(11.1096595733629,-0.313977126381285,
4.37858102033954));
#42527=CARTESIAN_POINT('Ctrl Pts',(11.1573754094257,-0.488245699001722,
3.94065893278431));
#42528=CARTESIAN_POINT('Ctrl Pts',(11.2050912454886,-0.214150733603143,
3.55723066033293));
#42529=CARTESIAN_POINT('Ctrl Pts',(11.2528070815514,0.256602145595791,3.58040428537983));
#42530=CARTESIAN_POINT('Ctrl Pts',(11.3005229176142,0.491713326162588,3.98889911147238));
#42531=CARTESIAN_POINT('Ctrl Pts',(11.3482387536771,0.275276593332242,4.40758805430897));
#42532=CARTESIAN_POINT('Ctrl Pts',(11.3959545897399,-0.193950870829933,
4.45198261532529));
#42533=CARTESIAN_POINT('Ctrl Pts',(11.4436704258028,-0.485070265991237,
4.08131458604192));
#42534=CARTESIAN_POINT('Ctrl Pts',(11.4913862618656,-0.330742172127369,
3.63597412121053));
#42535=CARTESIAN_POINT('Ctrl Pts',(11.5391020979284,0.127311547523522,3.52492422212962));
#42536=CARTESIAN_POINT('Ctrl Pts',(11.5868179339912,0.468453114143607,3.85014371984754));
#42537=CARTESIAN_POINT('Ctrl Pts',(11.6345337700541,0.379406977967949,4.31297854546471));
#42538=CARTESIAN_POINT('Ctrl Pts',(11.6822496061169,-0.0580544240024287,
4.48840035698771));
#42539=CARTESIAN_POINT('Ctrl Pts',(11.7299654421798,-0.44220355512924,4.21531660568344));
#42540=CARTESIAN_POINT('Ctrl Pts',(11.7776812782426,-0.420270357404582,
3.74450430230823));
#42541=CARTESIAN_POINT('Ctrl Pts',(11.8253971143054,-0.0123964237846327,
3.50831762943));
#42542=CARTESIAN_POINT('Ctrl Pts',(11.8731129503683,0.406861336540243,3.72365044295193));
#42543=CARTESIAN_POINT('Ctrl Pts',(11.9208287864311,0.452492071153857,4.1927593068956));
#42544=CARTESIAN_POINT('Ctrl Pts',(11.968544622494,0.0825923743414284,4.48485433333386));
#42545=CARTESIAN_POINT('Ctrl Pts',(12.0162604585568,-0.363153170675764,
4.33170016502878));
#42546=CARTESIAN_POINT('Ctrl Pts',(12.0639762946196,-0.475409571231627,
3.87394063131468));
#42547=CARTESIAN_POINT('Ctrl Pts',(12.1116921306825,-0.151090047408964,
3.53194335553704));
#42548=CARTESIAN_POINT('Ctrl Pts',(12.1594079667453,0.311977791768556,3.61976969834691));
#42549=CARTESIAN_POINT('Ctrl Pts',(12.2071238028081,0.488551624369653,4.05676737776005));
#42550=CARTESIAN_POINT('Ctrl Pts',(12.254839638871,0.216480982979095,4.44163470069774));
#42551=CARTESIAN_POINT('Ctrl Pts',(12.3025554749338,-0.254387476069249,
4.42094208256136));
#42552=CARTESIAN_POINT('Ctrl Pts',(12.3502713109967,-0.49164800158875,4.0136918729824));
#42553=CARTESIAN_POINT('Ctrl Pts',(12.3979871470595,-0.277420602272412,
3.59386820576715));
#42554=CARTESIAN_POINT('Ctrl Pts',(12.4457029831224,0.191566404775332,3.54700161433684));
#42555=CARTESIAN_POINT('Ctrl Pts',(12.4934188191852,0.484635034689867,3.91613041073711));
#42556=CARTESIAN_POINT('Ctrl Pts',(12.541134655248,0.332655855180181,4.362277941457));
#42557=CARTESIAN_POINT('Ctrl Pts',(12.5888504913109,-0.124806314709729,
4.47574006417428));
#42558=CARTESIAN_POINT('Ctrl Pts',(12.6365663273737,-0.4676569254097,4.15232276575852));
#42559=CARTESIAN_POINT('Ctrl Pts',(12.6842821634365,-0.381050985679211,
3.68902512775968));
#42560=CARTESIAN_POINT('Ctrl Pts',(12.7319979994994,0.0554799374235607,
3.5113004999026));
#42561=CARTESIAN_POINT('Ctrl Pts',(12.7797138355622,0.441062780321708,3.78235614259331));
#42562=CARTESIAN_POINT('Ctrl Pts',(12.8274296716251,0.421610885427219,4.2532774884218));
#42563=CARTESIAN_POINT('Ctrl Pts',(12.8751455076879,0.0149872271275763,
4.49161021945745));
#42564=CARTESIAN_POINT('Ctrl Pts',(12.9228613437507,-0.405399432451448,
4.27848972156979));
#42565=CARTESIAN_POINT('Ctrl Pts',(12.9705771798136,-0.453501555338242,
3.80962782724943));
#42566=CARTESIAN_POINT('Ctrl Pts',(13.0182930158764,-0.0851462219395619,
3.51558762841831));
#42567=CARTESIAN_POINT('Ctrl Pts',(13.0660088519392,0.361400197209248,3.66639076405307));
#42568=CARTESIAN_POINT('Ctrl Pts',(13.1137246880021,0.476067254403989,4.1235523942958));
#42569=CARTESIAN_POINT('Ctrl Pts',(13.1614405240649,0.153554426643267,4.46725395975876));
#42570=CARTESIAN_POINT('Ctrl Pts',(13.2091563601278,-0.30996979384252,4.38186902434892));
#42571=CARTESIAN_POINT('Ctrl Pts',(13.2568721961906,-0.488843983144383,
3.94580788806928));
#42572=CARTESIAN_POINT('Ctrl Pts',(13.3045880322534,-0.218805220893238,
3.55951220202843));
#42573=CARTESIAN_POINT('Ctrl Pts',(13.3523038683163,0.252165742455243,3.57772323864086));
#42574=CARTESIAN_POINT('Ctrl Pts',(13.4000197043791,0.491569024438394,3.98371752277252));
#42575=CARTESIAN_POINT('Ctrl Pts',(13.447735540442,0.279556907518101,4.40466425628032));
#42576=CARTESIAN_POINT('Ctrl Pts',(13.4954513765048,-0.189176619112,4.45400157668594));
#42577=CARTESIAN_POINT('Ctrl Pts',(13.5431672125676,-0.484186345555107,
4.08642226350871));
#42578=CARTESIAN_POINT('Ctrl Pts',(13.5908830486304,-0.334560300710407,
3.63948005597396));
#42579=CARTESIAN_POINT('Ctrl Pts',(13.6385988846933,0.122297616148583,3.52360886035071));
#42580=CARTESIAN_POINT('Ctrl Pts',(13.6863147207561,0.466847750307624,3.8452149784873));
#42581=CARTESIAN_POINT('Ctrl Pts',(13.734030556819,0.3826844119832,4.30896256355269));
#42582=CARTESIAN_POINT('Ctrl Pts',(13.7817463928818,-0.0529039102219543,
4.48898507250754));
#42583=CARTESIAN_POINT('Ctrl Pts',(13.8294622289446,-0.439909757638992,
4.21996506537626));
#42584=CARTESIAN_POINT('Ctrl Pts',(13.8771780650075,-0.422939705734467,
3.74894775411238));
#42585=CARTESIAN_POINT('Ctrl Pts',(13.9248939010703,-0.0175776142901187,
3.50847558318244));
#42586=CARTESIAN_POINT('Ctrl Pts',(13.9726097371332,0.403926270823208,3.71937784729135));
#42587=CARTESIAN_POINT('Ctrl Pts',(14.020325573196,0.454498446235019,4.18797975215946));
#42588=CARTESIAN_POINT('Ctrl Pts',(14.0680414092588,0.0876977051117048,
4.48395695817926));
#42589=CARTESIAN_POINT('Ctrl Pts',(14.1157572453217,-0.359637188018331,
4.33550904286807));
#42590=CARTESIAN_POINT('Ctrl Pts',(14.1634730813845,-0.476711717661702,
3.87895801102093));
#42591=CARTESIAN_POINT('Ctrl Pts',(14.2111889174473,-0.156014541823709,
3.53356170012368));
#42592=CARTESIAN_POINT('Ctrl Pts',(14.2589047535102,0.307953188363286,3.61650285707861));
#42593=CARTESIAN_POINT('Ctrl Pts',(14.306620589573,0.4891227672074,4.05161534124029));
#42594=CARTESIAN_POINT('Ctrl Pts',(14.3543364256359,0.2211233828038,4.4393286633369));
#42595=CARTESIAN_POINT('Ctrl Pts',(14.4020522616987,-0.249937006449114,
4.42359971395084));
#42596=CARTESIAN_POINT('Ctrl Pts',(14.4497680977616,-0.491476396904638,
4.01887262932433));
#42597=CARTESIAN_POINT('Ctrl Pts',(14.4974839338244,-0.281685449746218,
3.59681451879656));
#42598=CARTESIAN_POINT('Ctrl Pts',(14.5451997698872,0.186781580201919,3.54500783946397));
#42599=CARTESIAN_POINT('Ctrl Pts',(14.59291560595,0.483724211046603,3.91102746210588));
#42600=CARTESIAN_POINT('Ctrl Pts',(14.6406314420129,0.33645545583349,4.35875193531444));
#42601=CARTESIAN_POINT('Ctrl Pts',(14.6883472780757,-0.119785521504147,
4.47702898621568));
#42602=CARTESIAN_POINT('Ctrl Pts',(14.7360631141386,-0.466025611307368,
4.15724297904063));
#42603=CARTESIAN_POINT('Ctrl Pts',(14.7837789502014,-0.38430721152129,3.69305832471834));
#42604=CARTESIAN_POINT('Ctrl Pts',(14.8314947862642,0.0503264139313189,
3.51074293371195));
#42605=CARTESIAN_POINT('Ctrl Pts',(14.8792106223271,0.438744519099385,3.77771983486548));
#42606=CARTESIAN_POINT('Ctrl Pts',(14.9269264583899,0.42425678142631,4.24882003188202));
#42607=CARTESIAN_POINT('Ctrl Pts',(14.9746422944528,0.0201675133397715,
4.49142496503298));
#42608=CARTESIAN_POINT('Ctrl Pts',(15.0223581305156,-0.402441892563756,
4.28274679124913));
#42609=CARTESIAN_POINT('Ctrl Pts',(15.0700739665785,-0.455482716161518,
3.8144178884426));
#42610=CARTESIAN_POINT('Ctrl Pts',(15.1177898026413,-0.0902467530057116,
3.51651189422706));
#42611=CARTESIAN_POINT('Ctrl Pts',(15.1655056387041,0.357864192060027,3.66260046696357));
#42612=CARTESIAN_POINT('Ctrl Pts',(15.2132214747669,0.47734294310866,4.11852822244656));
#42613=CARTESIAN_POINT('Ctrl Pts',(15.2609373108298,0.15847032463534,4.46560968746574));
#42614=CARTESIAN_POINT('Ctrl Pts',(15.3086531468926,-0.305928031329979,
4.38511461215921));
#42615=CARTESIAN_POINT('Ctrl Pts',(15.3563689829555,-0.489387968817152,
3.95096286275689));
#42616=CARTESIAN_POINT('Ctrl Pts',(15.4040848190183,-0.223435404337718,
3.56184267101825));
#42617=CARTESIAN_POINT('Ctrl Pts',(15.4518006550811,0.24770132994065,3.57508909640066));
#42618=CARTESIAN_POINT('Ctrl Pts',(15.499516491144,0.491370121559653,3.97853774265298));
#42619=CARTESIAN_POINT('Ctrl Pts',(15.5472323272068,0.283806169849271,4.40169551006635));
#42620=CARTESIAN_POINT('Ctrl Pts',(15.5949481632697,-0.184381354552937,
4.4559701097059));
#42621=CARTESIAN_POINT('Ctrl Pts',(15.6426639993325,-0.483248643997369,
4.09152034160055));
#42622=CARTESIAN_POINT('Ctrl Pts',(15.6903798353953,-0.338341267922855,
3.64302603558196));
#42623=CARTESIAN_POINT('Ctrl Pts',(15.7380956714582,0.117270100534806,3.52234641383892));
#42624=CARTESIAN_POINT('Ctrl Pts',(15.785811507521,0.465190531238913,3.84030342991275));
#42625=CARTESIAN_POINT('Ctrl Pts',(15.8335273435838,0.385919339229949,4.30491226354526));
#42626=CARTESIAN_POINT('Ctrl Pts',(15.8812431796467,-0.0477475201261761,
4.48951547388594));
#42627=CARTESIAN_POINT('Ctrl Pts',(15.9289590157095,-0.437567097060412,
4.22458909239344));
#42628=CARTESIAN_POINT('Ctrl Pts',(15.9766748517724,-0.425562075928853,
3.75341909160864));
#42629=CARTESIAN_POINT('Ctrl Pts',(16.0243906878352,-0.0227568523576073,
3.50868813313462));
#42630=CARTESIAN_POINT('Ctrl Pts',(16.072106523898,0.400946338892803,3.71513642180785));
#42631=CARTESIAN_POINT('Ctrl Pts',(16.1198223599609,0.456454337785543,4.1831793175245));
#42632=CARTESIAN_POINT('Ctrl Pts',(16.1675381960237,0.0927932948370443,
4.4830058273823));
#42633=CARTESIAN_POINT('Ctrl Pts',(16.2152540320865,-0.356081258568678,
4.33928065395499));
#42634=CARTESIAN_POINT('Ctrl Pts',(16.2629698681494,-0.477960913216358,
3.88398883549692));
#42635=CARTESIAN_POINT('Ctrl Pts',(16.3106857042122,-0.160921706883503,
3.53523185446324));
#42636=CARTESIAN_POINT('Ctrl Pts',(16.358401540275,0.303894378979202,3.6132786128531));
#42637=CARTESIAN_POINT('Ctrl Pts',(16.4061173763379,0.489639580609251,4.04645757153336));
#42638=CARTESIAN_POINT('Ctrl Pts',(16.4538332124007,0.225741221292456,4.43697382743292));
#42639=CARTESIAN_POINT('Ctrl Pts',(16.5015490484636,-0.245458775012363,
4.42621029389423));
#42640=CARTESIAN_POINT('Ctrl Pts',(16.5492648845264,-0.4912502013546,4.02405128938415));
#42641=CARTESIAN_POINT('Ctrl Pts',(16.5969807205893,-0.285919008936969,
3.59980561575594));
#42642=CARTESIAN_POINT('Ctrl Pts',(16.6446965566521,0.181976008816936,3.54306460296116));
#42643=CARTESIAN_POINT('Ctrl Pts',(16.6924123927149,0.482759657613431,3.90593439612197));
#42644=CARTESIAN_POINT('Ctrl Pts',(16.7401282287778,0.340217684611379,4.35518608070932));
#42645=CARTESIAN_POINT('Ctrl Pts',(16.7878440648406,-0.114751423091257,
4.47826492214097));
#42646=CARTESIAN_POINT('Ctrl Pts',(16.8355599009034,-0.464342533291602,
4.16214572651883));
#42647=CARTESIAN_POINT('Ctrl Pts',(16.8832757369663,-0.387520750342007,
3.69712561530174));
#42648=CARTESIAN_POINT('Ctrl Pts',(16.9309915730291,0.0451673004198413,
3.51023971187451));
#42649=CARTESIAN_POINT('Ctrl Pts',(16.978707409092,0.436377524217892,3.7731082169636));
#42650=CARTESIAN_POINT('Ctrl Pts',(17.0264232451548,0.426855552995382,4.24433493759383));
#42651=CARTESIAN_POINT('Ctrl Pts',(17.0741390812176,0.0253455594402812,
4.49118512545541));
#42652=CARTESIAN_POINT('Ctrl Pts',(17.1218549172805,-0.399439651340385,
4.28697245475663));
#42653=CARTESIAN_POINT('Ctrl Pts',(17.1695707533433,-0.457413284126125,
3.81922856321607));
#42654=CARTESIAN_POINT('Ctrl Pts',(17.2172865894061,-0.0953372598908034,
3.51748986360026));
#42655=CARTESIAN_POINT('Ctrl Pts',(17.265002425469,0.354288437054553,3.6588476466131));
#42656=CARTESIAN_POINT('Ctrl Pts',(17.3127182615318,0.478565610824392,4.11349088504481));
#42657=CARTESIAN_POINT('Ctrl Pts',(17.3604340975947,0.163368620495752,4.46391369745815));
#42658=CARTESIAN_POINT('Ctrl Pts',(17.4081499336575,-0.301852287783465,
4.38831742326589));
#42659=CARTESIAN_POINT('Ctrl Pts',(17.4558657697204,-0.489877595596684,
3.956123284257));
#42660=CARTESIAN_POINT('Ctrl Pts',(17.5035816057832,-0.228040769637767,
3.56422180844494));
#42661=CARTESIAN_POINT('Ctrl Pts',(17.551297441846,0.243209403937772,3.57250215124727));
#42662=CARTESIAN_POINT('Ctrl Pts',(17.5990132779089,0.491116639619549,3.97336034645914));
#42663=CARTESIAN_POINT('Ctrl Pts',(17.6467291139717,0.288023908337871,4.39868214542132));
#42664=CARTESIAN_POINT('Ctrl Pts',(17.6944449500345,-0.179565609787963,
4.45788799572981));
#42665=CARTESIAN_POINT('Ctrl Pts',(17.7421607860973,-0.48225726547346,4.09660825404716));
#42666=CARTESIAN_POINT('Ctrl Pts',(17.7898766221602,-0.342084653792828,
3.64661166616396));
#42667=CARTESIAN_POINT('Ctrl Pts',(17.837592458223,0.112229559114723,3.52113702282083));
#42668=CARTESIAN_POINT('Ctrl Pts',(17.8853082942859,0.463481641013499,3.83540961967535));
#42669=CARTESIAN_POINT('Ctrl Pts',(17.9330241303487,0.389111400387848,4.30082809533052));
#42670=CARTESIAN_POINT('Ctrl Pts',(17.9807399664116,-0.0425858264624495,
4.48999150220845));
#42671=CARTESIAN_POINT('Ctrl Pts',(18.0284558024744,-0.435175833605105,
4.22918817311999));
#42672=CARTESIAN_POINT('Ctrl Pts',(18.0761716385373,-0.428137176707308,
3.75791781814212));
#42673=CARTESIAN_POINT('Ctrl Pts',(18.1238874746,-0.0279335627019553,3.5089552556775));
#42674=CARTESIAN_POINT('Ctrl Pts',(18.1716033106629,0.397921871745719,3.71092663761881));
#42675=CARTESIAN_POINT('Ctrl Pts',(18.2193191467257,0.458359528554279,4.17835853620019));
#42676=CARTESIAN_POINT('Ctrl Pts',(18.2670349827886,0.097878577523561,4.48200104659009));
#42677=CARTESIAN_POINT('Ctrl Pts',(18.3147508188514,-0.352485777302551,
4.34301457935691));
#42678=CARTESIAN_POINT('Ctrl Pts',(18.3624666549143,-0.479157019140895,
3.88903254594255));
#42679=CARTESIAN_POINT('Ctrl Pts',(18.4101824909771,-0.165810997523729,
3.5369536330429));
#42680=CARTESIAN_POINT('Ctrl Pts',(18.4578983270399,0.299801814449608,3.61009732380414));
#42681=CARTESIAN_POINT('Ctrl Pts',(18.5056141631028,0.49010200717001,4.04129464153984));
#42682=CARTESIAN_POINT('Ctrl Pts',(18.5533299991656,0.230333985517487,4.43457045454981));
#42683=CARTESIAN_POINT('Ctrl Pts',(18.6010458352284,-0.24095327917969,4.42877353242069));
#42684=CARTESIAN_POINT('Ctrl Pts',(18.6487616712913,-0.49096944006335,4.0292272779409));
#42685=CARTESIAN_POINT('Ctrl Pts',(18.6964775073541,-0.290120809601049,
3.60284116440841));
#42686=CARTESIAN_POINT('Ctrl Pts',(18.744193343417,0.177150224400508,3.54117212067402));
#42687=CARTESIAN_POINT('Ctrl Pts',(18.7919091794797,0.481741481528227,3.90085177849878));
#42688=CARTESIAN_POINT('Ctrl Pts',(18.8396250155427,0.343942123623612,4.35158077372017));
#42689=CARTESIAN_POINT('Ctrl Pts',(18.8873408516054,-0.109704578635382,
4.47944773466767));
#42690=CARTESIAN_POINT('Ctrl Pts',(18.9350566876684,-0.462607878309702,
4.16703046362027));
#42691=CARTESIAN_POINT('Ctrl Pts',(18.9827725237311,-0.39069124519864,3.70122654773242));
#42692=CARTESIAN_POINT('Ctrl Pts',(19.030488359794,0.0400031699426168,3.50979089028978));
#42693=CARTESIAN_POINT('Ctrl Pts',(19.0782041958568,0.433962058584907,3.76852180111673));
#42694=CARTESIAN_POINT('Ctrl Pts',(19.1259200319197,0.429406911488226,4.23982270375453));
#42695=CARTESIAN_POINT('Ctrl Pts',(19.1736358679825,0.0305207902517796,
4.49089072733801));
#42696=CARTESIAN_POINT('Ctrl Pts',(19.2213517040454,-0.396393042209671,
4.29116624277653));
#42697=CARTESIAN_POINT('Ctrl Pts',(19.2690675401082,-0.459293044881286,
3.82405931712685));
#42698=CARTESIAN_POINT('Ctrl Pts',(19.316783376171,-0.100417177000157,3.51852142809106));
#42699=CARTESIAN_POINT('Ctrl Pts',(19.3644992122339,0.350673329058588,3.65513271950473));
#42700=CARTESIAN_POINT('Ctrl Pts',(19.4122150482967,0.479735122332443,4.10844094226069));
#42701=CARTESIAN_POINT('Ctrl Pts',(19.4599308843596,0.168248769032157,4.46216617689766));
#42702=CARTESIAN_POINT('Ctrl Pts',(19.5076467204224,-0.297743013815871,
4.39147710422109));
#42703=CARTESIAN_POINT('Ctrl Pts',(19.5553625564852,-0.490312813065352,
3.96128857502183));
#42704=CARTESIAN_POINT('Ctrl Pts',(19.603078392548,-0.232620797759261,3.56664935826393));
#42705=CARTESIAN_POINT('Ctrl Pts',(19.6507942286109,0.238690449241969,3.56996267500769));
#42706=CARTESIAN_POINT('Ctrl Pts',(19.6985100646737,0.490808633485035,3.96818593857384));
#42707=CARTESIAN_POINT('Ctrl Pts',(19.7462259007366,0.292209604061002,4.39562444172689));
#42708=CARTESIAN_POINT('Ctrl Pts',(19.7939417367994,-0.174729824492781,
4.45975512619968));
#42709=CARTESIAN_POINT('Ctrl Pts',(19.8416575728622,-0.481212499922896,
4.10168523844358));
#42710=CARTESIAN_POINT('Ctrl Pts',(19.8893734089251,-0.345789702982467,
3.65023692191923));
#42711=CARTESIAN_POINT('Ctrl Pts',(19.9370892449879,0.107175910646637,3.51998011832295));
#42712=CARTESIAN_POINT('Ctrl Pts',(19.9848050810508,0.461722480014006,3.83053541934297));
#42713=CARTESIAN_POINT('Ctrl Pts',(20.0325209171136,0.392257955100357,4.29670800504879));
#42714=CARTESIAN_POINT('Ctrl Pts',(20.0802367531764,-0.0374150865130887,
4.49041783929577));
#42715=CARTESIAN_POINT('Ctrl Pts',(20.1279525892393,-0.432744382500041,
4.23375285658289));
#42716=CARTESIAN_POINT('Ctrl Pts',(20.1756684253021,-0.430649333670284,
3.76246031529274));
#42717=CARTESIAN_POINT('Ctrl Pts',(20.223384261365,-0.033136228617316,3.50924504180455));
#42718=CARTESIAN_POINT('Ctrl Pts',(20.2711000974278,0.394908089060633,3.70680919012016));
#42719=CARTESIAN_POINT('Ctrl Pts',(20.3188159334906,0.460110046434968,4.17340395051402));
#42720=CARTESIAN_POINT('Ctrl Pts',(20.3665317695535,0.103149962306437,4.48116018402389));
#42721=CARTESIAN_POINT('Ctrl Pts',(20.4142476056163,-0.34923165553999,4.34628168153608));
#42722=CARTESIAN_POINT('Ctrl Pts',(20.4540108023354,-0.457800032585507,
3.97025345815189));
#42723=CARTESIAN_POINT('Ctrl Pts',(20.4858213597105,-0.325993724402262,
3.71529210935379));
#42724=CARTESIAN_POINT('Ctrl Pts',(20.509679277742,-0.15096738523986,3.59329490328468));
#42725=CARTESIAN_POINT('Ctrl Pts',(20.5335371957734,0.0630371972956549,
3.57102347342756));
#42726=CARTESIAN_POINT('Ctrl Pts',(20.5573951138048,0.260511246441404,3.65349437971329));
#42727=CARTESIAN_POINT('Ctrl Pts',(20.5812530318362,0.394877283734959,3.82077798440408));
#42728=CARTESIAN_POINT('Ctrl Pts',(20.6051109498677,0.432370081305563,4.03184236506754));
#42729=CARTESIAN_POINT('Ctrl Pts',(20.6289688678991,0.364303478986858,4.23514367899931));
#42730=CARTESIAN_POINT('Ctrl Pts',(20.6528267859305,0.207066376217976,4.38093363836299));
#42731=CARTESIAN_POINT('Ctrl Pts',(20.6766847039619,-0.000757290757721993,
4.43358147160167));
#42732=CARTESIAN_POINT('Ctrl Pts',(20.7005426219933,-0.208420567790133,
4.38020336888205));
#42733=CARTESIAN_POINT('Ctrl Pts',(20.7244005400248,-0.365106210756856,
4.23385701605743));
#42734=CARTESIAN_POINT('Ctrl Pts',(20.7482584580562,-0.432520392530856,
4.03032528343114));
#42735=CARTESIAN_POINT('Ctrl Pts',(20.7721163760876,-0.394167874571092,
3.81937870627435));
#42736=CARTESIAN_POINT('Ctrl Pts',(20.795974294119,-0.259432524437891,3.65259868360638));
#42737=CARTESIAN_POINT('Ctrl Pts',(20.8198322121504,-0.0612578225112809,
3.57076788979259));
#42738=CARTESIAN_POINT('Ctrl Pts',(20.8436901301819,0.151895538690754,3.5938959627232));
#42739=CARTESIAN_POINT('Ctrl Pts',(20.8675480482132,0.327906592802717,3.71632757520176));
#42740=CARTESIAN_POINT('Ctrl Pts',(20.8914059662447,0.423735399567132,3.90812480123879));
#42741=CARTESIAN_POINT('Ctrl Pts',(20.9152638842761,0.415949440063929,4.12238802732943));
#42742=CARTESIAN_POINT('Ctrl Pts',(20.9391218023075,0.30645246920106,4.30672404095661));
#42743=CARTESIAN_POINT('Ctrl Pts',(20.962979720339,0.122019544809087,4.41605767475162));
#42744=CARTESIAN_POINT('Ctrl Pts',(20.9868376383703,-0.0922504941031022,
4.42365387220386));
#42745=CARTESIAN_POINT('Ctrl Pts',(21.0106955564018,-0.28396276796243,4.32765515869354));
#42746=CARTESIAN_POINT('Ctrl Pts',(21.0345534744332,-0.40623841344949,4.15153583326342));
#42747=CARTESIAN_POINT('Ctrl Pts',(21.0584113924646,-0.429177699343215,
3.93836186909709));
#42748=CARTESIAN_POINT('Ctrl Pts',(21.082269310496,-0.347171348131155,3.74026010679315));
#42749=CARTESIAN_POINT('Ctrl Pts',(21.1061272285274,-0.180272145040548,
3.605671823621));
#42750=CARTESIAN_POINT('Ctrl Pts',(21.1299851465589,0.0307085077608185,
3.56750752082027));
#42751=CARTESIAN_POINT('Ctrl Pts',(21.1538430645903,0.234180094072738,3.63509941005724));
#42752=CARTESIAN_POINT('Ctrl Pts',(21.1777009826217,0.380388268371489,3.79191943321731));
#42753=CARTESIAN_POINT('Ctrl Pts',(21.2015589006531,0.433581149524578,3.99962082296209));
#42754=CARTESIAN_POINT('Ctrl Pts',(21.2254168186846,0.380751629084578,4.2074149318183));
#42755=CARTESIAN_POINT('Ctrl Pts',(21.2492747367159,0.234817963878357,4.36449043997717));
#42756=CARTESIAN_POINT('Ctrl Pts',(21.2731326547474,0.0314649101850846,
4.43243810704058));
#42757=CARTESIAN_POINT('Ctrl Pts',(21.2969905727788,-0.179582171132277,
4.39464287755545));
#42758=CARTESIAN_POINT('Ctrl Pts',(21.3208484908102,-0.346716519889314,
4.26034671465164));
#42759=CARTESIAN_POINT('Ctrl Pts',(21.3447064088417,-0.429069235164158,
4.0623886883135));
#42760=CARTESIAN_POINT('Ctrl Pts',(21.368564326873,-0.406502834830527,3.8491749282489));
#42761=CARTESIAN_POINT('Ctrl Pts',(21.3924222449045,-0.284535418465691,
3.67284200661995));
#42762=CARTESIAN_POINT('Ctrl Pts',(21.4162801629359,-0.0929913416969399,
3.5765081259772));
#42763=CARTESIAN_POINT('Ctrl Pts',(21.4401380809674,0.121291651150069,3.58372954422009));
#42764=CARTESIAN_POINT('Ctrl Pts',(21.4639959989987,0.305915531372611,3.69274042788069));
#42765=CARTESIAN_POINT('Ctrl Pts',(21.4878539170302,0.415734731202803,3.87688464650718));
#42766=CARTESIAN_POINT('Ctrl Pts',(21.5117118350615,0.423895464867194,4.09113392265755));
#42767=CARTESIAN_POINT('Ctrl Pts',(21.535569753093,0.328402210690932,4.28309847227994));
#42768=CARTESIAN_POINT('Ctrl Pts',(21.5594276711244,0.152605670504114,4.40583773398234));
#42769=CARTESIAN_POINT('Ctrl Pts',(21.5832855891559,-0.0605071130159612,
4.42933861492812));
#42770=CARTESIAN_POINT('Ctrl Pts',(21.6071435071872,-0.258824259222961,
4.34785450957493));
#42771=CARTESIAN_POINT('Ctrl Pts',(21.6310014252187,-0.39385182381868,4.18131050126406));
#42772=CARTESIAN_POINT('Ctrl Pts',(21.6548593432501,-0.432571889182456,
3.97043113659525));
#42773=CARTESIAN_POINT('Ctrl Pts',(21.6787172612815,-0.365516344619441,
3.76678216446856));
#42774=CARTESIAN_POINT('Ctrl Pts',(21.702575179313,-0.209082097331647,3.62016130585559));
#42775=CARTESIAN_POINT('Ctrl Pts',(21.7264330973443,-0.00152158196427748,
3.56642135455923));
#42776=CARTESIAN_POINT('Ctrl Pts',(21.7502910153758,0.206411001640417,3.61870319251831));
#42777=CARTESIAN_POINT('Ctrl Pts',(21.7741489334072,0.363870472821225,3.76422248622317));
#42778=CARTESIAN_POINT('Ctrl Pts',(21.7980068514386,0.432353701764573,3.96739580449697));
#42779=CARTESIAN_POINT('Ctrl Pts',(21.82186476947,0.395114673548107,4.17854173669174));
#42780=CARTESIAN_POINT('Ctrl Pts',(21.8457226875014,0.261259344941517,4.3460293508861));
#42781=CARTESIAN_POINT('Ctrl Pts',(21.8695806055329,0.0635189899350569,
4.42890336313855));
#42782=CARTESIAN_POINT('Ctrl Pts',(21.8934385235643,-0.14975348833307,4.40689882001058));
#42783=CARTESIAN_POINT('Ctrl Pts',(21.9172964415957,-0.326407159500644,
4.28539643168872));
#42784=CARTESIAN_POINT('Ctrl Pts',(21.9411543596271,-0.423245389017799,
4.09410684177624));
#42785=CARTESIAN_POINT('Ctrl Pts',(21.9650122776585,-0.416588591947193,
3.87980556563057));
#42786=CARTESIAN_POINT('Ctrl Pts',(21.98887019569,-0.30806453650007,3.69489510271888));
#42787=CARTESIAN_POINT('Ctrl Pts',(22.0127281137213,-0.12421031036921,3.58459109808296));
#42788=CARTESIAN_POINT('Ctrl Pts',(22.0365860317528,0.0900167200678817,
3.57586588547707));
#42789=CARTESIAN_POINT('Ctrl Pts',(22.0604439497842,0.282232210442068,3.67085301705332));
#42790=CARTESIAN_POINT('Ctrl Pts',(22.0843018678157,0.405434237512275,3.8463255517439));
#42791=CARTESIAN_POINT('Ctrl Pts',(22.108159785847,0.429496549703537,4.05937567504088));
#42792=CARTESIAN_POINT('Ctrl Pts',(22.1320177038785,0.348535256241736,4.25790682842971));
#42793=CARTESIAN_POINT('Ctrl Pts',(22.1558756219099,0.182347598717988,4.39337273702606));
#42794=CARTESIAN_POINT('Ctrl Pts',(22.1797335399413,-0.0284290137391457,
4.43264829616218));
#42795=CARTESIAN_POINT('Ctrl Pts',(22.2035914579727,-0.232253957950086,
4.36612956178204));
#42796=CARTESIAN_POINT('Ctrl Pts',(22.2274493760041,-0.379286482964224,
4.21008217638027));
#42797=CARTESIAN_POINT('Ctrl Pts',(22.2513072940356,-0.433573131350875,
4.00266397632408));
#42798=CARTESIAN_POINT('Ctrl Pts',(22.275165212067,-0.381839338801546,3.79459436150246));
#42799=CARTESIAN_POINT('Ctrl Pts',(22.2990231300984,-0.236735426869051,
3.63675202040985));
#42800=CARTESIAN_POINT('Ctrl Pts',(22.3228810481298,-0.0337432544318164,
3.56773370504276));
#42801=CARTESIAN_POINT('Ctrl Pts',(22.3467389661613,0.177500062688638,3.60441627341574));
#42802=CARTESIAN_POINT('Ctrl Pts',(22.3705968841926,0.345339779804043,3.73782983856348));
#42803=CARTESIAN_POINT('Ctrl Pts',(22.3944548022241,0.428734513273282,3.93535114928888));
#42804=CARTESIAN_POINT('Ctrl Pts',(22.4183127202555,0.407291980919218,4.1486808655136));
#42805=CARTESIAN_POINT('Ctrl Pts',(22.4421706382869,0.286255462618544,4.32565405918856));
#42806=CARTESIAN_POINT('Ctrl Pts',(22.4660285563183,0.0952216904214238,
4.42299596654013));
#42807=CARTESIAN_POINT('Ctrl Pts',(22.4898864743497,-0.119096386717928,
4.41690383452019));
#42808=CARTESIAN_POINT('Ctrl Pts',(22.5137443923812,-0.304292138366774,
4.30886736509782));
#42809=CARTESIAN_POINT('Ctrl Pts',(22.5376023104126,-0.415080201412036,
4.12530439950267));
#42810=CARTESIAN_POINT('Ctrl Pts',(22.561460228444,-0.424369795825249,3.91110111771763));
#42811=CARTESIAN_POINT('Ctrl Pts',(22.5853181464754,-0.329889515310188,
3.71863599132299));
#42812=CARTESIAN_POINT('Ctrl Pts',(22.6091760645068,-0.154742073939436,
3.59497211022641));
#42813=CARTESIAN_POINT('Ctrl Pts',(22.6330339825383,0.0582436639512456,
3.57034842802071));
#42814=CARTESIAN_POINT('Ctrl Pts',(22.6568919005697,0.256987911016647,3.65078654733876));
#42815=CARTESIAN_POINT('Ctrl Pts',(22.6807498186011,0.39289034562191,3.81661632308649));
#42816=CARTESIAN_POINT('Ctrl Pts',(22.7046077366325,0.432722782933869,4.02728943245291));
#42817=CARTESIAN_POINT('Ctrl Pts',(22.7284656546639,0.366738191089385,4.2312875884069));
#42818=CARTESIAN_POINT('Ctrl Pts',(22.7523235726953,0.211084664509997,4.37873330099785));
#42819=CARTESIAN_POINT('Ctrl Pts',(22.7761814907268,0.00379901600965994,
4.43356145647204));
#42820=CARTESIAN_POINT('Ctrl Pts',(22.8000394087582,-0.204384723485633,
4.3823852668741));
#42821=CARTESIAN_POINT('Ctrl Pts',(22.8238973267896,-0.36265185203719,4.2376794731));
#42822=CARTESIAN_POINT('Ctrl Pts',(22.8398026054772,-0.408954280604672,
4.10250106973657));
#42823=CARTESIAN_POINT('Ctrl Pts',(22.847755244821,-0.414526965927561,4.03345758723954));
#42824=CARTESIAN_POINT('',(22.8,-0.592174260192535,4.04779597854866));
#42825=CARTESIAN_POINT('Ctrl Pts',(22.8,-0.19576256658266,4.36695865185836));
#42826=CARTESIAN_POINT('Ctrl Pts',(22.8,-0.195886593570853,4.36694806728808));
#42827=CARTESIAN_POINT('Ctrl Pts',(22.8,-0.196010613870461,4.36693742279878));
#42828=CARTESIAN_POINT('Ctrl Pts',(22.8,-0.196134627427637,4.36692671841166));
#42829=CARTESIAN_POINT('Ctrl Pts',(22.8,-0.216622178843513,4.36515830948628));
#42830=CARTESIAN_POINT('Ctrl Pts',(22.8,-0.236921239981942,4.36175743074964));
#42831=CARTESIAN_POINT('Ctrl Pts',(22.8,-0.256857422940798,4.35688458679081));
#42832=CARTESIAN_POINT('Ctrl Pts',(22.8,-0.271809560159941,4.35322995382169));
#42833=CARTESIAN_POINT('Ctrl Pts',(22.8,-0.286558947067823,4.34874691155445));
#42834=CARTESIAN_POINT('Ctrl Pts',(22.8,-0.301048271828705,4.34349077646485));
#42835=CARTESIAN_POINT('Ctrl Pts',(22.8,-0.310003423377303,4.3402422133286));
#42836=CARTESIAN_POINT('Ctrl Pts',(22.8,-0.318859482942331,4.33669811041118));
#42837=CARTESIAN_POINT('Ctrl Pts',(22.8,-0.327604744452034,4.33286912874946));
#42838=CARTESIAN_POINT('Ctrl Pts',(22.8,-0.333457186121174,4.33030672489195));
#42839=CARTESIAN_POINT('Ctrl Pts',(22.8,-0.33926207870774,4.32761569029118));
#42840=CARTESIAN_POINT('Ctrl Pts',(22.8,-0.345009487597299,4.32480202294401));
#42841=CARTESIAN_POINT('Ctrl Pts',(22.8,-0.365309066997251,4.31486428146495));
#42842=CARTESIAN_POINT('Ctrl Pts',(22.8,-0.384828901796994,4.30343044333042));
#42843=CARTESIAN_POINT('Ctrl Pts',(22.8,-0.403416958856431,4.29067119823496));
#42844=CARTESIAN_POINT('Ctrl Pts',(22.8,-0.409874425773003,4.28623865303559));
#42845=CARTESIAN_POINT('Ctrl Pts',(22.8,-0.416219739836017,4.28164578247975));
#42846=CARTESIAN_POINT('Ctrl Pts',(22.8,-0.422447327171508,4.27689854297234));
#42847=CARTESIAN_POINT('Ctrl Pts',(22.8,-0.43500295340691,4.2673274905416));
#42848=CARTESIAN_POINT('Ctrl Pts',(22.8,-0.447079966647781,4.25712966465555));
#42849=CARTESIAN_POINT('Ctrl Pts',(22.8,-0.458660056443695,4.24636133358853));
#42850=CARTESIAN_POINT('Ctrl Pts',(22.8,-0.465333929961841,4.24015529539631));
#42851=CARTESIAN_POINT('Ctrl Pts',(22.8,-0.471842796551704,4.23375955955572));
#42852=CARTESIAN_POINT('Ctrl Pts',(22.8,-0.478183280583292,4.22718326898633));
#42853=CARTESIAN_POINT('Ctrl Pts',(22.8,-0.48330469601013,4.22187138494));
#42854=CARTESIAN_POINT('Ctrl Pts',(22.8,-0.488310096860405,4.21644792156372));
#42855=CARTESIAN_POINT('Ctrl Pts',(22.8,-0.49319389770791,4.21092357737429));
#42856=CARTESIAN_POINT('Ctrl Pts',(22.8,-0.509882204568999,4.19204648678071));
#42857=CARTESIAN_POINT('Ctrl Pts',(22.8,-0.525164669297395,4.17198027236651));
#42858=CARTESIAN_POINT('Ctrl Pts',(22.8,-0.538985569877159,4.15095378743758));
#42859=CARTESIAN_POINT('Ctrl Pts',(22.8,-0.553292287721507,4.12918820238033));
#42860=CARTESIAN_POINT('Ctrl Pts',(22.8,-0.566034197593199,4.10639346234103));
#42861=CARTESIAN_POINT('Ctrl Pts',(22.8,-0.577149101532509,4.08276767497818));
#42862=CARTESIAN_POINT('Ctrl Pts',(22.8,-0.582543745751794,4.07130084468266));
#42863=CARTESIAN_POINT('Ctrl Pts',(22.8,-0.587554988912119,4.05963744408228));
#42864=CARTESIAN_POINT('Ctrl Pts',(22.8,-0.592174260192535,4.04779597854866));
#42865=CARTESIAN_POINT('Ctrl Pts',(22.8,-0.592174260192532,4.04779597854869));
#42866=CARTESIAN_POINT('Ctrl Pts',(22.7920473606562,-0.584213376873468,
4.14642833911734));
#42867=CARTESIAN_POINT('Ctrl Pts',(22.7840947213124,-0.551140611244481,
4.24298318064208));
#42868=CARTESIAN_POINT('Ctrl Pts',(22.7761420819686,-0.496922031827459,
4.32571394759471));
#42869=CARTESIAN_POINT('Ctrl Pts',(22.7681894426248,-0.442703452410443,
4.40844471454734));
#42870=CARTESIAN_POINT('Ctrl Pts',(22.760236803281,-0.367339059205388,4.47735140692785));
#42871=CARTESIAN_POINT('Ctrl Pts',(22.7522841639372,-0.280089901523161,
4.52398941366922));
#42872=CARTESIAN_POINT('Ctrl Pts',(22.7444712463773,-0.194373644734646,
4.56980802634291));
#42873=CARTESIAN_POINT('Ctrl Pts',(22.7366583288174,-0.0971865673270821,
4.59413356703531));
#42874=CARTESIAN_POINT('Ctrl Pts',(22.7288454112575,-7.11440487624268E-7,
4.59414971000239));
#42875=CARTESIAN_POINT('Origin',(27.2,0.3,2.9));
#42876=CARTESIAN_POINT('',(29.2,0.3,3.04606079858305));
#42877=CARTESIAN_POINT('',(27.2,0.3,3.04606079858305));
#42878=CARTESIAN_POINT('',(23.3,0.3,3.04606079858305));
#42879=CARTESIAN_POINT('',(29.2,0.3,3.35));
#42880=CARTESIAN_POINT('',(29.2,0.3,2.9));
#42881=CARTESIAN_POINT('',(27.2,0.3,3.35));
#42882=CARTESIAN_POINT('',(27.2,0.3,3.35));
#42883=CARTESIAN_POINT('',(27.2,0.3,2.9));
#42884=CARTESIAN_POINT('Origin',(27.2,0.,3.125));
#42885=CARTESIAN_POINT('',(27.2,-0.3,3.04606079858305));
#42886=CARTESIAN_POINT('Origin',(27.2,0.,4.));
#42887=CARTESIAN_POINT('',(27.2,-0.3,3.35));
#42888=CARTESIAN_POINT('',(27.2,0.3,3.35));
#42889=CARTESIAN_POINT('',(27.2,-0.3,3.35));
#42890=CARTESIAN_POINT('Origin',(27.2,0.3,3.35));
#42891=CARTESIAN_POINT('',(29.2,-0.3,3.35));
#42892=CARTESIAN_POINT('',(29.2,0.3,3.35));
#42893=CARTESIAN_POINT('',(27.2,-0.3,3.35));
#42894=CARTESIAN_POINT('Origin',(27.2,-0.3,3.35));
#42895=CARTESIAN_POINT('',(29.2,-0.3,3.04606079858305));
#42896=CARTESIAN_POINT('',(23.3,-0.3,3.04606079858305));
#42897=CARTESIAN_POINT('',(29.2,-0.3,3.35));
#42898=CARTESIAN_POINT('Origin',(29.2,0.,3.125));
#42899=CARTESIAN_POINT('Origin',(29.2,0.,4.));
#42900=CARTESIAN_POINT('Origin',(23.3,0.,4.));
#42901=CARTESIAN_POINT('',(29.4,-1.22464679914735E-16,5.));
#42902=CARTESIAN_POINT('Origin',(29.4,0.,4.));
#42903=CARTESIAN_POINT('',(23.3,-1.22464679914735E-16,5.));
#42904=CARTESIAN_POINT('',(23.3,-1.22464679914735E-16,5.));
#42905=CARTESIAN_POINT('Origin',(23.3,0.,4.));
#42906=CARTESIAN_POINT('Origin',(29.4,0.,4.));
#42907=CARTESIAN_POINT('Origin',(22.8,0.,4.));
#42908=CARTESIAN_POINT('',(22.8,-1.65327317884893E-16,5.35));
#42909=CARTESIAN_POINT('Origin',(22.8,0.,4.));
#42910=CARTESIAN_POINT('Origin',(22.8,0.,4.));
#42911=CARTESIAN_POINT('Origin',(22.8,0.,4.));
#42912=CARTESIAN_POINT('',(23.3,-1.65327317884893E-16,5.35));
#42913=CARTESIAN_POINT('Origin',(23.3,0.,4.));
#42914=CARTESIAN_POINT('',(22.8,-1.65327317884893E-16,5.35));
#42915=CARTESIAN_POINT('Origin',(23.3,0.,4.));
#42916=CARTESIAN_POINT('Origin',(4.,0.,4.));
#43443=UNCERTAINTY_MEASURE_WITH_UNIT(LENGTH_MEASURE(0.001),#43522,
'DISTANCE_ACCURACY_VALUE',
'Maximum model space distance between geometric entities at asserted c
onnectivities');
#43453=UNCERTAINTY_MEASURE_WITH_UNIT(LENGTH_MEASURE(0.001),#43522,
'DISTANCE_ACCURACY_VALUE',
'Maximum model space distance between geometric entities at asserted c
onnectivities');
#43511=(
GEOMETRIC_REPRESENTATION_CONTEXT(3)
GLOBAL_UNCERTAINTY_ASSIGNED_CONTEXT((#43443))
GLOBAL_UNIT_ASSIGNED_CONTEXT((#43522,#43524,#43525))
REPRESENTATION_CONTEXT('','3D')
);
#43521=(
GEOMETRIC_REPRESENTATION_CONTEXT(3)
GLOBAL_UNCERTAINTY_ASSIGNED_CONTEXT((#43453))
GLOBAL_UNIT_ASSIGNED_CONTEXT((#43522,#43524,#43525))
REPRESENTATION_CONTEXT('','3D')
);
#43522=(
LENGTH_UNIT()
NAMED_UNIT(*)
SI_UNIT(.CENTI.,.METRE.)
);
#43524=(
NAMED_UNIT(*)
PLANE_ANGLE_UNIT()
SI_UNIT($,.RADIAN.)
);
#43525=(
NAMED_UNIT(*)
SI_UNIT($,.STERADIAN.)
SOLID_ANGLE_UNIT()
);
#43583=SHAPE_DEFINITION_REPRESENTATION(#43770,#43851);
#43770=PRODUCT_DEFINITION_SHAPE('',$,#43919);
#43851=SHAPE_REPRESENTATION('',(#20899),#43511);
#43861=PRODUCT_DEFINITION_CONTEXT('part definition',#44064,'design');
#43919=PRODUCT_DEFINITION('Supported TR12x3 screw',
'Supported TR12x3 screw',#43986,#43861);
#43986=PRODUCT_DEFINITION_FORMATION('',$,#44123);
#44064=APPLICATION_CONTEXT(
'Core Data for Automotive Mechanical Design Process');
#44065=PRODUCT_CONTEXT('part definition',#44064,'mechanical');
#44123=PRODUCT('Supported TR12x3 screw','Supported TR12x3 screw',
'Supported TR12x3 screw',(#44065));
#44203=COLOUR_RGB('Black',0.12,0.14,0.17);
#44204=FILL_AREA_STYLE_COLOUR('',#44203);
#44205=FILL_AREA_STYLE('',(#44204));
#44206=SURFACE_STYLE_FILL_AREA(#44205);
#44207=SURFACE_SIDE_STYLE('',(#44206));
#44208=SURFACE_STYLE_USAGE(.BOTH.,#44207);
#44209=PRESENTATION_STYLE_ASSIGNMENT((#44208));
ENDSEC;
END-ISO-10303-21;
